ISO-10303-21;
HEADER;
FILE_DESCRIPTION (('STEP AP214'),
    '1' );
FILE_NAME ('Injection Molded Chain Links 5.step',
    '2026-10-08T22:59:04',
    ( '' ),
    ( '' ),
    'SwSTEP 2.0',
    'SolidWorks 2020',
    '' );
FILE_SCHEMA (( 'AUTOMOTIVE_DESIGN' ));
ENDSEC;

DATA;
#5=DIRECTION ( 'NONE',  ( 1.000000000000000000, -7.304098846218133681E-16, 0.000000000000000000 ) ) ;
#13=ORIENTED_EDGE ( 'NONE', *, *, #236887, .F. ) ;
#74=ORIENTED_EDGE ( 'NONE', *, *, #168378, .T. ) ;
#76=ORIENTED_EDGE ( 'NONE', *, *, #212684, .T. ) ;
#85=CIRCLE ( 'NONE', #249894, 12.87500000000000000 ) ;
#89=CIRCLE ( 'NONE', #91688, 0.2000000000000000944 ) ;
#94=EDGE_CURVE ( 'NONE', #19242, #16854, #137031, .T. ) ;
#99=AXIS2_PLACEMENT_3D ( 'NONE', #76575, #156148, #56984 ) ;
#156=DIRECTION ( 'NONE',  ( -1.000000000000000000, 0.000000000000000000, 0.000000000000000000 ) ) ;
#165=DIRECTION ( 'NONE',  ( -0.000000000000000000, 1.000000000000000000, 0.000000000000000000 ) ) ;
#178=EDGE_CURVE ( 'NONE', #224075, #38015, #66431, .T. ) ;
#179=ORIENTED_EDGE ( 'NONE', *, *, #45901, .T. ) ;
#209=DIRECTION ( 'NONE',  ( -0.7071067811865474617, -0.7071067811865474617, -2.044391222244499837E-16 ) ) ;
#214=AXIS2_PLACEMENT_3D ( 'NONE', #162739, #3632, #83138 ) ;
#215=DIRECTION ( 'NONE',  ( -1.000000000000000000, 0.000000000000000000, 0.000000000000000000 ) ) ;
#281=DIRECTION ( 'NONE',  ( 1.000000000000000000, 0.000000000000000000, 0.000000000000000000 ) ) ;
#282=DIRECTION ( 'NONE',  ( 0.000000000000000000, 1.776356839400155604E-15, 1.000000000000000000 ) ) ;
#293=DIRECTION ( 'NONE',  ( 0.000000000000000000, -1.000000000000000000, 0.000000000000000000 ) ) ;
#299=ORIENTED_EDGE ( 'NONE', *, *, #10132, .F. ) ;
#360=VERTEX_POINT ( 'NONE', #59665 ) ;
#363=ADVANCED_FACE ( 'NONE', ( #179658 ), #56124, .T. ) ;
#372=TOROIDAL_SURFACE ( 'NONE', #246093, 0.9750000000000019762, 0.1000000000000000056 ) ;
#385=CARTESIAN_POINT ( 'NONE',  ( 23.24999999999999289, 11.65000000001116298, -155.3500000000000227 ) ) ;
#418=ORIENTED_EDGE ( 'NONE', *, *, #6305, .F. ) ;
#420=CARTESIAN_POINT ( 'NONE',  ( -20.64999999999999858, 1.115625160336667635E-11, -169.5000000000000284 ) ) ;
#424=CARTESIAN_POINT ( 'NONE',  ( 23.14999999999999858, 5.000000000011153745, -146.4052660189131245 ) ) ;
#478=VECTOR ( 'NONE', #249908, 1000.000000000000000 ) ;
#484=CIRCLE ( 'NONE', #104535, 0.09999999999998898659 ) ;
#491=ADVANCED_FACE ( 'NONE', ( #30869 ), #107802, .F. ) ;
#571=CARTESIAN_POINT ( 'NONE',  ( -21.05000000000000071, 1.115649653272650466E-11, -171.5000000000000284 ) ) ;
#579=DIRECTION ( 'NONE',  ( 1.000000000000000000, 0.000000000000000000, 0.000000000000000000 ) ) ;
#586=AXIS2_PLACEMENT_3D ( 'NONE', #112751, #253528, #74936 ) ;
#594=DIRECTION ( 'NONE',  ( -1.000000000000000000, 0.000000000000000000, 0.000000000000000000 ) ) ;
#598=DIRECTION ( 'NONE',  ( -0.7071067811865474617, -0.7071067811865474617, -0.000000000000000000 ) ) ;
#640=CARTESIAN_POINT ( 'NONE',  ( 18.52928932188133970, 10.27928932189250411, -158.6500000000000057 ) ) ;
#641=EDGE_LOOP ( 'NONE', ( #78881, #244574, #237015, #68225, #250908, #111414, #247052, #30325, #136634, #124686, #247417, #184716 ) ) ;
#663=DIRECTION ( 'NONE',  ( 0.000000000000000000, 0.000000000000000000, -1.000000000000000000 ) ) ;
#674=ADVANCED_FACE ( 'NONE', ( #35989 ), #104880, .F. ) ;
#706=CARTESIAN_POINT ( 'NONE',  ( -23.15000000000000213, 1.115600667400684642E-11, -167.5000000000000284 ) ) ;
#708=DIRECTION ( 'NONE',  ( 0.000000000000000000, 1.000000000000000000, -0.000000000000000000 ) ) ;
#712=CIRCLE ( 'NONE', #213125, 0.8750000000000007772 ) ;
#730=ORIENTED_EDGE ( 'NONE', *, *, #103764, .F. ) ;
#742=DIRECTION ( 'NONE',  ( -1.000000000000000000, -0.000000000000000000, 0.000000000000000000 ) ) ;
#762=EDGE_CURVE ( 'NONE', #110751, #214790, #59667, .T. ) ;
#771=EDGE_CURVE ( 'NONE', #146335, #61093, #246950, .T. ) ;
#775=ORIENTED_EDGE ( 'NONE', *, *, #51382, .T. ) ;
#779=CARTESIAN_POINT ( 'NONE',  ( 20.95520789717937404, 10.57693059939611224, -141.5802329738748710 ) ) ;
#834=CARTESIAN_POINT ( 'NONE',  ( -18.40000000000000213, -9.519327731081286714, -140.9729763765593304 ) ) ;
#838=DIRECTION ( 'NONE',  ( 1.000000000000000000, 0.000000000000000000, 0.000000000000000000 ) ) ;
#864=CIRCLE ( 'NONE', #179979, 6.258578643762696458 ) ;
#876=EDGE_LOOP ( 'NONE', ( #135196, #248914, #189669, #154039 ) ) ;
#926=CARTESIAN_POINT ( 'NONE',  ( 21.14999999999999503, 1.115600667400684642E-11, -134.0000000000000000 ) ) ;
#962=DIRECTION ( 'NONE',  ( 1.000000000000000000, -0.000000000000000000, -0.000000000000000000 ) ) ;
#988=CARTESIAN_POINT ( 'NONE',  ( -1.739115166359751170E-14, 11.65000000001114699, -146.2500000000000284 ) ) ;
#991=VERTEX_POINT ( 'NONE', #173638 ) ;
#1016=FACE_OUTER_BOUND ( 'NONE', #23267, .T. ) ;
#1019=ORIENTED_EDGE ( 'NONE', *, *, #12800, .T. ) ;
#1075=CARTESIAN_POINT ( 'NONE',  ( 22.39999999999999503, 0.1000000000111554016, -126.2092204016266379 ) ) ;
#1081=ORIENTED_EDGE ( 'NONE', *, *, #230083, .T. ) ;
#1086=ORIENTED_EDGE ( 'NONE', *, *, #86462, .F. ) ;
#1090=ORIENTED_EDGE ( 'NONE', *, *, #72256, .T. ) ;
#1098=CARTESIAN_POINT ( 'NONE',  ( 23.14999999999999858, 5.500000000011153745, -146.4052660189131245 ) ) ;
#1119=DIRECTION ( 'NONE',  ( 1.000000000000000000, -0.000000000000000000, -0.000000000000000000 ) ) ;
#1134=EDGE_CURVE ( 'NONE', #176594, #123224, #5180, .T. ) ;
#1168=ORIENTED_EDGE ( 'NONE', *, *, #66721, .F. ) ;
#1171=DIRECTION ( 'NONE',  ( 0.000000000000000000, 0.000000000000000000, -1.000000000000000000 ) ) ;
#1189=ADVANCED_FACE ( 'NONE', ( #122614 ), #9245, .F. ) ;
#1191=CARTESIAN_POINT ( 'NONE',  ( -18.59999999999999787, 7.250000000011155521, -155.3500000000000227 ) ) ;
#1200=CARTESIAN_POINT ( 'NONE',  ( -20.85000000000000142, 6.846123162363745074, -171.2377262668498759 ) ) ;
#1203=LINE ( 'NONE', #44221, #137456 ) ;
#1215=FACE_OUTER_BOUND ( 'NONE', #255672, .T. ) ;
#1220=FACE_OUTER_BOUND ( 'NONE', #156586, .T. ) ;
#1221=AXIS2_PLACEMENT_3D ( 'NONE', #83190, #118526, #58505 ) ;
#1257=ORIENTED_EDGE ( 'NONE', *, *, #10705, .T. ) ;
#1264=CIRCLE ( 'NONE', #80355, 11.75000000000001066 ) ;
#1294=VERTEX_POINT ( 'NONE', #91167 ) ;
#1298=EDGE_LOOP ( 'NONE', ( #189655, #86851, #167928, #233536 ) ) ;
#1327=DIRECTION ( 'NONE',  ( 1.000000000000000000, 0.000000000000000000, 0.000000000000000000 ) ) ;
#1329=EDGE_CURVE ( 'NONE', #121951, #79366, #159296, .T. ) ;
#1340=DIRECTION ( 'NONE',  ( 1.000000000000000000, 0.000000000000000000, 0.000000000000000000 ) ) ;
#1371=ORIENTED_EDGE ( 'NONE', *, *, #163107, .F. ) ;
#1376=ORIENTED_EDGE ( 'NONE', *, *, #1643, .T. ) ;
#1423=ORIENTED_EDGE ( 'NONE', *, *, #186682, .F. ) ;
#1426=DIRECTION ( 'NONE',  ( -4.408576920032448588E-17, 0.1350103645451876944, -0.9908441862701601321 ) ) ;
#1476=B_SPLINE_CURVE_WITH_KNOTS ( 'NONE', 3,
 ( #18926, #174203, #254914, #149808, #215829, #236684, #75090, #154627, #115458, #169391, #195025, #257485, #214557, #248892, #97141, #234121, #196285, #98425, #176743 ),
 .UNSPECIFIED., .F., .F.,
 ( 4, 3, 3, 3, 3, 3, 4 ),
 ( 0.000000000000000000, 7.110282409889811541E-05, 0.0001508797727291456749, 0.0002027344179858454128, 0.0002343294522348951471, 0.0002454816334821100063, 0.0002619873080085602097 ),
 .UNSPECIFIED. ) ;
#1516=DIRECTION ( 'NONE',  ( 1.000000000000000000, -0.000000000000000000, -0.000000000000000000 ) ) ;
#1517=AXIS2_PLACEMENT_3D ( 'NONE', #15530, #95033, #174632 ) ;
#1557=EDGE_LOOP ( 'NONE', ( #199268, #132770, #118113, #188463 ) ) ;
#1566=LINE ( 'NONE', #83645, #180517 ) ;
#1582=TOROIDAL_SURFACE ( 'NONE', #180657, 0.2000000000000000111, 0.1000000000000000056 ) ;
#1605=DIRECTION ( 'NONE',  ( 1.000000000000000000, -0.000000000000000000, -0.000000000000000000 ) ) ;
#1610=LINE ( 'NONE', #81141, #79369 ) ;
#1637=LINE ( 'NONE', #201135, #51954 ) ;
#1639=DIRECTION ( 'NONE',  ( 0.000000000000000000, 0.000000000000000000, -1.000000000000000000 ) ) ;
#1643=EDGE_CURVE ( 'NONE', #257362, #43709, #111700, .T. ) ;
#1652=ADVANCED_FACE ( 'NONE', ( #68726 ), #166568, .T. ) ;
#1686=DIRECTION ( 'NONE',  ( 0.000000000000000000, 0.4999999999999413247, -0.8660254037844724584 ) ) ;
#1690=AXIS2_PLACEMENT_3D ( 'NONE', #73203, #246661, #92719 ) ;
#1707=CIRCLE ( 'NONE', #247410, 0.09999999999998898659 ) ;
#1736=ADVANCED_FACE ( 'NONE', ( #231663 ), #13887, .T. ) ;
#1741=CARTESIAN_POINT ( 'NONE',  ( 21.05000000000000071, -0.09999999998884338825, -127.4593430482987912 ) ) ;
#1758=ORIENTED_EDGE ( 'NONE', *, *, #83281, .T. ) ;
#1790=EDGE_CURVE ( 'NONE', #60110, #211620, #42940, .T. ) ;
#1799=EDGE_LOOP ( 'NONE', ( #72271, #44085, #66351, #123931 ) ) ;
#1815=CARTESIAN_POINT ( 'NONE',  ( -18.59999999999999787, 11.75000000001115197, -122.2500000000000284 ) ) ;
#1821=CARTESIAN_POINT ( 'NONE',  ( 21.97500000000000497, 9.750000000011153745, -155.1500000000000057 ) ) ;
#1908=DIRECTION ( 'NONE',  ( -1.000000000000000000, 0.000000000000000000, 0.000000000000000000 ) ) ;
#1999=DIRECTION ( 'NONE',  ( 0.000000000000000000, -1.000000000000000000, 0.000000000000000000 ) ) ;
#2039=EDGE_CURVE ( 'NONE', #83610, #99200, #209715, .T. ) ;
#2052=AXIS2_PLACEMENT_3D ( 'NONE', #79603, #220433, #200858 ) ;
#2054=AXIS2_PLACEMENT_3D ( 'NONE', #62377, #203158, #164046 ) ;
#2062=ORIENTED_EDGE ( 'NONE', *, *, #106889, .T. ) ;
#2109=EDGE_CURVE ( 'NONE', #23713, #81104, #130594, .T. ) ;
#2117=ORIENTED_EDGE ( 'NONE', *, *, #77030, .F. ) ;
#2118=ORIENTED_EDGE ( 'NONE', *, *, #171993, .F. ) ;
#2130=CARTESIAN_POINT ( 'NONE',  ( 18.59999999999999076, 1.835341550235567887, -145.5551512925629822 ) ) ;
#2138=FACE_OUTER_BOUND ( 'NONE', #13583, .T. ) ;
#2154=CARTESIAN_POINT ( 'NONE',  ( 22.57320508075688892, 11.75000000001115552, -134.0000000000000000 ) ) ;
#2172=DIRECTION ( 'NONE',  ( 0.000000000000000000, 1.000000000000000000, 2.891205793294679805E-16 ) ) ;
#2177=CARTESIAN_POINT ( 'NONE',  ( 21.53699400381585249, 6.787711793193205168, -134.0000000000000000 ) ) ;
#2188=EDGE_CURVE ( 'NONE', #56118, #23218, #180492, .T. ) ;
#2196=TOROIDAL_SURFACE ( 'NONE', #168860, 0.2000000000000000111, 0.1000000000000000056 ) ;
#2215=FACE_BOUND ( 'NONE', #82865, .T. ) ;
#2222=ORIENTED_EDGE ( 'NONE', *, *, #28885, .T. ) ;
#2265=VECTOR ( 'NONE', #40878, 1000.000000000000000 ) ;
#2267=DIRECTION ( 'NONE',  ( 0.000000000000000000, -0.1455152366551721865, -0.9893560106964475187 ) ) ;
#2275=DIRECTION ( 'NONE',  ( -0.000000000000000000, -0.000000000000000000, 1.000000000000000000 ) ) ;
#2306=CARTESIAN_POINT ( 'NONE',  ( 18.49999999999999645, 5.699452464332751767, -121.4577260434301991 ) ) ;
#2340=AXIS2_PLACEMENT_3D ( 'NONE', #135814, #217910, #198371 ) ;
#2349=DIRECTION ( 'NONE',  ( 0.000000000000000000, -0.000000000000000000, 1.000000000000000000 ) ) ;
#2355=FACE_OUTER_BOUND ( 'NONE', #256850, .T. ) ;
#2367=DIRECTION ( 'NONE',  ( 0.000000000000000000, -1.000000000000000000, 0.000000000000000000 ) ) ;
#2380=ORIENTED_EDGE ( 'NONE', *, *, #183415, .F. ) ;
#2390=DIRECTION ( 'NONE',  ( 0.000000000000000000, -1.000000000000000000, -2.891205793294679805E-16 ) ) ;
#2396=CYLINDRICAL_SURFACE ( 'NONE', #158089, 0.09999999999999939493 ) ;
#2404=CARTESIAN_POINT ( 'NONE',  ( 23.24999999999999645, -3.899999999988843502, -167.5000000000000284 ) ) ;
#2411=ORIENTED_EDGE ( 'NONE', *, *, #20635, .F. ) ;
#2415=DIRECTION ( 'NONE',  ( 1.000000000000000000, 1.836970198721029934E-16, 3.186635328391151676E-31 ) ) ;
#2420=FACE_OUTER_BOUND ( 'NONE', #249983, .T. ) ;
#2425=AXIS2_PLACEMENT_3D ( 'NONE', #153513, #135160, #16531 ) ;
#2447=ORIENTED_EDGE ( 'NONE', *, *, #86991, .F. ) ;
#2455=ORIENTED_EDGE ( 'NONE', *, *, #81482, .T. ) ;
#2483=ORIENTED_EDGE ( 'NONE', *, *, #71657, .T. ) ;
#2503=DIRECTION ( 'NONE',  ( 0.000000000000000000, 0.000000000000000000, -1.000000000000000000 ) ) ;
#2516=EDGE_CURVE ( 'NONE', #85055, #23218, #43308, .T. ) ;
#2542=EDGE_CURVE ( 'NONE', #72588, #174999, #143249, .T. ) ;
#2572=CARTESIAN_POINT ( 'NONE',  ( 20.94999999999999929, 4.813084112160680661, -145.9415177565238366 ) ) ;
#2597=EDGE_CURVE ( 'NONE', #123515, #187371, #193161, .T. ) ;
#2602=CARTESIAN_POINT ( 'NONE',  ( 20.94403535211772294, 10.30632246271647467, -173.0041836778896140 ) ) ;
#2609=DIRECTION ( 'NONE',  ( 0.000000000000000000, -1.000000000000000000, 0.000000000000000000 ) ) ;
#2618=DIRECTION ( 'NONE',  ( -1.000000000000000000, -0.000000000000000000, -0.000000000000000000 ) ) ;
#2630=DIRECTION ( 'NONE',  ( 0.000000000000000000, 0.000000000000000000, 1.000000000000000000 ) ) ;
#2639=DIRECTION ( 'NONE',  ( 1.000000000000000000, -7.304098846218133681E-16, 4.217023435051677994E-16 ) ) ;
#2640=ORIENTED_EDGE ( 'NONE', *, *, #159471, .F. ) ;
#2678=DIRECTION ( 'NONE',  ( 0.000000000000000000, 1.224646799142185182E-16, 1.000000000000000000 ) ) ;
#2689=ORIENTED_EDGE ( 'NONE', *, *, #84996, .T. ) ;
#2695=ORIENTED_EDGE ( 'NONE', *, *, #60445, .F. ) ;
#2721=CARTESIAN_POINT ( 'NONE',  ( -20.54999999999999716, 2.500000000011154633, -154.2753780772379173 ) ) ;
#2800=VERTEX_POINT ( 'NONE', #16546 ) ;
#2809=EDGE_CURVE ( 'NONE', #248652, #118509, #193150, .T. ) ;
#2819=FACE_OUTER_BOUND ( 'NONE', #252833, .T. ) ;
#2825=CARTESIAN_POINT ( 'NONE',  ( 20.95595012432478654, 10.60417921308711975, -141.5957693302180473 ) ) ;
#2837=DIRECTION ( 'NONE',  ( -1.000000000000000000, 0.000000000000000000, 0.000000000000000000 ) ) ;
#2882=ORIENTED_EDGE ( 'NONE', *, *, #241618, .T. ) ;
#2893=DIRECTION ( 'NONE',  ( 0.000000000000000000, 0.000000000000000000, -1.000000000000000000 ) ) ;
#2904=ORIENTED_EDGE ( 'NONE', *, *, #157741, .T. ) ;
#2907=DIRECTION ( 'NONE',  ( 0.000000000000000000, 0.000000000000000000, 1.000000000000000000 ) ) ;
#2950=TOROIDAL_SURFACE ( 'NONE', #107193, 12.97499999999999609, 0.1000000000000000056 ) ;
#2951=ADVANCED_FACE ( 'NONE', ( #48917 ), #176768, .T. ) ;
#2972=ORIENTED_EDGE ( 'NONE', *, *, #78032, .F. ) ;
#2979=CIRCLE ( 'NONE', #15496, 0.09999999999998898659 ) ;
#2983=CARTESIAN_POINT ( 'NONE',  ( -20.54999999999999716, -11.74999999998884626, -146.3500000000000227 ) ) ;
#2995=CARTESIAN_POINT ( 'NONE',  ( 21.05000000000000071, 11.65000000001115943, -134.1000000000000227 ) ) ;
#3010=AXIS2_PLACEMENT_3D ( 'NONE', #99260, #165, #232397 ) ;
#3035=ADVANCED_FACE ( 'NONE', ( #127187 ), #85445, .T. ) ;
#3048=CARTESIAN_POINT ( 'NONE',  ( 20.94999999999999929, 1.115600667400684642E-11, -164.6000000000000227 ) ) ;
#3091=PLANE ( 'NONE',  #149343 ) ;
#3121=CARTESIAN_POINT ( 'NONE',  ( -22.50000000000094147, 0.1000000000110504439, -122.3504291924551950 ) ) ;
#3131=VECTOR ( 'NONE', #229340, 1000.000000000000000 ) ;
#3132=ADVANCED_FACE ( 'NONE', ( #134852 ), #6048, .F. ) ;
#3146=EDGE_CURVE ( 'NONE', #192257, #198238, #114021, .T. ) ;
#3178=EDGE_LOOP ( 'NONE', ( #184403, #2222, #237367, #225597 ) ) ;
#3218=EDGE_LOOP ( 'NONE', ( #256453, #86591, #101772, #248090 ) ) ;
#3225=DIRECTION ( 'NONE',  ( 0.000000000000000000, 0.01562499999998609446, -0.9998779222360101304 ) ) ;
#3233=ORIENTED_EDGE ( 'NONE', *, *, #62140, .T. ) ;
#3235=ORIENTED_EDGE ( 'NONE', *, *, #61703, .F. ) ;
#3236=ORIENTED_EDGE ( 'NONE', *, *, #31490, .T. ) ;
#3296=DIRECTION ( 'NONE',  ( -1.000000000000000000, -0.000000000000000000, -0.000000000000000000 ) ) ;
#3314=ORIENTED_EDGE ( 'NONE', *, *, #87761, .T. ) ;
#3322=DIRECTION ( 'NONE',  ( 0.000000000000000000, -2.255140518769784599E-13, 1.000000000000000000 ) ) ;
#3368=CARTESIAN_POINT ( 'NONE',  ( 18.50211644919734866, 10.30207779525984790, -172.9895520716782755 ) ) ;
#3381=ORIENTED_EDGE ( 'NONE', *, *, #198032, .F. ) ;
#3387=LINE ( 'NONE', #163776, #126680 ) ;
#3405=CARTESIAN_POINT ( 'NONE',  ( 22.57320508075687115, 11.75000000001115552, -134.0000000000000000 ) ) ;
#3436=CARTESIAN_POINT ( 'NONE',  ( -18.33981767444291577, -9.569575789792940768, -174.3191618437252259 ) ) ;
#3442=CARTESIAN_POINT ( 'NONE',  ( 20.85000000000000142, -1.263275465206102233, -175.4018646667464338 ) ) ;
#3448=CIRCLE ( 'NONE', #245466, 0.4000000000000114575 ) ;
#3480=ADVANCED_FACE ( 'NONE', ( #253236 ), #231128, .T. ) ;
#3499=DIRECTION ( 'NONE',  ( 1.000000000000000000, 0.000000000000000000, 0.000000000000000000 ) ) ;
#3502=CYLINDRICAL_SURFACE ( 'NONE', #158986, 0.09999999999999939493 ) ;
#3503=DIRECTION ( 'NONE',  ( 0.000000000000000000, 0.000000000000000000, -1.000000000000000000 ) ) ;
#3505=AXIS2_PLACEMENT_3D ( 'NONE', #115541, #17711, #15180 ) ;
#3507=EDGE_CURVE ( 'NONE', #100941, #21635, #181051, .T. ) ;
#3523=CARTESIAN_POINT ( 'NONE',  ( -23.15000000000000213, 2.000000000011154189, -147.2246219227621111 ) ) ;
#3622=ORIENTED_EDGE ( 'NONE', *, *, #219274, .T. ) ;
#3632=DIRECTION ( 'NONE',  ( 0.000000000000000000, -0.8660254037844412611, -0.4999999999999956701 ) ) ;
#3685=CARTESIAN_POINT ( 'NONE',  ( 20.94999999999999929, 6.550000000011156231, -146.1500000000000341 ) ) ;
#3692=CYLINDRICAL_SURFACE ( 'NONE', #151941, 0.09999999999998898659 ) ;
#3705=CYLINDRICAL_SURFACE ( 'NONE', #68011, 0.09999999999998898659 ) ;
#3718=ORIENTED_EDGE ( 'NONE', *, *, #81496, .F. ) ;
#3724=EDGE_LOOP ( 'NONE', ( #134071, #184153, #130157, #227487 ) ) ;
#3763=EDGE_CURVE ( 'NONE', #73834, #174422, #152206, .T. ) ;
#3765=LINE ( 'NONE', #83270, #171587 ) ;
#3777=CIRCLE ( 'NONE', #7887, 0.09999999999998898659 ) ;
#3814=DIRECTION ( 'NONE',  ( 2.952720810173289112E-16, -1.000000000000000000, 0.000000000000000000 ) ) ;
#3843=DIRECTION ( 'NONE',  ( 0.000000000000000000, 0.000000000000000000, -1.000000000000000000 ) ) ;
#3881=FACE_OUTER_BOUND ( 'NONE', #8935, .T. ) ;
#3914=ORIENTED_EDGE ( 'NONE', *, *, #196909, .T. ) ;
#3952=ORIENTED_EDGE ( 'NONE', *, *, #184238, .T. ) ;
#3960=CIRCLE ( 'NONE', #87156, 4.049999999999998046 ) ;
#3968=CARTESIAN_POINT ( 'NONE',  ( 20.94999999999999929, 5.900000000011162093, -157.2809002353436654 ) ) ;
#3982=ORIENTED_EDGE ( 'NONE', *, *, #140128, .T. ) ;
#3992=VERTEX_POINT ( 'NONE', #33625 ) ;
#4042=CARTESIAN_POINT ( 'NONE',  ( -18.59999999999999787, 1.851028230152016674, -145.6539132694225032 ) ) ;
#4092=CIRCLE ( 'NONE', #149872, 12.87499999999999822 ) ;
#4110=VERTEX_POINT ( 'NONE', #11138 ) ;
#4134=FACE_OUTER_BOUND ( 'NONE', #203796, .T. ) ;
#4140=DIRECTION ( 'NONE',  ( -0.000000000000000000, 1.000000000000000000, -0.000000000000000000 ) ) ;
#4157=DIRECTION ( 'NONE',  ( 0.000000000000000000, -1.000000000000000000, -0.000000000000000000 ) ) ;
#4224=VERTEX_POINT ( 'NONE', #69846 ) ;
#4257=ADVANCED_FACE ( 'NONE', ( #151954 ), #73703, .F. ) ;
#4260=AXIS2_PLACEMENT_3D ( 'NONE', #174190, #175452, #257470 ) ;
#4316=CARTESIAN_POINT ( 'NONE',  ( -23.15000000000000213, 11.75000000001115552, -122.2500000000000284 ) ) ;
#4328=CARTESIAN_POINT ( 'NONE',  ( 20.72390388899090752, 10.58996311843487348, -141.5113482957463873 ) ) ;
#4345=EDGE_LOOP ( 'NONE', ( #249029, #104041, #136351 ) ) ;
#4356=CARTESIAN_POINT ( 'NONE',  ( -20.85000000000000142, 10.33248238083634440, -173.0948465439131496 ) ) ;
#4377=CIRCLE ( 'NONE', #200209, 11.70000000000001528 ) ;
#4389=EDGE_CURVE ( 'NONE', #219189, #179208, #238207, .T. ) ;
#4414=CARTESIAN_POINT ( 'NONE',  ( -22.45354308602486881, 2.198902233671630347E-07, -122.2495671095367271 ) ) ;
#4432=AXIS2_PLACEMENT_3D ( 'NONE', #7971, #69238, #27565 ) ;
#4503=TOROIDAL_SURFACE ( 'NONE', #208558, 3.899999999999999467, 0.1000000000000000056 ) ;
#4509=ADVANCED_FACE ( 'NONE', ( #227299 ), #246856, .F. ) ;
#4538=ORIENTED_EDGE ( 'NONE', *, *, #28793, .F. ) ;
#4563=ORIENTED_EDGE ( 'NONE', *, *, #93210, .F. ) ;
#4568=LINE ( 'NONE', #240629, #36491 ) ;
#4585=CIRCLE ( 'NONE', #112944, 0.09999999999999982514 ) ;
#4596=DIRECTION ( 'NONE',  ( -1.000000000000000000, 0.000000000000000000, 0.000000000000000000 ) ) ;
#4634=DIRECTION ( 'NONE',  ( 1.000000000000000000, -0.000000000000000000, -0.000000000000000000 ) ) ;
#4681=VERTEX_POINT ( 'NONE', #138446 ) ;
#4712=CARTESIAN_POINT ( 'NONE',  ( -18.50000000000000000, -9.399999999988850163, -174.3820418481726904 ) ) ;
#4713=CARTESIAN_POINT ( 'NONE',  ( -22.39999999999999858, 11.65000000001115588, -134.0000000000000284 ) ) ;
#4718=CIRCLE ( 'NONE', #150495, 0.1999999999999987899 ) ;
#4724=EDGE_LOOP ( 'NONE', ( #257166, #51514, #35181, #232346 ) ) ;
#4735=CARTESIAN_POINT ( 'NONE',  ( -21.44999999999999929, 7.350000000011155166, -146.3500000000000227 ) ) ;
#4769=FACE_OUTER_BOUND ( 'NONE', #202123, .T. ) ;
#4778=VECTOR ( 'NONE', #237927, 1000.000000000000000 ) ;
#4811=ORIENTED_EDGE ( 'NONE', *, *, #17564, .T. ) ;
#4814=DIRECTION ( 'NONE',  ( 0.000000000000000000, 1.000000000000000000, 0.000000000000000000 ) ) ;
#4831=ORIENTED_EDGE ( 'NONE', *, *, #1329, .T. ) ;
#4847=AXIS2_PLACEMENT_3D ( 'NONE', #43855, #240775, #838 ) ;
#4901=EDGE_LOOP ( 'NONE', ( #51368, #3718, #192595, #84933 ) ) ;
#4932=EDGE_LOOP ( 'NONE', ( #33198, #168707, #132928, #25831, #21150, #214008, #212168, #69739, #25757, #173618, #44280, #232212 ) ) ;
#4950=VERTEX_POINT ( 'NONE', #228298 ) ;
#4972=AXIS2_PLACEMENT_3D ( 'NONE', #118422, #119707, #160127 ) ;
#4984=EDGE_LOOP ( 'NONE', ( #126112, #175224, #76786, #211562 ) ) ;
#5020=EDGE_CURVE ( 'NONE', #220745, #159966, #178615, .T. ) ;
#5051=CARTESIAN_POINT ( 'NONE',  ( 22.49999999999999645, 0.1008583691098678403, -122.2504328765106152 ) ) ;
#5062=CARTESIAN_POINT ( 'NONE',  ( 23.14999999999999503, 6.550000000011156231, -155.2500000000000284 ) ) ;
#5087=CARTESIAN_POINT ( 'NONE',  ( 19.75857864376268935, 11.65000000001115943, -158.7500000000000284 ) ) ;
#5108=DIRECTION ( 'NONE',  ( 0.000000000000000000, 0.000000000000000000, 1.000000000000000000 ) ) ;
#5139=CIRCLE ( 'NONE', #75915, 0.09999999999998898659 ) ;
#5156=DIRECTION ( 'NONE',  ( 0.000000000000000000, 0.000000000000000000, -1.000000000000000000 ) ) ;
#5164=ORIENTED_EDGE ( 'NONE', *, *, #218595, .F. ) ;
#5180=LINE ( 'NONE', #243818, #171590 ) ;
#5242=CARTESIAN_POINT ( 'NONE',  ( -23.15000000000000213, 1.115600667400684642E-11, -134.0000000000000000 ) ) ;
#5257=ORIENTED_EDGE ( 'NONE', *, *, #248881, .F. ) ;
#5268=DIRECTION ( 'NONE',  ( 0.000000000000000000, 0.000000000000000000, -1.000000000000000000 ) ) ;
#5271=DIRECTION ( 'NONE',  ( 0.000000000000000000, 1.897661533703519897E-16, -1.000000000000000000 ) ) ;
#5303=FACE_OUTER_BOUND ( 'NONE', #73296, .T. ) ;
#5339=TOROIDAL_SURFACE ( 'NONE', #55389, 0.4000000000000010214, 0.1000000000000000056 ) ;
#5375=B_SPLINE_CURVE_WITH_KNOTS ( 'NONE', 3,
 ( #77278, #156859, #155582, #57709, #39484, #159409, #60280, #178999, #237651, #198516 ),
 .UNSPECIFIED., .F., .F.,
 ( 4, 2, 2, 2, 4 ),
 ( 0.000000000000000000, 4.221631689691002302E-05, 8.443263379382004604E-05, 0.0001688652675875677487, 0.0003377305351749838717 ),
 .UNSPECIFIED. ) ;
#5396=ORIENTED_EDGE ( 'NONE', *, *, #163258, .F. ) ;
#5400=CARTESIAN_POINT ( 'NONE',  ( -20.94999999999999929, 1.835341550235567887, -145.5551512925629822 ) ) ;
#5423=CIRCLE ( 'NONE', #109491, 4.000000000000003553 ) ;
#5428=DIRECTION ( 'NONE',  ( 1.000000000000000000, 0.000000000000000000, -0.000000000000000000 ) ) ;
#5441=EDGE_CURVE ( 'NONE', #13799, #85212, #56825, .T. ) ;
#5492=AXIS2_PLACEMENT_3D ( 'NONE', #118115, #215910, #52998 ) ;
#5507=CARTESIAN_POINT ( 'NONE',  ( -23.15000000000000213, 1.115600667400684642E-11, -134.0000000000000000 ) ) ;
#5546=LINE ( 'NONE', #227177, #18846 ) ;
#5554=DIRECTION ( 'NONE',  ( 1.000000000000000000, 0.000000000000000000, -0.000000000000000000 ) ) ;
#5614=ORIENTED_EDGE ( 'NONE', *, *, #113183, .T. ) ;
#5625=VECTOR ( 'NONE', #40415, 1000.000000000000000 ) ;
#5628=PLANE ( 'NONE',  #16445 ) ;
#5651=DIRECTION ( 'NONE',  ( 0.000000000000000000, 0.000000000000000000, -1.000000000000000000 ) ) ;
#5680=CYLINDRICAL_SURFACE ( 'NONE', #99218, 0.09999999999998898659 ) ;
#5749=EDGE_CURVE ( 'NONE', #45962, #165391, #119411, .T. ) ;
#5844=AXIS2_PLACEMENT_3D ( 'NONE', #92228, #51805, #130070 ) ;
#5872=EDGE_LOOP ( 'NONE', ( #232333, #241894, #46898, #25422 ) ) ;
#5922=ORIENTED_EDGE ( 'NONE', *, *, #28924, .T. ) ;
#5925=VERTEX_POINT ( 'NONE', #136778 ) ;
#5927=CARTESIAN_POINT ( 'NONE',  ( 21.00000000000000000, 9.750000000011153745, -146.3500000000000227 ) ) ;
#6006=CIRCLE ( 'NONE', #155889, 4.049999999999998046 ) ;
#6048=TOROIDAL_SURFACE ( 'NONE', #39418, 12.97499999999999787, 0.1000000000000000056 ) ;
#6067=CARTESIAN_POINT ( 'NONE',  ( 18.49999999999999289, 11.65000000001115943, -158.8500000000000227 ) ) ;
#6087=ORIENTED_EDGE ( 'NONE', *, *, #186968, .T. ) ;
#6095=CARTESIAN_POINT ( 'NONE',  ( 18.49999999999998934, 6.650000000011155876, -146.3500000000000227 ) ) ;
#6117=CARTESIAN_POINT ( 'NONE',  ( -20.85000000000000142, 10.33248238083634440, -173.0948465439131496 ) ) ;
#6121=EDGE_CURVE ( 'NONE', #47961, #246321, #58512, .T. ) ;
#6133=CIRCLE ( 'NONE', #210175, 0.09999999999999939493 ) ;
#6164=EDGE_CURVE ( 'NONE', #123515, #162622, #227930, .T. ) ;
#6192=LINE ( 'NONE', #24504, #218486 ) ;
#6215=CARTESIAN_POINT ( 'NONE',  ( -21.14999999999999858, 0.09779029131994770863, -127.7421853895239252 ) ) ;
#6216=DIRECTION ( 'NONE',  ( 0.000000000000000000, 0.000000000000000000, -1.000000000000000000 ) ) ;
#6229=AXIS2_PLACEMENT_3D ( 'NONE', #228561, #109867, #130726 ) ;
#6269=ORIENTED_EDGE ( 'NONE', *, *, #192947, .T. ) ;
#6295=ORIENTED_EDGE ( 'NONE', *, *, #119877, .F. ) ;
#6305=EDGE_CURVE ( 'NONE', #135871, #189087, #132067, .T. ) ;
#6309=VERTEX_POINT ( 'NONE', #52120 ) ;
#6315=DIRECTION ( 'NONE',  ( 0.000000000000000000, 4.336808689942494997E-15, -1.000000000000000000 ) ) ;
#6317=FACE_OUTER_BOUND ( 'NONE', #136998, .T. ) ;
#6323=LINE ( 'NONE', #66317, #75083 ) ;
#6338=EDGE_LOOP ( 'NONE', ( #138069, #96805, #146440, #85639, #237293, #119797, #214292, #19813, #201555, #226893, #63864, #34099, #246031, #198278, #182307, #138358, #110013, #79622, #4831, #258028, #43273, #38444, #115687, #99190, #85011 ) ) ;
#6367=EDGE_CURVE ( 'NONE', #114275, #169539, #111221, .T. ) ;
#6468=ORIENTED_EDGE ( 'NONE', *, *, #228087, .T. ) ;
#6476=DIRECTION ( 'NONE',  ( -3.787827842127535236E-15, 0.7397360091702777085, 0.6728971962616808744 ) ) ;
#6563=EDGE_LOOP ( 'NONE', ( #198308, #69993, #18518, #163987 ) ) ;
#6581=CARTESIAN_POINT ( 'NONE',  ( 21.05000000000000071, 5.850000000011156942, -157.3675027757221017 ) ) ;
#6597=VECTOR ( 'NONE', #2390, 1000.000000000000000 ) ;
#6646=B_SPLINE_CURVE_WITH_KNOTS ( 'NONE', 3,
 ( #211395, #31505, #73199, #150155, #13204, #253070, #34078, #247940, #9332, #113574 ),
 .UNSPECIFIED., .F., .F.,
 ( 4, 2, 2, 2, 4 ),
 ( 0.000000000000000000, 0.0001584437871624345463, 0.0002376656807436883299, 0.0002772766275343508378, 0.0003168875743250132914 ),
 .UNSPECIFIED. ) ;
#6647=DIRECTION ( 'NONE',  ( 0.000000000000000000, 0.2605042016806672911, -0.9654727137038716656 ) ) ;
#6708=DIRECTION ( 'NONE',  ( 2.952720810173289112E-16, -1.000000000000000000, -0.000000000000000000 ) ) ;
#6731=EDGE_CURVE ( 'NONE', #159966, #217031, #131686, .T. ) ;
#6773=EDGE_CURVE ( 'NONE', #91812, #180800, #33600, .T. ) ;
#6776=DIRECTION ( 'NONE',  ( 0.000000000000000000, 0.000000000000000000, -1.000000000000000000 ) ) ;
#6792=DIRECTION ( 'NONE',  ( -1.000000000000000000, 0.000000000000000000, 0.000000000000000000 ) ) ;
#6811=LINE ( 'NONE', #247984, #69995 ) ;
#6813=ORIENTED_EDGE ( 'NONE', *, *, #218258, .T. ) ;
#6824=EDGE_CURVE ( 'NONE', #174969, #245418, #65216, .T. ) ;
#6858=ORIENTED_EDGE ( 'NONE', *, *, #138586, .T. ) ;
#6872=DIRECTION ( 'NONE',  ( 0.000000000000000000, 0.000000000000000000, -1.000000000000000000 ) ) ;
#6875=ORIENTED_EDGE ( 'NONE', *, *, #256861, .F. ) ;
#6888=LINE ( 'NONE', #86395, #93401 ) ;
#6900=CIRCLE ( 'NONE', #40250, 11.75000000000001066 ) ;
#6937=CARTESIAN_POINT ( 'NONE',  ( -21.05000000000000071, -11.41227409413852989, -137.0000000000000000 ) ) ;
#6950=ORIENTED_EDGE ( 'NONE', *, *, #133997, .F. ) ;
#6997=CIRCLE ( 'NONE', #231888, 7.899999999999990585 ) ;
#7007=ORIENTED_EDGE ( 'NONE', *, *, #37064, .T. ) ;
#7008=CARTESIAN_POINT ( 'NONE',  ( 23.15000000000000213, -11.74999999998883560, -164.4000000000000057 ) ) ;
#7046=ORIENTED_EDGE ( 'NONE', *, *, #66721, .T. ) ;
#7078=CIRCLE ( 'NONE', #236039, 0.09999999999998898659 ) ;
#7095=DIRECTION ( 'NONE',  ( 0.000000000000000000, 0.000000000000000000, -1.000000000000000000 ) ) ;
#7114=EDGE_CURVE ( 'NONE', #123224, #33432, #36211, .T. ) ;
#7158=ORIENTED_EDGE ( 'NONE', *, *, #140661, .T. ) ;
#7159=DIRECTION ( 'NONE',  ( 0.000000000000000000, 0.000000000000000000, -1.000000000000000000 ) ) ;
#7205=ORIENTED_EDGE ( 'NONE', *, *, #63089, .T. ) ;
#7207=ORIENTED_EDGE ( 'NONE', *, *, #94401, .F. ) ;
#7303=CARTESIAN_POINT ( 'NONE',  ( -21.05000000000000071, 1.162701749949165642, -142.1000000000000227 ) ) ;
#7324=AXIS2_PLACEMENT_3D ( 'NONE', #133229, #212776, #41854 ) ;
#7342=DIRECTION ( 'NONE',  ( -1.000000000000000000, 0.000000000000000000, 0.000000000000000000 ) ) ;
#7354=DIRECTION ( 'NONE',  ( 0.000000000000000000, 0.6728971962617483760, -0.7397360091702162022 ) ) ;
#7359=CARTESIAN_POINT ( 'NONE',  ( -21.64999999999999858, 7.250000000011148416, -155.2500000000000284 ) ) ;
#7374=FACE_OUTER_BOUND ( 'NONE', #27606, .T. ) ;
#7378=VECTOR ( 'NONE', #12927, 1000.000000000000000 ) ;
#7405=CYLINDRICAL_SURFACE ( 'NONE', #234567, 0.09999999999999939493 ) ;
#7426=EDGE_CURVE ( 'NONE', #79795, #171400, #40507, .T. ) ;
#7438=CARTESIAN_POINT ( 'NONE',  ( 21.00000000000000000, 9.750000000011153745, -146.2500000000000284 ) ) ;
#7458=ADVANCED_FACE ( 'NONE', ( #81011 ), #236093, .F. ) ;
#7471=VERTEX_POINT ( 'NONE', #130426 ) ;
#7484=CARTESIAN_POINT ( 'NONE',  ( 22.39999999999999858, 7.790779598384538929, -133.9000000000000057 ) ) ;
#7498=ORIENTED_EDGE ( 'NONE', *, *, #197054, .F. ) ;
#7501=CIRCLE ( 'NONE', #136674, 11.80000000000000426 ) ;
#7502=DIRECTION ( 'NONE',  ( 0.000000000000000000, 0.000000000000000000, 1.000000000000000000 ) ) ;
#7553=AXIS2_PLACEMENT_3D ( 'NONE', #221879, #39459, #118971 ) ;
#7586=DIRECTION ( 'NONE',  ( 1.000000000000000000, -0.000000000000000000, -0.000000000000000000 ) ) ;
#7587=CARTESIAN_POINT ( 'NONE',  ( 21.05000000000000071, -9.499999999988844479, -157.6060308773475640 ) ) ;
#7594=ORIENTED_EDGE ( 'NONE', *, *, #132477, .T. ) ;
#7609=ORIENTED_EDGE ( 'NONE', *, *, #157263, .T. ) ;
#7614=DIRECTION ( 'NONE',  ( 0.000000000000000000, -1.000000000000000000, -0.000000000000000000 ) ) ;
#7645=VERTEX_POINT ( 'NONE', #176006 ) ;
#7648=CARTESIAN_POINT ( 'NONE',  ( -20.54999999999999716, 1.115600667400684642E-11, -167.5000000000000284 ) ) ;
#7656=AXIS2_PLACEMENT_3D ( 'NONE', #220481, #198330, #40587 ) ;
#7660=CARTESIAN_POINT ( 'NONE',  ( 21.05000000000000071, -1.162701749926853712, -141.9000000000000341 ) ) ;
#7668=ORIENTED_EDGE ( 'NONE', *, *, #193963, .T. ) ;
#7675=DIRECTION ( 'NONE',  ( 0.000000000000000000, -1.000000000000000000, 0.000000000000000000 ) ) ;
#7700=EDGE_LOOP ( 'NONE', ( #30733, #119395, #108441, #79226 ) ) ;
#7709=CARTESIAN_POINT ( 'NONE',  ( 20.94999999999999929, -9.399999999988844834, -157.6060308773475640 ) ) ;
#7727=CARTESIAN_POINT ( 'NONE',  ( 18.50000000000000355, -9.421456145483672273, -141.2419820840187015 ) ) ;
#7738=VERTEX_POINT ( 'NONE', #243651 ) ;
#7742=CARTESIAN_POINT ( 'NONE',  ( 21.07954640115206502, 0.06600770715102041719, -127.6707123039770835 ) ) ;
#7744=CARTESIAN_POINT ( 'NONE',  ( 22.60000000000000142, 1.115600667400684642E-11, -134.0000000000000000 ) ) ;
#7752=AXIS2_PLACEMENT_3D ( 'NONE', #142539, #61733, #242929 ) ;
#7755=ORIENTED_EDGE ( 'NONE', *, *, #129732, .F. ) ;
#7780=ORIENTED_EDGE ( 'NONE', *, *, #178777, .F. ) ;
#7785=DIRECTION ( 'NONE',  ( 1.000000000000000000, 0.000000000000000000, 0.000000000000000000 ) ) ;
#7811=ADVANCED_FACE ( 'NONE', ( #42892 ), #194793, .F. ) ;
#7843=ORIENTED_EDGE ( 'NONE', *, *, #71335, .T. ) ;
#7868=ORIENTED_EDGE ( 'NONE', *, *, #46523, .F. ) ;
#7887=AXIS2_PLACEMENT_3D ( 'NONE', #167629, #187189, #154497 ) ;
#7926=CARTESIAN_POINT ( 'NONE',  ( 20.94999999999999574, -11.48912529306490349, -137.1000000000000227 ) ) ;
#7936=DIRECTION ( 'NONE',  ( 0.000000000000000000, 0.000000000000000000, -1.000000000000000000 ) ) ;
#7971=CARTESIAN_POINT ( 'NONE',  ( 23.14999999999999858, 5.000000000011153745, -155.0947339810869323 ) ) ;
#7975=DIRECTION ( 'NONE',  ( -4.448008912761043807E-16, 1.000000000000000000, 0.000000000000000000 ) ) ;
#7980=DIRECTION ( 'NONE',  ( 1.000000000000000000, 0.000000000000000000, 0.000000000000000000 ) ) ;
#7982=EDGE_CURVE ( 'NONE', #155422, #159476, #203135, .T. ) ;
#8009=CARTESIAN_POINT ( 'NONE',  ( -23.25000000000000000, 4.350000000011156054, -146.2500000000000284 ) ) ;
#8013=DIRECTION ( 'NONE',  ( 0.000000000000000000, 0.000000000000000000, -1.000000000000000000 ) ) ;
#8029=TOROIDAL_SURFACE ( 'NONE', #20501, 11.70000000000000107, 0.1000000000000000056 ) ;
#8049=VERTEX_POINT ( 'NONE', #173154 ) ;
#8056=CARTESIAN_POINT ( 'NONE',  ( 18.49999999999999289, 10.25000000001115730, -158.6499999999999773 ) ) ;
#8062=B_SPLINE_CURVE_WITH_KNOTS ( 'NONE', 3,
 ( #219873, #17811, #195213, #253853, #118214, #176931, #97326, #41276, #59481, #56916 ),
 .UNSPECIFIED., .F., .F.,
 ( 4, 3, 3, 4 ),
 ( 0.000000000000000000, 0.0002000000000002884074, 0.001000000000045112589, 0.001967863649472103085 ),
 .UNSPECIFIED. ) ;
#8068=ORIENTED_EDGE ( 'NONE', *, *, #80450, .T. ) ;
#8081=CARTESIAN_POINT ( 'NONE',  ( 18.59999999999999076, 10.20857864377385127, -155.3500000000000227 ) ) ;
#8099=DIRECTION ( 'NONE',  ( 0.000000000000000000, 0.000000000000000000, -1.000000000000000000 ) ) ;
#8102=CARTESIAN_POINT ( 'NONE',  ( -23.15000000000000213, -8.663551401858004652, -143.5241011180673070 ) ) ;
#8109=LINE ( 'NONE', #107186, #126598 ) ;
#8198=PLANE ( 'NONE',  #52843 ) ;
#8211=VERTEX_POINT ( 'NONE', #221196 ) ;
#8215=CARTESIAN_POINT ( 'NONE',  ( 20.11144452914042091, 9.933610851134151432, -141.8902934539496243 ) ) ;
#8239=DIRECTION ( 'NONE',  ( 0.000000000000000000, 0.000000000000000000, 1.000000000000000000 ) ) ;
#8284=EDGE_CURVE ( 'NONE', #111708, #162622, #7501, .T. ) ;
#8286=CIRCLE ( 'NONE', #187911, 0.5000000000000004441 ) ;
#8288=EDGE_CURVE ( 'NONE', #13316, #159346, #153301, .T. ) ;
#8349=VERTEX_POINT ( 'NONE', #206787 ) ;
#8351=VERTEX_POINT ( 'NONE', #90676 ) ;
#8385=AXIS2_PLACEMENT_3D ( 'NONE', #32676, #27536, #211270 ) ;
#8389=VERTEX_POINT ( 'NONE', #151975 ) ;
#8501=ADVANCED_FACE ( 'NONE', ( #63099 ), #162239, .T. ) ;
#8502=CARTESIAN_POINT ( 'NONE',  ( 20.94999999999999929, -11.64999999998883595, -167.5000000000000000 ) ) ;
#8507=ADVANCED_FACE ( 'NONE', ( #41012 ), #160948, .T. ) ;
#8512=CIRCLE ( 'NONE', #141776, 0.09999999999999817368 ) ;
#8568=DIRECTION ( 'NONE',  ( 0.000000000000000000, -1.000000000000000000, 0.000000000000000000 ) ) ;
#8588=CARTESIAN_POINT ( 'NONE',  ( -18.59999999999999787, 11.65000000001115232, -146.1500000000000341 ) ) ;
#8592=DIRECTION ( 'NONE',  ( 0.000000000000000000, 0.000000000000000000, -1.000000000000000000 ) ) ;
#8602=VECTOR ( 'NONE', #204065, 1000.000000000000000 ) ;
#8610=CARTESIAN_POINT ( 'NONE',  ( 22.50000000000000000, 11.64957080755595520, -133.9000000000000057 ) ) ;
#8663=DIRECTION ( 'NONE',  ( 1.000000000000000000, -0.000000000000000000, -0.000000000000000000 ) ) ;
#8686=CARTESIAN_POINT ( 'NONE',  ( -23.25000000000000000, 11.75000000001115552, -146.1500000000000341 ) ) ;
#8689=DIRECTION ( 'NONE',  ( -1.000000000000000000, 0.000000000000000000, 0.000000000000000000 ) ) ;
#8714=EDGE_LOOP ( 'NONE', ( #255498, #165470, #247723, #119550 ) ) ;
#8726=DIRECTION ( 'NONE',  ( 0.000000000000000000, 0.000000000000000000, -1.000000000000000000 ) ) ;
#8732=ORIENTED_EDGE ( 'NONE', *, *, #61703, .T. ) ;
#8811=DIRECTION ( 'NONE',  ( 0.000000000000000000, 1.000000000000000000, 0.000000000000000000 ) ) ;
#8834=CARTESIAN_POINT ( 'NONE',  ( 20.94999999999999929, 1.115600667400684642E-11, -167.5000000000000284 ) ) ;
#8836=DIRECTION ( 'NONE',  ( 1.000000000000000000, 0.000000000000000000, -0.000000000000000000 ) ) ;
#8841=CIRCLE ( 'NONE', #174928, 0.09999999999998898659 ) ;
#8844=AXIS2_PLACEMENT_3D ( 'NONE', #3523, #139167, #180897 ) ;
#8873=CARTESIAN_POINT ( 'NONE',  ( -21.07933241753356413, 0.09337959043042155793, -127.6713540516202841 ) ) ;
#8880=ORIENTED_EDGE ( 'NONE', *, *, #155449, .F. ) ;
#8888=DIRECTION ( 'NONE',  ( 0.000000000000000000, 0.000000000000000000, -1.000000000000000000 ) ) ;
#8908=CARTESIAN_POINT ( 'NONE',  ( -21.05000000000000071, 11.65000000001115232, -140.7838656629781724 ) ) ;
#8933=AXIS2_PLACEMENT_3D ( 'NONE', #215153, #78196, #33993 ) ;
#8935=EDGE_LOOP ( 'NONE', ( #88604, #159533, #142555, #252267 ) ) ;
#8953=DIRECTION ( 'NONE',  ( 0.000000000000000000, -5.204170427930272346E-14, -1.000000000000000000 ) ) ;
#8967=ORIENTED_EDGE ( 'NONE', *, *, #50616, .F. ) ;
#9008=VERTEX_POINT ( 'NONE', #84569 ) ;
#9060=CARTESIAN_POINT ( 'NONE',  ( -23.15000000000000213, 4.250000000011156409, -146.2500000000000284 ) ) ;
#9066=EDGE_LOOP ( 'NONE', ( #53795, #98468, #10820, #242292 ) ) ;
#9075=CIRCLE ( 'NONE', #129856, 0.2000000000000057288 ) ;
#9095=AXIS2_PLACEMENT_3D ( 'NONE', #115723, #195286, #58290 ) ;
#9139=EDGE_LOOP ( 'NONE', ( #207304, #218850, #222035, #211932 ) ) ;
#9151=EDGE_CURVE ( 'NONE', #160216, #86831, #252666, .T. ) ;
#9154=ORIENTED_EDGE ( 'NONE', *, *, #53244, .F. ) ;
#9159=EDGE_CURVE ( 'NONE', #38036, #26254, #117023, .T. ) ;
#9168=CARTESIAN_POINT ( 'NONE',  ( 20.94999999999999929, 1.115600667400684642E-11, -167.5000000000000284 ) ) ;
#9175=EDGE_CURVE ( 'NONE', #241842, #198298, #95548, .T. ) ;
#9192=DIRECTION ( 'NONE',  ( 0.000000000000000000, 0.000000000000000000, 1.000000000000000000 ) ) ;
#9206=VECTOR ( 'NONE', #144673, 1000.000000000000000 ) ;
#9207=DIRECTION ( 'NONE',  ( 0.000000000000000000, -0.8700118002898322711, 0.4930308989875231140 ) ) ;
#9210=EDGE_CURVE ( 'NONE', #48580, #187169, #245401, .T. ) ;
#9219=ADVANCED_FACE ( 'NONE', ( #216111 ), #175739, .T. ) ;
#9227=DIRECTION ( 'NONE',  ( 0.000000000000000000, -1.265107689135680095E-16, 1.000000000000000000 ) ) ;
#9245=TOROIDAL_SURFACE ( 'NONE', #92438, 0.4000000000000005773, 0.1000000000000000056 ) ;
#9246=EDGE_CURVE ( 'NONE', #34631, #251858, #12192, .T. ) ;
#9306=DIRECTION ( 'NONE',  ( 0.000000000000000000, 0.000000000000000000, -1.000000000000000000 ) ) ;
#9307=CYLINDRICAL_SURFACE ( 'NONE', #103824, 0.09999999999998898659 ) ;
#9324=CARTESIAN_POINT ( 'NONE',  ( 18.56308993302939925, 10.38069115533503961, -158.7392226389382870 ) ) ;
#9330=EDGE_CURVE ( 'NONE', #144444, #18380, #3960, .T. ) ;
#9331=ORIENTED_EDGE ( 'NONE', *, *, #112672, .T. ) ;
#9332=CARTESIAN_POINT ( 'NONE',  ( 18.41356215285961184, -9.499999999988865795, -141.0320693966996544 ) ) ;
#9340=DIRECTION ( 'NONE',  ( 0.000000000000000000, -1.000000000000000000, -2.891205793294679805E-16 ) ) ;
#9348=AXIS2_PLACEMENT_3D ( 'NONE', #64988, #183669, #84506 ) ;
#9350=DIRECTION ( 'NONE',  ( 1.000000000000000000, 0.000000000000000000, 0.000000000000000000 ) ) ;
#9379=EDGE_CURVE ( 'NONE', #25295, #184016, #111584, .T. ) ;
#9400=CARTESIAN_POINT ( 'NONE',  ( 20.94999999999999929, 7.120270961708750512, -171.1595630418393625 ) ) ;
#9402=LINE ( 'NONE', #51064, #114930 ) ;
#9435=ORIENTED_EDGE ( 'NONE', *, *, #181041, .F. ) ;
#9450=CIRCLE ( 'NONE', #230211, 0.09999999999999939493 ) ;
#9466=CARTESIAN_POINT ( 'NONE',  ( -21.14999999999999858, 11.65000000001115588, -134.1000000000000227 ) ) ;
#9492=ORIENTED_EDGE ( 'NONE', *, *, #147576, .F. ) ;
#9519=VECTOR ( 'NONE', #579, 1000.000000000000000 ) ;
#9525=DIRECTION ( 'NONE',  ( 1.000000000000000000, 3.265361837132813093E-16, -0.000000000000000000 ) ) ;
#9546=ADVANCED_FACE ( 'NONE', ( #75054 ), #154590, .T. ) ;
#9590=ORIENTED_EDGE ( 'NONE', *, *, #12345, .F. ) ;
#9602=DIRECTION ( 'NONE',  ( -0.000000000000000000, -1.000000000000000000, -5.421010862427649374E-16 ) ) ;
#9603=AXIS2_PLACEMENT_3D ( 'NONE', #86969, #11319, #205648 ) ;
#9606=CIRCLE ( 'NONE', #209518, 0.1000000000000060701 ) ;
#9612=ADVANCED_FACE ( 'NONE', ( #117996 ), #114135, .F. ) ;
#9618=CARTESIAN_POINT ( 'NONE',  ( -23.25000000000000000, 1.115600667400684642E-11, -167.5000000000000284 ) ) ;
#9631=EDGE_CURVE ( 'NONE', #11797, #189027, #78846, .T. ) ;
#9695=LINE ( 'NONE', #248314, #17435 ) ;
#9714=CARTESIAN_POINT ( 'NONE',  ( -20.64999999999999858, 4.350000000011156054, -146.3500000000000227 ) ) ;
#9716=DIRECTION ( 'NONE',  ( 0.000000000000000000, 0.000000000000000000, -1.000000000000000000 ) ) ;
#9743=AXIS2_PLACEMENT_3D ( 'NONE', #171070, #194464, #193170 ) ;
#9754=FACE_OUTER_BOUND ( 'NONE', #156684, .T. ) ;
#9768=TOROIDAL_SURFACE ( 'NONE', #218044, 11.65000000000000036, 0.1000000000000000056 ) ;
#9788=AXIS2_PLACEMENT_3D ( 'NONE', #87704, #229798, #90271 ) ;
#9795=DIRECTION ( 'NONE',  ( 0.000000000000000000, 0.000000000000000000, -1.000000000000000000 ) ) ;
#9878=AXIS2_PLACEMENT_3D ( 'NONE', #176923, #76496, #60780 ) ;
#9940=EDGE_CURVE ( 'NONE', #154105, #203005, #112496, .T. ) ;
#9950=EDGE_CURVE ( 'NONE', #102830, #200535, #56416, .T. ) ;
#9964=CYLINDRICAL_SURFACE ( 'NONE', #54112, 11.80000000000000426 ) ;
#9967=CARTESIAN_POINT ( 'NONE',  ( -22.50000000000000000, 11.64957080755595520, -133.9000000000000057 ) ) ;
#9989=CARTESIAN_POINT ( 'NONE',  ( -20.94999027547553894, 10.29326151435327219, -172.9592822510415147 ) ) ;
#10005=AXIS2_PLACEMENT_3D ( 'NONE', #90717, #110282, #150706 ) ;
#10015=CARTESIAN_POINT ( 'NONE',  ( 20.04142135623730070, 11.75000000001115907, -158.6500000000000057 ) ) ;
#10016=ORIENTED_EDGE ( 'NONE', *, *, #131462, .F. ) ;
#10037=ORIENTED_EDGE ( 'NONE', *, *, #42460, .F. ) ;
#10094=ORIENTED_EDGE ( 'NONE', *, *, #256177, .F. ) ;
#10122=DIRECTION ( 'NONE',  ( -1.000000000000000000, -0.000000000000000000, 0.000000000000000000 ) ) ;
#10132=EDGE_CURVE ( 'NONE', #123224, #87130, #242274, .T. ) ;
#10146=AXIS2_PLACEMENT_3D ( 'NONE', #212663, #148840, #110983 ) ;
#10159=DIRECTION ( 'NONE',  ( 0.000000000000000000, 0.000000000000000000, -1.000000000000000000 ) ) ;
#10164=EDGE_CURVE ( 'NONE', #161970, #100003, #142324, .T. ) ;
#10180=TOROIDAL_SURFACE ( 'NONE', #43484, 11.70000000000000639, 0.1000000000000000056 ) ;
#10208=EDGE_CURVE ( 'NONE', #143423, #33482, #246400, .T. ) ;
#10219=CARTESIAN_POINT ( 'NONE',  ( 18.60000000000000497, 1.115600667400684642E-11, -134.0000000000000000 ) ) ;
#10233=ADVANCED_FACE ( 'NONE', ( #69209 ), #63202, .T. ) ;
#10277=DIRECTION ( 'NONE',  ( 0.000000000000000000, 1.897661533703519897E-16, -1.000000000000000000 ) ) ;
#10333=ORIENTED_EDGE ( 'NONE', *, *, #160485, .F. ) ;
#10358=PLANE ( 'NONE',  #111275 ) ;
#10375=ORIENTED_EDGE ( 'NONE', *, *, #228913, .F. ) ;
#10379=AXIS2_PLACEMENT_3D ( 'NONE', #110944, #247885, #208774 ) ;
#10395=CARTESIAN_POINT ( 'NONE',  ( -21.14999999999999858, 11.65000000001115588, -134.1000000000000227 ) ) ;
#10412=CARTESIAN_POINT ( 'NONE',  ( -21.14999999999999858, 11.75000000001115552, -134.1000000000000227 ) ) ;
#10442=ORIENTED_EDGE ( 'NONE', *, *, #199545, .T. ) ;
#10451=DIRECTION ( 'NONE',  ( 0.000000000000000000, -0.1568667991644863147, -0.9876197685951252359 ) ) ;
#10469=ORIENTED_EDGE ( 'NONE', *, *, #86991, .T. ) ;
#10484=FACE_OUTER_BOUND ( 'NONE', #49736, .T. ) ;
#10505=ORIENTED_EDGE ( 'NONE', *, *, #102097, .T. ) ;
#10506=DIRECTION ( 'NONE',  ( 0.000000000000000000, 0.000000000000000000, -1.000000000000000000 ) ) ;
#10539=ORIENTED_EDGE ( 'NONE', *, *, #17937, .T. ) ;
#10542=EDGE_CURVE ( 'NONE', #19242, #9008, #21728, .T. ) ;
#10545=LINE ( 'NONE', #47071, #135740 ) ;
#10574=EDGE_CURVE ( 'NONE', #153112, #123515, #3765, .T. ) ;
#10579=CARTESIAN_POINT ( 'NONE',  ( -23.25000000000000000, 2.000000000011154189, -154.2753780772379173 ) ) ;
#10612=EDGE_LOOP ( 'NONE', ( #250563, #91895, #37354, #185187 ) ) ;
#10617=ORIENTED_EDGE ( 'NONE', *, *, #69149, .F. ) ;
#10640=PLANE ( 'NONE',  #230559 ) ;
#10705=EDGE_CURVE ( 'NONE', #56702, #126714, #27215, .T. ) ;
#10706=CIRCLE ( 'NONE', #231293, 0.09999999999998898659 ) ;
#10710=CARTESIAN_POINT ( 'NONE',  ( 23.14999999999999858, 5.000000000011153745, -155.0947339810869323 ) ) ;
#10711=ORIENTED_EDGE ( 'NONE', *, *, #194735, .F. ) ;
#10725=ORIENTED_EDGE ( 'NONE', *, *, #255545, .F. ) ;
#10731=ORIENTED_EDGE ( 'NONE', *, *, #15932, .T. ) ;
#10743=CIRCLE ( 'NONE', #256371, 0.8750000000000007772 ) ;
#10745=AXIS2_PLACEMENT_3D ( 'NONE', #101978, #179022, #2893 ) ;
#10750=CARTESIAN_POINT ( 'NONE',  ( 22.57856590037848932, -0.004128330053175053270, -122.2499415373245739 ) ) ;
#10768=ORIENTED_EDGE ( 'NONE', *, *, #29607, .T. ) ;
#10820=ORIENTED_EDGE ( 'NONE', *, *, #234795, .F. ) ;
#10851=FACE_OUTER_BOUND ( 'NONE', #184599, .T. ) ;
#10898=ADVANCED_FACE ( 'NONE', ( #101220 ), #23127, .T. ) ;
#10910=EDGE_CURVE ( 'NONE', #160216, #209723, #51081, .T. ) ;
#10916=CARTESIAN_POINT ( 'NONE',  ( 20.94999999999999929, 11.65000000001115943, -160.7161343370219129 ) ) ;
#10922=DIRECTION ( 'NONE',  ( 0.000000000000000000, 0.000000000000000000, -1.000000000000000000 ) ) ;
#10931=FACE_OUTER_BOUND ( 'NONE', #27384, .T. ) ;
#10939=VECTOR ( 'NONE', #23021, 1000.000000000000114 ) ;
#11010=ADVANCED_FACE ( 'NONE', ( #68570 ), #13536, .F. ) ;
#11045=CARTESIAN_POINT ( 'NONE',  ( 20.94999999999999929, -11.48912529306489994, -164.5000000000000000 ) ) ;
#11051=CARTESIAN_POINT ( 'NONE',  ( -21.55000000000000071, 7.350000000011155166, -146.2500000000000284 ) ) ;
#11121=ADVANCED_FACE ( 'NONE', ( #231501 ), #69868, .T. ) ;
#11138=CARTESIAN_POINT ( 'NONE',  ( -20.64999999999999858, 4.250000000011156409, -146.3500000000000227 ) ) ;
#11142=CARTESIAN_POINT ( 'NONE',  ( 21.05000000000000071, -8.730841121484171907, -143.5980747189843783 ) ) ;
#11156=CARTESIAN_POINT ( 'NONE',  ( -23.25000000000000000, -1.249999999988843369, -175.3004807544151049 ) ) ;
#11174=VERTEX_POINT ( 'NONE', #228925 ) ;
#11200=CARTESIAN_POINT ( 'NONE',  ( -20.54999999999999716, 1.925233644870967487, -154.7697564668738721 ) ) ;
#11203=CARTESIAN_POINT ( 'NONE',  ( -21.40925344232282512, 6.658518859401606704, -133.9010498113803749 ) ) ;
#11243=CARTESIAN_POINT ( 'NONE',  ( 18.50000000000000355, -9.399999999988841282, -174.3820418481727188 ) ) ;
#11264=CARTESIAN_POINT ( 'NONE',  ( -20.54999999999999716, 1.115600667400684642E-11, -167.5000000000000284 ) ) ;
#11267=ORIENTED_EDGE ( 'NONE', *, *, #48514, .F. ) ;
#11290=AXIS2_PLACEMENT_3D ( 'NONE', #66628, #84860, #243971 ) ;
#11319=DIRECTION ( 'NONE',  ( 0.000000000000000000, 0.000000000000000000, -1.000000000000000000 ) ) ;
#11353=PRODUCT_DEFINITION_FORMATION_WITH_SPECIFIED_SOURCE ( 'ANY', '', #151478, .NOT_KNOWN. ) ;
#11357=CIRCLE ( 'NONE', #186140, 0.09999999999999939493 ) ;
#11358=CARTESIAN_POINT ( 'NONE',  ( -20.64999999999999858, 7.250000000011155521, -155.2500000000000284 ) ) ;
#11370=CARTESIAN_POINT ( 'NONE',  ( -23.15000000000000213, -9.499999999988848032, -143.8939691226524644 ) ) ;
#11371=AXIS2_PLACEMENT_3D ( 'NONE', #214657, #56839, #156002 ) ;
#11384=DIRECTION ( 'NONE',  ( 1.000000000000000000, 0.000000000000000000, 0.000000000000000000 ) ) ;
#11395=VERTEX_POINT ( 'NONE', #11842 ) ;
#11406=DIRECTION ( 'NONE',  ( -0.000000000000000000, 0.9876197685951276783, 0.1568667991644721316 ) ) ;
#11433=CARTESIAN_POINT ( 'NONE',  ( -18.50000000000000000, 1.162701749949165642, -142.1000000000000227 ) ) ;
#11454=DIRECTION ( 'NONE',  ( -0.000000000000000000, 0.000000000000000000, -1.000000000000000000 ) ) ;
#11455=LINE ( 'NONE', #70158, #57004 ) ;
#11460=EDGE_LOOP ( 'NONE', ( #140001, #110418, #188061, #219472 ) ) ;
#11473=ORIENTED_EDGE ( 'NONE', *, *, #137043, .F. ) ;
#11474=ORIENTED_EDGE ( 'NONE', *, *, #134225, .F. ) ;
#11500=ORIENTED_EDGE ( 'NONE', *, *, #139581, .F. ) ;
#11519=DIRECTION ( 'NONE',  ( 0.000000000000000000, 0.000000000000000000, -1.000000000000000000 ) ) ;
#11563=DIRECTION ( 'NONE',  ( 1.000000000000000000, 0.000000000000000000, 0.000000000000000000 ) ) ;
#11578=DIRECTION ( 'NONE',  ( 0.1538461538461510236, 0.9880948137434718559, 0.000000000000000000 ) ) ;
#11579=ADVANCED_FACE ( 'NONE', ( #57337 ), #37825, .F. ) ;
#11596=ORIENTED_EDGE ( 'NONE', *, *, #68975, .T. ) ;
#11615=CARTESIAN_POINT ( 'NONE',  ( 20.84999999999998721, -11.74999999998884448, -167.5000000000000000 ) ) ;
#11617=DIRECTION ( 'NONE',  ( -1.000000000000000000, 0.000000000000000000, 0.000000000000000000 ) ) ;
#11620=DIRECTION ( 'NONE',  ( 0.000000000000000000, 0.000000000000000000, -1.000000000000000000 ) ) ;
#11623=DIRECTION ( 'NONE',  ( 1.000000000000000000, 2.952720810173289112E-16, -0.000000000000000000 ) ) ;
#11643=CIRCLE ( 'NONE', #40872, 0.09999999999999939493 ) ;
#11662=ADVANCED_FACE ( 'NONE', ( #83308 ), #162909, .F. ) ;
#11674=CARTESIAN_POINT ( 'NONE',  ( 23.14999999999999503, 6.550000000011156231, -146.3500000000000227 ) ) ;
#11702=CYLINDRICAL_SURFACE ( 'NONE', #34214, 0.09999999999998898659 ) ;
#11722=VERTEX_POINT ( 'NONE', #243697 ) ;
#11748=ORIENTED_EDGE ( 'NONE', *, *, #235926, .T. ) ;
#11753=ORIENTED_EDGE ( 'NONE', *, *, #97434, .T. ) ;
#11757=( BOUNDED_SURFACE ( )  B_SPLINE_SURFACE ( 3, 2, ( 
 ( #202544, #145122, #207701 ),
 ( #224667, #46032, #66888 ),
 ( #125574, #205092, #105987 ),
 ( #186853, #206402, #162159 ),
 ( #47297, #146399, #225925 ),
 ( #29092, #8215, #27799 ),
 ( #167301, #68174, #48601 ),
 ( #147715, #128158, #188122 ),
 ( #241673, #63023, #142558 ),
 ( #222074, #4328, #43476 ),
 ( #123021, #83835, #112453 ),
 ( #210267, #35505, #90283 ) ),
 .UNSPECIFIED., .F., .F., .F. ) 
 B_SPLINE_SURFACE_WITH_KNOTS ( ( 4, 2, 2, 2, 2, 4 ),
 ( 3, 3 ),
 ( 3.174653483277205090, 3.943930578431714018, 4.713207673586222946, 5.482484768740731873, 5.867123316317986337, 6.251761863895240801 ),
 ( 0.000000000000000000, 1.000000000000000000 ),
 .UNSPECIFIED. ) 
 GEOMETRIC_REPRESENTATION_ITEM ( )  RATIONAL_B_SPLINE_SURFACE ( (
 ( 1.000000000000000000, 0.8659465255642228021, 1.000000000000000000),
 ( 1.000000000000000000, 0.8648614068488691409, 1.000000000000000000),
 ( 1.000000000000000000, 0.8489031841323105843, 1.000000000000000000),
 ( 1.000000000000000000, 0.7927507630162217156, 1.000000000000000000),
 ( 1.000000000000000000, 0.7523013859014273663, 1.000000000000000000),
 ( 1.000000000000000000, 0.6616226951191639394, 1.000000000000000000),
 ( 1.000000000000000000, 0.6112214368725639169, 1.000000000000000000),
 ( 1.000000000000000000, 0.5507684314497727218, 1.000000000000000000),
 ( 1.000000000000000000, 0.5333267243152293169, 1.000000000000000000),
 ( 1.000000000000000000, 0.5084565446480597828, 1.000000000000000000),
 ( 1.000000000000000000, 0.5010722703450565252, 1.000000000000000000),
 ( 1.000000000000000000, 0.5001234037138694299, 1.000000000000000000) ) ) 
 REPRESENTATION_ITEM ( '' )  SURFACE ( )  );
#11768=DIRECTION ( 'NONE',  ( 0.000000000000000000, 0.000000000000000000, -1.000000000000000000 ) ) ;
#11795=CARTESIAN_POINT ( 'NONE',  ( -23.25000000000000000, 11.75000000001115552, -167.5000000000000284 ) ) ;
#11797=VERTEX_POINT ( 'NONE', #226692 ) ;
#11808=CARTESIAN_POINT ( 'NONE',  ( -18.59999999999999787, 1.115600667400684642E-11, -167.5000000000000284 ) ) ;
#11822=AXIS2_PLACEMENT_3D ( 'NONE', #63021, #81281, #184260 ) ;
#11840=DIRECTION ( 'NONE',  ( -1.000000000000000000, -2.952720810173289112E-16, 0.000000000000000000 ) ) ;
#11842=CARTESIAN_POINT ( 'NONE',  ( 23.24999999999999289, 11.65000000001116298, -134.0000000000000000 ) ) ;
#11856=CARTESIAN_POINT ( 'NONE',  ( -23.24999999999999645, -9.599999999988845900, -174.1001893912220737 ) ) ;
#11874=DIRECTION ( 'NONE',  ( 0.000000000000000000, 0.000000000000000000, -1.000000000000000000 ) ) ;
#11900=CARTESIAN_POINT ( 'NONE',  ( -21.05000000000000071, 1.115600667400684642E-11, -167.5000000000000284 ) ) ;
#11907=CARTESIAN_POINT ( 'NONE',  ( 18.59999999999999076, 11.65000000001115943, -158.8500000000000227 ) ) ;
#11910=CARTESIAN_POINT ( 'NONE',  ( 20.94999999999999574, -1.851028230129704522, -145.6539132694225032 ) ) ;
#12051=ADVANCED_FACE ( 'NONE', ( #120906 ), #239544, .F. ) ;
#12066=EDGE_CURVE ( 'NONE', #109393, #256406, #178309, .T. ) ;
#12071=AXIS2_PLACEMENT_3D ( 'NONE', #91897, #72363, #29404 ) ;
#12078=CARTESIAN_POINT ( 'NONE',  ( -20.64999999999999858, -8.999999999988846255, -143.8939691226524644 ) ) ;
#12086=CARTESIAN_POINT ( 'NONE',  ( 18.58222699835054570, 10.33200063080772324, -173.0931674956643178 ) ) ;
#12106=DIRECTION ( 'NONE',  ( 0.000000000000000000, 1.000000000000000000, 0.000000000000000000 ) ) ;
#12111=CIRCLE ( 'NONE', #57847, 0.09999999999999939493 ) ;
#12175=ORIENTED_EDGE ( 'NONE', *, *, #39512, .F. ) ;
#12191=DIRECTION ( 'NONE',  ( -1.000000000000000000, 0.000000000000000000, 0.000000000000000000 ) ) ;
#12192=CIRCLE ( 'NONE', #203865, 0.09999999999998898659 ) ;
#12194=AXIS2_PLACEMENT_3D ( 'NONE', #242576, #219155, #2678 ) ;
#12198=FACE_OUTER_BOUND ( 'NONE', #22720, .T. ) ;
#12216=ORIENTED_EDGE ( 'NONE', *, *, #144821, .T. ) ;
#12222=DIRECTION ( 'NONE',  ( -0.000000000000000000, -0.000000000000000000, 1.000000000000000000 ) ) ;
#12231=FACE_OUTER_BOUND ( 'NONE', #198653, .T. ) ;
#12259=EDGE_CURVE ( 'NONE', #244686, #64807, #176583, .T. ) ;
#12274=CARTESIAN_POINT ( 'NONE',  ( 21.14999999999999858, 0.09779029131994770863, -127.7421853895238968 ) ) ;
#12297=AXIS2_PLACEMENT_3D ( 'NONE', #212563, #135561, #53476 ) ;
#12307=CARTESIAN_POINT ( 'NONE',  ( 21.07888907270776002, 10.72506921352637654, -146.2211935868332091 ) ) ;
#12322=DIRECTION ( 'NONE',  ( -0.000000000000000000, -1.265107689135680095E-16, 1.000000000000000000 ) ) ;
#12330=ORIENTED_EDGE ( 'NONE', *, *, #112389, .T. ) ;
#12335=ORIENTED_EDGE ( 'NONE', *, *, #113986, .F. ) ;
#12345=EDGE_CURVE ( 'NONE', #14142, #214434, #90720, .T. ) ;
#12349=EDGE_CURVE ( 'NONE', #100003, #91601, #121827, .T. ) ;
#12363=CARTESIAN_POINT ( 'NONE',  ( 23.24999999999999645, 1.115600667400684642E-11, -167.5000000000000284 ) ) ;
#12389=DIRECTION ( 'NONE',  ( 0.000000000000000000, 0.000000000000000000, -1.000000000000000000 ) ) ;
#12428=EDGE_CURVE ( 'NONE', #222155, #196636, #22473, .T. ) ;
#12429=ORIENTED_EDGE ( 'NONE', *, *, #105891, .T. ) ;
#12431=VERTEX_POINT ( 'NONE', #159704 ) ;
#12433=DIRECTION ( 'NONE',  ( 0.000000000000000000, 0.000000000000000000, -1.000000000000000000 ) ) ;
#12450=CIRCLE ( 'NONE', #212365, 3.899999999999987033 ) ;
#12464=CARTESIAN_POINT ( 'NONE',  ( 21.07928932188134397, 0.09889514566555242248, -127.6714833436067238 ) ) ;
#12488=CYLINDRICAL_SURFACE ( 'NONE', #102521, 0.09999999999999939493 ) ;
#12513=EDGE_LOOP ( 'NONE', ( #154372, #131344, #178907 ) ) ;
#12537=EDGE_CURVE ( 'NONE', #239010, #59872, #20195, .T. ) ;
#12545=CARTESIAN_POINT ( 'NONE',  ( 18.59999996954842771, -9.523204137847015360, -174.3830417119173433 ) ) ;
#12568=VERTEX_POINT ( 'NONE', #106113 ) ;
#12643=EDGE_LOOP ( 'NONE', ( #151097, #52115, #105909, #239456 ) ) ;
#12644=DIRECTION ( 'NONE',  ( 0.000000000000000000, 0.000000000000000000, -1.000000000000000000 ) ) ;
#12654=AXIS2_PLACEMENT_3D ( 'NONE', #167792, #132488, #247283 ) ;
#12657=CARTESIAN_POINT ( 'NONE',  ( -23.25000000000000000, 2.600000000011156054, -147.2246219227621111 ) ) ;
#12681=VECTOR ( 'NONE', #209, 1000.000000000000114 ) ;
#12718=CIRCLE ( 'NONE', #214, 0.1000000000000098310 ) ;
#12725=DIRECTION ( 'NONE',  ( 0.000000000000000000, 0.1575844902526560010, 0.9875055080513781558 ) ) ;
#12729=CARTESIAN_POINT ( 'NONE',  ( -21.07954763557624744, 0.06587591862980950175, -127.6707090099604471 ) ) ;
#12782=CIRCLE ( 'NONE', #212678, 0.5000000000000004441 ) ;
#12784=DIRECTION ( 'NONE',  ( 1.000000000000000000, 0.000000000000000000, 0.000000000000000000 ) ) ;
#12795=CYLINDRICAL_SURFACE ( 'NONE', #33833, 0.1000000000000101918 ) ;
#12800=EDGE_CURVE ( 'NONE', #17738, #106574, #218415, .T. ) ;
#12819=CARTESIAN_POINT ( 'NONE',  ( 23.15000000000000213, -8.596261682231828516, -158.0498724828497359 ) ) ;
#12857=CARTESIAN_POINT ( 'NONE',  ( 20.94999999999999574, 10.47338541492405994, -141.5786544642485580 ) ) ;
#12858=FACE_OUTER_BOUND ( 'NONE', #151456, .T. ) ;
#12885=CARTESIAN_POINT ( 'NONE',  ( -18.50000000000000000, 9.350000000011156942, -146.1500000000000341 ) ) ;
#12890=EDGE_LOOP ( 'NONE', ( #242595, #237755, #172582, #251650 ) ) ;
#12927=DIRECTION ( 'NONE',  ( 1.000000000000000000, 7.304098846218133681E-16, -4.217023435051677501E-16 ) ) ;
#12968=AXIS2_PLACEMENT_3D ( 'NONE', #133393, #192094, #190827 ) ;
#13023=ADVANCED_FACE ( 'NONE', ( #202365 ), #103241, .F. ) ;
#13044=VECTOR ( 'NONE', #162342, 1000.000000000000000 ) ;
#13109=CARTESIAN_POINT ( 'NONE',  ( -18.59999999999999787, -1.249999999988843369, -142.0000000000000284 ) ) ;
#13110=EDGE_CURVE ( 'NONE', #176594, #85588, #156219, .T. ) ;
#13120=EDGE_CURVE ( 'NONE', #21635, #149328, #34738, .T. ) ;
#13124=DIRECTION ( 'NONE',  ( 0.000000000000000000, 0.000000000000000000, 1.000000000000000000 ) ) ;
#13158=CARTESIAN_POINT ( 'NONE',  ( 21.05000000000000071, 8.876614585098257848, -142.3850804788446851 ) ) ;
#13189=ORIENTED_EDGE ( 'NONE', *, *, #216933, .F. ) ;
#13204=CARTESIAN_POINT ( 'NONE',  ( 18.46858270002952906, -9.474202674699409243, -141.1020219347038847 ) ) ;
#13206=DIRECTION ( 'NONE',  ( 0.000000000000000000, 0.8700118002898321601, -0.4930308989875230030 ) ) ;
#13223=ORIENTED_EDGE ( 'NONE', *, *, #78836, .F. ) ;
#13277=AXIS2_PLACEMENT_3D ( 'NONE', #18618, #177721, #254629 ) ;
#13305=EDGE_CURVE ( 'NONE', #172414, #89589, #69946, .T. ) ;
#13308=AXIS2_PLACEMENT_3D ( 'NONE', #132425, #15056, #172879 ) ;
#13316=VERTEX_POINT ( 'NONE', #169065 ) ;
#13322=CARTESIAN_POINT ( 'NONE',  ( 21.07946286933444568, 0.07668384326755511848, -127.6709626809923179 ) ) ;
#13324=ADVANCED_FACE ( 'NONE', ( #7374 ), #149484, .F. ) ;
#13356=ORIENTED_EDGE ( 'NONE', *, *, #10164, .F. ) ;
#13401=TOROIDAL_SURFACE ( 'NONE', #134178, 11.89999999999999858, 0.1000000000000000056 ) ;
#13422=VECTOR ( 'NONE', #102819, 1000.000000000000000 ) ;
#13453=CARTESIAN_POINT ( 'NONE',  ( 23.24999999999999289, 11.65000000001116298, -146.1500000000000341 ) ) ;
#13463=ORIENTED_EDGE ( 'NONE', *, *, #175310, .F. ) ;
#13514=EDGE_CURVE ( 'NONE', #8349, #95988, #51605, .T. ) ;
#13520=EDGE_LOOP ( 'NONE', ( #9154, #249941, #201130 ) ) ;
#13536=TOROIDAL_SURFACE ( 'NONE', #159292, 7.791421356237335338, 0.1000000000000000056 ) ;
#13541=VECTOR ( 'NONE', #208249, 1000.000000000000000 ) ;
#13549=VERTEX_POINT ( 'NONE', #121908 ) ;
#13558=LINE ( 'NONE', #74841, #172697 ) ;
#13559=EDGE_CURVE ( 'NONE', #126194, #38036, #82727, .T. ) ;
#13566=CARTESIAN_POINT ( 'NONE',  ( -23.15000000000000213, 5.950000000011163692, -157.1942976949652007 ) ) ;
#13578=CARTESIAN_POINT ( 'NONE',  ( 21.05000000000000071, 10.72371710471867701, -146.1500000000000341 ) ) ;
#13582=AXIS2_PLACEMENT_3D ( 'NONE', #116715, #191145, #256158 ) ;
#13583=EDGE_LOOP ( 'NONE', ( #151559, #63017, #251659 ) ) ;
#13585=CIRCLE ( 'NONE', #88572, 0.2000000000000057288 ) ;
#13629=DIRECTION ( 'NONE',  ( 0.000000000000000000, 1.776356839400277286E-15, -1.000000000000000000 ) ) ;
#13660=CIRCLE ( 'NONE', #46966, 0.09999999999999939493 ) ;
#13688=PLANE ( 'NONE',  #140588 ) ;
#13697=DIRECTION ( 'NONE',  ( 1.000000000000000000, 0.000000000000000000, 0.000000000000000000 ) ) ;
#13702=CARTESIAN_POINT ( 'NONE',  ( 21.08832698747859169, 8.775364393428372267, -146.2287174664641896 ) ) ;
#13713=ORIENTED_EDGE ( 'NONE', *, *, #167967, .T. ) ;
#13717=CARTESIAN_POINT ( 'NONE',  ( -18.51697539158857353, 10.31565961587945957, -173.0364194119178478 ) ) ;
#13739=ADVANCED_FACE ( 'NONE', ( #127985 ), #169716, .T. ) ;
#13749=ORIENTED_EDGE ( 'NONE', *, *, #15855, .T. ) ;
#13767=ADVANCED_FACE ( 'NONE', ( #187961 ), #70604, .T. ) ;
#13776=ADVANCED_FACE ( 'NONE', ( #230956 ), #31025, .T. ) ;
#13799=VERTEX_POINT ( 'NONE', #30184 ) ;
#13803=CARTESIAN_POINT ( 'NONE',  ( -18.59999999999999787, -1.164121893230052995, -175.2148480855716173 ) ) ;
#13822=CARTESIAN_POINT ( 'NONE',  ( -22.50000000000000000, 11.64976291804307884, -133.9111900236131021 ) ) ;
#13826=CARTESIAN_POINT ( 'NONE',  ( 20.94999999999999929, 11.65000000001115943, -160.7161343370219129 ) ) ;
#13829=VECTOR ( 'NONE', #213065, 1000.000000000000000 ) ;
#13887=PLANE ( 'NONE',  #5492 ) ;
#13935=CARTESIAN_POINT ( 'NONE',  ( -21.05000000000000071, 1.115600667400684642E-11, -167.5000000000000284 ) ) ;
#13942=AXIS2_PLACEMENT_3D ( 'NONE', #57140, #118440, #218791 ) ;
#13958=ORIENTED_EDGE ( 'NONE', *, *, #226682, .F. ) ;
#13966=EDGE_LOOP ( 'NONE', ( #217262, #248498, #200725 ) ) ;
#13981=DIRECTION ( 'NONE',  ( 0.000000000000000000, 0.000000000000000000, -1.000000000000000000 ) ) ;
#14032=FACE_OUTER_BOUND ( 'NONE', #121052, .T. ) ;
#14033=AXIS2_PLACEMENT_3D ( 'NONE', #115648, #76507, #12725 ) ;
#14067=EDGE_CURVE ( 'NONE', #212843, #46813, #143377, .T. ) ;
#14069=CARTESIAN_POINT ( 'NONE',  ( -23.15000000000000213, -8.999999999988844479, -158.1060308773475924 ) ) ;
#14078=TOROIDAL_SURFACE ( 'NONE', #88859, 0.2000000000000000111, 0.1000000000000000056 ) ;
#14080=CIRCLE ( 'NONE', #118107, 0.09999999999999817368 ) ;
#14101=DIRECTION ( 'NONE',  ( -0.000000000000000000, -0.8660254037844459241, -0.4999999999999873990 ) ) ;
#14102=EDGE_CURVE ( 'NONE', #176594, #360, #168594, .T. ) ;
#14121=DIRECTION ( 'NONE',  ( 0.000000000000000000, 1.000000000000000000, 0.000000000000000000 ) ) ;
#14133=ADVANCED_FACE ( 'NONE', ( #88517 ), #250190, .T. ) ;
#14142=VERTEX_POINT ( 'NONE', #12885 ) ;
#14213=CARTESIAN_POINT ( 'NONE',  ( -20.94999999999999929, 1.851028230152016674, -145.6539132694225032 ) ) ;
#14225=AXIS2_PLACEMENT_3D ( 'NONE', #48936, #188450, #124638 ) ;
#14287=CARTESIAN_POINT ( 'NONE',  ( -23.25000000000000000, 4.150000000011156764, -146.3500000000000227 ) ) ;
#14306=LINE ( 'NONE', #158950, #242611 ) ;
#14319=TOROIDAL_SURFACE ( 'NONE', #135062, 11.65000000000000036, 0.1000000000000000056 ) ;
#14329=CARTESIAN_POINT ( 'NONE',  ( -23.15000000000000213, 1.115626384983466744E-11, -165.4000000000000341 ) ) ;
#14347=CARTESIAN_POINT ( 'NONE',  ( -23.15000000000000213, 4.350000000011156054, -155.1500000000000057 ) ) ;
#14355=VERTEX_POINT ( 'NONE', #234460 ) ;
#14370=DIRECTION ( 'NONE',  ( -0.000000000000000000, -0.000000000000000000, -1.000000000000000000 ) ) ;
#14378=DIRECTION ( 'NONE',  ( 0.000000000000000000, 0.000000000000000000, -1.000000000000000000 ) ) ;
#14391=EDGE_CURVE ( 'NONE', #158124, #229990, #243739, .T. ) ;
#14392=CARTESIAN_POINT ( 'NONE',  ( 23.15000000000000213, -8.999999999988842703, -157.6060308773475640 ) ) ;
#14402=AXIS2_PLACEMENT_3D ( 'NONE', #146213, #129236, #185353 ) ;
#14407=DIRECTION ( 'NONE',  ( -0.000000000000000000, 0.1350103645451876666, 0.9908441862701600211 ) ) ;
#14475=ADVANCED_FACE ( 'NONE', ( #141773 ), #63520, .F. ) ;
#14477=DIRECTION ( 'NONE',  ( 1.000000000000000000, 0.000000000000000000, 0.000000000000000000 ) ) ;
#14487=DIRECTION ( 'NONE',  ( -1.000000000000000000, -0.000000000000000000, -0.000000000000000000 ) ) ;
#14493=ORIENTED_EDGE ( 'NONE', *, *, #90762, .F. ) ;
#14535=DIRECTION ( 'NONE',  ( -1.000000000000000000, 0.000000000000000000, 0.000000000000000000 ) ) ;
#14537=ORIENTED_EDGE ( 'NONE', *, *, #192046, .T. ) ;
#14538=DIRECTION ( 'NONE',  ( 1.000000000000000000, 0.000000000000000000, -0.000000000000000000 ) ) ;
#14541=CARTESIAN_POINT ( 'NONE',  ( 23.25000000000000000, 6.550000000011156231, -146.3500000000000227 ) ) ;
#14560=CARTESIAN_POINT ( 'NONE',  ( -21.05000000000000071, -11.74999999998884448, -164.6000000000000227 ) ) ;
#14561=ORIENTED_EDGE ( 'NONE', *, *, #182169, .T. ) ;
#14630=DIRECTION ( 'NONE',  ( -1.000000000000000000, 0.000000000000000000, 0.000000000000000000 ) ) ;
#14657=CARTESIAN_POINT ( 'NONE',  ( -21.45000000000000284, 7.708578643773852157, -155.1500000000000057 ) ) ;
#14668=CARTESIAN_POINT ( 'NONE',  ( 23.14999999999999858, 1.115600667400684642E-11, -134.0000000000000000 ) ) ;
#14683=DIRECTION ( 'NONE',  ( 0.000000000000000000, 0.000000000000000000, -1.000000000000000000 ) ) ;
#14684=DIRECTION ( 'NONE',  ( 0.000000000000000000, 0.1575844902526835067, 0.9875055080513738259 ) ) ;
#14691=ORIENTED_EDGE ( 'NONE', *, *, #178030, .F. ) ;
#14770=VECTOR ( 'NONE', #217522, 1000.000000000000000 ) ;
#14827=VECTOR ( 'NONE', #118774, 1000.000000000000000 ) ;
#14844=ORIENTED_EDGE ( 'NONE', *, *, #87761, .F. ) ;
#14862=EDGE_CURVE ( 'NONE', #251548, #1294, #135572, .T. ) ;
#14904=DIRECTION ( 'NONE',  ( 0.000000000000000000, 0.000000000000000000, 1.000000000000000000 ) ) ;
#14908=FACE_OUTER_BOUND ( 'NONE', #59589, .T. ) ;
#14910=EDGE_LOOP ( 'NONE', ( #198925, #75826, #165276, #72603 ) ) ;
#14917=( GEOMETRIC_REPRESENTATION_CONTEXT ( 3 ) GLOBAL_UNCERTAINTY_ASSIGNED_CONTEXT ( ( #16711 ) ) GLOBAL_UNIT_ASSIGNED_CONTEXT ( ( #218277, #123066, #200034 ) ) REPRESENTATION_CONTEXT ( 'NONE', 'WORKASPACE' ) );
#14931=ORIENTED_EDGE ( 'NONE', *, *, #132450, .F. ) ;
#14950=ADVANCED_FACE ( 'NONE', ( #120041 ), #238672, .T. ) ;
#14953=DIRECTION ( 'NONE',  ( 1.000000000000000000, 0.000000000000000000, 0.000000000000000000 ) ) ;
#14995=DIRECTION ( 'NONE',  ( 1.000000000000000000, 0.000000000000000000, 0.000000000000000000 ) ) ;
#15022=AXIS2_PLACEMENT_3D ( 'NONE', #41526, #201856, #40247 ) ;
#15041=CARTESIAN_POINT ( 'NONE',  ( -22.60000000000080789, 0.04781698047652390565, -122.2499775688472567 ) ) ;
#15056=DIRECTION ( 'NONE',  ( -1.000000000000000000, 0.000000000000000000, 0.000000000000000000 ) ) ;
#15099=CARTESIAN_POINT ( 'NONE',  ( 18.31572054635715574, -9.548475435767818098, -174.3505701647482624 ) ) ;
#15117=CARTESIAN_POINT ( 'NONE',  ( 21.05000000000000071, -8.663551401857999323, -157.9758988819327215 ) ) ;
#15137=CARTESIAN_POINT ( 'NONE',  ( 21.14999999999999503, -0.09999999998884338825, -122.3504291924552234 ) ) ;
#15146=DIRECTION ( 'NONE',  ( 0.000000000000000000, -1.000000000000000000, 0.000000000000000000 ) ) ;
#15156=AXIS2_PLACEMENT_3D ( 'NONE', #60674, #140209, #222302 ) ;
#15173=VERTEX_POINT ( 'NONE', #108154 ) ;
#15180=DIRECTION ( 'NONE',  ( 0.000000000000000000, 0.000000000000000000, 1.000000000000000000 ) ) ;
#15216=EDGE_LOOP ( 'NONE', ( #134559, #82947, #197092, #139887 ) ) ;
#15231=FACE_OUTER_BOUND ( 'NONE', #120734, .T. ) ;
#15239=AXIS2_PLACEMENT_3D ( 'NONE', #153044, #73496, #35660 ) ;
#15240=DIRECTION ( 'NONE',  ( -3.440080580676165868E-14, -0.1298341882520124002, -0.9915357197604841577 ) ) ;
#15242=EDGE_LOOP ( 'NONE', ( #157551, #208439, #99121, #177452 ) ) ;
#15243=CARTESIAN_POINT ( 'NONE',  ( 21.14999999999999858, 11.75000000001116263, -146.1500000000000341 ) ) ;
#15259=CARTESIAN_POINT ( 'NONE',  ( -23.15000000000000213, 2.000000000011154189, -147.2246219227621111 ) ) ;
#15272=CARTESIAN_POINT ( 'NONE',  ( 20.94999999999999929, 5.400000000011154988, -155.0947339810869323 ) ) ;
#15289=DIRECTION ( 'NONE',  ( 1.000000000000000000, 0.000000000000000000, 0.000000000000000000 ) ) ;
#15310=DIRECTION ( 'NONE',  ( -0.000000000000000000, 0.1350103645451876666, 0.9908441862701600211 ) ) ;
#15315=ORIENTED_EDGE ( 'NONE', *, *, #173741, .T. ) ;
#15321=EDGE_CURVE ( 'NONE', #148927, #157514, #237082, .T. ) ;
#15347=AXIS2_PLACEMENT_3D ( 'NONE', #149617, #229132, #170494 ) ;
#15367=LINE ( 'NONE', #253939, #224022 ) ;
#15392=CARTESIAN_POINT ( 'NONE',  ( -20.54999999999999716, 1.115625160336667635E-11, -169.5000000000000284 ) ) ;
#15408=DIRECTION ( 'NONE',  ( -1.000000000000000000, 0.000000000000000000, 0.000000000000000000 ) ) ;
#15422=AXIS2_PLACEMENT_3D ( 'NONE', #139072, #38738, #158707 ) ;
#15447=CIRCLE ( 'NONE', #65486, 0.09999999999998898659 ) ;
#15449=CARTESIAN_POINT ( 'NONE',  ( -18.59999999999999787, 11.75000000001115197, -155.3500000000000227 ) ) ;
#15484=LINE ( 'NONE', #153749, #7378 ) ;
#15487=CARTESIAN_POINT ( 'NONE',  ( -22.00411653962163072, 7.253442868381378084, -133.9009618942314148 ) ) ;
#15496=AXIS2_PLACEMENT_3D ( 'NONE', #78642, #197309, #120395 ) ;
#15530=CARTESIAN_POINT ( 'NONE',  ( 20.85000000000000142, 11.65000000001115943, -160.7161343370219129 ) ) ;
#15548=CIRCLE ( 'NONE', #223796, 0.09999999999999158173 ) ;
#15560=DIRECTION ( 'NONE',  ( 1.000000000000000000, 0.000000000000000000, 0.000000000000000000 ) ) ;
#15561=DIRECTION ( 'NONE',  ( -0.000000000000000000, -0.000000000000000000, -1.000000000000000000 ) ) ;
#15575=CIRCLE ( 'NONE', #198701, 11.89999999999999325 ) ;
#15661=DIRECTION ( 'NONE',  ( 0.000000000000000000, -0.8660254037844384856, 0.5000000000000003331 ) ) ;
#15682=DIRECTION ( 'NONE',  ( -1.000000000000000000, 0.000000000000000000, 0.000000000000000000 ) ) ;
#15683=AXIS2_PLACEMENT_3D ( 'NONE', #102895, #82036, #159069 ) ;
#15699=ORIENTED_EDGE ( 'NONE', *, *, #98140, .F. ) ;
#15703=DIRECTION ( 'NONE',  ( 7.304098846218134667E-16, 1.000000000000000000, -0.000000000000000000 ) ) ;
#15706=SPHERICAL_SURFACE ( 'NONE', #138301, 0.1000000000000000056 ) ;
#15714=DIRECTION ( 'NONE',  ( 0.000000000000000000, 1.000000000000000000, 1.224646799147353207E-16 ) ) ;
#15740=ADVANCED_FACE ( 'NONE', ( #18990 ), #111013, .F. ) ;
#15774=EDGE_CURVE ( 'NONE', #8389, #200654, #127584, .T. ) ;
#15838=FACE_OUTER_BOUND ( 'NONE', #135539, .T. ) ;
#15851=ORIENTED_EDGE ( 'NONE', *, *, #9379, .T. ) ;
#15855=EDGE_CURVE ( 'NONE', #222619, #94122, #84056, .T. ) ;
#15875=PLANE ( 'NONE',  #29933 ) ;
#15896=DIRECTION ( 'NONE',  ( 0.000000000000000000, -1.000000000000000000, 0.000000000000000000 ) ) ;
#15898=CIRCLE ( 'NONE', #257585, 0.09999999999998898659 ) ;
#15915=ORIENTED_EDGE ( 'NONE', *, *, #44975, .T. ) ;
#15920=DIRECTION ( 'NONE',  ( -1.000000000000000000, -1.836970198721029934E-16, -3.186635328391151676E-31 ) ) ;
#15932=EDGE_CURVE ( 'NONE', #125446, #87825, #186217, .T. ) ;
#15953=LINE ( 'NONE', #171189, #188650 ) ;
#15954=ORIENTED_EDGE ( 'NONE', *, *, #95767, .T. ) ;
#15962=FACE_OUTER_BOUND ( 'NONE', #1298, .T. ) ;
#15968=CARTESIAN_POINT ( 'NONE',  ( -20.94999999999999929, 7.070967871809997973, -171.2465642218683115 ) ) ;
#15981=CARTESIAN_POINT ( 'NONE',  ( 18.59999999999999076, 6.982009704867611077, -171.1961521182563217 ) ) ;
#16023=SPHERICAL_SURFACE ( 'NONE', #182564, 0.1000000000000000056 ) ;
#16038=DIRECTION ( 'NONE',  ( 0.000000000000000000, 0.000000000000000000, 1.000000000000000000 ) ) ;
#16041=DIRECTION ( 'NONE',  ( -1.000000000000000000, 0.000000000000000000, 0.000000000000000000 ) ) ;
#16053=ORIENTED_EDGE ( 'NONE', *, *, #89303, .T. ) ;
#16089=ORIENTED_EDGE ( 'NONE', *, *, #234291, .T. ) ;
#16104=AXIS2_PLACEMENT_3D ( 'NONE', #184490, #239349, #1999 ) ;
#16112=CARTESIAN_POINT ( 'NONE',  ( 21.04999999999999716, 10.62872031401550466, -146.1500000000000341 ) ) ;
#16125=EDGE_LOOP ( 'NONE', ( #84967, #46722, #10094, #257880 ) ) ;
#16140=B_SPLINE_CURVE_WITH_KNOTS ( 'NONE', 3,
 ( #1741, #66872, #44749, #225908, #185537, #81267, #160853, #203807 ),
 .UNSPECIFIED., .F., .F.,
 ( 4, 2, 2, 4 ),
 ( 0.000000000000000000, 0.0001881495939909161091, 0.0002822243909863741637, 0.0003762991879818322182 ),
 .UNSPECIFIED. ) ;
#16180=DIRECTION ( 'NONE',  ( 0.000000000000000000, 0.000000000000000000, -1.000000000000000000 ) ) ;
#16191=DIRECTION ( 'NONE',  ( 0.000000000000000000, 0.000000000000000000, -1.000000000000000000 ) ) ;
#16234=FACE_OUTER_BOUND ( 'NONE', #218423, .T. ) ;
#16248=DIRECTION ( 'NONE',  ( 0.000000000000000000, -0.4999999999999543698, -0.8660254037844650199 ) ) ;
#16251=ADVANCED_FACE ( 'NONE', ( #114606 ), #208891, .F. ) ;
#16273=VERTEX_POINT ( 'NONE', #9400 ) ;
#16288=DIRECTION ( 'NONE',  ( -1.000000000000000000, -0.000000000000000000, -0.000000000000000000 ) ) ;
#16317=AXIS2_PLACEMENT_3D ( 'NONE', #153679, #76636, #233183 ) ;
#16319=AXIS2_PLACEMENT_3D ( 'NONE', #250629, #190703, #194555 ) ;
#16328=CARTESIAN_POINT ( 'NONE',  ( -22.50485643085239928, -0.07878633906603056680, -122.2502050608276107 ) ) ;
#16374=FACE_BOUND ( 'NONE', #85381, .T. ) ;
#16382=VECTOR ( 'NONE', #115113, 1000.000000000000000 ) ;
#16393=ORIENTED_EDGE ( 'NONE', *, *, #95399, .F. ) ;
#16407=FACE_OUTER_BOUND ( 'NONE', #108730, .T. ) ;
#16445=AXIS2_PLACEMENT_3D ( 'NONE', #6937, #225953, #86443 ) ;
#16449=ORIENTED_EDGE ( 'NONE', *, *, #91654, .T. ) ;
#16452=DIRECTION ( 'NONE',  ( 1.000000000000000000, -0.000000000000000000, -0.000000000000000000 ) ) ;
#16470=VERTEX_POINT ( 'NONE', #139276 ) ;
#16480=CARTESIAN_POINT ( 'NONE',  ( -20.85000000106584750, 11.75000000001115197, -160.6555046564734539 ) ) ;
#16492=CARTESIAN_POINT ( 'NONE',  ( 23.14999999999999503, 11.65000000001116298, -146.1500000000000341 ) ) ;
#16493=CARTESIAN_POINT ( 'NONE',  ( -20.64999999999999858, 4.350000000011156054, -146.3500000000000227 ) ) ;
#16531=DIRECTION ( 'NONE',  ( 1.000000000000000000, 0.000000000000000000, 0.000000000000000000 ) ) ;
#16533=AXIS2_PLACEMENT_3D ( 'NONE', #57394, #97791, #136947 ) ;
#16546=CARTESIAN_POINT ( 'NONE',  ( -21.05000000000000071, -11.64999999998884483, -134.0000000000000000 ) ) ;
#16552=EDGE_LOOP ( 'NONE', ( #20389, #53373, #223723, #69689 ) ) ;
#16585=ORIENTED_EDGE ( 'NONE', *, *, #123296, .T. ) ;
#16595=CYLINDRICAL_SURFACE ( 'NONE', #28215, 0.09999999999999939493 ) ;
#16609=CARTESIAN_POINT ( 'NONE',  ( -21.07954640115340439, 6.329287696035428290, -133.9339922928604381 ) ) ;
#16618=CARTESIAN_POINT ( 'NONE',  ( 18.59999999999998366, 1.115600667400684642E-11, -167.5000000000000284 ) ) ;
#16622=AXIS2_PLACEMENT_3D ( 'NONE', #119703, #141804, #25721 ) ;
#16653=DIRECTION ( 'NONE',  ( 0.000000000000000000, 0.000000000000000000, -1.000000000000000000 ) ) ;
#16693=ORIENTED_EDGE ( 'NONE', *, *, #184880, .T. ) ;
#16695=CARTESIAN_POINT ( 'NONE',  ( -20.85000000000000142, -1.164121893230052995, -175.4148480855716059 ) ) ;
#16711=UNCERTAINTY_MEASURE_WITH_UNIT (LENGTH_MEASURE( 1.000000000000000082E-05 ), #218277, 'distance_accuracy_value', 'NONE');
#16736=DIRECTION ( 'NONE',  ( 2.952720810173289112E-16, -1.000000000000000000, 0.000000000000000000 ) ) ;
#16747=AXIS2_PLACEMENT_3D ( 'NONE', #96521, #216490, #59963 ) ;
#16762=CARTESIAN_POINT ( 'NONE',  ( -18.50000000000000000, 7.021664781911246322, -171.3335654018973173 ) ) ;
#16827=CARTESIAN_POINT ( 'NONE',  ( 20.85000000000000142, -1.835859311432481045, -179.0044391687985410 ) ) ;
#16854=VERTEX_POINT ( 'NONE', #38618 ) ;
#16865=AXIS2_PLACEMENT_3D ( 'NONE', #18308, #97812, #255582 ) ;
#16876=ORIENTED_EDGE ( 'NONE', *, *, #167200, .F. ) ;
#16928=DIRECTION ( 'NONE',  ( -7.304098846218134667E-16, -1.000000000000000000, 0.000000000000000000 ) ) ;
#16991=DIRECTION ( 'NONE',  ( 0.000000000000000000, 0.000000000000000000, 1.000000000000000000 ) ) ;
#17034=DIRECTION ( 'NONE',  ( 0.000000000000000000, 0.000000000000000000, -1.000000000000000000 ) ) ;
#17040=CARTESIAN_POINT ( 'NONE',  ( 23.24999999999999645, 1.115600667400684642E-11, -134.0000000000000000 ) ) ;
#17072=CARTESIAN_POINT ( 'NONE',  ( -22.50000000000000000, 0.1000000000111554016, -122.3504291924552234 ) ) ;
#17077=CARTESIAN_POINT ( 'NONE',  ( -22.39999999999999858, 0.1000000000111554016, -126.2092204016266379 ) ) ;
#17153=ORIENTED_EDGE ( 'NONE', *, *, #184238, .F. ) ;
#17168=ORIENTED_EDGE ( 'NONE', *, *, #136809, .F. ) ;
#17173=EDGE_CURVE ( 'NONE', #146335, #165316, #82484, .T. ) ;
#17188=CARTESIAN_POINT ( 'NONE',  ( -23.15000000000000213, -9.599999999988847676, -143.8939691226524644 ) ) ;
#17203=EDGE_CURVE ( 'NONE', #149928, #220244, #143839, .T. ) ;
#17315=LINE ( 'NONE', #197212, #178360 ) ;
#17318=ORIENTED_EDGE ( 'NONE', *, *, #163785, .T. ) ;
#17331=DIRECTION ( 'NONE',  ( 0.000000000000000000, 4.336808689942494997E-15, -1.000000000000000000 ) ) ;
#17379=CARTESIAN_POINT ( 'NONE',  ( -23.25000000000000000, 1.115626384983466906E-11, -165.4000000000000341 ) ) ;
#17390=CARTESIAN_POINT ( 'NONE',  ( -23.25000000000000000, 1.115600667400684642E-11, -138.0500000000000114 ) ) ;
#17401=CARTESIAN_POINT ( 'NONE',  ( 18.59999999999999432, 1.162701749949165642, -142.0000000000000284 ) ) ;
#17406=FACE_OUTER_BOUND ( 'NONE', #214394, .T. ) ;
#17414=ORIENTED_EDGE ( 'NONE', *, *, #170281, .T. ) ;
#17425=CARTESIAN_POINT ( 'NONE',  ( -20.94999999999999929, -1.835341550213255957, -145.6551512925629766 ) ) ;
#17435=VECTOR ( 'NONE', #68397, 1000.000000000000000 ) ;
#17454=EDGE_CURVE ( 'NONE', #221551, #206051, #190497, .T. ) ;
#17461=DIRECTION ( 'NONE',  ( -0.8660254037843277963, 0.000000000000000000, -0.5000000000001921796 ) ) ;
#17469=CARTESIAN_POINT ( 'NONE',  ( 23.14999999999999858, 1.115649653272650466E-11, -163.5000000000000284 ) ) ;
#17477=ORIENTED_EDGE ( 'NONE', *, *, #209843, .F. ) ;
#17526=FACE_OUTER_BOUND ( 'NONE', #66391, .T. ) ;
#17540=CARTESIAN_POINT ( 'NONE',  ( -21.05000000000000071, 1.750000000011155743, -145.6695115579016715 ) ) ;
#17549=ORIENTED_EDGE ( 'NONE', *, *, #97517, .T. ) ;
#17564=EDGE_CURVE ( 'NONE', #51770, #25295, #144666, .T. ) ;
#17650=CARTESIAN_POINT ( 'NONE',  ( 18.59999999999999432, -1.162701749926855266, -142.1000000000000227 ) ) ;
#17661=EDGE_CURVE ( 'NONE', #148690, #175914, #123847, .T. ) ;
#17683=ORIENTED_EDGE ( 'NONE', *, *, #36955, .F. ) ;
#17685=EDGE_CURVE ( 'NONE', #25818, #30259, #248736, .T. ) ;
#17711=DIRECTION ( 'NONE',  ( -1.000000000000000000, 0.000000000000000000, 0.000000000000000000 ) ) ;
#17719=CARTESIAN_POINT ( 'NONE',  ( -21.05000000000000071, 11.75000000001115197, -160.4851942293460638 ) ) ;
#17731=VERTEX_POINT ( 'NONE', #113418 ) ;
#17738=VERTEX_POINT ( 'NONE', #252917 ) ;
#17751=DIRECTION ( 'NONE',  ( 0.000000000000000000, -2.168404344970946706E-14, -1.000000000000000000 ) ) ;
#17769=EDGE_CURVE ( 'NONE', #11722, #83610, #236433, .T. ) ;
#17798=ORIENTED_EDGE ( 'NONE', *, *, #137459, .T. ) ;
#17811=CARTESIAN_POINT ( 'NONE',  ( 22.42357213249528769, 7.672932386371071445, -133.9009130359984567 ) ) ;
#17841=DIRECTION ( 'NONE',  ( -0.000000000000000000, 0.000000000000000000, 1.000000000000000000 ) ) ;
#17851=EDGE_CURVE ( 'NONE', #79888, #186782, #119753, .T. ) ;
#17860=ADVANCED_FACE ( 'NONE', ( #22032 ), #196789, .F. ) ;
#17862=ORIENTED_EDGE ( 'NONE', *, *, #64704, .F. ) ;
#17873=CARTESIAN_POINT ( 'NONE',  ( 22.59999999999999432, 11.74956712350054566, -133.8991416309013118 ) ) ;
#17886=DIRECTION ( 'NONE',  ( 0.000000000000000000, 0.000000000000000000, -1.000000000000000000 ) ) ;
#17891=CARTESIAN_POINT ( 'NONE',  ( -23.25000000000000000, 4.350000000011156054, -146.3500000000000227 ) ) ;
#17908=CARTESIAN_POINT ( 'NONE',  ( 21.14999999999999503, 11.75000000001115552, -134.0000000000000284 ) ) ;
#17928=LINE ( 'NONE', #55745, #211176 ) ;
#17937=EDGE_CURVE ( 'NONE', #206030, #185310, #136456, .T. ) ;
#17944=ORIENTED_EDGE ( 'NONE', *, *, #102054, .F. ) ;
#17949=ADVANCED_FACE ( 'NONE', ( #145798 ), #45429, .F. ) ;
#17975=AXIS2_PLACEMENT_3D ( 'NONE', #179777, #98904, #143184 ) ;
#18003=ORIENTED_EDGE ( 'NONE', *, *, #113526, .T. ) ;
#18096=DIRECTION ( 'NONE',  ( 0.7071359030028288029, 0.000000000000000000, -0.7070776581708504427 ) ) ;
#18101=SPHERICAL_SURFACE ( 'NONE', #37827, 0.1000000000000000056 ) ;
#18105=ORIENTED_EDGE ( 'NONE', *, *, #204836, .T. ) ;
#18111=ORIENTED_EDGE ( 'NONE', *, *, #186388, .T. ) ;
#18126=DIRECTION ( 'NONE',  ( 0.000000000000000000, 0.000000000000000000, -1.000000000000000000 ) ) ;
#18148=DIRECTION ( 'NONE',  ( -1.000000000000000000, 0.000000000000000000, 0.000000000000000000 ) ) ;
#18220=CARTESIAN_POINT ( 'NONE',  ( 20.85000000000000142, -1.164121893230052995, -175.4148480855716059 ) ) ;
#18258=LINE ( 'NONE', #53532, #235243 ) ;
#18262=ORIENTED_EDGE ( 'NONE', *, *, #168992, .F. ) ;
#18270=LINE ( 'NONE', #183766, #72846 ) ;
#18299=AXIS2_PLACEMENT_3D ( 'NONE', #52645, #111354, #167499 ) ;
#18306=DIRECTION ( 'NONE',  ( -1.000000000000000000, -0.000000000000000000, -0.000000000000000000 ) ) ;
#18308=CARTESIAN_POINT ( 'NONE',  ( -20.64999999999999858, 1.115623935689868526E-11, -165.6000000000000227 ) ) ;
#18309=VERTEX_POINT ( 'NONE', #77808 ) ;
#18347=CARTESIAN_POINT ( 'NONE',  ( 22.39999999999999858, 1.115600667400684642E-11, -134.0000000000000000 ) ) ;
#18372=CYLINDRICAL_SURFACE ( 'NONE', #105716, 0.09999999999999939493 ) ;
#18380=VERTEX_POINT ( 'NONE', #204176 ) ;
#18389=ORIENTED_EDGE ( 'NONE', *, *, #43134, .F. ) ;
#18429=EDGE_CURVE ( 'NONE', #89005, #25173, #170044, .T. ) ;
#18445=EDGE_CURVE ( 'NONE', #224075, #94099, #15898, .T. ) ;
#18447=ADVANCED_FACE ( 'NONE', ( #154526 ), #211911, .T. ) ;
#18450=DIRECTION ( 'NONE',  ( -1.000000000000000000, 0.000000000000000000, 0.000000000000000000 ) ) ;
#18452=ORIENTED_EDGE ( 'NONE', *, *, #113758, .F. ) ;
#18462=AXIS2_PLACEMENT_3D ( 'NONE', #238662, #196954, #75749 ) ;
#18518=ORIENTED_EDGE ( 'NONE', *, *, #203059, .F. ) ;
#18524=EDGE_CURVE ( 'NONE', #24271, #85212, #218284, .T. ) ;
#18536=LINE ( 'NONE', #139740, #163035 ) ;
#18559=AXIS2_PLACEMENT_3D ( 'NONE', #211651, #128254, #48697 ) ;
#18582=VERTEX_POINT ( 'NONE', #60499 ) ;
#18590=ORIENTED_EDGE ( 'NONE', *, *, #235884, .T. ) ;
#18599=FACE_OUTER_BOUND ( 'NONE', #234478, .T. ) ;
#18611=VERTEX_POINT ( 'NONE', #21424 ) ;
#18613=EDGE_LOOP ( 'NONE', ( #181104, #208922, #113591, #240406 ) ) ;
#18618=CARTESIAN_POINT ( 'NONE',  ( 23.14999999999999858, 1.115600667400684642E-11, -167.5000000000000284 ) ) ;
#18623=ORIENTED_EDGE ( 'NONE', *, *, #240316, .F. ) ;
#18648=TOROIDAL_SURFACE ( 'NONE', #197694, 11.65000000000000036, 0.1000000000000000056 ) ;
#18654=CARTESIAN_POINT ( 'NONE',  ( 21.08804281139612868, 10.62183430185230826, -146.3499999673788636 ) ) ;
#18708=LINE ( 'NONE', #151827, #232750 ) ;
#18717=ADVANCED_FACE ( 'NONE', ( #184309 ), #3091, .T. ) ;
#18727=ORIENTED_EDGE ( 'NONE', *, *, #99089, .T. ) ;
#18729=ADVANCED_FACE ( 'NONE', ( #85179 ), #63079, .F. ) ;
#18737=CARTESIAN_POINT ( 'NONE',  ( -20.54999999999999716, 7.250000000011155521, -155.2500000000000284 ) ) ;
#18746=EDGE_CURVE ( 'NONE', #50997, #164020, #43538, .T. ) ;
#18761=AXIS2_PLACEMENT_3D ( 'NONE', #106765, #127632, #186328 ) ;
#18782=DIRECTION ( 'NONE',  ( -1.000000000000000000, 0.000000000000000000, 0.000000000000000000 ) ) ;
#18810=PRESENTATION_STYLE_ASSIGNMENT (( #117906 ) ) ;
#18830=SPHERICAL_SURFACE ( 'NONE', #62651, 0.1000000000000000056 ) ;
#18845=DIRECTION ( 'NONE',  ( 0.000000000000000000, -0.000000000000000000, 1.000000000000000000 ) ) ;
#18846=VECTOR ( 'NONE', #184193, 1000.000000000000114 ) ;
#18862=LINE ( 'NONE', #257417, #168459 ) ;
#18888=CARTESIAN_POINT ( 'NONE',  ( -22.39999999999999858, 0.1000000000111554016, -134.0000000000000000 ) ) ;
#18907=DIRECTION ( 'NONE',  ( -0.000000000000000000, -0.1298341882519737922, -0.9915357197604890427 ) ) ;
#18926=CARTESIAN_POINT ( 'NONE',  ( 21.14999999999999858, 6.540656951712400691, -134.0000000000000000 ) ) ;
#18928=DIRECTION ( 'NONE',  ( 0.000000000000000000, 0.000000000000000000, -1.000000000000000000 ) ) ;
#18972=ORIENTED_EDGE ( 'NONE', *, *, #257998, .F. ) ;
#18990=FACE_OUTER_BOUND ( 'NONE', #107341, .T. ) ;
#19017=CARTESIAN_POINT ( 'NONE',  ( -21.05000000000000071, 11.75000000001115197, -160.6583993101029364 ) ) ;
#19040=CARTESIAN_POINT ( 'NONE',  ( 23.14999999999999503, 11.75000000001116263, -155.3500000000000227 ) ) ;
#19044=ORIENTED_EDGE ( 'NONE', *, *, #224253, .F. ) ;
#19056=TOROIDAL_SURFACE ( 'NONE', #60734, 0.2000000000000000111, 0.1000000000000000056 ) ;
#19081=ORIENTED_EDGE ( 'NONE', *, *, #91399, .F. ) ;
#19092=CARTESIAN_POINT ( 'NONE',  ( -23.15000000000000213, 1.115600667400684642E-11, -167.5000000000000284 ) ) ;
#19113=ORIENTED_EDGE ( 'NONE', *, *, #149217, .F. ) ;
#19145=CARTESIAN_POINT ( 'NONE',  ( -18.45037301276647312, -9.490200447530892092, -141.0126741364146312 ) ) ;
#19164=CARTESIAN_POINT ( 'NONE',  ( 22.49544290803751423, 11.74987023786900942, -133.9346880407421452 ) ) ;
#19170=CARTESIAN_POINT ( 'NONE',  ( -18.50000000000000000, 11.65000000001115232, -141.0148057706540214 ) ) ;
#19176=AXIS2_PLACEMENT_3D ( 'NONE', #28538, #244959, #188841 ) ;
#19180=ORIENTED_EDGE ( 'NONE', *, *, #137926, .T. ) ;
#19181=ORIENTED_EDGE ( 'NONE', *, *, #198190, .F. ) ;
#19204=DIRECTION ( 'NONE',  ( -0.000000000000000000, -0.000000000000000000, -1.000000000000000000 ) ) ;
#19205=AXIS2_PLACEMENT_3D ( 'NONE', #237356, #216498, #139520 ) ;
#19223=AXIS2_PLACEMENT_3D ( 'NONE', #180690, #99822, #176851 ) ;
#19227=FACE_OUTER_BOUND ( 'NONE', #101525, .T. ) ;
#19242=VERTEX_POINT ( 'NONE', #60862 ) ;
#19292=CARTESIAN_POINT ( 'NONE',  ( -20.94999999999999929, -11.64999999998884306, -137.1000000000000227 ) ) ;
#19308=CARTESIAN_POINT ( 'NONE',  ( 20.94999999999999574, 1.162701749949165642, -142.0000000000000284 ) ) ;
#19318=DIRECTION ( 'NONE',  ( 0.000000000000000000, 0.000000000000000000, 1.000000000000000000 ) ) ;
#19324=ORIENTED_EDGE ( 'NONE', *, *, #132832, .T. ) ;
#19331=LINE ( 'NONE', #20632, #193475 ) ;
#19343=ORIENTED_EDGE ( 'NONE', *, *, #168005, .T. ) ;
#19357=CARTESIAN_POINT ( 'NONE',  ( 22.39999999999999503, -0.09999999998884338825, -122.3504291924552234 ) ) ;
#19366=EDGE_CURVE ( 'NONE', #41279, #91128, #69881, .T. ) ;
#19397=DIRECTION ( 'NONE',  ( 1.000000000000000000, 0.000000000000000000, 0.000000000000000000 ) ) ;
#19433=ORIENTED_EDGE ( 'NONE', *, *, #28620, .F. ) ;
#19476=B_SPLINE_CURVE_WITH_KNOTS ( 'NONE', 3,
 ( #197186, #53835, #133379, #113804, #193362, #142346, #81079, #180215 ),
 .UNSPECIFIED., .F., .F.,
 ( 4, 2, 2, 4 ),
 ( 0.000000000000000000, 0.0001049670497869906649, 0.0002099340995739813298, 0.0004198681991480182249 ),
 .UNSPECIFIED. ) ;
#19481=DIRECTION ( 'NONE',  ( 0.000000000000000000, 0.000000000000000000, -1.000000000000000000 ) ) ;
#19503=EDGE_CURVE ( 'NONE', #148396, #245147, #104344, .T. ) ;
#19507=EDGE_CURVE ( 'NONE', #96104, #20283, #146053, .T. ) ;
#19512=CARTESIAN_POINT ( 'NONE',  ( 18.57071067811864040, 10.17928932189250091, -155.3500000000000227 ) ) ;
#19517=CIRCLE ( 'NONE', #115180, 0.09999999999998898659 ) ;
#19528=B_SPLINE_CURVE_WITH_KNOTS ( 'NONE', 3,
 ( #51604, #32105, #111622, #191179, #92048, #251106, #171628, #181505, #218020, #60243 ),
 .UNSPECIFIED., .F., .F.,
 ( 4, 2, 2, 2, 4 ),
 ( 0.000000000000000000, 0.0001660831991682680617, 0.0002491247987524029600, 0.0002906455985444370157, 0.0003321663983364710171 ),
 .UNSPECIFIED. ) ;
#19569=CARTESIAN_POINT ( 'NONE',  ( -23.25000000000000000, -8.999999999988844479, -157.6060308773475924 ) ) ;
#19813=ORIENTED_EDGE ( 'NONE', *, *, #15774, .F. ) ;
#19821=AXIS2_PLACEMENT_3D ( 'NONE', #6215, #22284, #127460 ) ;
#19888=VECTOR ( 'NONE', #92419, 1000.000000000000000 ) ;
#19902=CARTESIAN_POINT ( 'NONE',  ( 23.14999999999999858, 1.115600667400684642E-11, -134.0000000000000000 ) ) ;
#19910=ORIENTED_EDGE ( 'NONE', *, *, #6305, .T. ) ;
#19971=AXIS2_PLACEMENT_3D ( 'NONE', #11156, #73720, #110246 ) ;
#20005=ORIENTED_EDGE ( 'NONE', *, *, #176783, .F. ) ;
#20019=CARTESIAN_POINT ( 'NONE',  ( -20.94999999999999929, 5.850000000011108092, -144.1324972242779836 ) ) ;
#20037=ORIENTED_EDGE ( 'NONE', *, *, #110135, .F. ) ;
#20045=EDGE_LOOP ( 'NONE', ( #19343, #100321, #206300, #212968 ) ) ;
#20135=LINE ( 'NONE', #63088, #137625 ) ;
#20166=ORIENTED_EDGE ( 'NONE', *, *, #4389, .F. ) ;
#20172=ORIENTED_EDGE ( 'NONE', *, *, #246019, .F. ) ;
#20195=LINE ( 'NONE', #184382, #64323 ) ;
#20218=ORIENTED_EDGE ( 'NONE', *, *, #32920, .T. ) ;
#20221=ORIENTED_EDGE ( 'NONE', *, *, #93068, .F. ) ;
#20229=DIRECTION ( 'NONE',  ( -0.000000000000000000, 0.6132151058540549204, -0.7899159663865520375 ) ) ;
#20248=CARTESIAN_POINT ( 'NONE',  ( -18.50000000000000000, 1.637172712981535883, -145.5821533654720383 ) ) ;
#20259=CARTESIAN_POINT ( 'NONE',  ( -20.54999999999999716, 4.250000000011156409, -146.3500000000000227 ) ) ;
#20271=FACE_OUTER_BOUND ( 'NONE', #142795, .T. ) ;
#20277=CARTESIAN_POINT ( 'NONE',  ( 21.05000000000000071, 4.850467289730772791, -146.0342674090016999 ) ) ;
#20283=VERTEX_POINT ( 'NONE', #250448 ) ;
#20325=CARTESIAN_POINT ( 'NONE',  ( -23.15000000000000213, 11.65000000001115588, -155.3500000000000227 ) ) ;
#20336=VECTOR ( 'NONE', #148539, 1000.000000000000000 ) ;
#20341=ORIENTED_EDGE ( 'NONE', *, *, #30230, .F. ) ;
#20343=DIRECTION ( 'NONE',  ( 0.000000000000000000, -0.8777080977375715243, 0.4791956752370512551 ) ) ;
#20355=VECTOR ( 'NONE', #29848, 1000.000000000000000 ) ;
#20360=AXIS2_PLACEMENT_3D ( 'NONE', #100855, #121776, #180450 ) ;
#20363=CARTESIAN_POINT ( 'NONE',  ( 20.94999999999999574, -11.48912529306490349, -137.0000000000000000 ) ) ;
#20376=EDGE_CURVE ( 'NONE', #189870, #121616, #165337, .T. ) ;
#20387=CARTESIAN_POINT ( 'NONE',  ( 21.14999999999999503, -11.64999999998883595, -136.9000000000000341 ) ) ;
#20389=ORIENTED_EDGE ( 'NONE', *, *, #145031, .F. ) ;
#20408=CARTESIAN_POINT ( 'NONE',  ( 18.59999999999999787, -1.835341550213255957, -145.5551512925629822 ) ) ;
#20426=CARTESIAN_POINT ( 'NONE',  ( 19.99999999999998934, 11.75000000001115907, -158.8500000000000227 ) ) ;
#20431=TOROIDAL_SURFACE ( 'NONE', #228534, 0.2000000000000000111, 0.1000000000000000056 ) ;
#20459=ORIENTED_EDGE ( 'NONE', *, *, #39512, .T. ) ;
#20501=AXIS2_PLACEMENT_3D ( 'NONE', #145890, #121251, #105455 ) ;
#20509=DIRECTION ( 'NONE',  ( 0.000000000000000000, 0.000000000000000000, -1.000000000000000000 ) ) ;
#20538=CARTESIAN_POINT ( 'NONE',  ( 18.59999999999999076, 11.65000000001115943, -122.2500000000000284 ) ) ;
#20545=( BOUNDED_SURFACE ( )  B_SPLINE_SURFACE ( 3, 2, ( 
 ( #47732, #46451, #145557 ),
 ( #106413, #206826, #184683 ),
 ( #242089, #161301, #103850 ),
 ( #66028, #166453, #28225 ) ),
 .UNSPECIFIED., .F., .F., .T. ) 
 B_SPLINE_SURFACE_WITH_KNOTS ( ( 4, 4 ),
 ( 3, 3 ),
 ( -3.469446951953614189E-18, 0.001979672783031543714 ),
 ( 0.000000000000000000, 1.000000000000000000 ),
 .UNSPECIFIED. ) 
 GEOMETRIC_REPRESENTATION_ITEM ( )  RATIONAL_B_SPLINE_SURFACE ( (
 ( 1.000000000000000000, 0.7103081912008198939, 1.000000000000000000),
 ( 1.000000000000000000, 0.7104998333558710799, 1.000000000000000000),
 ( 1.000000000000000000, 0.7107238315755350921, 1.000000000000000000),
 ( 1.000000000000000000, 0.7110073749539379540, 1.000000000000000000) ) ) 
 REPRESENTATION_ITEM ( '' )  SURFACE ( )  );
#20584=CYLINDRICAL_SURFACE ( 'NONE', #209434, 0.09999999999998898659 ) ;
#20589=EDGE_CURVE ( 'NONE', #158228, #192257, #44669, .T. ) ;
#20597=CIRCLE ( 'NONE', #157999, 0.4000000000000114575 ) ;
#20621=DIRECTION ( 'NONE',  ( 0.000000000000000000, 0.4930308989874718772, 0.8700118002898612479 ) ) ;
#20626=ADVANCED_FACE ( 'NONE', ( #83744 ), #103331, .F. ) ;
#20627=DIRECTION ( 'NONE',  ( 1.000000000000000000, -0.000000000000000000, -0.000000000000000000 ) ) ;
#20632=CARTESIAN_POINT ( 'NONE',  ( 21.04999999999998650, 6.650000000011155876, -146.2500000000000284 ) ) ;
#20635=EDGE_CURVE ( 'NONE', #255163, #235252, #36736, .T. ) ;
#20658=ORIENTED_EDGE ( 'NONE', *, *, #184123, .F. ) ;
#20673=CARTESIAN_POINT ( 'NONE',  ( -23.25000000000000000, 1.115600667400684642E-11, -134.0000000000000000 ) ) ;
#20688=ORIENTED_EDGE ( 'NONE', *, *, #222485, .F. ) ;
#20719=CARTESIAN_POINT ( 'NONE',  ( 21.14999999999999858, 1.115600667400684642E-11, -134.1000000000000227 ) ) ;
#20723=ORIENTED_EDGE ( 'NONE', *, *, #256177, .T. ) ;
#20750=CARTESIAN_POINT ( 'NONE',  ( -23.15000000000000213, 11.75000000001115552, -134.0000000000000000 ) ) ;
#20753=CARTESIAN_POINT ( 'NONE',  ( -21.05000000000000071, -11.39257802169451139, -164.4260504201680817 ) ) ;
#20781=DIRECTION ( 'NONE',  ( 1.000000000000000000, 3.265361837132813093E-16, -0.000000000000000000 ) ) ;
#20787=DIRECTION ( 'NONE',  ( 0.000000000000000000, 0.000000000000000000, -1.000000000000000000 ) ) ;
#20824=ORIENTED_EDGE ( 'NONE', *, *, #249384, .T. ) ;
#20852=EDGE_CURVE ( 'NONE', #104663, #115992, #28564, .T. ) ;
#20854=CYLINDRICAL_SURFACE ( 'NONE', #38993, 0.09999999999998898659 ) ;
#20921=ORIENTED_EDGE ( 'NONE', *, *, #9159, .F. ) ;
#20940=VERTEX_POINT ( 'NONE', #29636 ) ;
#20943=ORIENTED_EDGE ( 'NONE', *, *, #7982, .T. ) ;
#21028=CARTESIAN_POINT ( 'NONE',  ( 23.14999999999999858, 1.115600667400684642E-11, -167.5000000000000284 ) ) ;
#21032=CARTESIAN_POINT ( 'NONE',  ( 20.94999999999999929, 1.115600667400684642E-11, -167.5000000000000284 ) ) ;
#21038=ORIENTED_EDGE ( 'NONE', *, *, #173636, .T. ) ;
#21080=AXIS2_PLACEMENT_3D ( 'NONE', #132260, #211812, #14904 ) ;
#21082=DIRECTION ( 'NONE',  ( 0.000000000000000000, 0.000000000000000000, -1.000000000000000000 ) ) ;
#21150=ORIENTED_EDGE ( 'NONE', *, *, #69149, .T. ) ;
#21155=CARTESIAN_POINT ( 'NONE',  ( -23.15000000000000213, 2.500000000011154633, -154.2753780772379173 ) ) ;
#21184=CARTESIAN_POINT ( 'NONE',  ( 21.05000000000000071, 1.360870587203197646, -142.0729979270909951 ) ) ;
#21220=ORIENTED_EDGE ( 'NONE', *, *, #98216, .F. ) ;
#21232=AXIS2_PLACEMENT_3D ( 'NONE', #44626, #87575, #147570 ) ;
#21262=CARTESIAN_POINT ( 'NONE',  ( -20.94999999999999929, 1.835341550235569663, -145.5551512925629822 ) ) ;
#21274=EDGE_CURVE ( 'NONE', #175518, #16470, #178571, .T. ) ;
#21316=CARTESIAN_POINT ( 'NONE',  ( -22.59999999999999787, 0.1000000000111554016, -122.3504291924552234 ) ) ;
#21354=CARTESIAN_POINT ( 'NONE',  ( -18.59999999999999787, 11.75000000001115197, -146.1500000000000341 ) ) ;
#21424=CARTESIAN_POINT ( 'NONE',  ( 18.59999999999999076, -1.851617760457748618, -179.1031897196036766 ) ) ;
#21427=FACE_OUTER_BOUND ( 'NONE', #203772, .T. ) ;
#21428=EDGE_CURVE ( 'NONE', #39562, #185781, #94750, .T. ) ;
#21482=ORIENTED_EDGE ( 'NONE', *, *, #168378, .F. ) ;
#21497=ORIENTED_EDGE ( 'NONE', *, *, #194735, .T. ) ;
#21499=ORIENTED_EDGE ( 'NONE', *, *, #43939, .T. ) ;
#21503=DIRECTION ( 'NONE',  ( -1.000000000000000000, 0.000000000000000000, -0.000000000000000000 ) ) ;
#21512=EDGE_LOOP ( 'NONE', ( #207023, #251003, #109555, #191976, #160953, #17798 ) ) ;
#21534=AXIS2_PLACEMENT_3D ( 'NONE', #165012, #202848, #46333 ) ;
#21548=ORIENTED_EDGE ( 'NONE', *, *, #13305, .T. ) ;
#21549=CIRCLE ( 'NONE', #175680, 0.1000000000000111355 ) ;
#21563=LINE ( 'NONE', #180632, #40056 ) ;
#21564=EDGE_CURVE ( 'NONE', #143423, #231425, #119928, .T. ) ;
#21629=ADVANCED_FACE ( 'NONE', ( #223324 ), #157332, .T. ) ;
#21635=VERTEX_POINT ( 'NONE', #185503 ) ;
#21671=CARTESIAN_POINT ( 'NONE',  ( 19.97071067811865674, 11.72071067812981937, -158.6500000000000057 ) ) ;
#21675=ADVANCED_FACE ( 'NONE', ( #29038, #168559 ), #244171, .T. ) ;
#21693=VERTEX_POINT ( 'NONE', #86363 ) ;
#21694=ORIENTED_EDGE ( 'NONE', *, *, #102054, .T. ) ;
#21716=LINE ( 'NONE', #84182, #26305 ) ;
#21720=CARTESIAN_POINT ( 'NONE',  ( 20.85000000000000142, -11.64999999998883595, -167.5000000000000000 ) ) ;
#21724=CARTESIAN_POINT ( 'NONE',  ( -18.54159361262949801, -9.463132135481945539, -141.0491222162928864 ) ) ;
#21726=ORIENTED_EDGE ( 'NONE', *, *, #226467, .F. ) ;
#21728=CIRCLE ( 'NONE', #167488, 11.90000000000000213 ) ;
#21746=DIRECTION ( 'NONE',  ( 0.000000000000000000, 0.000000000000000000, 1.000000000000000000 ) ) ;
#21766=ADVANCED_FACE ( 'NONE', ( #152827 ), #148961, .F. ) ;
#21819=EDGE_CURVE ( 'NONE', #192257, #113536, #120109, .T. ) ;
#21826=AXIS2_PLACEMENT_3D ( 'NONE', #4735, #140406, #2172 ) ;
#21840=DIRECTION ( 'NONE',  ( 1.000000000000000000, 0.000000000000000000, -0.000000000000000000 ) ) ;
#21849=DIRECTION ( 'NONE',  ( 1.000000000000000000, 0.000000000000000000, 0.000000000000000000 ) ) ;
#21857=DIRECTION ( 'NONE',  ( 0.000000000000000000, -0.9893560106964500722, 0.1455152366551550613 ) ) ;
#21858=DIRECTION ( 'NONE',  ( -1.000000000000000000, 0.000000000000000000, 0.000000000000000000 ) ) ;
#21865=AXIS2_PLACEMENT_3D ( 'NONE', #38158, #134645, #137235 ) ;
#21875=CARTESIAN_POINT ( 'NONE',  ( 21.03670563405603033, 10.62482368933940258, -146.3255468862092528 ) ) ;
#21880=CARTESIAN_POINT ( 'NONE',  ( 22.49066049874202022, 0.05634325154338429287, -122.3499877624829111 ) ) ;
#21893=DIRECTION ( 'NONE',  ( 0.000000000000000000, 0.000000000000000000, -1.000000000000000000 ) ) ;
#21928=DIRECTION ( 'NONE',  ( 0.000000000000000000, -0.9908441862701600211, -0.1350103645451876666 ) ) ;
#21955=CYLINDRICAL_SURFACE ( 'NONE', #138952, 0.09999999999998898659 ) ;
#21969=( BOUNDED_SURFACE ( )  B_SPLINE_SURFACE ( 3, 2, ( 
 ( #200356, #99938, #834 ),
 ( #159967, #238179, #118250 ),
 ( #216050, #19145, #59522 ),
 ( #139054, #81649, #82936 ),
 ( #178253, #60825, #21724 ),
 ( #257695, #79097, #219913 ),
 ( #218610, #41310, #240773 ),
 ( #185921, #146765, #124675 ) ),
 .UNSPECIFIED., .F., .F., .F. ) 
 B_SPLINE_SURFACE_WITH_KNOTS ( ( 4, 2, 2, 4 ),
 ( 3, 3 ),
 ( 0.0001723339234021422576, 0.0002782939632049988743, 0.0003842540030078555181, 0.0005961740826135687515 ),
 ( 0.000000000000000000, 1.000000000000000000 ),
 .UNSPECIFIED. ) 
 GEOMETRIC_REPRESENTATION_ITEM ( )  RATIONAL_B_SPLINE_SURFACE ( (
 ( 1.000000000000000000, 0.9504532311154454405, 1.000000000000000000),
 ( 1.000000000000000000, 0.9506023220706004695, 1.000000000000000000),
 ( 1.000000000000000000, 0.9395774818186980459, 1.000000000000000000),
 ( 1.000000000000000000, 0.9079328464641933660, 1.000000000000000000),
 ( 1.000000000000000000, 0.8875702416205810685, 1.000000000000000000),
 ( 1.000000000000000000, 0.8205919608039069502, 1.000000000000000000),
 ( 1.000000000000000000, 0.7666842783599246980, 1.000000000000000000),
 ( 1.000000000000000000, 0.7071067811864361063, 1.000000000000000000) ) ) 
 REPRESENTATION_ITEM ( '' )  SURFACE ( )  );
#21972=DIRECTION ( 'NONE',  ( 1.000000000000000000, 0.000000000000000000, 0.000000000000000000 ) ) ;
#21980=ORIENTED_EDGE ( 'NONE', *, *, #239232, .T. ) ;
#22007=DIRECTION ( 'NONE',  ( 0.000000000000000000, 0.000000000000000000, -1.000000000000000000 ) ) ;
#22026=ORIENTED_EDGE ( 'NONE', *, *, #119203, .T. ) ;
#22029=EDGE_LOOP ( 'NONE', ( #222995, #82118, #195485, #47375 ) ) ;
#22032=FACE_OUTER_BOUND ( 'NONE', #227349, .T. ) ;
#22066=CARTESIAN_POINT ( 'NONE',  ( 21.05000000000000071, 4.850467289730776344, -155.4657325909983570 ) ) ;
#22068=TOROIDAL_SURFACE ( 'NONE', #201114, 12.77499999999999858, 0.1000000000000000056 ) ;
#22086=AXIS2_PLACEMENT_3D ( 'NONE', #69493, #149030, #49900 ) ;
#22144=CARTESIAN_POINT ( 'NONE',  ( -23.25000000000000000, 1.115600667400684642E-11, -167.5000000000000284 ) ) ;
#22225=EDGE_CURVE ( 'NONE', #91601, #70632, #170190, .T. ) ;
#22241=ORIENTED_EDGE ( 'NONE', *, *, #207874, .F. ) ;
#22284=DIRECTION ( 'NONE',  ( 0.000000000000000000, 0.9998779222360096863, -0.01562500000001061998 ) ) ;
#22299=ORIENTED_EDGE ( 'NONE', *, *, #66446, .F. ) ;
#22303=VERTEX_POINT ( 'NONE', #163218 ) ;
#22325=ORIENTED_EDGE ( 'NONE', *, *, #129588, .F. ) ;
#22328=ORIENTED_EDGE ( 'NONE', *, *, #9950, .F. ) ;
#22330=LINE ( 'NONE', #2721, #47179 ) ;
#22335=DIRECTION ( 'NONE',  ( 0.000000000000000000, -0.9908441862701782288, 0.1350103645450542456 ) ) ;
#22383=LINE ( 'NONE', #141036, #136152 ) ;
#22401=TOROIDAL_SURFACE ( 'NONE', #226360, 0.2000000000000000111, 0.1000000000000000056 ) ;
#22418=ORIENTED_EDGE ( 'NONE', *, *, #47686, .T. ) ;
#22433=CARTESIAN_POINT ( 'NONE',  ( -18.59999999999999787, 11.75000000001115197, -122.2500000000000284 ) ) ;
#22434=DIRECTION ( 'NONE',  ( 0.000000000000000000, 0.1350103645451876666, 0.9908441862701600211 ) ) ;
#22446=DIRECTION ( 'NONE',  ( 0.000000000000000000, 0.000000000000000000, -1.000000000000000000 ) ) ;
#22473=CIRCLE ( 'NONE', #168241, 0.09999999999999939493 ) ;
#22505=CYLINDRICAL_SURFACE ( 'NONE', #193597, 0.09999999999999939493 ) ;
#22520=ORIENTED_EDGE ( 'NONE', *, *, #180898, .F. ) ;
#22555=DIRECTION ( 'NONE',  ( 0.000000000000000000, 0.000000000000000000, 1.000000000000000000 ) ) ;
#22557=CARTESIAN_POINT ( 'NONE',  ( -20.64999999999999858, 1.115600667400684642E-11, -167.5000000000000284 ) ) ;
#22558=ORIENTED_EDGE ( 'NONE', *, *, #30630, .T. ) ;
#22581=PLANE ( 'NONE',  #114723 ) ;
#22586=LINE ( 'NONE', #162102, #102200 ) ;
#22590=DIRECTION ( 'NONE',  ( 2.952720810173289112E-16, -1.000000000000000000, 0.000000000000000000 ) ) ;
#22596=ORIENTED_EDGE ( 'NONE', *, *, #230854, .T. ) ;
#22611=CIRCLE ( 'NONE', #47509, 0.09999999999998898659 ) ;
#22616=ADVANCED_FACE ( 'NONE', ( #44248 ), #8029, .F. ) ;
#22644=VECTOR ( 'NONE', #213465, 1000.000000000000227 ) ;
#22653=ORIENTED_EDGE ( 'NONE', *, *, #249770, .T. ) ;
#22654=AXIS2_PLACEMENT_3D ( 'NONE', #64634, #223692, #45074 ) ;
#22663=CARTESIAN_POINT ( 'NONE',  ( -21.03922262424684675, 11.62390063401601381, -140.8592080428932718 ) ) ;
#22701=ORIENTED_EDGE ( 'NONE', *, *, #192464, .F. ) ;
#22720=EDGE_LOOP ( 'NONE', ( #140434, #254809 ) ) ;
#22733=CARTESIAN_POINT ( 'NONE',  ( -22.50000000000088463, 0.04536165659896403135, -122.3494911657900843 ) ) ;
#22815=DIRECTION ( 'NONE',  ( -0.000000000000000000, 0.000000000000000000, 1.000000000000000000 ) ) ;
#22821=AXIS2_PLACEMENT_3D ( 'NONE', #247617, #48126, #171976 ) ;
#22845=CARTESIAN_POINT ( 'NONE',  ( -21.05000000000000071, 1.835341550235567887, -145.6551512925629766 ) ) ;
#22859=ORIENTED_EDGE ( 'NONE', *, *, #164497, .F. ) ;
#22882=ORIENTED_EDGE ( 'NONE', *, *, #154566, .T. ) ;
#22891=DIRECTION ( 'NONE',  ( 0.000000000000000000, 0.000000000000000000, 1.000000000000000000 ) ) ;
#22940=EDGE_CURVE ( 'NONE', #147657, #11395, #139142, .T. ) ;
#22960=AXIS2_PLACEMENT_3D ( 'NONE', #253485, #71032, #214370 ) ;
#22976=CARTESIAN_POINT ( 'NONE',  ( 19.80993210785717551, 11.75000000001116263, -158.7671177488815317 ) ) ;
#22989=ORIENTED_EDGE ( 'NONE', *, *, #126178, .T. ) ;
#23005=CARTESIAN_POINT ( 'NONE',  ( -18.59999999999999787, 11.65000000001115232, -141.0148057706540214 ) ) ;
#23021=DIRECTION ( 'NONE',  ( -2.557131231893036985E-16, 0.8660254037844384856, -0.5000000000000002220 ) ) ;
#23043=CARTESIAN_POINT ( 'NONE',  ( -18.50000000000001066, -9.480686695267808162, -174.4411151687578752 ) ) ;
#23046=DIRECTION ( 'NONE',  ( -3.469446951953635015E-14, -1.000000000000000000, 0.000000000000000000 ) ) ;
#23051=ADVANCED_FACE ( 'NONE', ( #45205 ), #24384, .F. ) ;
#23056=AXIS2_PLACEMENT_3D ( 'NONE', #37223, #134995, #175458 ) ;
#23063=ADVANCED_FACE ( 'NONE', ( #165160 ), #64765, .T. ) ;
#23127=( BOUNDED_SURFACE ( )  B_SPLINE_SURFACE ( 3, 2, ( 
 ( #17873, #37466, #199091 ),
 ( #218635, #197796, #157436 ),
 ( #116987, #19164, #82952 ),
 ( #2154, #239510, #81667 ) ),
 .UNSPECIFIED., .F., .F., .T. ) 
 B_SPLINE_SURFACE_WITH_KNOTS ( ( 4, 4 ),
 ( 3, 3 ),
 ( 0.0006461284895273780972, 0.0007503702773985577784 ),
 ( 0.000000000000000000, 1.000000000000000000 ),
 .UNSPECIFIED. ) 
 GEOMETRIC_REPRESENTATION_ITEM ( )  RATIONAL_B_SPLINE_SURFACE ( (
 ( 1.000000000000000000, 0.7071067811865475727, 1.000000000000000000),
 ( 1.000000000000000000, 0.7076476444648740483, 1.000000000000000000),
 ( 1.000000000000000000, 0.7075727925191939160, 1.000000000000000000),
 ( 1.000000000000000000, 0.7071067811865475727, 1.000000000000000000) ) ) 
 REPRESENTATION_ITEM ( '' )  SURFACE ( )  );
#23137=TOROIDAL_SURFACE ( 'NONE', #181542, 11.65000000000000036, 0.1000000000000000056 ) ;
#23153=EDGE_LOOP ( 'NONE', ( #240828, #65203, #101227, #186971 ) ) ;
#23160=CARTESIAN_POINT ( 'NONE',  ( -20.94999999999999929, 14.05000000001115623, -139.5136950707610026 ) ) ;
#23175=EDGE_CURVE ( 'NONE', #14355, #104087, #171612, .T. ) ;
#23183=CARTESIAN_POINT ( 'NONE',  ( 22.39999999999999503, 1.115600667400684642E-11, -122.3504291924552234 ) ) ;
#23215=DIRECTION ( 'NONE',  ( 1.000000000000000000, 0.000000000000000000, 0.000000000000000000 ) ) ;
#23218=VERTEX_POINT ( 'NONE', #129866 ) ;
#23225=CARTESIAN_POINT ( 'NONE',  ( -20.85000000000000142, -11.74999999998884448, -167.5000000000000000 ) ) ;
#23244=CARTESIAN_POINT ( 'NONE',  ( -20.94999999999999929, 5.850000000011160495, -157.3675027757221017 ) ) ;
#23252=DIRECTION ( 'NONE',  ( 0.000000000000000000, 0.000000000000000000, -1.000000000000000000 ) ) ;
#23267=EDGE_LOOP ( 'NONE', ( #21548, #108253, #221185, #33459, #34787, #125301, #213278, #207014, #76, #157364, #208564, #120178, #73910, #93161, #22558, #27944, #71878, #37934, #151114, #21482, #217801, #79406, #179593 ) ) ;
#23273=EDGE_LOOP ( 'NONE', ( #26077, #218139, #51448, #140965 ) ) ;
#23289=DIRECTION ( 'NONE',  ( -1.000000000000000000, -2.952720810173289112E-16, 0.000000000000000000 ) ) ;
#23296=CIRCLE ( 'NONE', #160669, 0.09999999999998898659 ) ;
#23305=EDGE_LOOP ( 'NONE', ( #81453, #224277, #221447, #219782 ) ) ;
#23330=CARTESIAN_POINT ( 'NONE',  ( -20.12071067811865888, 9.320710678129810134, -146.3500000000000227 ) ) ;
#23364=CARTESIAN_POINT ( 'NONE',  ( 18.49999999999999645, 1.115600667400684642E-11, -134.0000000000000000 ) ) ;
#23366=CARTESIAN_POINT ( 'NONE',  ( -18.39999999999999858, -9.519327731081281385, -140.9729763765593589 ) ) ;
#23376=DIRECTION ( 'NONE',  ( 0.000000000000000000, 0.000000000000000000, -1.000000000000000000 ) ) ;
#23410=FACE_BOUND ( 'NONE', #201613, .T. ) ;
#23417=EDGE_CURVE ( 'NONE', #243619, #212843, #137348, .T. ) ;
#23419=CARTESIAN_POINT ( 'NONE',  ( 21.05000000000000071, 5.500000000011153745, -146.4052660189131245 ) ) ;
#23438=FACE_OUTER_BOUND ( 'NONE', #58694, .T. ) ;
#23442=DIRECTION ( 'NONE',  ( 3.469446951953243109E-14, 0.4999999999999608646, 0.8660254037844612451 ) ) ;
#23482=CARTESIAN_POINT ( 'NONE',  ( 21.05000000000000071, -0.09999999998884512298, -127.4593430482987912 ) ) ;
#23518=CARTESIAN_POINT ( 'NONE',  ( -20.54999999999999716, 1.115600667400684642E-11, -134.0000000000000000 ) ) ;
#23522=DIRECTION ( 'NONE',  ( 0.000000000000000000, 0.000000000000000000, -1.000000000000000000 ) ) ;
#23530=CIRCLE ( 'NONE', #202369, 0.09999999999998807065 ) ;
#23542=LINE ( 'NONE', #224259, #105580 ) ;
#23561=ORIENTED_EDGE ( 'NONE', *, *, #130024, .T. ) ;
#23578=LINE ( 'NONE', #3968, #193981 ) ;
#23602=ORIENTED_EDGE ( 'NONE', *, *, #123869, .T. ) ;
#23648=CYLINDRICAL_SURFACE ( 'NONE', #32815, 0.09999999999999939493 ) ;
#23651=EDGE_LOOP ( 'NONE', ( #40309, #156661, #30934, #133444 ) ) ;
#23708=ORIENTED_EDGE ( 'NONE', *, *, #34887, .T. ) ;
#23710=FACE_OUTER_BOUND ( 'NONE', #199621, .T. ) ;
#23713=VERTEX_POINT ( 'NONE', #161681 ) ;
#23752=EDGE_LOOP ( 'NONE', ( #157790, #202216, #116557, #164669 ) ) ;
#23774=FACE_OUTER_BOUND ( 'NONE', #78388, .T. ) ;
#23822=DIRECTION ( 'NONE',  ( -1.000000000000000000, -0.000000000000000000, 0.000000000000000000 ) ) ;
#23830=CARTESIAN_POINT ( 'NONE',  ( -21.05000000000000071, 1.115600667400684642E-11, -134.0000000000000000 ) ) ;
#23832=EDGE_CURVE ( 'NONE', #172414, #170581, #208659, .T. ) ;
#23834=CARTESIAN_POINT ( 'NONE',  ( -21.05000000000000071, 5.850000000011156942, -157.3675027757221017 ) ) ;
#23885=DIRECTION ( 'NONE',  ( 0.000000000000000000, 0.9999631594459056361, -0.008583690987128059571 ) ) ;
#23909=VERTEX_POINT ( 'NONE', #223253 ) ;
#23935=EDGE_LOOP ( 'NONE', ( #20658, #216973, #158050 ) ) ;
#23938=CARTESIAN_POINT ( 'NONE',  ( -21.05000000000000071, -1.835341550213257733, -145.5551512925629822 ) ) ;
#24015=AXIS2_PLACEMENT_3D ( 'NONE', #193673, #215776, #35899 ) ;
#24019=CARTESIAN_POINT ( 'NONE',  ( 21.14999999999999858, 1.115600667400684642E-11, -134.0000000000000000 ) ) ;
#24037=FACE_OUTER_BOUND ( 'NONE', #29350, .T. ) ;
#24040=CARTESIAN_POINT ( 'NONE',  ( 21.05000000000000071, 1.115650877919449575E-11, -163.4000000000000341 ) ) ;
#24087=AXIS2_PLACEMENT_3D ( 'NONE', #225323, #70156, #10159 ) ;
#24116=FACE_OUTER_BOUND ( 'NONE', #81539, .T. ) ;
#24159=DIRECTION ( 'NONE',  ( 1.000000000000000000, 0.000000000000000000, 0.000000000000000000 ) ) ;
#24160=ORIENTED_EDGE ( 'NONE', *, *, #164698, .T. ) ;
#24195=DIRECTION ( 'NONE',  ( -1.000000000000000000, -1.836970198721029934E-16, 0.000000000000000000 ) ) ;
#24241=CYLINDRICAL_SURFACE ( 'NONE', #100597, 0.09999999999998898659 ) ;
#24271=VERTEX_POINT ( 'NONE', #114876 ) ;
#24309=TOROIDAL_SURFACE ( 'NONE', #111769, 0.2000000000000000111, 0.1000000000000000056 ) ;
#24315=ORIENTED_EDGE ( 'NONE', *, *, #49065, .F. ) ;
#24343=CARTESIAN_POINT ( 'NONE',  ( 20.02499999999999858, 9.750000000011153745, -155.1500000000000057 ) ) ;
#24350=CARTESIAN_POINT ( 'NONE',  ( 22.47007471830799474, 7.720710651937603863, -134.0000000000000000 ) ) ;
#24351=AXIS2_PLACEMENT_3D ( 'NONE', #154014, #134372, #17034 ) ;
#24376=CARTESIAN_POINT ( 'NONE',  ( -23.25000000000000000, 6.982009704867601307, -171.1961521182563217 ) ) ;
#24384=CYLINDRICAL_SURFACE ( 'NONE', #141454, 2.000000000000001776 ) ;
#24392=EDGE_CURVE ( 'NONE', #176500, #253862, #254606, .T. ) ;
#24416=AXIS2_PLACEMENT_3D ( 'NONE', #58819, #197060, #234926 ) ;
#24426=CARTESIAN_POINT ( 'NONE',  ( 18.59999999999999787, -1.736705739456431807, -179.0174225876237415 ) ) ;
#24443=CARTESIAN_POINT ( 'NONE',  ( -21.52071067811865746, 7.779289321892505882, -155.1500000000000057 ) ) ;
#24464=CARTESIAN_POINT ( 'NONE',  ( 20.95512820512820795, 10.62384868372303615, -146.2001620194244538 ) ) ;
#24469=CARTESIAN_POINT ( 'NONE',  ( 22.49999999999999645, 0.08880997639808871358, -122.3502370819681033 ) ) ;
#24470=AXIS2_PLACEMENT_3D ( 'NONE', #222159, #18845, #120546 ) ;
#24483=DIRECTION ( 'NONE',  ( 0.000000000000000000, 1.084202172485623868E-14, 1.000000000000000000 ) ) ;
#24494=CARTESIAN_POINT ( 'NONE',  ( 21.14999999999999503, 1.115600667400684642E-11, -134.0000000000000000 ) ) ;
#24497=CARTESIAN_POINT ( 'NONE',  ( -23.25000000000000000, 11.75000000001115552, -134.0000000000000000 ) ) ;
#24504=CARTESIAN_POINT ( 'NONE',  ( -18.50000000000000000, -9.499999999988849808, -142.1000000000000227 ) ) ;
#24551=CARTESIAN_POINT ( 'NONE',  ( -18.54270223418606989, -9.624105502871749707, -174.2409350504074723 ) ) ;
#24559=EDGE_LOOP ( 'NONE', ( #179470, #31265, #180473, #215496 ) ) ;
#24563=VERTEX_POINT ( 'NONE', #14213 ) ;
#24567=CARTESIAN_POINT ( 'NONE',  ( -20.64999999999999858, 7.250000000011155521, -146.2500000000000284 ) ) ;
#24593=ADVANCED_FACE ( 'NONE', ( #93721 ), #75473, .F. ) ;
#24610=VECTOR ( 'NONE', #251634, 1000.000000000000000 ) ;
#24611=ORIENTED_EDGE ( 'NONE', *, *, #203258, .T. ) ;
#24641=DIRECTION ( 'NONE',  ( -1.000000000000000000, 0.000000000000000000, -0.000000000000000000 ) ) ;
#24672=TOROIDAL_SURFACE ( 'NONE', #49588, 0.2000000000000000111, 0.1000000000000000056 ) ;
#24728=EDGE_CURVE ( 'NONE', #26254, #250075, #123555, .T. ) ;
#24737=ORIENTED_EDGE ( 'NONE', *, *, #66674, .F. ) ;
#24757=EDGE_LOOP ( 'NONE', ( #181875, #22299, #18452, #21726, #157025 ) ) ;
#24762=CARTESIAN_POINT ( 'NONE',  ( 21.04999999999999716, -0.01454569055791622018, -127.5029822135672077 ) ) ;
#24827=DIRECTION ( 'NONE',  ( -1.000000000000000000, 0.000000000000000000, 0.000000000000000000 ) ) ;
#24868=DIRECTION ( 'NONE',  ( 0.000000000000000000, 0.000000000000000000, -1.000000000000000000 ) ) ;
#24888=VECTOR ( 'NONE', #2415, 1000.000000000000000 ) ;
#24909=DIRECTION ( 'NONE',  ( 0.000000000000000000, -0.1455152366551721865, -0.9893560106964475187 ) ) ;
#24931=EDGE_CURVE ( 'NONE', #99200, #256904, #1264, .T. ) ;
#24954=DIRECTION ( 'NONE',  ( 0.000000000000000000, 0.000000000000000000, 1.000000000000000000 ) ) ;
#24971=DIRECTION ( 'NONE',  ( -1.000000000000000000, 0.000000000000000000, 0.000000000000000000 ) ) ;
#25002=CARTESIAN_POINT ( 'NONE',  ( -21.05000000000000071, -1.249999999988843369, -142.0000000000000284 ) ) ;
#25009=CARTESIAN_POINT ( 'NONE',  ( -20.64999999999999858, 7.250000000011155521, -155.1500000000000057 ) ) ;
#25016=ADVANCED_FACE ( 'NONE', ( #155975 ), #97099, .T. ) ;
#25067=EDGE_CURVE ( 'NONE', #38015, #189087, #97276, .T. ) ;
#25070=ORIENTED_EDGE ( 'NONE', *, *, #10542, .F. ) ;
#25085=FACE_OUTER_BOUND ( 'NONE', #115869, .T. ) ;
#25105=ORIENTED_EDGE ( 'NONE', *, *, #128872, .T. ) ;
#25128=ORIENTED_EDGE ( 'NONE', *, *, #129878, .T. ) ;
#25137=AXIS2_PLACEMENT_3D ( 'NONE', #183787, #121287, #5108 ) ;
#25143=ORIENTED_EDGE ( 'NONE', *, *, #22225, .F. ) ;
#25151=CIRCLE ( 'NONE', #58419, 0.09999999999998898659 ) ;
#25158=CARTESIAN_POINT ( 'NONE',  ( -18.50000000000000000, 11.65000000001115232, -146.1500000000000341 ) ) ;
#25173=VERTEX_POINT ( 'NONE', #42416 ) ;
#25206=AXIS2_PLACEMENT_3D ( 'NONE', #250370, #151287, #230830 ) ;
#25214=EDGE_CURVE ( 'NONE', #226065, #147930, #172390, .T. ) ;
#25221=AXIS2_PLACEMENT_3D ( 'NONE', #77759, #219850, #157356 ) ;
#25230=ORIENTED_EDGE ( 'NONE', *, *, #248462, .F. ) ;
#25234=DIRECTION ( 'NONE',  ( 0.000000000000000000, 0.000000000000000000, -1.000000000000000000 ) ) ;
#25243=LINE ( 'NONE', #166045, #90868 ) ;
#25295=VERTEX_POINT ( 'NONE', #250879 ) ;
#25335=ADVANCED_FACE ( 'NONE', ( #154402 ), #147212, .T. ) ;
#25337=EDGE_CURVE ( 'NONE', #200535, #142216, #27083, .T. ) ;
#25346=ORIENTED_EDGE ( 'NONE', *, *, #177185, .F. ) ;
#25353=DIRECTION ( 'NONE',  ( 1.000000000000000000, 0.000000000000000000, 0.000000000000000000 ) ) ;
#25372=DIRECTION ( 'NONE',  ( 0.000000000000000000, 0.000000000000000000, -1.000000000000000000 ) ) ;
#25380=AXIS2_PLACEMENT_3D ( 'NONE', #157403, #114387, #193936 ) ;
#25400=DIRECTION ( 'NONE',  ( -1.000000000000000000, 0.000000000000000000, 0.000000000000000000 ) ) ;
#25407=DIRECTION ( 'NONE',  ( -1.000000000000000000, 0.000000000000000000, 0.000000000000000000 ) ) ;
#25422=ORIENTED_EDGE ( 'NONE', *, *, #51710, .F. ) ;
#25483=ORIENTED_EDGE ( 'NONE', *, *, #66715, .F. ) ;
#25486=CIRCLE ( 'NONE', #58774, 7.800000000000000711 ) ;
#25508=ORIENTED_EDGE ( 'NONE', *, *, #103494, .T. ) ;
#25521=DIRECTION ( 'NONE',  ( -1.000000000000000000, 6.938893903907270030E-14, 0.000000000000000000 ) ) ;
#25533=CARTESIAN_POINT ( 'NONE',  ( 18.50596464788227280, 10.30632246271648889, -173.0041836778896140 ) ) ;
#25544=DIRECTION ( 'NONE',  ( 1.000000000000000000, -0.000000000000000000, -0.000000000000000000 ) ) ;
#25573=DIRECTION ( 'NONE',  ( -1.000000000000000000, -3.265361837132813093E-16, 0.000000000000000000 ) ) ;
#25594=CARTESIAN_POINT ( 'NONE',  ( -18.54260524012587297, -9.624219390062703994, -174.2407730457707089 ) ) ;
#25620=PLANE ( 'NONE',  #213021 ) ;
#25651=EDGE_CURVE ( 'NONE', #61093, #149809, #134887, .T. ) ;
#25653=CARTESIAN_POINT ( 'NONE',  ( -20.00857864376270001, 9.150000000011157653, -155.2500000000000284 ) ) ;
#25687=CARTESIAN_POINT ( 'NONE',  ( -21.05000000000000071, 1.162701749949165642, -142.1000000000000227 ) ) ;
#25703=DIRECTION ( 'NONE',  ( -1.000000000000000000, -0.000000000000000000, -0.000000000000000000 ) ) ;
#25715=EDGE_LOOP ( 'NONE', ( #253750, #193825, #84515, #195190 ) ) ;
#25721=DIRECTION ( 'NONE',  ( -1.000000000000000000, 0.000000000000000000, 0.000000000000000000 ) ) ;
#25731=DIRECTION ( 'NONE',  ( 1.000000000000000000, 0.000000000000000000, 0.000000000000000000 ) ) ;
#25750=AXIS2_PLACEMENT_3D ( 'NONE', #188877, #143320, #8953 ) ;
#25757=ORIENTED_EDGE ( 'NONE', *, *, #119405, .T. ) ;
#25806=EDGE_CURVE ( 'NONE', #7738, #113603, #112522, .T. ) ;
#25818=VERTEX_POINT ( 'NONE', #189491 ) ;
#25831=ORIENTED_EDGE ( 'NONE', *, *, #138813, .T. ) ;
#25845=ADVANCED_FACE ( 'NONE', ( #10851 ), #5339, .F. ) ;
#25900=EDGE_LOOP ( 'NONE', ( #197043, #182394, #25143 ) ) ;
#25910=EDGE_LOOP ( 'NONE', ( #235028, #61536, #238740 ) ) ;
#25926=CYLINDRICAL_SURFACE ( 'NONE', #173071, 0.09999999999998898659 ) ;
#25984=LINE ( 'NONE', #7709, #94048 ) ;
#25999=ORIENTED_EDGE ( 'NONE', *, *, #55270, .F. ) ;
#26004=CARTESIAN_POINT ( 'NONE',  ( 18.59999994388910238, -9.363566187060129664, -141.1811172368007590 ) ) ;
#26058=FACE_OUTER_BOUND ( 'NONE', #94109, .T. ) ;
#26065=DIRECTION ( 'NONE',  ( 0.000000000000000000, -0.6728971962617388280, 0.7397360091702248619 ) ) ;
#26077=ORIENTED_EDGE ( 'NONE', *, *, #104139, .T. ) ;
#26116=AXIS2_PLACEMENT_3D ( 'NONE', #203673, #184101, #245378 ) ;
#26120=AXIS2_PLACEMENT_3D ( 'NONE', #47989, #192655, #70159 ) ;
#26159=TOROIDAL_SURFACE ( 'NONE', #142638, 4.149999999999999467, 0.1000000000000000056 ) ;
#26166=ORIENTED_EDGE ( 'NONE', *, *, #79899, .F. ) ;
#26205=CARTESIAN_POINT ( 'NONE',  ( -21.45000000000000284, 7.708578643773852157, -146.3500000000000227 ) ) ;
#26219=DIRECTION ( 'NONE',  ( 0.000000000000000000, 0.000000000000000000, 1.000000000000000000 ) ) ;
#26229=LINE ( 'NONE', #30096, #144556 ) ;
#26242=AXIS2_PLACEMENT_3D ( 'NONE', #85617, #244714, #66092 ) ;
#26252=CARTESIAN_POINT ( 'NONE',  ( 23.24999999999999645, 5.600000000011153389, -146.4052660189131245 ) ) ;
#26254=VERTEX_POINT ( 'NONE', #197831 ) ;
#26261=DIRECTION ( 'NONE',  ( 0.000000000000000000, 0.000000000000000000, -1.000000000000000000 ) ) ;
#26264=CARTESIAN_POINT ( 'NONE',  ( -22.50000000000000000, 0.09263750062063520752, -122.3503027929592690 ) ) ;
#26284=DIRECTION ( 'NONE',  ( 1.000000000000000000, 3.265361837132813093E-16, -0.000000000000000000 ) ) ;
#26305=VECTOR ( 'NONE', #85488, 1000.000000000000000 ) ;
#26307=ORIENTED_EDGE ( 'NONE', *, *, #130286, .F. ) ;
#26371=ADVANCED_FACE ( 'NONE', ( #63452 ), #20545, .F. ) ;
#26384=FACE_OUTER_BOUND ( 'NONE', #139021, .T. ) ;
#26441=ORIENTED_EDGE ( 'NONE', *, *, #81482, .F. ) ;
#26450=ADVANCED_FACE ( 'NONE', ( #34632 ), #152017, .F. ) ;
#26457=ORIENTED_EDGE ( 'NONE', *, *, #71435, .T. ) ;
#26467=EDGE_CURVE ( 'NONE', #189027, #113973, #52831, .T. ) ;
#26525=DIRECTION ( 'NONE',  ( -3.265361837132813093E-16, 1.000000000000000000, -0.000000000000000000 ) ) ;
#26571=AXIS2_PLACEMENT_3D ( 'NONE', #200949, #43169, #142256 ) ;
#26579=VERTEX_POINT ( 'NONE', #174165 ) ;
#26641=( GEOMETRIC_REPRESENTATION_CONTEXT ( 3 ) GLOBAL_UNCERTAINTY_ASSIGNED_CONTEXT ( ( #170380 ) ) GLOBAL_UNIT_ASSIGNED_CONTEXT ( ( #57419, #53592, #96539 ) ) REPRESENTATION_CONTEXT ( 'NONE', 'WORKASPACE' ) );
#26660=EDGE_LOOP ( 'NONE', ( #118270, #223598, #84733, #40495, #150949, #77498, #154174, #71609 ) ) ;
#26681=DIRECTION ( 'NONE',  ( 1.000000000000000000, -0.000000000000000000, -0.000000000000000000 ) ) ;
#26684=DIRECTION ( 'NONE',  ( 0.000000000000000000, 0.000000000000000000, -1.000000000000000000 ) ) ;
#26696=CARTESIAN_POINT ( 'NONE',  ( 21.05000000000000071, 1.115600667400684642E-11, -146.1500000000000341 ) ) ;
#26727=ORIENTED_EDGE ( 'NONE', *, *, #34071, .F. ) ;
#26821=ORIENTED_EDGE ( 'NONE', *, *, #90139, .F. ) ;
#26827=CARTESIAN_POINT ( 'NONE',  ( 20.04142135623731136, 11.75000000001116263, -158.6500000000000057 ) ) ;
#26891=CARTESIAN_POINT ( 'NONE',  ( 21.05000000000000071, -1.162701749926853712, -142.1000000000000227 ) ) ;
#26954=DIRECTION ( 'NONE',  ( 0.000000000000000000, -1.000000000000000000, 0.000000000000000000 ) ) ;
#26979=FACE_OUTER_BOUND ( 'NONE', #205445, .T. ) ;
#26988=ADVANCED_FACE ( 'NONE', ( #18599 ), #14319, .T. ) ;
#27004=CARTESIAN_POINT ( 'NONE',  ( 23.15000000000000213, -11.64999999998884483, -134.0000000000000000 ) ) ;
#27014=AXIS2_PLACEMENT_3D ( 'NONE', #246108, #150848, #232975 ) ;
#27018=DIRECTION ( 'NONE',  ( -0.000000000000000000, 0.1350103645451876666, 0.9908441862701600211 ) ) ;
#27020=DIRECTION ( 'NONE',  ( 0.000000000000000000, 0.000000000000000000, 1.000000000000000000 ) ) ;
#27025=CIRCLE ( 'NONE', #85397, 4.000000000000003553 ) ;
#27049=ORIENTED_EDGE ( 'NONE', *, *, #255904, .T. ) ;
#27083=B_SPLINE_CURVE_WITH_KNOTS ( 'NONE', 3,
 ( #13578, #53970, #73572, #233896, #151818, #190947, #55224, #12307, #59654, #98768, #122234, #180922, #201755, #158816, #197902, #240897 ),
 .UNSPECIFIED., .F., .F.,
 ( 4, 3, 3, 3, 3, 4 ),
 ( 0.000000000000000000, 3.357088238232317244E-05, 6.714213034886757942E-05, 0.0001007408646120921551, 0.0001343627955914185768, 0.0001573956632895995484 ),
 .UNSPECIFIED. ) ;
#27132=CARTESIAN_POINT ( 'NONE',  ( -18.52328366898031931, -9.642321089030097880, -174.2148193375701055 ) ) ;
#27147=DIRECTION ( 'NONE',  ( 0.000000000000000000, -1.000000000000000000, 0.000000000000000000 ) ) ;
#27152=DIRECTION ( 'NONE',  ( 0.000000000000000000, 3.552713678800493041E-15, -1.000000000000000000 ) ) ;
#27192=CARTESIAN_POINT ( 'NONE',  ( -20.85000000000000142, -1.263275465206102233, -175.4018646667464338 ) ) ;
#27193=CARTESIAN_POINT ( 'NONE',  ( 21.05000000000000071, 1.115600667400684642E-11, -167.5000000000000284 ) ) ;
#27200=FACE_OUTER_BOUND ( 'NONE', #152400, .T. ) ;
#27215=LINE ( 'NONE', #149723, #138211 ) ;
#27280=FACE_OUTER_BOUND ( 'NONE', #49231, .T. ) ;
#27307=EDGE_CURVE ( 'NONE', #202658, #197481, #46342, .T. ) ;
#27310=ORIENTED_EDGE ( 'NONE', *, *, #256074, .F. ) ;
#27318=CARTESIAN_POINT ( 'NONE',  ( -23.15000000000000213, 11.75000000001115552, -164.4000000000000057 ) ) ;
#27375=VERTEX_POINT ( 'NONE', #233502 ) ;
#27384=EDGE_LOOP ( 'NONE', ( #17414, #230155, #20218, #238816 ) ) ;
#27447=VECTOR ( 'NONE', #146364, 1000.000000000000000 ) ;
#27456=ORIENTED_EDGE ( 'NONE', *, *, #188476, .F. ) ;
#27502=VERTEX_POINT ( 'NONE', #227691 ) ;
#27511=DIRECTION ( 'NONE',  ( 0.000000000000000000, 0.000000000000000000, 1.000000000000000000 ) ) ;
#27517=DIRECTION ( 'NONE',  ( 0.000000000000000000, 1.000000000000000000, 0.000000000000000000 ) ) ;
#27536=DIRECTION ( 'NONE',  ( 0.000000000000000000, -1.000000000000000000, 0.000000000000000000 ) ) ;
#27537=DIRECTION ( 'NONE',  ( 3.469446951953635015E-14, -0.000000000000000000, 1.000000000000000000 ) ) ;
#27565=DIRECTION ( 'NONE',  ( 0.000000000000000000, -1.000000000000000000, 5.551115123125768187E-14 ) ) ;
#27583=DIRECTION ( 'NONE',  ( 1.000000000000000000, -0.000000000000000000, -0.000000000000000000 ) ) ;
#27585=CARTESIAN_POINT ( 'NONE',  ( 21.05000000000000071, 10.48459288120560551, -141.4567135705834460 ) ) ;
#27598=DIRECTION ( 'NONE',  ( -1.000000000000000000, 0.000000000000000000, 0.000000000000000000 ) ) ;
#27606=EDGE_LOOP ( 'NONE', ( #99406, #4538, #146482, #82487 ) ) ;
#27617=ADVANCED_FACE ( 'NONE', ( #76311 ), #157183, .T. ) ;
#27625=AXIS2_PLACEMENT_3D ( 'NONE', #62700, #206056, #160538 ) ;
#27634=ORIENTED_EDGE ( 'NONE', *, *, #182122, .T. ) ;
#27645=CARTESIAN_POINT ( 'NONE',  ( -20.94999999999999929, -11.39257802169451317, -164.4260504201680817 ) ) ;
#27648=FACE_OUTER_BOUND ( 'NONE', #116905, .T. ) ;
#27651=LINE ( 'NONE', #147558, #35710 ) ;
#27654=VERTEX_POINT ( 'NONE', #253667 ) ;
#27656=EDGE_CURVE ( 'NONE', #79888, #42512, #160435, .T. ) ;
#27681=ORIENTED_EDGE ( 'NONE', *, *, #156495, .F. ) ;
#27699=ORIENTED_EDGE ( 'NONE', *, *, #127928, .T. ) ;
#27727=DIRECTION ( 'NONE',  ( 1.000000000000000000, 0.000000000000000000, -0.000000000000000000 ) ) ;
#27737=VECTOR ( 'NONE', #167797, 1000.000000000000000 ) ;
#27755=CARTESIAN_POINT ( 'NONE',  ( -21.05000000000000426, -0.09999999998884341601, -127.5229329788753176 ) ) ;
#27781=CARTESIAN_POINT ( 'NONE',  ( -23.25000000000000000, 2.000000000011154189, -154.8753780772379116 ) ) ;
#27791=CIRCLE ( 'NONE', #65737, 0.09999999999998898659 ) ;
#27799=CARTESIAN_POINT ( 'NONE',  ( 20.12518398540832365, 9.975088720679844201, -141.9966682524667760 ) ) ;
#27841=AXIS2_PLACEMENT_3D ( 'NONE', #50111, #147943, #248320 ) ;
#27856=CARTESIAN_POINT ( 'NONE',  ( 18.59999999999999432, 5.699452464332755319, -121.4577260434301991 ) ) ;
#27871=CARTESIAN_POINT ( 'NONE',  ( -22.39999999999999858, 0.1000000000111554016, -126.2092204016266379 ) ) ;
#27888=AXIS2_PLACEMENT_3D ( 'NONE', #146167, #223135, #9227 ) ;
#27898=DIRECTION ( 'NONE',  ( 1.000000000000000000, 0.000000000000000000, 0.000000000000000000 ) ) ;
#27944=ORIENTED_EDGE ( 'NONE', *, *, #204836, .F. ) ;
#27969=ORIENTED_EDGE ( 'NONE', *, *, #9210, .T. ) ;
#27970=ADVANCED_FACE ( 'NONE', ( #12231 ), #139891, .T. ) ;
#27992=ORIENTED_EDGE ( 'NONE', *, *, #145875, .T. ) ;
#27997=CARTESIAN_POINT ( 'NONE',  ( -20.85000000000000142, -1.851617760457748618, -179.1031897196036766 ) ) ;
#28029=AXIS2_PLACEMENT_3D ( 'NONE', #255380, #41552, #76795 ) ;
#28035=DIRECTION ( 'NONE',  ( 1.000000000000000000, 0.000000000000000000, 0.000000000000000000 ) ) ;
#28104=CARTESIAN_POINT ( 'NONE',  ( 21.05000000000000071, -11.48912529306490349, -137.1000000000000227 ) ) ;
#28119=CARTESIAN_POINT ( 'NONE',  ( 21.14999999999999503, 11.65000000001116298, -134.0000000000000284 ) ) ;
#28159=CYLINDRICAL_SURFACE ( 'NONE', #66034, 0.09999999999999939493 ) ;
#28160=CARTESIAN_POINT ( 'NONE',  ( -20.93284271247462058, 11.75000000001115019, -160.4851942293460354 ) ) ;
#28172=ORIENTED_EDGE ( 'NONE', *, *, #148815, .T. ) ;
#28203=EDGE_CURVE ( 'NONE', #222619, #231078, #52414, .T. ) ;
#28215=AXIS2_PLACEMENT_3D ( 'NONE', #256396, #77810, #157406 ) ;
#28225=CARTESIAN_POINT ( 'NONE',  ( 21.07094088545367327, 0.09889370256337753906, -127.6798327780828686 ) ) ;
#28244=EDGE_CURVE ( 'NONE', #123059, #95323, #27651, .T. ) ;
#28264=VERTEX_POINT ( 'NONE', #130554 ) ;
#28295=DIRECTION ( 'NONE',  ( 0.000000000000000000, -0.000000000000000000, -1.000000000000000000 ) ) ;
#28305=CARTESIAN_POINT ( 'NONE',  ( -20.94403535211772294, 10.30632246271647467, -173.0041836778896140 ) ) ;
#28306=EDGE_CURVE ( 'NONE', #128012, #79795, #177423, .T. ) ;
#28319=ORIENTED_EDGE ( 'NONE', *, *, #155869, .F. ) ;
#28323=CARTESIAN_POINT ( 'NONE',  ( 21.05000000000000071, 1.162701749949165642, -141.9000000000000341 ) ) ;
#28326=CARTESIAN_POINT ( 'NONE',  ( 20.94999999999999574, -11.41227409413852989, -137.0000000000000000 ) ) ;
#28354=DIRECTION ( 'NONE',  ( 0.000000000000000000, 0.000000000000000000, -1.000000000000000000 ) ) ;
#28371=DIRECTION ( 'NONE',  ( 0.000000000000000000, 0.000000000000000000, 1.000000000000000000 ) ) ;
#28375=CARTESIAN_POINT ( 'NONE',  ( -20.85000000000000142, -1.835859311432481045, -179.0044391687985410 ) ) ;
#28380=CIRCLE ( 'NONE', #90872, 0.09999999999998898659 ) ;
#28392=ORIENTED_EDGE ( 'NONE', *, *, #117314, .F. ) ;
#28397=AXIS2_PLACEMENT_3D ( 'NONE', #14392, #92596, #30100 ) ;
#28410=CARTESIAN_POINT ( 'NONE',  ( -23.25000000000000000, 4.150000000011156764, -155.1500000000000057 ) ) ;
#28466=VECTOR ( 'NONE', #52539, 1000.000000000000114 ) ;
#28478=DIRECTION ( 'NONE',  ( -0.000000000000000000, 3.469446951953635015E-14, 1.000000000000000000 ) ) ;
#28516=CARTESIAN_POINT ( 'NONE',  ( -20.94999999999999929, 11.60000000001115161, -140.9282032302755852 ) ) ;
#28531=FACE_OUTER_BOUND ( 'NONE', #238433, .T. ) ;
#28538=CARTESIAN_POINT ( 'NONE',  ( -20.85000000000000142, 7.021664781911246322, -171.1335654018973003 ) ) ;
#28564=CIRCLE ( 'NONE', #178380, 0.1000000000000089567 ) ;
#28586=DIRECTION ( 'NONE',  ( 0.000000000000000000, 0.000000000000000000, 1.000000000000000000 ) ) ;
#28602=AXIS2_PLACEMENT_3D ( 'NONE', #57956, #140059, #180503 ) ;
#28617=DIRECTION ( 'NONE',  ( -1.000000000000000000, -2.952720810173289112E-16, 0.000000000000000000 ) ) ;
#28618=CARTESIAN_POINT ( 'NONE',  ( 18.49713797159854778, -9.446482327567771620, -141.0714581216099077 ) ) ;
#28620=EDGE_CURVE ( 'NONE', #8351, #159233, #144664, .T. ) ;
#28646=VECTOR ( 'NONE', #46309, 1000.000000000000000 ) ;
#28674=CARTESIAN_POINT ( 'NONE',  ( -22.50000000000000000, 11.75000000001115552, -134.0000000000000284 ) ) ;
#28691=CARTESIAN_POINT ( 'NONE',  ( 18.58685178364169488, -9.406733083793085370, -141.1244204690877098 ) ) ;
#28693=ORIENTED_EDGE ( 'NONE', *, *, #125140, .T. ) ;
#28694=DIRECTION ( 'NONE',  ( 0.000000000000000000, 0.000000000000000000, 1.000000000000000000 ) ) ;
#28702=ORIENTED_EDGE ( 'NONE', *, *, #134047, .F. ) ;
#28706=ORIENTED_EDGE ( 'NONE', *, *, #222517, .T. ) ;
#28746=AXIS2_PLACEMENT_3D ( 'NONE', #87251, #207235, #250197 ) ;
#28769=FACE_OUTER_BOUND ( 'NONE', #154240, .T. ) ;
#28772=DIRECTION ( 'NONE',  ( -0.000000000000000000, 0.000000000000000000, 1.000000000000000000 ) ) ;
#28793=EDGE_CURVE ( 'NONE', #37340, #4110, #219720, .T. ) ;
#28880=CARTESIAN_POINT ( 'NONE',  ( 20.95512828230152280, 8.876151312336450161, -146.2024302655031534 ) ) ;
#28885=EDGE_CURVE ( 'NONE', #173825, #221150, #144342, .T. ) ;
#28894=CARTESIAN_POINT ( 'NONE',  ( 20.94999999999999929, -1.835341550213257733, -145.5551512925629822 ) ) ;
#28896=EDGE_CURVE ( 'NONE', #91733, #143423, #181897, .T. ) ;
#28923=CARTESIAN_POINT ( 'NONE',  ( -18.59999999999999787, 11.65000000001115232, -155.3500000000000227 ) ) ;
#28924=EDGE_CURVE ( 'NONE', #84861, #42519, #221001, .T. ) ;
#28940=LINE ( 'NONE', #211386, #93061 ) ;
#28946=AXIS2_PLACEMENT_3D ( 'NONE', #231960, #11623, #29912 ) ;
#29004=EDGE_LOOP ( 'NONE', ( #215813, #86730, #187208, #198955 ) ) ;
#29018=DIRECTION ( 'NONE',  ( -1.000000000000000000, -0.000000000000000000, -0.000000000000000000 ) ) ;
#29021=AXIS2_PLACEMENT_3D ( 'NONE', #232905, #208197, #131200 ) ;
#29033=ORIENTED_EDGE ( 'NONE', *, *, #215428, .T. ) ;
#29038=FACE_BOUND ( 'NONE', #103028, .T. ) ;
#29064=VERTEX_POINT ( 'NONE', #150486 ) ;
#29092=CARTESIAN_POINT ( 'NONE',  ( 20.22516295850462598, 9.899364295461838381, -141.9100657120906135 ) ) ;
#29096=DIRECTION ( 'NONE',  ( -1.000000000000000000, 0.000000000000000000, -0.000000000000000000 ) ) ;
#29128=FACE_OUTER_BOUND ( 'NONE', #196089, .T. ) ;
#29130=CARTESIAN_POINT ( 'NONE',  ( -23.15000000000000213, 1.115600667400684642E-11, -167.5000000000000284 ) ) ;
#29135=ORIENTED_EDGE ( 'NONE', *, *, #13559, .F. ) ;
#29163=LINE ( 'NONE', #249464, #45775 ) ;
#29171=LINE ( 'NONE', #111231, #132268 ) ;
#29182=AXIS2_PLACEMENT_3D ( 'NONE', #19092, #238132, #122055 ) ;
#29187=DIRECTION ( 'NONE',  ( 0.000000000000000000, 1.000000000000000000, 0.000000000000000000 ) ) ;
#29213=AXIS2_PLACEMENT_3D ( 'NONE', #107489, #223566, #187057 ) ;
#29216=DIRECTION ( 'NONE',  ( 0.000000000000000000, 0.000000000000000000, -1.000000000000000000 ) ) ;
#29226=CARTESIAN_POINT ( 'NONE',  ( 20.99142135623731065, 11.60000000001116049, -160.5717967697245285 ) ) ;
#29242=ADVANCED_FACE ( 'NONE', ( #221965 ), #239003, .F. ) ;
#29312=EDGE_CURVE ( 'NONE', #37324, #245081, #256938, .T. ) ;
#29323=AXIS2_PLACEMENT_3D ( 'NONE', #243976, #6647, #185294 ) ;
#29350=EDGE_LOOP ( 'NONE', ( #230393, #111070, #191712, #20005 ) ) ;
#29353=ADVANCED_FACE ( 'NONE', ( #30233 ), #245426, .T. ) ;
#29370=CARTESIAN_POINT ( 'NONE',  ( -18.59999999999999787, 11.65000000001115232, -122.2500000000000284 ) ) ;
#29400=FACE_OUTER_BOUND ( 'NONE', #110387, .T. ) ;
#29404=DIRECTION ( 'NONE',  ( 0.000000000000000000, 0.9908441862701782288, -0.1350103645450542456 ) ) ;
#29411=CARTESIAN_POINT ( 'NONE',  ( -20.85000000000000142, -1.135018845899022466, -175.2169768834323520 ) ) ;
#29440=ORIENTED_EDGE ( 'NONE', *, *, #94096, .F. ) ;
#29450=DIRECTION ( 'NONE',  ( 0.000000000000000000, 0.000000000000000000, -1.000000000000000000 ) ) ;
#29453=CARTESIAN_POINT ( 'NONE',  ( 20.94999999999999574, -1.261786168553869603, -142.0864989635454947 ) ) ;
#29455=ORIENTED_EDGE ( 'NONE', *, *, #161265, .F. ) ;
#29472=CARTESIAN_POINT ( 'NONE',  ( -18.50211644919735576, 10.30207779525982836, -172.9895520716782755 ) ) ;
#29516=AXIS2_PLACEMENT_3D ( 'NONE', #184807, #20627, #24483 ) ;
#29534=CARTESIAN_POINT ( 'NONE',  ( 23.24999999999999289, 6.450000000011156587, -146.3500000000000227 ) ) ;
#29559=DIRECTION ( 'NONE',  ( 0.000000000000000000, 0.000000000000000000, 1.000000000000000000 ) ) ;
#29588=DIRECTION ( 'NONE',  ( -1.000000000000000000, -3.265361837132813093E-16, 0.000000000000000000 ) ) ;
#29605=DIRECTION ( 'NONE',  ( -1.000000000000000000, 7.304098846218135653E-16, 0.000000000000000000 ) ) ;
#29607=EDGE_CURVE ( 'NONE', #148927, #67744, #22611, .T. ) ;
#29620=VECTOR ( 'NONE', #234046, 1000.000000000000114 ) ;
#29636=CARTESIAN_POINT ( 'NONE',  ( -23.15000000000000213, 11.75000000001115552, -155.3500000000000227 ) ) ;
#29689=EDGE_CURVE ( 'NONE', #243619, #172429, #45633, .T. ) ;
#29697=ORIENTED_EDGE ( 'NONE', *, *, #214819, .F. ) ;
#29713=ORIENTED_EDGE ( 'NONE', *, *, #157938, .F. ) ;
#29770=CARTESIAN_POINT ( 'NONE',  ( 20.94999999999999574, -11.41227409413852989, -136.9000000000000341 ) ) ;
#29803=ORIENTED_EDGE ( 'NONE', *, *, #76642, .F. ) ;
#29830=ORIENTED_EDGE ( 'NONE', *, *, #227667, .F. ) ;
#29839=LINE ( 'NONE', #91066, #224279 ) ;
#29846=ORIENTED_EDGE ( 'NONE', *, *, #113534, .T. ) ;
#29848=DIRECTION ( 'NONE',  ( 0.000000000000000000, -0.1350103645451876666, -0.9908441862701600211 ) ) ;
#29853=CARTESIAN_POINT ( 'NONE',  ( -20.64999999999999858, 1.115600667400684642E-11, -134.0000000000000000 ) ) ;
#29873=CARTESIAN_POINT ( 'NONE',  ( -20.94999999999999929, -11.41227409413852989, -137.0000000000000000 ) ) ;
#29912=DIRECTION ( 'NONE',  ( 0.000000000000000000, -1.000000000000000000, 0.000000000000000000 ) ) ;
#29933=AXIS2_PLACEMENT_3D ( 'NONE', #131936, #150238, #190653 ) ;
#29950=CARTESIAN_POINT ( 'NONE',  ( 18.49999999999999289, 6.846123162363745074, -171.2377262668498759 ) ) ;
#29954=CARTESIAN_POINT ( 'NONE',  ( 18.39999999999999858, -9.519327731081283162, -140.9729763765593589 ) ) ;
#30034=DIRECTION ( 'NONE',  ( 0.000000000000000000, 1.000000000000000000, 0.000000000000000000 ) ) ;
#30056=EDGE_CURVE ( 'NONE', #221551, #33482, #19331, .T. ) ;
#30077=DIRECTION ( 'NONE',  ( 0.000000000000000000, 0.000000000000000000, -1.000000000000000000 ) ) ;
#30095=DIRECTION ( 'NONE',  ( 2.840903330521631775E-16, -0.8700118002898321601, 0.4930308989875230585 ) ) ;
#30096=CARTESIAN_POINT ( 'NONE',  ( -1.820710678118657944, -9.929289321870186313, -158.7500000000000284 ) ) ;
#30100=DIRECTION ( 'NONE',  ( 2.952720810173289112E-16, -1.000000000000000000, 0.000000000000000000 ) ) ;
#30113=CARTESIAN_POINT ( 'NONE',  ( 20.85000000000000142, 1.115600667400684642E-11, -167.5000000000000284 ) ) ;
#30123=DIRECTION ( 'NONE',  ( 0.000000000000000000, 0.000000000000000000, -1.000000000000000000 ) ) ;
#30125=AXIS2_PLACEMENT_3D ( 'NONE', #126824, #167266, #129391 ) ;
#30135=CARTESIAN_POINT ( 'NONE',  ( 21.06086055315971350, 8.774707514967413857, -146.2023221551539507 ) ) ;
#30141=CARTESIAN_POINT ( 'NONE',  ( -23.25000000000000000, 1.115600667400684642E-11, -134.0000000000000000 ) ) ;
#30156=AXIS2_PLACEMENT_3D ( 'NONE', #15259, #253835, #94772 ) ;
#30162=ORIENTED_EDGE ( 'NONE', *, *, #195277, .F. ) ;
#30181=ORIENTED_EDGE ( 'NONE', *, *, #49065, .T. ) ;
#30184=CARTESIAN_POINT ( 'NONE',  ( -21.14999999999999858, -0.1008583690875562017, -122.2504328765106294 ) ) ;
#30208=FACE_OUTER_BOUND ( 'NONE', #218990, .T. ) ;
#30210=CIRCLE ( 'NONE', #63497, 4.049999999999998046 ) ;
#30220=ORIENTED_EDGE ( 'NONE', *, *, #203419, .T. ) ;
#30230=EDGE_CURVE ( 'NONE', #195640, #73222, #6006, .T. ) ;
#30233=FACE_OUTER_BOUND ( 'NONE', #129243, .T. ) ;
#30234=ORIENTED_EDGE ( 'NONE', *, *, #51710, .T. ) ;
#30259=VERTEX_POINT ( 'NONE', #153446 ) ;
#30273=ORIENTED_EDGE ( 'NONE', *, *, #24931, .F. ) ;
#30277=ORIENTED_EDGE ( 'NONE', *, *, #128764, .F. ) ;
#30281=FACE_OUTER_BOUND ( 'NONE', #20045, .T. ) ;
#30295=EDGE_LOOP ( 'NONE', ( #148723, #207330, #213304 ) ) ;
#30306=EDGE_LOOP ( 'NONE', ( #193109, #35014, #136946, #100787 ) ) ;
#30325=ORIENTED_EDGE ( 'NONE', *, *, #156919, .T. ) ;
#30343=ORIENTED_EDGE ( 'NONE', *, *, #34532, .F. ) ;
#30380=CARTESIAN_POINT ( 'NONE',  ( 20.94999999999999929, -1.135018845899022466, -175.2169768834323520 ) ) ;
#30382=CARTESIAN_POINT ( 'NONE',  ( -18.50000000000000711, 11.65000000001115232, -141.0148057706539930 ) ) ;
#30404=CYLINDRICAL_SURFACE ( 'NONE', #179100, 0.1000000000000004496 ) ;
#30440=CARTESIAN_POINT ( 'NONE',  ( -20.94999999999999929, 1.162701749949165642, -141.9000000000000341 ) ) ;
#30487=ORIENTED_EDGE ( 'NONE', *, *, #249502, .T. ) ;
#30530=EDGE_CURVE ( 'NONE', #33482, #44736, #43802, .T. ) ;
#30549=EDGE_CURVE ( 'NONE', #157514, #69302, #190636, .T. ) ;
#30578=ORIENTED_EDGE ( 'NONE', *, *, #129878, .F. ) ;
#30599=CIRCLE ( 'NONE', #230507, 11.80000000000000426 ) ;
#30630=EDGE_CURVE ( 'NONE', #192232, #202799, #178794, .T. ) ;
#30632=DIRECTION ( 'NONE',  ( 1.000000000000000000, 0.000000000000000000, 0.000000000000000000 ) ) ;
#30652=AXIS2_PLACEMENT_3D ( 'NONE', #190579, #9340, #229688 ) ;
#30713=AXIS2_PLACEMENT_3D ( 'NONE', #200174, #183187, #123201 ) ;
#30716=CIRCLE ( 'NONE', #93044, 0.09999999999999939493 ) ;
#30733=ORIENTED_EDGE ( 'NONE', *, *, #171763, .F. ) ;
#30742=EDGE_LOOP ( 'NONE', ( #190759, #113482, #77033, #228735 ) ) ;
#30752=CYLINDRICAL_SURFACE ( 'NONE', #236677, 11.80000000000000426 ) ;
#30765=EDGE_LOOP ( 'NONE', ( #69633, #158889, #161773, #184413 ) ) ;
#30803=DIRECTION ( 'NONE',  ( 0.000000000000000000, 0.000000000000000000, -1.000000000000000000 ) ) ;
#30810=AXIS2_PLACEMENT_3D ( 'NONE', #237303, #132106, #255517 ) ;
#30816=CARTESIAN_POINT ( 'NONE',  ( -18.50000000000000000, 5.950000000011100632, -144.3057023050348846 ) ) ;
#30841=DIRECTION ( 'NONE',  ( 1.000000000000000000, 0.000000000000000000, 0.000000000000000000 ) ) ;
#30842=DIRECTION ( 'NONE',  ( -0.000000000000000000, 0.8660254037844383745, -0.5000000000000003331 ) ) ;
#30850=DIRECTION ( 'NONE',  ( 0.000000000000000000, 0.000000000000000000, -1.000000000000000000 ) ) ;
#30868=FACE_OUTER_BOUND ( 'NONE', #126654, .T. ) ;
#30869=FACE_OUTER_BOUND ( 'NONE', #187512, .T. ) ;
#30891=ORIENTED_EDGE ( 'NONE', *, *, #228875, .F. ) ;
#30934=ORIENTED_EDGE ( 'NONE', *, *, #234197, .F. ) ;
#30951=LINE ( 'NONE', #11358, #97277 ) ;
#30966=AXIS2_PLACEMENT_3D ( 'NONE', #116207, #73244, #193172 ) ;
#30970=AXIS2_PLACEMENT_3D ( 'NONE', #10579, #227039, #8013 ) ;
#30983=CIRCLE ( 'NONE', #226554, 1.900000000000012790 ) ;
#30993=DIRECTION ( 'NONE',  ( 0.000000000000000000, 0.000000000000000000, -1.000000000000000000 ) ) ;
#31006=CARTESIAN_POINT ( 'NONE',  ( -20.54999999999999716, 7.150000000011155876, -146.2500000000000284 ) ) ;
#31013=DIRECTION ( 'NONE',  ( -0.000000000000000000, 0.1350103645451876666, -0.9908441862701600211 ) ) ;
#31023=ADVANCED_FACE ( 'NONE', ( #85578, #2215, #143006 ), #46477, .F. ) ;
#31025=TOROIDAL_SURFACE ( 'NONE', #197567, 0.2000000000000000111, 0.1000000000000000056 ) ;
#31115=DIRECTION ( 'NONE',  ( -0.000000000000000000, 0.7397360091702694929, 0.6728971962616898672 ) ) ;
#31121=ORIENTED_EDGE ( 'NONE', *, *, #194289, .F. ) ;
#31136=DIRECTION ( 'NONE',  ( 0.000000000000000000, 0.000000000000000000, -1.000000000000000000 ) ) ;
#31157=ORIENTED_EDGE ( 'NONE', *, *, #120083, .T. ) ;
#31161=AXIS2_PLACEMENT_3D ( 'NONE', #22144, #97770, #3843 ) ;
#31258=DIRECTION ( 'NONE',  ( -0.000000000000000000, -0.9876197685951252359, -0.1568667991644863424 ) ) ;
#31265=ORIENTED_EDGE ( 'NONE', *, *, #186678, .T. ) ;
#31286=CARTESIAN_POINT ( 'NONE',  ( 20.95512820512820795, 8.876151316299273120, -146.2001728591287701 ) ) ;
#31307=VERTEX_POINT ( 'NONE', #117376 ) ;
#31344=ORIENTED_EDGE ( 'NONE', *, *, #234189, .F. ) ;
#31386=DIRECTION ( 'NONE',  ( 1.000000000000000000, 0.000000000000000000, 0.000000000000000000 ) ) ;
#31388=DIRECTION ( 'NONE',  ( 0.000000000000000000, -3.552713678800376289E-15, 1.000000000000000000 ) ) ;
#31404=AXIS2_PLACEMENT_3D ( 'NONE', #87623, #122931, #145038 ) ;
#31423=CARTESIAN_POINT ( 'NONE',  ( -21.05000000000000071, 1.115600667400684642E-11, -134.0000000000000000 ) ) ;
#31441=EDGE_LOOP ( 'NONE', ( #123018, #62527, #193804, #54241 ) ) ;
#31461=ORIENTED_EDGE ( 'NONE', *, *, #125284, .F. ) ;
#31464=CARTESIAN_POINT ( 'NONE',  ( 21.05000000000000071, 8.776282648982402179, -142.4875923785201053 ) ) ;
#31465=AXIS2_PLACEMENT_3D ( 'NONE', #134034, #96183, #175761 ) ;
#31490=EDGE_CURVE ( 'NONE', #4950, #99917, #25984, .T. ) ;
#31492=CARTESIAN_POINT ( 'NONE',  ( 21.14999999999999858, 1.115600667400684642E-11, -127.4593430482987912 ) ) ;
#31505=CARTESIAN_POINT ( 'NONE',  ( 18.50000000000000000, -9.419209763398095347, -141.2477694627589244 ) ) ;
#31509=LINE ( 'NONE', #34080, #42693 ) ;
#31518=DIRECTION ( 'NONE',  ( 1.000000000000000000, 0.000000000000000000, 0.000000000000000000 ) ) ;
#31520=AXIS2_PLACEMENT_3D ( 'NONE', #54290, #90855, #133838 ) ;
#31522=CARTESIAN_POINT ( 'NONE',  ( -20.54999999999999716, -9.399999999988846611, -157.6060308773475924 ) ) ;
#31546=EDGE_LOOP ( 'NONE', ( #6875, #117031, #418 ) ) ;
#31589=ORIENTED_EDGE ( 'NONE', *, *, #145470, .F. ) ;
#31594=EDGE_LOOP ( 'NONE', ( #128548, #95649, #132110, #51705 ) ) ;
#31632=ADVANCED_FACE ( 'NONE', ( #131487 ), #93665, .T. ) ;
#31656=CARTESIAN_POINT ( 'NONE',  ( 18.51697539158856642, 10.31565961587946134, -173.0364194119178478 ) ) ;
#31661=DIRECTION ( 'NONE',  ( -1.000000000000000000, 7.304098846218133681E-16, -4.217023435051677994E-16 ) ) ;
#31669=CARTESIAN_POINT ( 'NONE',  ( 20.94999999999999574, -11.74999999998883560, -136.9000000000000341 ) ) ;
#31740=CIRCLE ( 'NONE', #19821, 0.09999999999998715472 ) ;
#31745=CARTESIAN_POINT ( 'NONE',  ( -18.50000000000000000, 1.115600667400684642E-11, -134.0000000000000000 ) ) ;
#31778=AXIS2_PLACEMENT_3D ( 'NONE', #247122, #64644, #166351 ) ;
#31804=CARTESIAN_POINT ( 'NONE',  ( 23.14999999999999503, 11.75000000001115552, -155.2500000000000284 ) ) ;
#31814=LINE ( 'NONE', #36952, #125725 ) ;
#31821=VECTOR ( 'NONE', #110873, 1000.000000000000000 ) ;
#31827=ORIENTED_EDGE ( 'NONE', *, *, #244084, .F. ) ;
#31830=CARTESIAN_POINT ( 'NONE',  ( 19.58285714285715073, 10.38499851036257837, -141.6296846673899665 ) ) ;
#31837=CARTESIAN_POINT ( 'NONE',  ( -21.05000000000000071, -11.48912529306490349, -137.1000000000000227 ) ) ;
#31843=CIRCLE ( 'NONE', #52644, 7.720710678118663850 ) ;
#31844=CARTESIAN_POINT ( 'NONE',  ( -20.94999999999999929, -1.164121893230052995, -175.2148480855716173 ) ) ;
#31890=CARTESIAN_POINT ( 'NONE',  ( -21.05000000000000071, 1.115600667400684642E-11, -163.4000000000000341 ) ) ;
#31936=VECTOR ( 'NONE', #219173, 1000.000000000000000 ) ;
#31977=VECTOR ( 'NONE', #217307, 1000.000000000000000 ) ;
#32067=CARTESIAN_POINT ( 'NONE',  ( -18.50000000000000000, -9.399999999988850163, -141.2972597596633193 ) ) ;
#32105=CARTESIAN_POINT ( 'NONE',  ( 18.50000000000000000, -9.419078080838369615, -174.3299253502083559 ) ) ;
#32119=CYLINDRICAL_SURFACE ( 'NONE', #172660, 0.5000000000000004441 ) ;
#32147=CARTESIAN_POINT ( 'NONE',  ( -21.05000000000000071, 1.115600667400684642E-11, -167.5000000000000284 ) ) ;
#32173=ORIENTED_EDGE ( 'NONE', *, *, #82564, .F. ) ;
#32191=EDGE_LOOP ( 'NONE', ( #118612, #170034, #215307, #253962 ) ) ;
#32212=CARTESIAN_POINT ( 'NONE',  ( -21.53752568622129004, 0.09897446127764164547, -127.2131921254514566 ) ) ;
#32216=CIRCLE ( 'NONE', #215349, 11.65000000000000036 ) ;
#32228=EDGE_CURVE ( 'NONE', #218074, #68733, #148015, .T. ) ;
#32230=ADVANCED_FACE ( 'NONE', ( #27648 ), #73866, .T. ) ;
#32236=AXIS2_PLACEMENT_3D ( 'NONE', #217711, #15714, #113496 ) ;
#32239=AXIS2_PLACEMENT_3D ( 'NONE', #223634, #239370, #179411 ) ;
#32240=ORIENTED_EDGE ( 'NONE', *, *, #255063, .F. ) ;
#32243=CARTESIAN_POINT ( 'NONE',  ( -20.64999999999999858, 2.500000000011156409, -147.2246219227621111 ) ) ;
#32247=EDGE_CURVE ( 'NONE', #149328, #165926, #75271, .T. ) ;
#32292=CARTESIAN_POINT ( 'NONE',  ( -21.04999999999999716, 0.09843750001115456061, -127.7007690899131234 ) ) ;
#32313=LINE ( 'NONE', #171833, #134054 ) ;
#32315=CARTESIAN_POINT ( 'NONE',  ( -21.13498764882296044, 0.001656394742485926743, -127.5043818565260665 ) ) ;
#32316=DIRECTION ( 'NONE',  ( -1.000000000000000000, -0.000000000000000000, -0.000000000000000000 ) ) ;
#32317=CARTESIAN_POINT ( 'NONE',  ( -22.50000000000000000, 1.115600667400684642E-11, -134.0000000000000000 ) ) ;
#32323=ORIENTED_EDGE ( 'NONE', *, *, #199209, .T. ) ;
#32332=FACE_OUTER_BOUND ( 'NONE', #115813, .T. ) ;
#32360=CIRCLE ( 'NONE', #52968, 0.09999999999998898659 ) ;
#32363=EDGE_CURVE ( 'NONE', #151810, #24271, #251787, .T. ) ;
#32429=DIRECTION ( 'NONE',  ( -1.000000000000000000, 0.000000000000000000, 0.000000000000000000 ) ) ;
#32497=DIRECTION ( 'NONE',  ( -1.000000000000000000, 0.000000000000000000, 0.000000000000000000 ) ) ;
#32512=AXIS2_PLACEMENT_3D ( 'NONE', #247098, #208009, #167603 ) ;
#32522=AXIS2_PLACEMENT_3D ( 'NONE', #225453, #108104, #143365 ) ;
#32529=ORIENTED_EDGE ( 'NONE', *, *, #28244, .T. ) ;
#32568=CARTESIAN_POINT ( 'NONE',  ( -23.15000000000000213, 4.150000000011156764, -122.2500000000000284 ) ) ;
#32572=DIRECTION ( 'NONE',  ( 0.000000000000000000, 0.000000000000000000, -1.000000000000000000 ) ) ;
#32637=ADVANCED_FACE ( 'NONE', ( #130233 ), #23137, .T. ) ;
#32638=CARTESIAN_POINT ( 'NONE',  ( -23.25000000000000000, 1.115600667400684642E-11, -134.0000000000000000 ) ) ;
#32666=DIRECTION ( 'NONE',  ( 1.000000000000000000, 0.000000000000000000, 0.000000000000000000 ) ) ;
#32675=CARTESIAN_POINT ( 'NONE',  ( -20.54999999999999716, 1.115600667400684642E-11, -134.0000000000000000 ) ) ;
#32676=CARTESIAN_POINT ( 'NONE',  ( 18.59999999999999076, 10.49142135624846439, -158.8500000000000227 ) ) ;
#32706=ADVANCED_FACE ( 'NONE', ( #211072 ), #169083, .T. ) ;
#32709=DIRECTION ( 'NONE',  ( 1.875376730785737719E-16, -1.000000000000000000, 0.000000000000000000 ) ) ;
#32743=CARTESIAN_POINT ( 'NONE',  ( 22.49436431346199683, 11.64995094766461392, -133.9330964702777749 ) ) ;
#32782=CARTESIAN_POINT ( 'NONE',  ( 18.49999999999999289, 10.41716543472752399, -158.8499999994178040 ) ) ;
#32815=AXIS2_PLACEMENT_3D ( 'NONE', #164414, #226945, #45738 ) ;
#32886=EDGE_CURVE ( 'NONE', #83171, #20283, #194201, .T. ) ;
#32896=VERTEX_POINT ( 'NONE', #42694 ) ;
#32910=VECTOR ( 'NONE', #6708, 1000.000000000000000 ) ;
#32920=EDGE_CURVE ( 'NONE', #121012, #111004, #43979, .T. ) ;
#32931=LINE ( 'NONE', #54988, #170574 ) ;
#32937=DIRECTION ( 'NONE',  ( 1.000000000000000000, 0.000000000000000000, 0.000000000000000000 ) ) ;
#32982=DIRECTION ( 'NONE',  ( -0.000000000000000000, -0.000000000000000000, 1.000000000000000000 ) ) ;
#32987=EDGE_CURVE ( 'NONE', #245147, #158190, #23530, .T. ) ;
#33035=ADVANCED_FACE ( 'NONE', ( #30868 ), #110364, .F. ) ;
#33068=ORIENTED_EDGE ( 'NONE', *, *, #180184, .F. ) ;
#33069=B_SPLINE_CURVE_WITH_KNOTS ( 'NONE', 3,
 ( #247478, #8873, #54410, #233077, #88379, #90968, #250049, #170571, #68863, #148386, #150953, #51822, #227920, #230491, #131378, #210922, #32315, #77809, #216041 ),
 .UNSPECIFIED., .F., .F.,
 ( 4, 3, 3, 3, 3, 3, 4 ),
 ( 0.000000000000000000, 1.655171619025768090E-05, 2.773500582848307641E-05, 5.941817267378768900E-05, 0.0001114174635873506033, 0.0001914169455916434233, 0.0002627181070750764539 ),
 .UNSPECIFIED. ) ;
#33099=ORIENTED_EDGE ( 'NONE', *, *, #218258, .F. ) ;
#33100=EDGE_CURVE ( 'NONE', #237128, #160394, #130621, .T. ) ;
#33162=AXIS2_PLACEMENT_3D ( 'NONE', #225658, #9207, #146145 ) ;
#33198=ORIENTED_EDGE ( 'NONE', *, *, #178275, .F. ) ;
#33234=DIRECTION ( 'NONE',  ( 0.000000000000000000, 0.000000000000000000, 1.000000000000000000 ) ) ;
#33269=EDGE_CURVE ( 'NONE', #200852, #101749, #177644, .T. ) ;
#33297=CARTESIAN_POINT ( 'NONE',  ( -23.25000000000000000, 1.115600667400684642E-11, -167.5000000000000284 ) ) ;
#33301=ADVANCED_FACE ( 'NONE', ( #20271 ), #157232, .F. ) ;
#33321=ORIENTED_EDGE ( 'NONE', *, *, #137461, .T. ) ;
#33325=CARTESIAN_POINT ( 'NONE',  ( -18.54148534481894472, 10.32532329027886320, -173.0699343018359855 ) ) ;
#33329=ORIENTED_EDGE ( 'NONE', *, *, #23175, .T. ) ;
#33336=AXIS2_PLACEMENT_3D ( 'NONE', #143370, #84639, #62563 ) ;
#33365=AXIS2_PLACEMENT_3D ( 'NONE', #193587, #172779, #18782 ) ;
#33397=ORIENTED_EDGE ( 'NONE', *, *, #170133, .F. ) ;
#33423=DIRECTION ( 'NONE',  ( 1.000000000000000000, 0.000000000000000000, 0.000000000000000000 ) ) ;
#33432=VERTEX_POINT ( 'NONE', #86621 ) ;
#33435=DIRECTION ( 'NONE',  ( 0.000000000000000000, -0.8660254037844383745, 0.5000000000000003331 ) ) ;
#33452=CIRCLE ( 'NONE', #179187, 0.09999999999999939493 ) ;
#33459=ORIENTED_EDGE ( 'NONE', *, *, #87901, .T. ) ;
#33460=PLANE ( 'NONE',  #213762 ) ;
#33482=VERTEX_POINT ( 'NONE', #147923 ) ;
#33486=DIRECTION ( 'NONE',  ( 1.000000000000000000, 0.000000000000000000, 0.000000000000000000 ) ) ;
#33494=ADVANCED_FACE ( 'NONE', ( #39230 ), #177462, .F. ) ;
#33519=CARTESIAN_POINT ( 'NONE',  ( -21.46681500598102232, 1.115539681028482333E-11, -127.1424888405744724 ) ) ;
#33563=ORIENTED_EDGE ( 'NONE', *, *, #122180, .F. ) ;
#33581=CARTESIAN_POINT ( 'NONE',  ( -18.59999999999999787, 7.070967871809997973, -171.2465642218683115 ) ) ;
#33595=ORIENTED_EDGE ( 'NONE', *, *, #37815, .F. ) ;
#33600=LINE ( 'NONE', #54392, #152569 ) ;
#33601=EDGE_CURVE ( 'NONE', #249928, #254695, #144441, .T. ) ;
#33611=VECTOR ( 'NONE', #183681, 1000.000000000000000 ) ;
#33614=EDGE_LOOP ( 'NONE', ( #131629, #132624, #129988, #205289 ) ) ;
#33616=EDGE_LOOP ( 'NONE', ( #74634, #93436, #257144, #114465, #219677 ) ) ;
#33620=FACE_OUTER_BOUND ( 'NONE', #232116, .T. ) ;
#33625=CARTESIAN_POINT ( 'NONE',  ( 22.39999999999999503, 11.65000000001116298, -134.0000000000000284 ) ) ;
#33676=ADVANCED_FACE ( 'NONE', ( #165585 ), #90478, .F. ) ;
#33693=CARTESIAN_POINT ( 'NONE',  ( 18.59999999999999432, 1.261786168576181755, -142.0864989635454947 ) ) ;
#33710=ADVANCED_FACE ( 'NONE', ( #125170 ), #65359, .T. ) ;
#33725=CIRCLE ( 'NONE', #158592, 0.2000000000000005107 ) ;
#33753=CARTESIAN_POINT ( 'NONE',  ( -22.39999999999999858, 11.65000000001115588, -133.9000000000000057 ) ) ;
#33785=DIRECTION ( 'NONE',  ( 0.000000000000000000, 1.734723475976997999E-14, 1.000000000000000000 ) ) ;
#33827=CARTESIAN_POINT ( 'NONE',  ( 21.05000000000000071, 5.850000000011105428, -144.1324972242779836 ) ) ;
#33833=AXIS2_PLACEMENT_3D ( 'NONE', #204854, #132731, #243990 ) ;
#33915=VERTEX_POINT ( 'NONE', #113293 ) ;
#33917=AXIS2_PLACEMENT_3D ( 'NONE', #81462, #181890, #138861 ) ;
#33947=DIRECTION ( 'NONE',  ( 1.000000000000000000, 0.000000000000000000, 0.000000000000000000 ) ) ;
#33948=DIRECTION ( 'NONE',  ( -1.000000000000000000, 0.000000000000000000, 0.000000000000000000 ) ) ;
#33949=ORIENTED_EDGE ( 'NONE', *, *, #12259, .T. ) ;
#33993=DIRECTION ( 'NONE',  ( 0.000000000000000000, 0.000000000000000000, -1.000000000000000000 ) ) ;
#33995=ORIENTED_EDGE ( 'NONE', *, *, #8288, .T. ) ;
#34002=CARTESIAN_POINT ( 'NONE',  ( 20.84999999999998721, 10.33248238083634440, -173.0948465439131496 ) ) ;
#34014=ORIENTED_EDGE ( 'NONE', *, *, #22940, .T. ) ;
#34035=DIRECTION ( 'NONE',  ( 0.000000000000000000, 0.000000000000000000, -1.000000000000000000 ) ) ;
#34071=EDGE_CURVE ( 'NONE', #219189, #257964, #200528, .T. ) ;
#34078=CARTESIAN_POINT ( 'NONE',  ( 18.44364597020195617, -9.490487317151101720, -141.0579778896838832 ) ) ;
#34080=CARTESIAN_POINT ( 'NONE',  ( -20.85000000000000142, 10.33248238083635151, -173.0948465439131780 ) ) ;
#34098=CIRCLE ( 'NONE', #154889, 0.1999999999999987899 ) ;
#34099=ORIENTED_EDGE ( 'NONE', *, *, #78032, .T. ) ;
#34104=EDGE_CURVE ( 'NONE', #206061, #212047, #69850, .T. ) ;
#34132=ORIENTED_EDGE ( 'NONE', *, *, #98140, .T. ) ;
#34177=DIRECTION ( 'NONE',  ( -0.000000000000000000, 1.000000000000000000, 0.000000000000000000 ) ) ;
#34214=AXIS2_PLACEMENT_3D ( 'NONE', #10412, #52074, #132929 ) ;
#34253=AXIS2_PLACEMENT_3D ( 'NONE', #130797, #231208, #52537 ) ;
#34275=DIRECTION ( 'NONE',  ( -1.000000000000000000, -0.000000000000000000, -0.000000000000000000 ) ) ;
#34303=CARTESIAN_POINT ( 'NONE',  ( 18.49999999999999289, 10.32573593129922607, -158.8499999999999943 ) ) ;
#34304=DIRECTION ( 'NONE',  ( 1.000000000000000000, 0.000000000000000000, 0.000000000000000000 ) ) ;
#34321=CARTESIAN_POINT ( 'NONE',  ( -21.14999999999999858, 11.65000000001115588, -134.0000000000000284 ) ) ;
#34341=EDGE_CURVE ( 'NONE', #177617, #26579, #190655, .T. ) ;
#34378=EDGE_LOOP ( 'NONE', ( #103584, #217825, #114339, #23561 ) ) ;
#34399=DIRECTION ( 'NONE',  ( 0.000000000000000000, -2.602085213965497408E-13, 1.000000000000000000 ) ) ;
#34422=FACE_OUTER_BOUND ( 'NONE', #177388, .T. ) ;
#34443=ORIENTED_EDGE ( 'NONE', *, *, #84996, .F. ) ;
#34458=DIRECTION ( 'NONE',  ( 0.000000000000000000, 0.000000000000000000, 1.000000000000000000 ) ) ;
#34476=AXIS2_PLACEMENT_3D ( 'NONE', #48395, #152675, #11874 ) ;
#34532=EDGE_CURVE ( 'NONE', #115992, #241817, #17315, .T. ) ;
#34558=CARTESIAN_POINT ( 'NONE',  ( -20.94999999999999929, -11.48912529306490349, -137.1000000000000227 ) ) ;
#34574=CARTESIAN_POINT ( 'NONE',  ( 21.05000000000000071, 8.776282895303632259, -146.1500000000000341 ) ) ;
#34593=LINE ( 'NONE', #210641, #29620 ) ;
#34596=CARTESIAN_POINT ( 'NONE',  ( 21.78635804494511419, 0.09900506551883611617, -126.9643385148468440 ) ) ;
#34604=CARTESIAN_POINT ( 'NONE',  ( 18.49999999999999645, -1.164121893230052995, -175.4148480855716059 ) ) ;
#34625=CIRCLE ( 'NONE', #222013, 4.300000000000025580 ) ;
#34631=VERTEX_POINT ( 'NONE', #104504 ) ;
#34632=FACE_OUTER_BOUND ( 'NONE', #70770, .T. ) ;
#34643=EDGE_LOOP ( 'NONE', ( #217292, #207456, #205201, #253407, #201040 ) ) ;
#34670=ADVANCED_FACE ( 'NONE', ( #82846 ), #99208, .T. ) ;
#34680=CIRCLE ( 'NONE', #247028, 0.6000000000000015321 ) ;
#34683=FACE_OUTER_BOUND ( 'NONE', #117405, .T. ) ;
#34699=EDGE_LOOP ( 'NONE', ( #69110, #148040, #121039, #132937 ) ) ;
#34738=CIRCLE ( 'NONE', #184540, 0.09999999999999939493 ) ;
#34765=AXIS2_PLACEMENT_3D ( 'NONE', #218167, #181650, #142494 ) ;
#34776=TOROIDAL_SURFACE ( 'NONE', #172172, 0.2000000000000000111, 0.1000000000000000056 ) ;
#34780=CARTESIAN_POINT ( 'NONE',  ( -18.59999999999999787, -1.263275465206102233, -175.4018646667464338 ) ) ;
#34787=ORIENTED_EDGE ( 'NONE', *, *, #81416, .F. ) ;
#34840=CARTESIAN_POINT ( 'NONE',  ( 20.95378194480896639, 10.53491199155394220, -141.5650541481478797 ) ) ;
#34851=CARTESIAN_POINT ( 'NONE',  ( 21.05000000000000071, 5.500000000011153745, -155.0947339810869323 ) ) ;
#34857=DIRECTION ( 'NONE',  ( 0.000000000000000000, 0.000000000000000000, 1.000000000000000000 ) ) ;
#34861=B_SPLINE_CURVE_WITH_KNOTS ( 'NONE', 3,
 ( #115830, #157569, #194108, #158832, #37593, #137939, #154984, #76689, #234481, #156275 ),
 .UNSPECIFIED., .F., .F.,
 ( 4, 3, 3, 4 ),
 ( 0.000000000000000000, 3.394313611811197040E-05, 6.779740500699018625E-05, 0.0001049857339142625727 ),
 .UNSPECIFIED. ) ;
#34863=DIRECTION ( 'NONE',  ( 0.000000000000000000, 0.000000000000000000, -1.000000000000000000 ) ) ;
#34887=EDGE_CURVE ( 'NONE', #101749, #4681, #187150, .T. ) ;
#34906=ADVANCED_FACE ( 'NONE', ( #87996 ), #228832, .F. ) ;
#34939=ORIENTED_EDGE ( 'NONE', *, *, #86462, .T. ) ;
#34986=DIRECTION ( 'NONE',  ( -0.000000000000000000, -0.000000000000000000, 1.000000000000000000 ) ) ;
#34987=CARTESIAN_POINT ( 'NONE',  ( -23.15000000000000213, -8.999999999988844479, -157.6060308773475924 ) ) ;
#35008=ORIENTED_EDGE ( 'NONE', *, *, #2188, .T. ) ;
#35009=DIRECTION ( 'NONE',  ( 1.000000000000000000, 0.000000000000000000, 0.000000000000000000 ) ) ;
#35014=ORIENTED_EDGE ( 'NONE', *, *, #222466, .F. ) ;
#35033=ORIENTED_EDGE ( 'NONE', *, *, #238614, .T. ) ;
#35049=CIRCLE ( 'NONE', #226514, 0.09999999999998898659 ) ;
#35054=CIRCLE ( 'NONE', #164209, 0.09999999999999939493 ) ;
#35068=CARTESIAN_POINT ( 'NONE',  ( -21.05000000000000071, 6.413759733821436271, -134.0856130608038939 ) ) ;
#35088=AXIS2_PLACEMENT_3D ( 'NONE', #201417, #22815, #41095 ) ;
#35101=FACE_OUTER_BOUND ( 'NONE', #165577, .T. ) ;
#35102=ORIENTED_EDGE ( 'NONE', *, *, #137459, .F. ) ;
#35128=AXIS2_PLACEMENT_3D ( 'NONE', #184743, #246020, #170382 ) ;
#35135=ORIENTED_EDGE ( 'NONE', *, *, #157938, .T. ) ;
#35136=CARTESIAN_POINT ( 'NONE',  ( 20.97239005616515684, 8.874843841361279573, -146.2501528021531954 ) ) ;
#35141=VERTEX_POINT ( 'NONE', #222059 ) ;
#35150=DIRECTION ( 'NONE',  ( 1.000000000000000000, -0.000000000000000000, -0.000000000000000000 ) ) ;
#35175=DIRECTION ( 'NONE',  ( 0.000000000000000000, -0.000000000000000000, -1.000000000000000000 ) ) ;
#35181=ORIENTED_EDGE ( 'NONE', *, *, #186099, .F. ) ;
#35198=ORIENTED_EDGE ( 'NONE', *, *, #68575, .F. ) ;
#35218=EDGE_LOOP ( 'NONE', ( #116706, #17477, #87316 ) ) ;
#35262=CARTESIAN_POINT ( 'NONE',  ( -23.15000000000000213, 2.000000000011154189, -154.7753780772379173 ) ) ;
#35271=SHAPE_DEFINITION_REPRESENTATION ( #51454, #88607 ) ;
#35321=CARTESIAN_POINT ( 'NONE',  ( 21.04999999999999716, 8.871279686006802834, -142.5586289951409640 ) ) ;
#35357=EDGE_LOOP ( 'NONE', ( #76984, #82794, #192357 ) ) ;
#35362=EDGE_LOOP ( 'NONE', ( #208361, #22241, #169891, #53061 ) ) ;
#35381=ORIENTED_EDGE ( 'NONE', *, *, #147076, .F. ) ;
#35396=EDGE_CURVE ( 'NONE', #47883, #21693, #32931, .T. ) ;
#35407=DIRECTION ( 'NONE',  ( 2.952720810173289112E-16, -1.000000000000000000, 0.000000000000000000 ) ) ;
#35423=ORIENTED_EDGE ( 'NONE', *, *, #140617, .F. ) ;
#35469=DIRECTION ( 'NONE',  ( -0.000000000000000000, 0.000000000000000000, -1.000000000000000000 ) ) ;
#35479=DIRECTION ( 'NONE',  ( 0.000000000000000000, 0.000000000000000000, -1.000000000000000000 ) ) ;
#35486=LINE ( 'NONE', #215364, #164842 ) ;
#35497=ORIENTED_EDGE ( 'NONE', *, *, #107833, .F. ) ;
#35505=CARTESIAN_POINT ( 'NONE',  ( 20.96937028524355640, 10.62446937163783289, -141.4914261011695942 ) ) ;
#35508=VERTEX_POINT ( 'NONE', #87069 ) ;
#35538=DIRECTION ( 'NONE',  ( 1.000000000000000000, 0.000000000000000000, -0.000000000000000000 ) ) ;
#35556=ORIENTED_EDGE ( 'NONE', *, *, #62671, .F. ) ;
#35632=AXIS2_PLACEMENT_3D ( 'NONE', #171022, #50989, #246643 ) ;
#35648=CYLINDRICAL_SURFACE ( 'NONE', #67429, 12.87499999999999822 ) ;
#35660=DIRECTION ( 'NONE',  ( 2.694716079187272946E-16, -1.000000000000000000, 0.000000000000000000 ) ) ;
#35682=FACE_OUTER_BOUND ( 'NONE', #176285, .T. ) ;
#35697=DIRECTION ( 'NONE',  ( 0.000000000000000000, 0.000000000000000000, -1.000000000000000000 ) ) ;
#35710=VECTOR ( 'NONE', #204944, 1000.000000000000000 ) ;
#35717=CARTESIAN_POINT ( 'NONE',  ( 21.05000000000000071, 6.540656951712402467, -134.0000000000000284 ) ) ;
#35747=ORIENTED_EDGE ( 'NONE', *, *, #207477, .F. ) ;
#35759=VERTEX_POINT ( 'NONE', #140320 ) ;
#35760=CARTESIAN_POINT ( 'NONE',  ( 23.14999999999999503, 6.650000000011155876, -155.1500000000000057 ) ) ;
#35769=( BOUNDED_CURVE ( )  B_SPLINE_CURVE ( 3, ( #178703, #187334, #181255, #238641 ),
 .UNSPECIFIED., .F., .T. ) 
 B_SPLINE_CURVE_WITH_KNOTS ( ( 4, 4 ),
 ( 0.000000000000000000, 1.570796326794916320 ),
 .UNSPECIFIED. ) 
 CURVE ( )  GEOMETRIC_REPRESENTATION_ITEM ( )  RATIONAL_B_SPLINE_CURVE ( ( 1.000000000000000000, 0.8047378541243603856, 0.8047378541243603856, 1.000000000000000000 ) ) 
 REPRESENTATION_ITEM ( '' )  );
#35777=ADVANCED_FACE ( 'NONE', ( #235576 ), #219869, .F. ) ;
#35844=DIRECTION ( 'NONE',  ( 0.000000000000000000, -1.000000000000000000, 0.000000000000000000 ) ) ;
#35850=CARTESIAN_POINT ( 'NONE',  ( -20.94999999999999929, -1.835341550213257733, -145.5551512925629822 ) ) ;
#35888=ORIENTED_EDGE ( 'NONE', *, *, #76724, .F. ) ;
#35899=DIRECTION ( 'NONE',  ( 0.000000000000000000, 0.000000000000000000, 1.000000000000000000 ) ) ;
#35918=CARTESIAN_POINT ( 'NONE',  ( -22.01447462590972748, 7.263800201241075172, -133.9009629999404751 ) ) ;
#35952=CARTESIAN_POINT ( 'NONE',  ( 18.50000000000000355, -9.480686695267808162, -174.4411151687578752 ) ) ;
#35953=CARTESIAN_POINT ( 'NONE',  ( 18.49999999999998934, 11.65000000001115943, -158.7500000000000284 ) ) ;
#35989=FACE_OUTER_BOUND ( 'NONE', #206035, .T. ) ;
#35997=VECTOR ( 'NONE', #226211, 1000.000000000000114 ) ;
#36014=LINE ( 'NONE', #236747, #72205 ) ;
#36054=CARTESIAN_POINT ( 'NONE',  ( -22.39999999999999503, 1.115541036281197940E-11, -126.2092204016266379 ) ) ;
#36098=ORIENTED_EDGE ( 'NONE', *, *, #56341, .T. ) ;
#36118=DIRECTION ( 'NONE',  ( -1.000000000000000000, 0.000000000000000000, 0.000000000000000000 ) ) ;
#36147=ORIENTED_EDGE ( 'NONE', *, *, #89091, .T. ) ;
#36211=CIRCLE ( 'NONE', #140206, 0.09999999999999939493 ) ;
#36222=CARTESIAN_POINT ( 'NONE',  ( -23.25000000000000000, 1.115600667400684642E-11, -167.5000000000000284 ) ) ;
#36246=DIRECTION ( 'NONE',  ( 1.000000000000000000, -0.000000000000000000, -0.000000000000000000 ) ) ;
#36309=DIRECTION ( 'NONE',  ( 1.000000000000000000, -0.000000000000000000, -0.000000000000000000 ) ) ;
#36353=CIRCLE ( 'NONE', #227855, 0.5000000000000004441 ) ;
#36357=EDGE_CURVE ( 'NONE', #201727, #120967, #61984, .T. ) ;
#36384=DIRECTION ( 'NONE',  ( -1.000000000000000000, -2.952720810173289112E-16, 0.000000000000000000 ) ) ;
#36396=CARTESIAN_POINT ( 'NONE',  ( -18.50000000000000000, -1.164121893230052995, -175.4148480855716059 ) ) ;
#36409=CARTESIAN_POINT ( 'NONE',  ( -23.15000000000000213, 1.925233644870967487, -154.7697564668738721 ) ) ;
#36428=ADVANCED_FACE ( 'NONE', ( #171203 ), #108610, .T. ) ;
#36430=CARTESIAN_POINT ( 'NONE',  ( -18.50000000000000000, 3.912899247244609580, -145.4818229730109920 ) ) ;
#36432=DIRECTION ( 'NONE',  ( -4.391705002472929091E-16, 1.000000000000000000, 0.000000000000000000 ) ) ;
#36438=ORIENTED_EDGE ( 'NONE', *, *, #224303, .F. ) ;
#36439=EDGE_LOOP ( 'NONE', ( #38572, #107240, #35008, #38537 ) ) ;
#36440=DIRECTION ( 'NONE',  ( 1.000000000000000000, 0.000000000000000000, 0.000000000000000000 ) ) ;
#36469=FACE_OUTER_BOUND ( 'NONE', #15216, .T. ) ;
#36474=CARTESIAN_POINT ( 'NONE',  ( 18.39999999999999858, -9.599999999988842347, -141.0320693966996828 ) ) ;
#36491=VECTOR ( 'NONE', #223609, 1000.000000000000000 ) ;
#36543=CARTESIAN_POINT ( 'NONE',  ( 21.05000000000000071, 5.500000000011153745, -155.0947339810869323 ) ) ;
#36571=DIRECTION ( 'NONE',  ( 0.000000000000000000, 0.000000000000000000, -1.000000000000000000 ) ) ;
#36589=EDGE_CURVE ( 'NONE', #139686, #117646, #87087, .T. ) ;
#36595=AXIS2_PLACEMENT_3D ( 'NONE', #140037, #37133, #35844 ) ;
#36599=DIRECTION ( 'NONE',  ( 1.000000000000000000, 0.000000000000000000, -0.000000000000000000 ) ) ;
#36619=EDGE_LOOP ( 'NONE', ( #183884, #167924, #178292, #152997 ) ) ;
#36621=ORIENTED_EDGE ( 'NONE', *, *, #97874, .F. ) ;
#36625=DIRECTION ( 'NONE',  ( -1.000000000000000000, 0.000000000000000000, 0.000000000000000000 ) ) ;
#36651=LINE ( 'NONE', #233551, #72518 ) ;
#36655=VERTEX_POINT ( 'NONE', #96721 ) ;
#36731=ORIENTED_EDGE ( 'NONE', *, *, #220299, .F. ) ;
#36736=CIRCLE ( 'NONE', #124203, 0.09999999999998898659 ) ;
#36811=LINE ( 'NONE', #53767, #120929 ) ;
#36840=DIRECTION ( 'NONE',  ( 0.000000000000000000, 0.000000000000000000, -1.000000000000000000 ) ) ;
#36841=ADVANCED_FACE ( 'NONE', ( #187870 ), #110880, .T. ) ;
#36906=EDGE_CURVE ( 'NONE', #115616, #126399, #216464, .T. ) ;
#36923=CARTESIAN_POINT ( 'NONE',  ( -23.25000000000000000, 11.65000000001115588, -122.2500000000000284 ) ) ;
#36952=CARTESIAN_POINT ( 'NONE',  ( -2.995603634470829482E-16, 6.650000000011155876, -155.2500000000000284 ) ) ;
#36955=EDGE_CURVE ( 'NONE', #174669, #253265, #241426, .T. ) ;
#36981=EDGE_CURVE ( 'NONE', #154130, #61931, #158080, .T. ) ;
#36989=CIRCLE ( 'NONE', #128546, 0.09999999999998898659 ) ;
#36998=CARTESIAN_POINT ( 'NONE',  ( 21.07954763557436806, 6.329290990048848542, -133.9341240813815546 ) ) ;
#37017=CYLINDRICAL_SURFACE ( 'NONE', #195348, 12.87499999999999822 ) ;
#37040=ORIENTED_EDGE ( 'NONE', *, *, #64935, .F. ) ;
#37047=DIRECTION ( 'NONE',  ( 1.000000000000000000, 0.000000000000000000, -0.000000000000000000 ) ) ;
#37051=VERTEX_POINT ( 'NONE', #23366 ) ;
#37056=AXIS2_PLACEMENT_3D ( 'NONE', #121329, #125150, #200830 ) ;
#37064=EDGE_CURVE ( 'NONE', #163189, #146973, #120633, .T. ) ;
#37133=DIRECTION ( 'NONE',  ( -1.000000000000000000, -2.952720810173289112E-16, 0.000000000000000000 ) ) ;
#37152=ORIENTED_EDGE ( 'NONE', *, *, #158306, .F. ) ;
#37170=DIRECTION ( 'NONE',  ( 0.000000000000000000, -1.000000000000000000, -0.000000000000000000 ) ) ;
#37182=DIRECTION ( 'NONE',  ( 1.000000000000000000, 0.000000000000000000, 0.000000000000000000 ) ) ;
#37213=AXIS2_PLACEMENT_3D ( 'NONE', #211861, #48910, #248406 ) ;
#37216=DIRECTION ( 'NONE',  ( 0.000000000000000000, 0.000000000000000000, 1.000000000000000000 ) ) ;
#37223=CARTESIAN_POINT ( 'NONE',  ( -18.59999999999999787, -1.162701749926853712, -142.1000000000000227 ) ) ;
#37224=CIRCLE ( 'NONE', #74670, 0.1000000000000089567 ) ;
#37249=EDGE_CURVE ( 'NONE', #121012, #175390, #55507, .T. ) ;
#37252=DIRECTION ( 'NONE',  ( 0.000000000000000000, 0.000000000000000000, -1.000000000000000000 ) ) ;
#37263=ORIENTED_EDGE ( 'NONE', *, *, #195890, .F. ) ;
#37323=CARTESIAN_POINT ( 'NONE',  ( -20.94560253601877164, 11.75000000001115197, -160.5100835125150809 ) ) ;
#37324=VERTEX_POINT ( 'NONE', #140054 ) ;
#37326=ORIENTED_EDGE ( 'NONE', *, *, #248462, .T. ) ;
#37334=ORIENTED_EDGE ( 'NONE', *, *, #68975, .F. ) ;
#37340=VERTEX_POINT ( 'NONE', #177935 ) ;
#37354=ORIENTED_EDGE ( 'NONE', *, *, #221045, .T. ) ;
#37365=EDGE_CURVE ( 'NONE', #44063, #222155, #171870, .T. ) ;
#37422=CARTESIAN_POINT ( 'NONE',  ( -20.64999999999999858, -8.663551401858004652, -143.5241011180673070 ) ) ;
#37434=CIRCLE ( 'NONE', #158261, 0.09999999999999949207 ) ;
#37436=CARTESIAN_POINT ( 'NONE',  ( 21.05000000000000071, -11.48912529306489994, -164.5000000000000000 ) ) ;
#37451=CARTESIAN_POINT ( 'NONE',  ( 18.59999999999999076, 1.115600667400684642E-11, -167.5000000000000284 ) ) ;
#37466=CARTESIAN_POINT ( 'NONE',  ( 22.49999999999999645, 11.74956712350054744, -133.8991416309012834 ) ) ;
#37467=ORIENTED_EDGE ( 'NONE', *, *, #91654, .F. ) ;
#37485=AXIS2_PLACEMENT_3D ( 'NONE', #254872, #217072, #231538 ) ;
#37512=ORIENTED_EDGE ( 'NONE', *, *, #131462, .T. ) ;
#37522=DIRECTION ( 'NONE',  ( -0.000000000000000000, -0.8700118002898321601, 0.4930308989875230030 ) ) ;
#37525=AXIS2_PLACEMENT_3D ( 'NONE', #104709, #60471, #25234 ) ;
#37548=DIRECTION ( 'NONE',  ( 0.000000000000000000, 0.000000000000000000, -1.000000000000000000 ) ) ;
#37554=ADVANCED_FACE ( 'NONE', ( #160943 ), #201334, .F. ) ;
#37573=ORIENTED_EDGE ( 'NONE', *, *, #189185, .F. ) ;
#37593=CARTESIAN_POINT ( 'NONE',  ( 20.95289811251229750, 8.893168004469753640, -142.5018094939185573 ) ) ;
#37643=DIRECTION ( 'NONE',  ( 1.000000000000000000, 0.000000000000000000, 0.000000000000000000 ) ) ;
#37655=ORIENTED_EDGE ( 'NONE', *, *, #75139, .F. ) ;
#37673=DIRECTION ( 'NONE',  ( 0.000000000000000000, -0.000000000000000000, 1.000000000000000000 ) ) ;
#37697=CARTESIAN_POINT ( 'NONE',  ( 21.00000000000000000, 9.750000000011153745, -146.3500000000000227 ) ) ;
#37733=ORIENTED_EDGE ( 'NONE', *, *, #150856, .T. ) ;
#37769=AXIS2_PLACEMENT_3D ( 'NONE', #215844, #257498, #37252 ) ;
#37772=VERTEX_POINT ( 'NONE', #238875 ) ;
#37776=EDGE_LOOP ( 'NONE', ( #254551, #63318, #55210, #219016, #73505 ) ) ;
#37815=EDGE_CURVE ( 'NONE', #165316, #224878, #162674, .T. ) ;
#37825=PLANE ( 'NONE',  #255249 ) ;
#37827=AXIS2_PLACEMENT_3D ( 'NONE', #62375, #160213, #21972 ) ;
#37834=DIRECTION ( 'NONE',  ( 0.000000000000000000, -0.8660254037844383745, 0.5000000000000003331 ) ) ;
#37850=AXIS2_PLACEMENT_3D ( 'NONE', #71015, #250895, #193521 ) ;
#37880=CYLINDRICAL_SURFACE ( 'NONE', #233252, 0.09999999999999939493 ) ;
#37883=DIRECTION ( 'NONE',  ( 0.000000000000000000, -0.9908441862701783398, 0.1350103645450536627 ) ) ;
#37899=DIRECTION ( 'NONE',  ( 0.000000000000000000, 0.8660254037844482555, 0.4999999999999837907 ) ) ;
#37900=PRESENTATION_STYLE_ASSIGNMENT (( #216508 ) ) ;
#37913=TOROIDAL_SURFACE ( 'NONE', #146206, 11.90000000000000213, 0.1000000000000000056 ) ;
#37916=CARTESIAN_POINT ( 'NONE',  ( 20.94983749550516450, 10.29766095125295244, -172.9743663933275855 ) ) ;
#37934=ORIENTED_EDGE ( 'NONE', *, *, #34532, .T. ) ;
#37942=AXIS2_PLACEMENT_3D ( 'NONE', #113507, #193057, #173537 ) ;
#37947=ORIENTED_EDGE ( 'NONE', *, *, #74067, .F. ) ;
#37951=ADVANCED_FACE ( 'NONE', ( #23710 ), #103191, .T. ) ;
#37970=VECTOR ( 'NONE', #66757, 1000.000000000000000 ) ;
#37973=CARTESIAN_POINT ( 'NONE',  ( 21.05000000000000071, -11.74999999998883560, -136.9000000000000341 ) ) ;
#37997=EDGE_CURVE ( 'NONE', #236893, #245147, #25486, .T. ) ;
#38015=VERTEX_POINT ( 'NONE', #225691 ) ;
#38022=EDGE_CURVE ( 'NONE', #67207, #227353, #33725, .T. ) ;
#38036=VERTEX_POINT ( 'NONE', #148774 ) ;
#38044=DIRECTION ( 'NONE',  ( -2.812466655313719426E-14, 0.1350103645451904977, 0.9908441862701596881 ) ) ;
#38048=DIRECTION ( 'NONE',  ( -1.000000000000000000, 7.304098846218134667E-16, -4.217023435051678980E-16 ) ) ;
#38150=ORIENTED_EDGE ( 'NONE', *, *, #117914, .T. ) ;
#38152=DIRECTION ( 'NONE',  ( 3.616040088954497272E-32, -1.224646799147352961E-16, 1.000000000000000000 ) ) ;
#38158=CARTESIAN_POINT ( 'NONE',  ( -18.59999999999999787, 9.150000000011157653, -146.3500000000000227 ) ) ;
#38236=DIRECTION ( 'NONE',  ( 0.000000000000000000, 0.000000000000000000, -1.000000000000000000 ) ) ;
#38246=EDGE_LOOP ( 'NONE', ( #167600, #80397, #254341, #2689 ) ) ;
#38283=CARTESIAN_POINT ( 'NONE',  ( -20.64999999999999858, 7.150000000011155876, -146.3500000000000227 ) ) ;
#38344=AXIS2_PLACEMENT_3D ( 'NONE', #180572, #181857, #1908 ) ;
#38354=AXIS2_PLACEMENT_3D ( 'NONE', #244918, #105370, #246212 ) ;
#38355=ORIENTED_EDGE ( 'NONE', *, *, #212684, .F. ) ;
#38361=ORIENTED_EDGE ( 'NONE', *, *, #62102, .F. ) ;
#38366=DIRECTION ( 'NONE',  ( 0.000000000000000000, -1.000000000000000000, -0.000000000000000000 ) ) ;
#38376=ORIENTED_EDGE ( 'NONE', *, *, #112639, .F. ) ;
#38384=ORIENTED_EDGE ( 'NONE', *, *, #122054, .F. ) ;
#38386=EDGE_CURVE ( 'NONE', #140176, #228115, #242605, .T. ) ;
#38390=EDGE_LOOP ( 'NONE', ( #195455, #130990, #188766, #37263 ) ) ;
#38443=CIRCLE ( 'NONE', #184175, 12.97499999999998721 ) ;
#38444=ORIENTED_EDGE ( 'NONE', *, *, #130866, .F. ) ;
#38474=EDGE_CURVE ( 'NONE', #12568, #47711, #185954, .T. ) ;
#38489=PLANE ( 'NONE',  #82974 ) ;
#38537=ORIENTED_EDGE ( 'NONE', *, *, #2516, .F. ) ;
#38542=CARTESIAN_POINT ( 'NONE',  ( -20.85000000000000142, 1.115600667400684642E-11, -167.5000000000000284 ) ) ;
#38572=ORIENTED_EDGE ( 'NONE', *, *, #90006, .F. ) ;
#38580=ORIENTED_EDGE ( 'NONE', *, *, #124829, .F. ) ;
#38591=CARTESIAN_POINT ( 'NONE',  ( -20.87155475150660777, 11.75000000001115197, -160.5955865291576572 ) ) ;
#38593=ADVANCED_FACE ( 'NONE', ( #95811 ), #174135, .T. ) ;
#38599=LINE ( 'NONE', #118134, #101981 ) ;
#38618=CARTESIAN_POINT ( 'NONE',  ( 18.60000000000000142, -9.321008403350125704, -141.2359382490778899 ) ) ;
#38630=DIRECTION ( 'NONE',  ( 1.000000000000000000, -0.000000000000000000, -0.000000000000000000 ) ) ;
#38700=DIRECTION ( 'NONE',  ( 1.000000000000000000, 0.000000000000000000, 0.000000000000000000 ) ) ;
#38703=AXIS2_PLACEMENT_3D ( 'NONE', #254015, #157540, #75423 ) ;
#38738=DIRECTION ( 'NONE',  ( 1.000000000000000000, 0.000000000000000000, 0.000000000000000000 ) ) ;
#38793=DIRECTION ( 'NONE',  ( -3.265361837132813093E-16, 1.000000000000000000, 0.000000000000000000 ) ) ;
#38815=CARTESIAN_POINT ( 'NONE',  ( 20.94999999999999929, 1.115600667400684642E-11, -134.0000000000000000 ) ) ;
#38824=AXIS2_PLACEMENT_3D ( 'NONE', #224489, #4157, #206220 ) ;
#38862=DIRECTION ( 'NONE',  ( -0.000000000000000000, -0.8660254037844411501, -0.4999999999999956701 ) ) ;
#38937=ADVANCED_FACE ( 'NONE', ( #92958 ), #68017, .F. ) ;
#38950=EDGE_CURVE ( 'NONE', #8389, #113973, #192924, .T. ) ;
#38971=AXIS2_PLACEMENT_3D ( 'NONE', #59482, #43815, #200319 ) ;
#38977=ORIENTED_EDGE ( 'NONE', *, *, #32228, .T. ) ;
#38983=CIRCLE ( 'NONE', #242959, 0.5000000000000004441 ) ;
#38993=AXIS2_PLACEMENT_3D ( 'NONE', #79498, #116089, #136921 ) ;
#39007=DIRECTION ( 'NONE',  ( 0.000000000000000000, -1.000000000000000000, 0.000000000000000000 ) ) ;
#39011=ORIENTED_EDGE ( 'NONE', *, *, #209001, .T. ) ;
#39018=DIRECTION ( 'NONE',  ( 2.952720810173289112E-16, -1.000000000000000000, 0.000000000000000000 ) ) ;
#39086=DIRECTION ( 'NONE',  ( 0.7071067811865388020, -0.7071067811865561215, 0.000000000000000000 ) ) ;
#39114=MECHANICAL_DESIGN_GEOMETRIC_PRESENTATION_REPRESENTATION('',(#197476),#26641);
#39136=DIRECTION ( 'NONE',  ( 0.000000000000000000, 0.000000000000000000, 1.000000000000000000 ) ) ;
#39230=FACE_OUTER_BOUND ( 'NONE', #124352, .T. ) ;
#39238=AXIS2_PLACEMENT_3D ( 'NONE', #148355, #89647, #248745 ) ;
#39252=ADVANCED_FACE ( 'NONE', ( #224458 ), #44557, .F. ) ;
#39263=DIRECTION ( 'NONE',  ( -1.000000000000000000, 0.000000000000000000, 0.000000000000000000 ) ) ;
#39301=ORIENTED_EDGE ( 'NONE', *, *, #164436, .F. ) ;
#39303=ORIENTED_EDGE ( 'NONE', *, *, #218646, .F. ) ;
#39313=EDGE_LOOP ( 'NONE', ( #103973, #66145, #228859, #72116 ) ) ;
#39315=AXIS2_PLACEMENT_3D ( 'NONE', #124991, #67572, #8888 ) ;
#39322=ORIENTED_EDGE ( 'NONE', *, *, #91206, .T. ) ;
#39337=EDGE_CURVE ( 'NONE', #178251, #112934, #194359, .T. ) ;
#39366=EDGE_CURVE ( 'NONE', #31307, #58852, #151426, .T. ) ;
#39395=ADVANCED_FACE ( 'NONE', ( #131782 ), #20854, .F. ) ;
#39416=DIRECTION ( 'NONE',  ( 1.000000000000000000, 0.000000000000000000, 0.000000000000000000 ) ) ;
#39418=AXIS2_PLACEMENT_3D ( 'NONE', #253531, #14953, #210573 ) ;
#39436=CARTESIAN_POINT ( 'NONE',  ( 18.52928932188133970, 10.27928932189250411, -158.6500000000000057 ) ) ;
#39443=LINE ( 'NONE', #139769, #123222 ) ;
#39459=DIRECTION ( 'NONE',  ( 0.000000000000000000, 1.000000000000000000, 1.626303258728238113E-15 ) ) ;
#39460=ORIENTED_EDGE ( 'NONE', *, *, #159936, .T. ) ;
#39464=DIRECTION ( 'NONE',  ( -1.836970198721029934E-16, 1.000000000000000000, 0.000000000000000000 ) ) ;
#39468=CARTESIAN_POINT ( 'NONE',  ( -18.59999999999999787, 9.350000000011156942, -155.3500000000000227 ) ) ;
#39482=EDGE_LOOP ( 'NONE', ( #61649, #151980, #167263, #122401 ) ) ;
#39484=CARTESIAN_POINT ( 'NONE',  ( -18.45140287520616695, -9.486077739518414376, -174.1405231266861051 ) ) ;
#39498=CIRCLE ( 'NONE', #152090, 0.1000000000000043493 ) ;
#39512=EDGE_CURVE ( 'NONE', #187169, #25173, #224151, .T. ) ;
#39553=DIRECTION ( 'NONE',  ( 1.000000000000000000, 0.000000000000000000, 0.000000000000000000 ) ) ;
#39562=VERTEX_POINT ( 'NONE', #68964 ) ;
#39595=ORIENTED_EDGE ( 'NONE', *, *, #132156, .F. ) ;
#39599=ORIENTED_EDGE ( 'NONE', *, *, #235926, .F. ) ;
#39661=ORIENTED_EDGE ( 'NONE', *, *, #71346, .F. ) ;
#39684=CARTESIAN_POINT ( 'NONE',  ( -23.15000000000000213, 4.250000000011156409, -155.2500000000000284 ) ) ;
#39718=FACE_OUTER_BOUND ( 'NONE', #191416, .T. ) ;
#39857=AXIS2_PLACEMENT_3D ( 'NONE', #48862, #168863, #226180 ) ;
#39869=ORIENTED_EDGE ( 'NONE', *, *, #94, .F. ) ;
#39878=EDGE_LOOP ( 'NONE', ( #6813, #230069, #62584, #217769 ) ) ;
#39881=VERTEX_POINT ( 'NONE', #43614 ) ;
#39897=DIRECTION ( 'NONE',  ( 1.000000000000000000, 0.000000000000000000, -0.000000000000000000 ) ) ;
#39926=EDGE_LOOP ( 'NONE', ( #8068, #211227, #197109, #53360 ) ) ;
#40033=LINE ( 'NONE', #178256, #192167 ) ;
#40056=VECTOR ( 'NONE', #147929, 1000.000000000000114 ) ;
#40075=DIRECTION ( 'NONE',  ( -0.000000000000000000, 0.01283462868039629209, -0.9999176327611372095 ) ) ;
#40089=CIRCLE ( 'NONE', #210739, 0.5000000000000004441 ) ;
#40121=DIRECTION ( 'NONE',  ( 0.000000000000000000, -8.881784197001840025E-16, -1.000000000000000000 ) ) ;
#40146=CARTESIAN_POINT ( 'NONE',  ( 20.94999999999999574, 6.350000000011161383, -143.8438220896831581 ) ) ;
#40191=EDGE_LOOP ( 'NONE', ( #165727, #46376, #194117, #13958 ) ) ;
#40199=DIRECTION ( 'NONE',  ( 1.000000000000000000, 0.000000000000000000, 0.000000000000000000 ) ) ;
#40210=ORIENTED_EDGE ( 'NONE', *, *, #3146, .T. ) ;
#40226=FACE_OUTER_BOUND ( 'NONE', #163635, .T. ) ;
#40247=DIRECTION ( 'NONE',  ( 2.940209281316622495E-16, -1.000000000000000000, 0.000000000000000000 ) ) ;
#40250=AXIS2_PLACEMENT_3D ( 'NONE', #117654, #212908, #176370 ) ;
#40256=ORIENTED_EDGE ( 'NONE', *, *, #234197, .T. ) ;
#40257=EDGE_LOOP ( 'NONE', ( #227275, #10711, #255707, #25070 ) ) ;
#40267=CARTESIAN_POINT ( 'NONE',  ( -20.85000000000000142, 1.115600667400684642E-11, -175.4000000000000341 ) ) ;
#40309=ORIENTED_EDGE ( 'NONE', *, *, #141257, .T. ) ;
#40327=AXIS2_PLACEMENT_3D ( 'NONE', #156097, #196461, #72704 ) ;
#40378=VECTOR ( 'NONE', #190235, 1000.000000000000000 ) ;
#40392=FACE_OUTER_BOUND ( 'NONE', #236160, .T. ) ;
#40415=DIRECTION ( 'NONE',  ( 1.000000000000000000, -0.000000000000000000, -0.000000000000000000 ) ) ;
#40431=CIRCLE ( 'NONE', #186133, 0.09999999999998898659 ) ;
#40433=CARTESIAN_POINT ( 'NONE',  ( -20.85000000000000142, 7.021664781911246322, -171.3335654018973173 ) ) ;
#40448=EDGE_CURVE ( 'NONE', #75879, #147930, #115914, .T. ) ;
#40460=AXIS2_PLACEMENT_3D ( 'NONE', #122610, #241274, #199592 ) ;
#40467=DIRECTION ( 'NONE',  ( 1.000000000000000000, 0.000000000000000000, 0.000000000000000000 ) ) ;
#40494=ADVANCED_FACE ( 'NONE', ( #193098 ), #75719, .F. ) ;
#40495=ORIENTED_EDGE ( 'NONE', *, *, #225133, .T. ) ;
#40498=CARTESIAN_POINT ( 'NONE',  ( 20.89878130938411616, 10.32747123227773045, -173.0774032850249569 ) ) ;
#40507=CIRCLE ( 'NONE', #173801, 0.09999999999998898659 ) ;
#40508=ADVANCED_FACE ( 'NONE', ( #253050 ), #74461, .T. ) ;
#40553=TOROIDAL_SURFACE ( 'NONE', #186273, 11.90000000000000391, 0.1000000000000000056 ) ;
#40580=VERTEX_POINT ( 'NONE', #256851 ) ;
#40587=DIRECTION ( 'NONE',  ( 0.7071067811865388020, -0.7071067811865561215, 0.000000000000000000 ) ) ;
#40591=LINE ( 'NONE', #256975, #31936 ) ;
#40607=ORIENTED_EDGE ( 'NONE', *, *, #48420, .T. ) ;
#40626=DIRECTION ( 'NONE',  ( 1.000000000000000000, 7.304098846218134667E-16, -0.000000000000000000 ) ) ;
#40630=DIRECTION ( 'NONE',  ( 0.000000000000000000, 0.000000000000000000, -1.000000000000000000 ) ) ;
#40689=ORIENTED_EDGE ( 'NONE', *, *, #762, .T. ) ;
#40731=AXIS2_PLACEMENT_3D ( 'NONE', #16618, #82950, #165095 ) ;
#40735=ORIENTED_EDGE ( 'NONE', *, *, #125140, .F. ) ;
#40740=FACE_OUTER_BOUND ( 'NONE', #76777, .T. ) ;
#40746=DIRECTION ( 'NONE',  ( 2.952720810173289112E-16, -1.000000000000000000, 0.000000000000000000 ) ) ;
#40772=ORIENTED_EDGE ( 'NONE', *, *, #165006, .T. ) ;
#40776=CARTESIAN_POINT ( 'NONE',  ( -23.15000000000000213, 1.115625160336667635E-11, -169.5000000000000284 ) ) ;
#40790=CIRCLE ( 'NONE', #161382, 0.09999999999998986089 ) ;
#40800=FACE_OUTER_BOUND ( 'NONE', #6563, .T. ) ;
#40853=ADVANCED_FACE ( 'NONE', ( #152399 ), #20431, .T. ) ;
#40862=AXIS2_PLACEMENT_3D ( 'NONE', #8588, #168986, #165091 ) ;
#40872=AXIS2_PLACEMENT_3D ( 'NONE', #20387, #156059, #154770 ) ;
#40878=DIRECTION ( 'NONE',  ( -0.000000000000000000, 0.000000000000000000, 1.000000000000000000 ) ) ;
#40920=LINE ( 'NONE', #98249, #106937 ) ;
#40935=VERTEX_POINT ( 'NONE', #221300 ) ;
#40936=EDGE_CURVE ( 'NONE', #175804, #177617, #205557, .T. ) ;
#40941=DIRECTION ( 'NONE',  ( 0.000000000000000000, 0.008583690987128059571, -0.9999631594459056361 ) ) ;
#41005=EDGE_LOOP ( 'NONE', ( #218032, #133068, #184152, #218135 ) ) ;
#41012=FACE_OUTER_BOUND ( 'NONE', #184869, .T. ) ;
#41031=CARTESIAN_POINT ( 'NONE',  ( 21.05000000000000071, 8.776282895303632259, -134.0000000000000000 ) ) ;
#41034=CARTESIAN_POINT ( 'NONE',  ( -20.54999999999999716, -8.730841121484170131, -157.9019252810156786 ) ) ;
#41050=VERTEX_POINT ( 'NONE', #243448 ) ;
#41055=EDGE_CURVE ( 'NONE', #63728, #230402, #91146, .T. ) ;
#41061=CIRCLE ( 'NONE', #220103, 0.09999999999999917288 ) ;
#41068=DIRECTION ( 'NONE',  ( 0.000000000000000000, 0.000000000000000000, -1.000000000000000000 ) ) ;
#41095=DIRECTION ( 'NONE',  ( 1.000000000000000000, 0.000000000000000000, 0.000000000000000000 ) ) ;
#41131=DIRECTION ( 'NONE',  ( 0.000000000000000000, 0.000000000000000000, -1.000000000000000000 ) ) ;
#41151=ADVANCED_FACE ( 'NONE', ( #50360 ), #72539, .F. ) ;
#41169=TOROIDAL_SURFACE ( 'NONE', #191191, 11.65000000000000036, 0.1000000000000000056 ) ;
#41193=EDGE_CURVE ( 'NONE', #81104, #23713, #112205, .T. ) ;
#41219=CARTESIAN_POINT ( 'NONE',  ( -18.50000000000000000, 7.021664781911246322, -171.3335654018973173 ) ) ;
#41221=DIRECTION ( 'NONE',  ( -0.000000000000000000, 0.1350103645451876666, 0.9908441862701600211 ) ) ;
#41261=ORIENTED_EDGE ( 'NONE', *, *, #205610, .T. ) ;
#41276=CARTESIAN_POINT ( 'NONE',  ( 21.53551880898956838, 6.784797761427480367, -133.9010302654283748 ) ) ;
#41279=VERTEX_POINT ( 'NONE', #77625 ) ;
#41282=CARTESIAN_POINT ( 'NONE',  ( -21.05000000000000071, -0.09999999998884476216, -127.4593430482987912 ) ) ;
#41285=CYLINDRICAL_SURFACE ( 'NONE', #80871, 4.049999999999998046 ) ;
#41310=CARTESIAN_POINT ( 'NONE',  ( -18.51555513499593175, -9.352657054493597855, -141.1951698956972052 ) ) ;
#41327=DIRECTION ( 'NONE',  ( 0.000000000000000000, 1.000000000000000000, 0.000000000000000000 ) ) ;
#41353=CARTESIAN_POINT ( 'NONE',  ( 21.53752568617686691, 6.786807874514976469, -133.9010255387156008 ) ) ;
#41391=CARTESIAN_POINT ( 'NONE',  ( 20.95512820512820440, 8.876151316299271343, -155.2500000000000284 ) ) ;
#41400=CIRCLE ( 'NONE', #257802, 7.899999999999990585 ) ;
#41408=EDGE_CURVE ( 'NONE', #118232, #79366, #49635, .T. ) ;
#41412=EDGE_CURVE ( 'NONE', #214434, #159346, #182930, .T. ) ;
#41438=DIRECTION ( 'NONE',  ( 0.000000000000000000, 0.000000000000000000, 1.000000000000000000 ) ) ;
#41446=ADVANCED_FACE ( 'NONE', ( #184454 ), #245724, .F. ) ;
#41447=AXIS2_PLACEMENT_3D ( 'NONE', #172594, #252073, #17331 ) ;
#41450=DIRECTION ( 'NONE',  ( -1.000000000000000000, 0.000000000000000000, 0.000000000000000000 ) ) ;
#41479=SPHERICAL_SURFACE ( 'NONE', #13942, 0.1000000000000000056 ) ;
#41480=DIRECTION ( 'NONE',  ( -0.000000000000000000, -0.000000000000000000, -1.000000000000000000 ) ) ;
#41485=ORIENTED_EDGE ( 'NONE', *, *, #148501, .T. ) ;
#41526=CARTESIAN_POINT ( 'NONE',  ( 23.14999999999999858, 1.115600667400684642E-11, -167.5000000000000284 ) ) ;
#41535=EDGE_CURVE ( 'NONE', #151810, #171180, #191506, .T. ) ;
#41545=VERTEX_POINT ( 'NONE', #117447 ) ;
#41548=ORIENTED_EDGE ( 'NONE', *, *, #155449, .T. ) ;
#41552=DIRECTION ( 'NONE',  ( 0.000000000000000000, 1.000000000000000000, 0.000000000000000000 ) ) ;
#41580=CIRCLE ( 'NONE', #104065, 12.97499999999998721 ) ;
#41581=DIRECTION ( 'NONE',  ( 1.000000000000000000, -0.000000000000000000, -0.000000000000000000 ) ) ;
#41585=CARTESIAN_POINT ( 'NONE',  ( -23.25000000000000000, 1.115600667400684642E-11, -138.0500000000000114 ) ) ;
#41648=FACE_OUTER_BOUND ( 'NONE', #49537, .T. ) ;
#41658=CARTESIAN_POINT ( 'NONE',  ( -18.59999999999999787, 1.835341550235567887, -145.6551512925629766 ) ) ;
#41669=CARTESIAN_POINT ( 'NONE',  ( -23.25000000000000000, 1.115600667400684642E-11, -134.0000000000000000 ) ) ;
#41704=EDGE_LOOP ( 'NONE', ( #138727, #170878, #247738, #197920 ) ) ;
#41705=VECTOR ( 'NONE', #99633, 1000.000000000000000 ) ;
#41733=CARTESIAN_POINT ( 'NONE',  ( -23.25000000000000000, 10.33248238083634440, -173.0948465439131496 ) ) ;
#41773=VERTEX_POINT ( 'NONE', #205961 ) ;
#41787=DIRECTION ( 'NONE',  ( 0.000000000000000000, 8.881784197000685330E-16, -1.000000000000000000 ) ) ;
#41804=AXIS2_PLACEMENT_3D ( 'NONE', #191578, #207280, #7785 ) ;
#41822=EDGE_CURVE ( 'NONE', #116413, #220134, #257654, .T. ) ;
#41828=ADVANCED_FACE ( 'NONE', ( #26058 ), #90566, .F. ) ;
#41851=CARTESIAN_POINT ( 'NONE',  ( 18.49999999999999645, 1.115600667400684642E-11, -167.5000000000000284 ) ) ;
#41854=DIRECTION ( 'NONE',  ( 0.000000000000000000, 0.000000000000000000, -1.000000000000000000 ) ) ;
#41909=VECTOR ( 'NONE', #153582, 1000.000000000000114 ) ;
#41912=ORIENTED_EDGE ( 'NONE', *, *, #34071, .T. ) ;
#41921=ORIENTED_EDGE ( 'NONE', *, *, #60769, .T. ) ;
#41935=ORIENTED_EDGE ( 'NONE', *, *, #137017, .F. ) ;
#41957=CARTESIAN_POINT ( 'NONE',  ( -20.94999999999999929, 11.65000000001115232, -167.5000000000000284 ) ) ;
#41991=AXIS2_PLACEMENT_3D ( 'NONE', #64504, #144021, #223552 ) ;
#42010=VERTEX_POINT ( 'NONE', #72685 ) ;
#42034=CARTESIAN_POINT ( 'NONE',  ( 20.85000000106584750, 11.75000000001115907, -160.6555046564734539 ) ) ;
#42074=DIRECTION ( 'NONE',  ( 0.000000000000000000, 0.000000000000000000, 1.000000000000000000 ) ) ;
#42090=AXIS2_PLACEMENT_3D ( 'NONE', #156204, #113198, #14121 ) ;
#42093=CARTESIAN_POINT ( 'NONE',  ( 21.87500000000000355, 9.750000000011153745, -146.3500000000000227 ) ) ;
#42112=ORIENTED_EDGE ( 'NONE', *, *, #142596, .T. ) ;
#42121=CARTESIAN_POINT ( 'NONE',  ( 20.94999999999999929, -12.41227409413852811, -164.5000000000000000 ) ) ;
#42124=ORIENTED_EDGE ( 'NONE', *, *, #104048, .T. ) ;
#42129=SPHERICAL_SURFACE ( 'NONE', #71839, 0.1000000000000000056 ) ;
#42134=VERTEX_POINT ( 'NONE', #219856 ) ;
#42159=ORIENTED_EDGE ( 'NONE', *, *, #225924, .T. ) ;
#42167=DIRECTION ( 'NONE',  ( 1.000000000000000000, 0.000000000000000000, 0.000000000000000000 ) ) ;
#42181=DIRECTION ( 'NONE',  ( 0.000000000000000000, 1.000000000000000000, 0.000000000000000000 ) ) ;
#42193=ORIENTED_EDGE ( 'NONE', *, *, #193338, .F. ) ;
#42196=ORIENTED_EDGE ( 'NONE', *, *, #117727, .T. ) ;
#42207=CARTESIAN_POINT ( 'NONE',  ( -21.05000000000000071, 11.63687328911514030, -140.8217592133249525 ) ) ;
#42234=DIRECTION ( 'NONE',  ( -1.000000000000000000, -0.000000000000000000, -0.000000000000000000 ) ) ;
#42273=ORIENTED_EDGE ( 'NONE', *, *, #152535, .F. ) ;
#42278=CARTESIAN_POINT ( 'NONE',  ( -22.39999999999999858, -0.1008583690875575894, -122.2504328765106294 ) ) ;
#42280=ORIENTED_EDGE ( 'NONE', *, *, #41535, .T. ) ;
#42304=CARTESIAN_POINT ( 'NONE',  ( 20.85000000000000142, 11.65000000001115943, -167.5000000000000284 ) ) ;
#42346=CIRCLE ( 'NONE', #96481, 0.09999999999999817368 ) ;
#42396=AXIS2_PLACEMENT_3D ( 'NONE', #184315, #168671, #68236 ) ;
#42416=CARTESIAN_POINT ( 'NONE',  ( -18.59999999999999787, -1.835341550213255957, -145.6551512925629766 ) ) ;
#42426=VERTEX_POINT ( 'NONE', #4042 ) ;
#42431=ORIENTED_EDGE ( 'NONE', *, *, #68313, .T. ) ;
#42460=EDGE_CURVE ( 'NONE', #230402, #29064, #191301, .T. ) ;
#42509=AXIS2_PLACEMENT_3D ( 'NONE', #136234, #239217, #254865 ) ;
#42512=VERTEX_POINT ( 'NONE', #126570 ) ;
#42519=VERTEX_POINT ( 'NONE', #181425 ) ;
#42548=FACE_OUTER_BOUND ( 'NONE', #157993, .T. ) ;
#42584=AXIS2_PLACEMENT_3D ( 'NONE', #38542, #118069, #155946 ) ;
#42585=DIRECTION ( 'NONE',  ( 1.000000000000000000, 0.000000000000000000, 0.000000000000000000 ) ) ;
#42596=CARTESIAN_POINT ( 'NONE',  ( -20.00857864376270001, 9.150000000011157653, -146.2500000000000284 ) ) ;
#42606=CARTESIAN_POINT ( 'NONE',  ( 21.46681500593256331, 6.857511159395965450, -134.0000000000000000 ) ) ;
#42614=DIRECTION ( 'NONE',  ( -0.000000000000000000, -0.000000000000000000, -1.000000000000000000 ) ) ;
#42623=CARTESIAN_POINT ( 'NONE',  ( -20.54999999999999716, -8.999999999988844479, -157.6060308773475924 ) ) ;
#42642=CARTESIAN_POINT ( 'NONE',  ( 18.59999999999999787, 1.115600667400684642E-11, -134.0000000000000000 ) ) ;
#42688=ORIENTED_EDGE ( 'NONE', *, *, #254388, .F. ) ;
#42693=VECTOR ( 'NONE', #13206, 1000.000000000000227 ) ;
#42694=CARTESIAN_POINT ( 'NONE',  ( -18.59999999999999787, 9.350000000011156942, -146.2500000000000284 ) ) ;
#42707=ORIENTED_EDGE ( 'NONE', *, *, #214625, .F. ) ;
#42717=ORIENTED_EDGE ( 'NONE', *, *, #209373, .F. ) ;
#42725=ORIENTED_EDGE ( 'NONE', *, *, #173386, .F. ) ;
#42758=CARTESIAN_POINT ( 'NONE',  ( 20.12500000000000000, 9.750000000011153745, -142.1117712821142902 ) ) ;
#42770=EDGE_LOOP ( 'NONE', ( #200309, #140821, #254104, #157909 ) ) ;
#42814=ORIENTED_EDGE ( 'NONE', *, *, #96210, .T. ) ;
#42831=VERTEX_POINT ( 'NONE', #145807 ) ;
#42832=ADVANCED_FACE ( 'NONE', ( #144518 ), #123701, .T. ) ;
#42892=FACE_OUTER_BOUND ( 'NONE', #240091, .T. ) ;
#42940=CIRCLE ( 'NONE', #188669, 0.09999999999998898659 ) ;
#42948=ORIENTED_EDGE ( 'NONE', *, *, #233532, .T. ) ;
#42975=VECTOR ( 'NONE', #228626, 1000.000000000000000 ) ;
#43031=CIRCLE ( 'NONE', #130494, 0.5999999999999894307 ) ;
#43033=FACE_OUTER_BOUND ( 'NONE', #46591, .T. ) ;
#43085=EDGE_CURVE ( 'NONE', #34631, #60110, #74025, .T. ) ;
#43090=CARTESIAN_POINT ( 'NONE',  ( -20.54999999999999716, 1.115600667400684642E-11, -167.5000000000000284 ) ) ;
#43103=DIRECTION ( 'NONE',  ( 1.000000000000000000, -0.000000000000000000, -0.000000000000000000 ) ) ;
#43134=EDGE_CURVE ( 'NONE', #55107, #174088, #96096, .T. ) ;
#43161=ORIENTED_EDGE ( 'NONE', *, *, #152465, .F. ) ;
#43169=DIRECTION ( 'NONE',  ( -1.000000000000000000, 0.000000000000000000, 0.000000000000000000 ) ) ;
#43176=ORIENTED_EDGE ( 'NONE', *, *, #251543, .T. ) ;
#43246=CIRCLE ( 'NONE', #134970, 7.800000000000001599 ) ;
#43264=DIRECTION ( 'NONE',  ( 0.000000000000000000, -1.953992523340280244E-14, -1.000000000000000000 ) ) ;
#43273=ORIENTED_EDGE ( 'NONE', *, *, #237204, .T. ) ;
#43288=ORIENTED_EDGE ( 'NONE', *, *, #105078, .T. ) ;
#43308=CIRCLE ( 'NONE', #201497, 0.5999999999999894307 ) ;
#43347=DIRECTION ( 'NONE',  ( 0.000000000000000000, -1.000000000000000000, 0.000000000000000000 ) ) ;
#43380=DIRECTION ( 'NONE',  ( 0.000000000000000000, 0.000000000000000000, -1.000000000000000000 ) ) ;
#43383=AXIS2_PLACEMENT_3D ( 'NONE', #128628, #208175, #129887 ) ;
#43387=ORIENTED_EDGE ( 'NONE', *, *, #133304, .T. ) ;
#43395=ORIENTED_EDGE ( 'NONE', *, *, #13559, .T. ) ;
#43398=EDGE_CURVE ( 'NONE', #59451, #105943, #125191, .T. ) ;
#43399=ORIENTED_EDGE ( 'NONE', *, *, #148646, .T. ) ;
#43447=ADVANCED_FACE ( 'NONE', ( #217020 ), #18830, .T. ) ;
#43473=VERTEX_POINT ( 'NONE', #236584 ) ;
#43476=CARTESIAN_POINT ( 'NONE',  ( 20.74897398619109268, 10.59569302167756888, -141.6793114562569542 ) ) ;
#43484=AXIS2_PLACEMENT_3D ( 'NONE', #79180, #3499, #219989 ) ;
#43487=CARTESIAN_POINT ( 'NONE',  ( 20.94999999999999929, 1.115650877919449575E-11, -163.4000000000000341 ) ) ;
#43497=CIRCLE ( 'NONE', #222534, 0.09999999999999817368 ) ;
#43510=FACE_OUTER_BOUND ( 'NONE', #6338, .T. ) ;
#43515=EDGE_CURVE ( 'NONE', #185781, #253858, #20135, .T. ) ;
#43538=LINE ( 'NONE', #195586, #215937 ) ;
#43542=AXIS2_PLACEMENT_3D ( 'NONE', #91030, #53184, #130144 ) ;
#43601=VECTOR ( 'NONE', #152365, 1000.000000000000000 ) ;
#43614=CARTESIAN_POINT ( 'NONE',  ( -23.25000000000000000, 1.910280373842930812, -154.8686321448010972 ) ) ;
#43624=CARTESIAN_POINT ( 'NONE',  ( -23.25000000000000000, -11.64999999998884483, -164.4000000000000057 ) ) ;
#43640=CARTESIAN_POINT ( 'NONE',  ( -18.59999999999999787, -9.399999999988787991, -141.2972597596633193 ) ) ;
#43656=VERTEX_POINT ( 'NONE', #147784 ) ;
#43678=DIRECTION ( 'NONE',  ( 1.000000000000000000, -0.000000000000000000, -0.000000000000000000 ) ) ;
#43709=VERTEX_POINT ( 'NONE', #244290 ) ;
#43734=ORIENTED_EDGE ( 'NONE', *, *, #112123, .T. ) ;
#43742=DIRECTION ( 'NONE',  ( 0.000000000000000000, 0.000000000000000000, -1.000000000000000000 ) ) ;
#43801=VERTEX_POINT ( 'NONE', #75944 ) ;
#43802=CIRCLE ( 'NONE', #168764, 0.09999999999998898659 ) ;
#43806=CARTESIAN_POINT ( 'NONE',  ( 18.55121869061587958, 10.32747123227773400, -173.0774032850249569 ) ) ;
#43815=DIRECTION ( 'NONE',  ( 1.000000000000000000, 0.000000000000000000, 0.000000000000000000 ) ) ;
#43824=ORIENTED_EDGE ( 'NONE', *, *, #209218, .F. ) ;
#43855=CARTESIAN_POINT ( 'NONE',  ( -18.59999999999999787, -1.835859311432481045, -179.0044391687985410 ) ) ;
#43864=ORIENTED_EDGE ( 'NONE', *, *, #25214, .T. ) ;
#43908=DIRECTION ( 'NONE',  ( -4.408576920032448588E-17, 0.1350103645451876944, 0.9908441862701601321 ) ) ;
#43924=DIRECTION ( 'NONE',  ( 0.000000000000000000, 0.000000000000000000, 1.000000000000000000 ) ) ;
#43939=EDGE_CURVE ( 'NONE', #255163, #63952, #200384, .T. ) ;
#43944=LINE ( 'NONE', #98743, #255719 ) ;
#43946=ORIENTED_EDGE ( 'NONE', *, *, #148192, .F. ) ;
#43974=DIRECTION ( 'NONE',  ( 0.000000000000000000, 1.000000000000000000, -6.308085367188393199E-16 ) ) ;
#43979=LINE ( 'NONE', #23160, #94209 ) ;
#43986=ORIENTED_EDGE ( 'NONE', *, *, #195646, .T. ) ;
#44033=VERTEX_POINT ( 'NONE', #14069 ) ;
#44041=ADVANCED_FACE ( 'NONE', ( #184018 ), #12795, .T. ) ;
#44063=VERTEX_POINT ( 'NONE', #26252 ) ;
#44085=ORIENTED_EDGE ( 'NONE', *, *, #61038, .F. ) ;
#44174=LINE ( 'NONE', #159005, #33611 ) ;
#44186=CARTESIAN_POINT ( 'NONE',  ( 21.14999999999999858, 11.65000000001115943, -134.1000000000000227 ) ) ;
#44198=DIRECTION ( 'NONE',  ( -0.000000000000000000, -0.000000000000000000, 1.000000000000000000 ) ) ;
#44205=DIRECTION ( 'NONE',  ( 1.000000000000000000, 1.836970198721029934E-16, 0.000000000000000000 ) ) ;
#44221=CARTESIAN_POINT ( 'NONE',  ( 20.85000000000000142, 11.75000000001115907, -167.5000000000000284 ) ) ;
#44224=CARTESIAN_POINT ( 'NONE',  ( 22.40000000000020819, -0.1008583690885111045, -122.2504328765103168 ) ) ;
#44248=FACE_OUTER_BOUND ( 'NONE', #165025, .T. ) ;
#44280=ORIENTED_EDGE ( 'NONE', *, *, #151923, .T. ) ;
#44285=DIRECTION ( 'NONE',  ( 0.000000000000000000, -1.000000000000000000, -0.000000000000000000 ) ) ;
#44324=CARTESIAN_POINT ( 'NONE',  ( 23.14999999999999503, 11.75000000001116263, -122.2500000000000284 ) ) ;
#44428=SPHERICAL_SURFACE ( 'NONE', #27625, 0.1000000000000000056 ) ;
#44452=VERTEX_POINT ( 'NONE', #245945 ) ;
#44456=DIRECTION ( 'NONE',  ( -1.000000000000000000, 0.000000000000000000, 0.000000000000000000 ) ) ;
#44458=PLANE ( 'NONE',  #224158 ) ;
#44470=EDGE_CURVE ( 'NONE', #73222, #184550, #166433, .T. ) ;
#44503=DIRECTION ( 'NONE',  ( 0.000000000000000000, -1.000000000000000000, 0.000000000000000000 ) ) ;
#44557=CYLINDRICAL_SURFACE ( 'NONE', #163878, 0.09999999999998898659 ) ;
#44560=ORIENTED_EDGE ( 'NONE', *, *, #2039, .F. ) ;
#44626=CARTESIAN_POINT ( 'NONE',  ( -23.15000000000000213, -11.48912529306489994, -164.4000000000000057 ) ) ;
#44644=CARTESIAN_POINT ( 'NONE',  ( 21.13461538461538325, 10.61458296203669427, -146.3500000000000227 ) ) ;
#44658=ADVANCED_FACE ( 'NONE', ( #24037 ), #162263, .T. ) ;
#44669=LINE ( 'NONE', #65495, #207413 ) ;
#44688=CARTESIAN_POINT ( 'NONE',  ( 23.14999999999999858, 1.115600667400684642E-11, -167.5000000000000284 ) ) ;
#44689=VERTEX_POINT ( 'NONE', #41034 ) ;
#44723=ORIENTED_EDGE ( 'NONE', *, *, #244606, .F. ) ;
#44736=VERTEX_POINT ( 'NONE', #160974 ) ;
#44749=CARTESIAN_POINT ( 'NONE',  ( 21.04999999999999716, -0.08561306079281094661, -127.5862402661897050 ) ) ;
#44759=EDGE_CURVE ( 'NONE', #159790, #122938, #250617, .T. ) ;
#44760=CARTESIAN_POINT ( 'NONE',  ( -21.05000000000000071, 5.900000000011102586, -144.2190997646564483 ) ) ;
#44770=CARTESIAN_POINT ( 'NONE',  ( 23.14999999999999858, 4.000000000011155521, -167.5000000000000284 ) ) ;
#44773=CARTESIAN_POINT ( 'NONE',  ( -23.15000000000000213, -11.39257802169451139, -164.4260504201680817 ) ) ;
#44801=VERTEX_POINT ( 'NONE', #87814 ) ;
#44806=ORIENTED_EDGE ( 'NONE', *, *, #84445, .F. ) ;
#44847=ADVANCED_FACE ( 'NONE', ( #169997, #167405 ), #245634, .T. ) ;
#44885=CIRCLE ( 'NONE', #219652, 12.97499999999998721 ) ;
#44925=LINE ( 'NONE', #167464, #89341 ) ;
#44975=EDGE_CURVE ( 'NONE', #174088, #38036, #200929, .T. ) ;
#44976=DIRECTION ( 'NONE',  ( 0.000000000000000000, -8.881784197001644782E-16, -1.000000000000000000 ) ) ;
#45023=AXIS2_PLACEMENT_3D ( 'NONE', #238917, #236341, #195954 ) ;
#45028=CARTESIAN_POINT ( 'NONE',  ( -18.39999999999999858, -9.599999999988845900, -174.2001893912220680 ) ) ;
#45033=EDGE_LOOP ( 'NONE', ( #160107, #98866, #165113, #3381 ) ) ;
#45052=ADVANCED_FACE ( 'NONE', ( #220634 ), #63350, .T. ) ;
#45074=DIRECTION ( 'NONE',  ( 1.000000000000000000, 0.000000000000000000, 0.000000000000000000 ) ) ;
#45085=EDGE_CURVE ( 'NONE', #14142, #32896, #192554, .T. ) ;
#45096=ORIENTED_EDGE ( 'NONE', *, *, #104125, .F. ) ;
#45144=CARTESIAN_POINT ( 'NONE',  ( -18.48408745364672967, -9.664322258652006781, -174.1830785333283416 ) ) ;
#45157=DIRECTION ( 'NONE',  ( -1.000000000000000000, -7.304098846218134667E-16, 0.000000000000000000 ) ) ;
#45205=FACE_OUTER_BOUND ( 'NONE', #69178, .T. ) ;
#45209=ADVANCED_FACE ( 'NONE', ( #115955 ), #22068, .T. ) ;
#45213=CARTESIAN_POINT ( 'NONE',  ( 21.97500000000000497, 9.750000000011153745, -155.2500000000000000 ) ) ;
#45220=ORIENTED_EDGE ( 'NONE', *, *, #254847, .F. ) ;
#45224=EDGE_CURVE ( 'NONE', #125446, #232714, #14306, .T. ) ;
#45227=CARTESIAN_POINT ( 'NONE',  ( 18.39999999999999858, -9.682403433465237796, -174.1568433774128266 ) ) ;
#45231=CIRCLE ( 'NONE', #107771, 11.80000000000000426 ) ;
#45242=PRODUCT_DEFINITION_CONTEXT ( 'detailed design', #242380, 'design' ) ;
#45247=DIRECTION ( 'NONE',  ( 0.000000000000000000, 0.000000000000000000, -1.000000000000000000 ) ) ;
#45248=FACE_OUTER_BOUND ( 'NONE', #98563, .T. ) ;
#45263=CARTESIAN_POINT ( 'NONE',  ( -21.05000000000000071, -1.851028230129704522, -145.6539132694225032 ) ) ;
#45297=VERTEX_POINT ( 'NONE', #203176 ) ;
#45334=EDGE_LOOP ( 'NONE', ( #132820, #13749, #163899, #223913 ) ) ;
#45360=ORIENTED_EDGE ( 'NONE', *, *, #238209, .F. ) ;
#45409=CYLINDRICAL_SURFACE ( 'NONE', #97421, 0.09999999999999817368 ) ;
#45411=CARTESIAN_POINT ( 'NONE',  ( 23.14999999999999858, 1.115600667400684642E-11, -167.5000000000000284 ) ) ;
#45426=ORIENTED_EDGE ( 'NONE', *, *, #56936, .F. ) ;
#45429=CYLINDRICAL_SURFACE ( 'NONE', #24087, 0.5000000000000004441 ) ;
#45452=DIRECTION ( 'NONE',  ( 1.000000000000000000, 0.000000000000000000, 0.000000000000000000 ) ) ;
#45475=DIRECTION ( 'NONE',  ( 0.000000000000000000, 0.9654727137038715545, 0.2605042016806676242 ) ) ;
#45482=ADVANCED_FACE ( 'NONE', ( #247435 ), #26159, .T. ) ;
#45484=DIRECTION ( 'NONE',  ( 0.000000000000000000, 0.000000000000000000, -1.000000000000000000 ) ) ;
#45486=DIRECTION ( 'NONE',  ( 0.000000000000000000, -0.8068669527897506244, -0.5907332058516622242 ) ) ;
#45512=EDGE_CURVE ( 'NONE', #43656, #115992, #184341, .T. ) ;
#45513=CARTESIAN_POINT ( 'NONE',  ( -23.25000000000000000, -8.999999999988844479, -158.2060308773475867 ) ) ;
#45538=EDGE_CURVE ( 'NONE', #174969, #13316, #67515, .T. ) ;
#45559=CARTESIAN_POINT ( 'NONE',  ( 18.52165635395197896, -9.481150711271054021, -141.0248375828624319 ) ) ;
#45561=CARTESIAN_POINT ( 'NONE',  ( -21.14999999999999858, 6.540656951712397138, -134.0000000000000000 ) ) ;
#45570=DIRECTION ( 'NONE',  ( 0.000000000000000000, 0.000000000000000000, -1.000000000000000000 ) ) ;
#45598=LINE ( 'NONE', #44324, #88525 ) ;
#45633=LINE ( 'NONE', #83434, #134987 ) ;
#45687=DIRECTION ( 'NONE',  ( -1.000000000000000000, 0.000000000000000000, 0.000000000000000000 ) ) ;
#45706=ORIENTED_EDGE ( 'NONE', *, *, #172243, .F. ) ;
#45728=DIRECTION ( 'NONE',  ( 1.000000000000000000, 0.000000000000000000, -0.000000000000000000 ) ) ;
#45737=EDGE_CURVE ( 'NONE', #208746, #176500, #209845, .T. ) ;
#45738=DIRECTION ( 'NONE',  ( -1.000000000000000000, 0.000000000000000000, 0.000000000000000000 ) ) ;
#45749=CARTESIAN_POINT ( 'NONE',  ( 21.93642651522410603, 7.327166239336949438, -134.0000000000000000 ) ) ;
#45751=ORIENTED_EDGE ( 'NONE', *, *, #68313, .F. ) ;
#45755=CIRCLE ( 'NONE', #179064, 11.64999999999999325 ) ;
#45773=AXIS2_PLACEMENT_3D ( 'NONE', #234775, #56114, #37883 ) ;
#45775=VECTOR ( 'NONE', #49952, 1000.000000000000000 ) ;
#45788=CARTESIAN_POINT ( 'NONE',  ( -20.94999999999999929, -11.48912529306490349, -137.0000000000000000 ) ) ;
#45813=CARTESIAN_POINT ( 'NONE',  ( -22.49072729836729678, 0.05648193274477466413, -122.3499917508450920 ) ) ;
#45821=CARTESIAN_POINT ( 'NONE',  ( 21.05000000000000071, 10.72371681401022592, -141.5943992358848220 ) ) ;
#45823=AXIS2_PLACEMENT_3D ( 'NONE', #175892, #36384, #71651 ) ;
#45836=LINE ( 'NONE', #125385, #32910 ) ;
#45852=DIRECTION ( 'NONE',  ( -1.000000000000000000, 0.000000000000000000, 0.000000000000000000 ) ) ;
#45857=CARTESIAN_POINT ( 'NONE',  ( -18.59999999999999787, 9.350000000011156942, -155.2500000000000284 ) ) ;
#45886=ORIENTED_EDGE ( 'NONE', *, *, #129744, .F. ) ;
#45901=EDGE_CURVE ( 'NONE', #42426, #153822, #109701, .T. ) ;
#45949=EDGE_LOOP ( 'NONE', ( #220138, #231610, #129435, #3235 ) ) ;
#45962=VERTEX_POINT ( 'NONE', #168714 ) ;
#45980=LINE ( 'NONE', #164659, #110423 ) ;
#45988=ORIENTED_EDGE ( 'NONE', *, *, #90139, .T. ) ;
#45999=TOROIDAL_SURFACE ( 'NONE', #116738, 3.899999999999999467, 0.1000000000000000056 ) ;
#46007=DIRECTION ( 'NONE',  ( 1.000000000000000000, 0.000000000000000000, 0.000000000000000000 ) ) ;
#46032=CARTESIAN_POINT ( 'NONE',  ( 20.75572585718235530, 8.882316728409755058, -142.4972583987020585 ) ) ;
#46034=CARTESIAN_POINT ( 'NONE',  ( 21.00000000000000000, 9.750000000011153745, -155.2500000000000284 ) ) ;
#46075=CONICAL_SURFACE ( 'NONE', #100225, 4.299999999999970512, 0.7853981633974466137 ) ;
#46089=EDGE_LOOP ( 'NONE', ( #77570, #61552, #199715, #129280 ) ) ;
#46096=ORIENTED_EDGE ( 'NONE', *, *, #99391, .T. ) ;
#46116=B_SPLINE_CURVE_WITH_KNOTS ( 'NONE', 3,
 ( #148102, #249766, #172846, #227621, #112822, #211934, #90677, #33325, #69866, #149405, #13717, #188504, #111538, #29472, #71148, #110245, #88088, #248483, #129808 ),
 .UNSPECIFIED., .F., .F.,
 ( 4, 3, 3, 3, 3, 3, 4 ),
 ( 0.000000000000000000, 2.646747978908405501E-05, 5.271166642127181513E-05, 9.008788829882518278E-05, 0.0001426648776560658801, 0.0001897378458659452290, 0.0001917382627805908253 ),
 .UNSPECIFIED. ) ;
#46126=EDGE_CURVE ( 'NONE', #159966, #196636, #196875, .T. ) ;
#46141=ADVANCED_FACE ( 'NONE', ( #138170 ), #219004, .F. ) ;
#46164=CARTESIAN_POINT ( 'NONE',  ( -20.94999999999999929, -11.64999999998884483, -167.5000000000000000 ) ) ;
#46166=CARTESIAN_POINT ( 'NONE',  ( 21.05000000000000071, 11.60000000001116227, -160.5717967697245285 ) ) ;
#46233=CARTESIAN_POINT ( 'NONE',  ( 20.94999999999999929, 1.115600667400684642E-11, -171.6000000000000227 ) ) ;
#46243=CIRCLE ( 'NONE', #12968, 0.5000000000000004441 ) ;
#46288=ORIENTED_EDGE ( 'NONE', *, *, #202565, .T. ) ;
#46307=ORIENTED_EDGE ( 'NONE', *, *, #190794, .T. ) ;
#46309=DIRECTION ( 'NONE',  ( -0.000000000000000000, 0.000000000000000000, 1.000000000000000000 ) ) ;
#46322=VERTEX_POINT ( 'NONE', #190170 ) ;
#46333=DIRECTION ( 'NONE',  ( -3.265361837132813093E-16, 1.000000000000000000, 0.000000000000000000 ) ) ;
#46337=CARTESIAN_POINT ( 'NONE',  ( 23.25000000000000000, -9.599999999988849453, -122.2500000000000284 ) ) ;
#46342=B_SPLINE_CURVE_WITH_KNOTS ( 'NONE', 3,
 ( #229632, #206216, #130516, #91408, #168426, #210078 ),
 .UNSPECIFIED., .F., .F.,
 ( 4, 2, 4 ),
 ( 0.000000000000000000, 0.0002113392456165905737, 0.0004226784912331811475 ),
 .UNSPECIFIED. ) ;
#46376=ORIENTED_EDGE ( 'NONE', *, *, #120018, .F. ) ;
#46391=EDGE_LOOP ( 'NONE', ( #231378, #116224, #150652, #257615 ) ) ;
#46409=ADVANCED_FACE ( 'NONE', ( #137863 ), #75373, .F. ) ;
#46415=CARTESIAN_POINT ( 'NONE',  ( -18.41809261886923466, -9.682403314745256395, -174.1568435500915086 ) ) ;
#46451=CARTESIAN_POINT ( 'NONE',  ( 22.47007471830798764, 1.115784145324971765E-11, -126.2792893480735330 ) ) ;
#46477=PLANE ( 'NONE',  #73074 ) ;
#46506=CARTESIAN_POINT ( 'NONE',  ( -23.15000000000000213, -8.999999999988844479, -157.6060308773475924 ) ) ;
#46523=EDGE_CURVE ( 'NONE', #7471, #44689, #218199, .T. ) ;
#46528=CARTESIAN_POINT ( 'NONE',  ( -20.93975676684922504, 10.31104185824063535, -173.0204516983106089 ) ) ;
#46550=ORIENTED_EDGE ( 'NONE', *, *, #1329, .F. ) ;
#46556=VERTEX_POINT ( 'NONE', #185996 ) ;
#46560=CARTESIAN_POINT ( 'NONE',  ( 23.14999999999999858, 5.600000000011153389, -146.4052660189131245 ) ) ;
#46563=CIRCLE ( 'NONE', #586, 0.09999999999998898659 ) ;
#46577=CYLINDRICAL_SURFACE ( 'NONE', #198306, 2.000000000000001776 ) ;
#46591=EDGE_LOOP ( 'NONE', ( #11748, #49771, #109496 ) ) ;
#46597=ADVANCED_FACE ( 'NONE', ( #182153 ), #145571, .F. ) ;
#46600=CARTESIAN_POINT ( 'NONE',  ( 21.05000000000000071, 6.350000000011161383, -143.8438220896831581 ) ) ;
#46622=DIRECTION ( 'NONE',  ( 1.000000000000000000, 0.000000000000000000, 0.000000000000000000 ) ) ;
#46635=CARTESIAN_POINT ( 'NONE',  ( -20.85000000000000142, -1.164121893230052995, -175.3148480855716400 ) ) ;
#46644=CARTESIAN_POINT ( 'NONE',  ( -18.50000000000000000, 6.846123162363745074, -171.2377262668498759 ) ) ;
#46672=AXIS2_PLACEMENT_3D ( 'NONE', #10219, #50592, #152312 ) ;
#46676=DIRECTION ( 'NONE',  ( 0.000000000000000000, 0.9908441862701782288, 0.1350103645450542456 ) ) ;
#46686=DIRECTION ( 'NONE',  ( 6.938893903907991995E-14, 0.000000000000000000, 1.000000000000000000 ) ) ;
#46704=EDGE_LOOP ( 'NONE', ( #164926, #145529, #112525, #149977 ) ) ;
#46705=DIRECTION ( 'NONE',  ( 0.000000000000000000, 0.000000000000000000, -1.000000000000000000 ) ) ;
#46722=ORIENTED_EDGE ( 'NONE', *, *, #172998, .T. ) ;
#46726=DIRECTION ( 'NONE',  ( -3.265361837132813093E-16, 1.000000000000000000, 0.000000000000000000 ) ) ;
#46772=LINE ( 'NONE', #165466, #96312 ) ;
#46813=VERTEX_POINT ( 'NONE', #158456 ) ;
#46834=CIRCLE ( 'NONE', #210019, 0.09999999999998898659 ) ;
#46898=ORIENTED_EDGE ( 'NONE', *, *, #95767, .F. ) ;
#46918=ORIENTED_EDGE ( 'NONE', *, *, #27307, .F. ) ;
#46930=ORIENTED_EDGE ( 'NONE', *, *, #129732, .T. ) ;
#46944=VERTEX_POINT ( 'NONE', #142699 ) ;
#46960=EDGE_CURVE ( 'NONE', #189027, #64247, #180565, .T. ) ;
#46966=AXIS2_PLACEMENT_3D ( 'NONE', #240914, #2275, #41450 ) ;
#46983=FACE_OUTER_BOUND ( 'NONE', #120728, .T. ) ;
#46990=VECTOR ( 'NONE', #61620, 1000.000000000000114 ) ;
#47021=DIRECTION ( 'NONE',  ( 1.000000000000000000, 0.000000000000000000, 0.000000000000000000 ) ) ;
#47035=CARTESIAN_POINT ( 'NONE',  ( 23.24999999999997513, 11.65000000001116298, -160.4851942293460638 ) ) ;
#47036=DIRECTION ( 'NONE',  ( 1.000000000000000000, 2.952720810173289112E-16, -0.000000000000000000 ) ) ;
#47051=AXIS2_PLACEMENT_3D ( 'NONE', #11264, #170385, #227727 ) ;
#47054=DIRECTION ( 'NONE',  ( 1.000000000000000000, 0.000000000000000000, 0.000000000000000000 ) ) ;
#47071=CARTESIAN_POINT ( 'NONE',  ( -20.54999999999999716, 2.500000000011156409, -147.2246219227621111 ) ) ;
#47080=ORIENTED_EDGE ( 'NONE', *, *, #151635, .T. ) ;
#47097=DIRECTION ( 'NONE',  ( 0.000000000000000000, 0.000000000000000000, -1.000000000000000000 ) ) ;
#47171=DIRECTION ( 'NONE',  ( -0.000000000000000000, -1.265107689135680095E-16, 1.000000000000000000 ) ) ;
#47179=VECTOR ( 'NONE', #18450, 1000.000000000000000 ) ;
#47196=LINE ( 'NONE', #180635, #172113 ) ;
#47255=ORIENTED_EDGE ( 'NONE', *, *, #36906, .F. ) ;
#47297=CARTESIAN_POINT ( 'NONE',  ( 20.22483756094572271, 9.501904678881089694, -142.1395391287154837 ) ) ;
#47375=ORIENTED_EDGE ( 'NONE', *, *, #17454, .T. ) ;
#47385=CARTESIAN_POINT ( 'NONE',  ( -18.59999999999999787, 7.021664781911246322, -171.3335654018973173 ) ) ;
#47453=VERTEX_POINT ( 'NONE', #69314 ) ;
#47476=CIRCLE ( 'NONE', #164031, 0.09999999999998898659 ) ;
#47501=EDGE_CURVE ( 'NONE', #111920, #196020, #197350, .T. ) ;
#47509=AXIS2_PLACEMENT_3D ( 'NONE', #212721, #14535, #155337 ) ;
#47530=CARTESIAN_POINT ( 'NONE',  ( 23.14999999999999858, -2.099999999988846344, -167.5000000000000284 ) ) ;
#47547=EDGE_CURVE ( 'NONE', #153155, #89497, #72476, .T. ) ;
#47610=CARTESIAN_POINT ( 'NONE',  ( 20.94999999999999929, -9.499999999988848032, -143.8939691226524644 ) ) ;
#47676=CARTESIAN_POINT ( 'NONE',  ( 20.84999999999999787, 11.75000000001116085, -160.5808527540413309 ) ) ;
#47682=ORIENTED_EDGE ( 'NONE', *, *, #171027, .T. ) ;
#47686=EDGE_CURVE ( 'NONE', #47453, #64807, #43246, .T. ) ;
#47694=EDGE_LOOP ( 'NONE', ( #33563, #163068, #105677, #154335 ) ) ;
#47696=CARTESIAN_POINT ( 'NONE',  ( -18.39999999999999503, -9.499999999988849808, -174.4221498493304239 ) ) ;
#47698=DIRECTION ( 'NONE',  ( 1.000000000000000000, 0.000000000000000000, 0.000000000000000000 ) ) ;
#47711=VERTEX_POINT ( 'NONE', #160417 ) ;
#47728=EDGE_LOOP ( 'NONE', ( #92932, #29697, #108879 ) ) ;
#47732=CARTESIAN_POINT ( 'NONE',  ( 22.39999999999999503, 1.115541036281197940E-11, -126.2092204016266379 ) ) ;
#47733=CIRCLE ( 'NONE', #85313, 0.09999999999999864553 ) ;
#47750=FACE_OUTER_BOUND ( 'NONE', #148970, .T. ) ;
#47769=EDGE_CURVE ( 'NONE', #149928, #242592, #35769, .T. ) ;
#47779=AXIS2_PLACEMENT_3D ( 'NONE', #152665, #232192, #211328 ) ;
#47784=LINE ( 'NONE', #81760, #191530 ) ;
#47840=AXIS2_PLACEMENT_3D ( 'NONE', #187734, #168195, #70366 ) ;
#47867=ADVANCED_FACE ( 'NONE', ( #34683 ), #32119, .F. ) ;
#47876=VERTEX_POINT ( 'NONE', #71240 ) ;
#47877=DIRECTION ( 'NONE',  ( 1.000000000000000000, -0.000000000000000000, -0.000000000000000000 ) ) ;
#47879=TOROIDAL_SURFACE ( 'NONE', #193654, 11.65000000000000036, 0.1000000000000000056 ) ;
#47883=VERTEX_POINT ( 'NONE', #131183 ) ;
#47893=LINE ( 'NONE', #88285, #125134 ) ;
#47896=EDGE_CURVE ( 'NONE', #131063, #46944, #200162, .T. ) ;
#47918=ORIENTED_EDGE ( 'NONE', *, *, #79356, .T. ) ;
#47945=CARTESIAN_POINT ( 'NONE',  ( -18.50000000000000000, 11.65000000001115232, -146.2500000000000284 ) ) ;
#47955=EDGE_CURVE ( 'NONE', #70299, #158625, #135159, .T. ) ;
#47961=VERTEX_POINT ( 'NONE', #257496 ) ;
#47974=CARTESIAN_POINT ( 'NONE',  ( 21.05000000000000071, -11.39257802169451139, -164.4260504201680817 ) ) ;
#47989=CARTESIAN_POINT ( 'NONE',  ( 20.94999999999999574, 14.00000000001115730, -139.4270925303825663 ) ) ;
#48025=CARTESIAN_POINT ( 'NONE',  ( -20.85000000000000142, 11.75000000001115197, -160.6583993101029364 ) ) ;
#48048=CIRCLE ( 'NONE', #152125, 0.09999999999998898659 ) ;
#48051=CIRCLE ( 'NONE', #235298, 12.97499999999998721 ) ;
#48100=EDGE_CURVE ( 'NONE', #79366, #46322, #125743, .T. ) ;
#48126=DIRECTION ( 'NONE',  ( 0.000000000000000000, 1.000000000000000000, 0.000000000000000000 ) ) ;
#48153=CARTESIAN_POINT ( 'NONE',  ( 22.39999999999999503, 11.65000000001116298, -134.1000000000000227 ) ) ;
#48159=DIRECTION ( 'NONE',  ( 0.000000000000000000, 0.000000000000000000, -1.000000000000000000 ) ) ;
#48266=CARTESIAN_POINT ( 'NONE',  ( -20.54999999999999716, 2.000000000011154189, -147.2246219227621111 ) ) ;
#48269=ORIENTED_EDGE ( 'NONE', *, *, #93210, .T. ) ;
#48282=EDGE_LOOP ( 'NONE', ( #118221, #185413, #193918, #134767 ) ) ;
#48285=ORIENTED_EDGE ( 'NONE', *, *, #64187, .F. ) ;
#48286=CARTESIAN_POINT ( 'NONE',  ( -20.94999999999999929, -1.135018845899022466, -175.2169768834323520 ) ) ;
#48305=FACE_OUTER_BOUND ( 'NONE', #61971, .T. ) ;
#48353=EDGE_LOOP ( 'NONE', ( #220066, #63540, #239460, #81828 ) ) ;
#48395=CARTESIAN_POINT ( 'NONE',  ( 20.94999999999999929, -8.999999999988842703, -157.6060308773475640 ) ) ;
#48420=EDGE_CURVE ( 'NONE', #42512, #154148, #1637, .T. ) ;
#48427=CARTESIAN_POINT ( 'NONE',  ( -23.15000000000000213, 2.000000000011154189, -147.2246219227621111 ) ) ;
#48448=CARTESIAN_POINT ( 'NONE',  ( 18.59999999999999076, 10.49142135624846617, -158.7500000000000284 ) ) ;
#48514=EDGE_CURVE ( 'NONE', #114275, #253143, #87591, .T. ) ;
#48535=CIRCLE ( 'NONE', #56870, 0.09999999999998898659 ) ;
#48544=FACE_OUTER_BOUND ( 'NONE', #206435, .T. ) ;
#48571=AXIS2_PLACEMENT_3D ( 'NONE', #21032, #161830, #97943 ) ;
#48578=DIRECTION ( 'NONE',  ( -1.000000000000000000, -1.836970198721029934E-16, 0.000000000000000000 ) ) ;
#48580=VERTEX_POINT ( 'NONE', #128034 ) ;
#48583=CARTESIAN_POINT ( 'NONE',  ( -21.14999999999999858, 6.540656951712397138, -134.0000000000000000 ) ) ;
#48601=CARTESIAN_POINT ( 'NONE',  ( 20.21567752745019320, 10.19811410124265905, -141.8826203476516810 ) ) ;
#48633=DIRECTION ( 'NONE',  ( 0.000000000000000000, 0.9908441862701782288, 0.1350103645450542456 ) ) ;
#48692=ORIENTED_EDGE ( 'NONE', *, *, #101979, .T. ) ;
#48697=DIRECTION ( 'NONE',  ( 0.000000000000000000, 0.000000000000000000, 1.000000000000000000 ) ) ;
#48821=ORIENTED_EDGE ( 'NONE', *, *, #253131, .T. ) ;
#48862=CARTESIAN_POINT ( 'NONE',  ( -20.64999999999999858, -8.999999999988846255, -143.8939691226524644 ) ) ;
#48883=CARTESIAN_POINT ( 'NONE',  ( -23.15000000000000213, -8.999999999988846255, -143.8939691226524644 ) ) ;
#48884=DIRECTION ( 'NONE',  ( 0.000000000000000000, 0.000000000000000000, -1.000000000000000000 ) ) ;
#48896=CARTESIAN_POINT ( 'NONE',  ( -21.44999999999999929, 7.350000000011155166, -155.1500000000000057 ) ) ;
#48901=ORIENTED_EDGE ( 'NONE', *, *, #105977, .T. ) ;
#48910=DIRECTION ( 'NONE',  ( -0.000000000000000000, 0.8660254037844502539, 0.4999999999999799050 ) ) ;
#48914=CYLINDRICAL_SURFACE ( 'NONE', #158765, 0.09999999999998898659 ) ;
#48917=FACE_OUTER_BOUND ( 'NONE', #173664, .T. ) ;
#48936=CARTESIAN_POINT ( 'NONE',  ( -23.25000000000000000, 1.115600667400684642E-11, -134.0000000000000000 ) ) ;
#48956=EDGE_CURVE ( 'NONE', #73222, #51735, #247667, .T. ) ;
#48961=AXIS2_PLACEMENT_3D ( 'NONE', #138633, #102083, #181660 ) ;
#48981=DIRECTION ( 'NONE',  ( 0.000000000000000000, 0.4999999999999348299, -0.8660254037844762331 ) ) ;
#49024=ADVANCED_FACE ( 'NONE', ( #248964 ), #10358, .F. ) ;
#49065=EDGE_CURVE ( 'NONE', #237934, #179358, #122141, .T. ) ;
#49073=CARTESIAN_POINT ( 'NONE',  ( -18.59999999999999787, -1.835859311432481045, -179.0044391687985410 ) ) ;
#49090=CARTESIAN_POINT ( 'NONE',  ( 21.14999999999999858, -11.74999999998884448, -146.2500000000000284 ) ) ;
#49097=EDGE_CURVE ( 'NONE', #113536, #111115, #90410, .T. ) ;
#49107=CARTESIAN_POINT ( 'NONE',  ( -20.94999999999999929, -0.2561057920810652089, -133.9651035583277121 ) ) ;
#49126=LINE ( 'NONE', #28326, #106655 ) ;
#49179=ORIENTED_EDGE ( 'NONE', *, *, #173741, .F. ) ;
#49231=EDGE_LOOP ( 'NONE', ( #76206, #163142 ) ) ;
#49239=ORIENTED_EDGE ( 'NONE', *, *, #255314, .F. ) ;
#49247=CIRCLE ( 'NONE', #115895, 0.2000000000000057288 ) ;
#49286=ORIENTED_EDGE ( 'NONE', *, *, #230286, .F. ) ;
#49287=DIRECTION ( 'NONE',  ( -0.7071067811865474617, 0.7071067811865474617, 0.000000000000000000 ) ) ;
#49298=ORIENTED_EDGE ( 'NONE', *, *, #9631, .F. ) ;
#49313=CARTESIAN_POINT ( 'NONE',  ( 20.85000000000000142, -1.835859311432481045, -179.0044391687985410 ) ) ;
#49390=EDGE_CURVE ( 'NONE', #37051, #101165, #19476, .T. ) ;
#49401=ORIENTED_EDGE ( 'NONE', *, *, #168005, .F. ) ;
#49408=LINE ( 'NONE', #29873, #3131 ) ;
#49455=CIRCLE ( 'NONE', #228532, 0.5999999999999894307 ) ;
#49465=ORIENTED_EDGE ( 'NONE', *, *, #148630, .T. ) ;
#49505=VECTOR ( 'NONE', #598, 1000.000000000000114 ) ;
#49537=EDGE_LOOP ( 'NONE', ( #7780, #24315, #113264, #107744 ) ) ;
#49547=VERTEX_POINT ( 'NONE', #126645 ) ;
#49550=ORIENTED_EDGE ( 'NONE', *, *, #110613, .T. ) ;
#49585=DIRECTION ( 'NONE',  ( 0.000000000000000000, 0.000000000000000000, -1.000000000000000000 ) ) ;
#49588=AXIS2_PLACEMENT_3D ( 'NONE', #194231, #96361, #254156 ) ;
#49609=LINE ( 'NONE', #126582, #145669 ) ;
#49615=EDGE_LOOP ( 'NONE', ( #214324, #20921, #58372, #18389 ) ) ;
#49635=CIRCLE ( 'NONE', #145483, 0.09999999999999939493 ) ;
#49643=ADVANCED_FACE ( 'NONE', ( #69255 ), #100455, .F. ) ;
#49670=DIRECTION ( 'NONE',  ( -0.000000000000000000, -0.000000000000000000, 1.000000000000000000 ) ) ;
#49680=EDGE_CURVE ( 'NONE', #161202, #94122, #257544, .T. ) ;
#49685=DIRECTION ( 'NONE',  ( 0.000000000000000000, 1.000000000000000000, 0.000000000000000000 ) ) ;
#49688=CARTESIAN_POINT ( 'NONE',  ( 23.24999999999999289, 6.650000000011155876, -146.1500000000000341 ) ) ;
#49695=CARTESIAN_POINT ( 'NONE',  ( 22.49231231312462853, 11.64998490368843953, -133.9389471123986368 ) ) ;
#49698=ADVANCED_FACE ( 'NONE', ( #134327 ), #170961, .F. ) ;
#49704=EDGE_LOOP ( 'NONE', ( #256476, #193398, #90804, #136158 ) ) ;
#49715=DIRECTION ( 'NONE',  ( -0.000000000000000000, 0.000000000000000000, 1.000000000000000000 ) ) ;
#49718=DIRECTION ( 'NONE',  ( 1.000000000000000000, 0.000000000000000000, 0.000000000000000000 ) ) ;
#49719=CARTESIAN_POINT ( 'NONE',  ( -23.15000000000000213, 11.75000000001115552, -155.3500000000000227 ) ) ;
#49736=EDGE_LOOP ( 'NONE', ( #199599, #775, #114087, #73608 ) ) ;
#49768=CARTESIAN_POINT ( 'NONE',  ( 21.14999999999999858, 11.65000000001116298, -146.2500000000000284 ) ) ;
#49771=ORIENTED_EDGE ( 'NONE', *, *, #214107, .T. ) ;
#49845=EDGE_LOOP ( 'NONE', ( #22026, #53683, #250638, #171721 ) ) ;
#49869=CARTESIAN_POINT ( 'NONE',  ( -21.07946286933445279, 6.329037319018852692, -133.9233161567436525 ) ) ;
#49873=CARTESIAN_POINT ( 'NONE',  ( 20.94999999999999929, -1.164121893230052995, -175.4148480855716059 ) ) ;
#49875=FACE_OUTER_BOUND ( 'NONE', #191954, .T. ) ;
#49891=EDGE_LOOP ( 'NONE', ( #15915, #30487, #171675, #21980 ) ) ;
#49900=DIRECTION ( 'NONE',  ( 0.000000000000000000, 0.000000000000000000, -1.000000000000000000 ) ) ;
#49952=DIRECTION ( 'NONE',  ( 3.265361837132813093E-16, -1.000000000000000000, -0.000000000000000000 ) ) ;
#50000=CYLINDRICAL_SURFACE ( 'NONE', #216258, 0.09999999999999939493 ) ;
#50006=CIRCLE ( 'NONE', #99, 0.1000000000000002554 ) ;
#50042=VERTEX_POINT ( 'NONE', #130173 ) ;
#50063=CIRCLE ( 'NONE', #8385, 0.09999999999998898659 ) ;
#50090=DIRECTION ( 'NONE',  ( 0.000000000000000000, -1.000000000000000000, 0.000000000000000000 ) ) ;
#50103=ORIENTED_EDGE ( 'NONE', *, *, #82679, .F. ) ;
#50111=CARTESIAN_POINT ( 'NONE',  ( -20.94999999999999929, -11.74999999998884448, -136.9000000000000341 ) ) ;
#50147=CARTESIAN_POINT ( 'NONE',  ( 20.85000000000000142, 1.115600667400684642E-11, -167.5000000000000284 ) ) ;
#50148=ORIENTED_EDGE ( 'NONE', *, *, #90762, .T. ) ;
#50161=CARTESIAN_POINT ( 'NONE',  ( -20.94999999999999929, 7.021664781911246322, -171.3335654018973173 ) ) ;
#50173=ORIENTED_EDGE ( 'NONE', *, *, #98270, .T. ) ;
#50186=ORIENTED_EDGE ( 'NONE', *, *, #134126, .T. ) ;
#50188=DIRECTION ( 'NONE',  ( -0.000000000000000000, -0.000000000000000000, -1.000000000000000000 ) ) ;
#50219=CYLINDRICAL_SURFACE ( 'NONE', #60976, 0.1000000000000098310 ) ;
#50264=AXIS2_PLACEMENT_3D ( 'NONE', #236137, #99169, #237426 ) ;
#50267=CARTESIAN_POINT ( 'NONE',  ( 22.24259225415828212, 0.09906588346399246292, -126.5080621294346059 ) ) ;
#50290=EDGE_CURVE ( 'NONE', #139686, #72782, #244675, .T. ) ;
#50311=ORIENTED_EDGE ( 'NONE', *, *, #227660, .T. ) ;
#50357=CARTESIAN_POINT ( 'NONE',  ( 23.24999999999999289, 11.65000000001116298, -160.4851942293460922 ) ) ;
#50360=FACE_OUTER_BOUND ( 'NONE', #99781, .T. ) ;
#50371=CARTESIAN_POINT ( 'NONE',  ( -20.94983749550516450, 10.29766095125295244, -172.9743663933275855 ) ) ;
#50383=ORIENTED_EDGE ( 'NONE', *, *, #53963, .T. ) ;
#50404=ORIENTED_EDGE ( 'NONE', *, *, #221842, .T. ) ;
#50410=TOROIDAL_SURFACE ( 'NONE', #192118, 0.6000000000000004219, 0.1000000000000000056 ) ;
#50421=EDGE_LOOP ( 'NONE', ( #217848, #147207, #89159, #75857 ) ) ;
#50460=CARTESIAN_POINT ( 'NONE',  ( 18.59999999999999432, -1.866714910046153308, -145.7526752462820241 ) ) ;
#50476=ADVANCED_FACE ( 'NONE', ( #16374, #137561, #164544 ), #38489, .F. ) ;
#50515=CARTESIAN_POINT ( 'NONE',  ( 23.14999999999999858, -1.999999999988846699, -167.5000000000000284 ) ) ;
#50534=PLANE ( 'NONE',  #125957 ) ;
#50563=CARTESIAN_POINT ( 'NONE',  ( -23.15000000000000213, 1.115600667400684642E-11, -146.7750000000000057 ) ) ;
#50566=CARTESIAN_POINT ( 'NONE',  ( 18.59999999999998366, 1.115600667400684642E-11, -167.5000000000000284 ) ) ;
#50592=DIRECTION ( 'NONE',  ( -1.000000000000000000, -3.265361837132813093E-16, 0.000000000000000000 ) ) ;
#50606=ORIENTED_EDGE ( 'NONE', *, *, #87451, .F. ) ;
#50607=DIRECTION ( 'NONE',  ( 1.000000000000000000, 0.000000000000000000, 0.000000000000000000 ) ) ;
#50616=EDGE_CURVE ( 'NONE', #233607, #25295, #141449, .T. ) ;
#50627=VECTOR ( 'NONE', #206667, 1000.000000000000000 ) ;
#50664=CARTESIAN_POINT ( 'NONE',  ( 18.54147908293624170, -9.463261657917028558, -141.0489488967557179 ) ) ;
#50711=ADVANCED_FACE ( 'NONE', ( #110977 ), #166609, .F. ) ;
#50716=DIRECTION ( 'NONE',  ( 1.000000000000000000, -0.000000000000000000, -0.000000000000000000 ) ) ;
#50784=CARTESIAN_POINT ( 'NONE',  ( -20.64999999999999858, 2.000000000011154189, -147.2246219227621111 ) ) ;
#50786=ADVANCED_FACE ( 'NONE', ( #255565 ), #37880, .T. ) ;
#50799=VERTEX_POINT ( 'NONE', #193091 ) ;
#50844=CARTESIAN_POINT ( 'NONE',  ( -20.85000000000000142, -11.64999999998884306, -167.5000000000000000 ) ) ;
#50848=DIRECTION ( 'NONE',  ( 0.000000000000000000, 0.000000000000000000, -1.000000000000000000 ) ) ;
#50871=DIRECTION ( 'NONE',  ( -1.000000000000000000, -0.000000000000000000, -0.000000000000000000 ) ) ;
#50874=CARTESIAN_POINT ( 'NONE',  ( -21.14999999999999858, 1.115600667400684642E-11, -134.0000000000000000 ) ) ;
#50877=AXIS2_PLACEMENT_3D ( 'NONE', #107409, #205211, #241780 ) ;
#50881=DIRECTION ( 'NONE',  ( 0.000000000000000000, -1.000000000000000000, 0.000000000000000000 ) ) ;
#50884=CYLINDRICAL_SURFACE ( 'NONE', #257122, 0.5000000000000004441 ) ;
#50894=ADVANCED_FACE ( 'NONE', ( #80808 ), #143367, .F. ) ;
#50909=DIRECTION ( 'NONE',  ( 0.000000000000000000, 1.000000000000000000, 0.000000000000000000 ) ) ;
#50916=DIRECTION ( 'NONE',  ( 1.000000000000000000, -0.000000000000000000, -0.000000000000000000 ) ) ;
#50918=CIRCLE ( 'NONE', #146596, 0.5999999999999894307 ) ;
#50942=CARTESIAN_POINT ( 'NONE',  ( -23.15000000000000213, -8.663551401858001100, -157.9758988819327215 ) ) ;
#50976=DIRECTION ( 'NONE',  ( -0.000000000000000000, 0.000000000000000000, 1.000000000000000000 ) ) ;
#50989=DIRECTION ( 'NONE',  ( -1.000000000000000000, -2.952720810173289112E-16, 0.000000000000000000 ) ) ;
#50997=VERTEX_POINT ( 'NONE', #228051 ) ;
#51035=ADVANCED_FACE ( 'NONE', ( #68997 ), #115715, .T. ) ;
#51062=ORIENTED_EDGE ( 'NONE', *, *, #243215, .F. ) ;
#51064=CARTESIAN_POINT ( 'NONE',  ( 23.15000000000000213, -12.41227409413852811, -164.5000000000000000 ) ) ;
#51065=EDGE_LOOP ( 'NONE', ( #119440, #39595, #42717, #38580 ) ) ;
#51070=ORIENTED_EDGE ( 'NONE', *, *, #90479, .F. ) ;
#51080=CARTESIAN_POINT ( 'NONE',  ( -23.25000000000000000, -0.1008583690875562017, -122.2504328765106294 ) ) ;
#51081=CIRCLE ( 'NONE', #142677, 0.09999999999999939493 ) ;
#51142=CARTESIAN_POINT ( 'NONE',  ( 20.85000000000000142, 6.846123162363745074, -171.2377262668498759 ) ) ;
#51159=CONICAL_SURFACE ( 'NONE', #213689, 6.250000000000005329, 0.7853981633974431720 ) ;
#51180=ORIENTED_EDGE ( 'NONE', *, *, #17661, .F. ) ;
#51221=DIRECTION ( 'NONE',  ( 1.000000000000000000, 0.000000000000000000, 0.000000000000000000 ) ) ;
#51247=CARTESIAN_POINT ( 'NONE',  ( -21.44999999999999929, 7.350000000011155166, -155.2500000000000284 ) ) ;
#51284=CIRCLE ( 'NONE', #97058, 2.099999999999990763 ) ;
#51294=AXIS2_PLACEMENT_3D ( 'NONE', #130460, #47054, #146164 ) ;
#51316=TOROIDAL_SURFACE ( 'NONE', #193013, 4.099999999999999645, 0.1000000000000000056 ) ;
#51362=CARTESIAN_POINT ( 'NONE',  ( -20.94999999999999929, -11.48912529306489994, -164.6000000000000227 ) ) ;
#51368=ORIENTED_EDGE ( 'NONE', *, *, #133450, .T. ) ;
#51382=EDGE_CURVE ( 'NONE', #14355, #243100, #133624, .T. ) ;
#51406=DIRECTION ( 'NONE',  ( 0.000000000000000000, 0.000000000000000000, 1.000000000000000000 ) ) ;
#51410=AXIS2_PLACEMENT_3D ( 'NONE', #74423, #190504, #170967 ) ;
#51448=ORIENTED_EDGE ( 'NONE', *, *, #222121, .F. ) ;
#51454=PRODUCT_DEFINITION_SHAPE ( 'NONE', 'NONE',  #206229 ) ;
#51476=CARTESIAN_POINT ( 'NONE',  ( 23.14999999999999503, 14.05000000001115623, -161.9863049292391111 ) ) ;
#51514=ORIENTED_EDGE ( 'NONE', *, *, #75089, .T. ) ;
#51525=DIRECTION ( 'NONE',  ( -1.000000000000000000, 0.000000000000000000, 0.000000000000000000 ) ) ;
#51562=CIRCLE ( 'NONE', #1517, 0.09999999999999939493 ) ;
#51604=CARTESIAN_POINT ( 'NONE',  ( 18.50000000000000000, -9.399999999988843058, -174.3820418481727188 ) ) ;
#51605=CIRCLE ( 'NONE', #143220, 11.75000000000001066 ) ;
#51606=EDGE_CURVE ( 'NONE', #154148, #152529, #201439, .T. ) ;
#51621=CARTESIAN_POINT ( 'NONE',  ( -21.05000000000000071, 1.115600667400684642E-11, -134.0000000000000000 ) ) ;
#51627=ADVANCED_FACE ( 'NONE', ( #157213, #141468 ), #78901, .F. ) ;
#51635=ORIENTED_EDGE ( 'NONE', *, *, #15774, .T. ) ;
#51663=DIRECTION ( 'NONE',  ( 0.000000000000000000, -0.8068669527897506244, -0.5907332058516622242 ) ) ;
#51700=DIRECTION ( 'NONE',  ( -0.000000000000000000, 0.9274965247785350586, 0.3738317757009704811 ) ) ;
#51705=ORIENTED_EDGE ( 'NONE', *, *, #55553, .F. ) ;
#51710=EDGE_CURVE ( 'NONE', #2800, #232714, #137885, .T. ) ;
#51712=DIRECTION ( 'NONE',  ( 1.000000000000000000, -0.000000000000000000, -0.000000000000000000 ) ) ;
#51726=AXIS2_PLACEMENT_3D ( 'NONE', #134052, #192767, #235722 ) ;
#51735=VERTEX_POINT ( 'NONE', #224852 ) ;
#51770=VERTEX_POINT ( 'NONE', #144027 ) ;
#51782=DIRECTION ( 'NONE',  ( 1.000000000000000000, 0.000000000000000000, 0.000000000000000000 ) ) ;
#51794=ORIENTED_EDGE ( 'NONE', *, *, #124086, .F. ) ;
#51801=VERTEX_POINT ( 'NONE', #223558 ) ;
#51805=DIRECTION ( 'NONE',  ( 1.000000000000000000, 2.952720810173289112E-16, -0.000000000000000000 ) ) ;
#51822=CARTESIAN_POINT ( 'NONE',  ( -21.09813707148783735, 0.03135149954059197192, -127.6149378942633348 ) ) ;
#51860=EDGE_CURVE ( 'NONE', #95323, #99517, #93054, .T. ) ;
#51885=LINE ( 'NONE', #246267, #162434 ) ;
#51945=CYLINDRICAL_SURFACE ( 'NONE', #249440, 0.09999999999998898659 ) ;
#51952=CARTESIAN_POINT ( 'NONE',  ( 21.07928932188134397, 6.328516656404459262, -133.9011048543456184 ) ) ;
#51954=VECTOR ( 'NONE', #141172, 1000.000000000000000 ) ;
#51996=AXIS2_PLACEMENT_3D ( 'NONE', #185074, #84646, #164245 ) ;
#52013=CYLINDRICAL_SURFACE ( 'NONE', #41804, 0.8750000000000007772 ) ;
#52015=ORIENTED_EDGE ( 'NONE', *, *, #92937, .F. ) ;
#52033=DIRECTION ( 'NONE',  ( -2.952720810173289112E-16, 1.000000000000000000, 0.000000000000000000 ) ) ;
#52074=DIRECTION ( 'NONE',  ( 0.000000000000000000, -1.000000000000000000, 6.308085367188393199E-16 ) ) ;
#52111=AXIS2_PLACEMENT_3D ( 'NONE', #192349, #231488, #170268 ) ;
#52115=ORIENTED_EDGE ( 'NONE', *, *, #254847, .T. ) ;
#52120=CARTESIAN_POINT ( 'NONE',  ( 22.39999999999999503, 1.115600667400684642E-11, -122.3504291924552234 ) ) ;
#52123=ORIENTED_EDGE ( 'NONE', *, *, #82563, .T. ) ;
#52170=CIRCLE ( 'NONE', #152162, 4.049999999999998934 ) ;
#52173=CARTESIAN_POINT ( 'NONE',  ( -20.94999999999999929, -11.64999999998884483, -164.6000000000000227 ) ) ;
#52180=DIRECTION ( 'NONE',  ( -0.000000000000000000, 1.000000000000000000, 1.626303258728266709E-15 ) ) ;
#52181=EDGE_LOOP ( 'NONE', ( #85390, #232981, #215337, #32173 ) ) ;
#52220=DIRECTION ( 'NONE',  ( 1.000000000000000000, 0.000000000000000000, 0.000000000000000000 ) ) ;
#52223=CARTESIAN_POINT ( 'NONE',  ( -21.05000000000000071, -1.835341550213255957, -145.5551512925629822 ) ) ;
#52236=CARTESIAN_POINT ( 'NONE',  ( 23.14999999999999858, 11.60000000001116227, -160.5717967697245285 ) ) ;
#52254=DIRECTION ( 'NONE',  ( -1.000000000000000000, 0.000000000000000000, 0.000000000000000000 ) ) ;
#52279=EDGE_CURVE ( 'NONE', #114275, #131063, #213094, .T. ) ;
#52296=EDGE_CURVE ( 'NONE', #45297, #98196, #96381, .T. ) ;
#52307=CIRCLE ( 'NONE', #110590, 0.09999999999999062417 ) ;
#52308=EDGE_LOOP ( 'NONE', ( #40256, #56695, #196172 ) ) ;
#52359=APPLICATION_CONTEXT ( 'automotive_design' ) ;
#52374=CARTESIAN_POINT ( 'NONE',  ( -20.54999999999999716, 2.400000000011155432, -147.2246219227621111 ) ) ;
#52387=VERTEX_POINT ( 'NONE', #19308 ) ;
#52404=ADVANCED_FACE ( 'NONE', ( #100098 ), #71655, .F. ) ;
#52411=ORIENTED_EDGE ( 'NONE', *, *, #144477, .F. ) ;
#52414=CIRCLE ( 'NONE', #10745, 0.09999999999998898659 ) ;
#52418=ORIENTED_EDGE ( 'NONE', *, *, #116819, .F. ) ;
#52420=EDGE_CURVE ( 'NONE', #6309, #139646, #86597, .T. ) ;
#52421=DIRECTION ( 'NONE',  ( 1.000000000000000000, -0.000000000000000000, -0.000000000000000000 ) ) ;
#52449=CARTESIAN_POINT ( 'NONE',  ( 18.50016250449482058, 10.29766095125179959, -172.9743663933279265 ) ) ;
#52506=CARTESIAN_POINT ( 'NONE',  ( 23.14999999999999858, 2.100000000011158274, -167.5000000000000284 ) ) ;
#52537=DIRECTION ( 'NONE',  ( 0.000000000000000000, 0.000000000000000000, 1.000000000000000000 ) ) ;
#52539=DIRECTION ( 'NONE',  ( -0.000000000000000000, 0.8660254037844383745, -0.5000000000000003331 ) ) ;
#52552=DIRECTION ( 'NONE',  ( -1.000000000000000000, 0.000000000000000000, 0.000000000000000000 ) ) ;
#52558=VERTEX_POINT ( 'NONE', #105210 ) ;
#52565=VERTEX_POINT ( 'NONE', #227769 ) ;
#52644=AXIS2_PLACEMENT_3D ( 'NONE', #101783, #122693, #149957 ) ;
#52645=CARTESIAN_POINT ( 'NONE',  ( -20.64999999999999858, 1.115600667400684642E-11, -134.0000000000000000 ) ) ;
#52687=DIRECTION ( 'NONE',  ( 1.000000000000000000, -0.000000000000000000, -0.000000000000000000 ) ) ;
#52716=EDGE_CURVE ( 'NONE', #164020, #178186, #142535, .T. ) ;
#52743=FACE_OUTER_BOUND ( 'NONE', #9139, .T. ) ;
#52794=AXIS2_PLACEMENT_3D ( 'NONE', #215746, #93240, #91961 ) ;
#52827=B_SPLINE_CURVE_WITH_KNOTS ( 'NONE', 3,
 ( #163149, #207414, #243947, #124020, #45749, #88705, #84838 ),
 .UNSPECIFIED., .F., .F.,
 ( 4, 3, 4 ),
 ( 0.000000000000000000, 0.0007844235214594269838, 0.001767853679404345069 ),
 .UNSPECIFIED. ) ;
#52831=B_SPLINE_CURVE_WITH_KNOTS ( 'NONE', 3,
 ( #68607, #93290, #92006, #227662, #192400, #231537, #232831, #52872, #132430, #32067 ),
 .UNSPECIFIED., .F., .F.,
 ( 4, 2, 2, 2, 4 ),
 ( 0.000000000000000000, 3.990160268013653969E-05, 7.980320536027307938E-05, 0.0001596064107205525013, 0.0003192128214411112910 ),
 .UNSPECIFIED. ) ;
#52838=DIRECTION ( 'NONE',  ( 1.000000000000000000, -0.000000000000000000, -0.000000000000000000 ) ) ;
#52843=AXIS2_PLACEMENT_3D ( 'NONE', #92525, #172122, #251612 ) ;
#52872=CARTESIAN_POINT ( 'NONE',  ( -18.49499033040907037, -9.438148771733509079, -141.1981532259235053 ) ) ;
#52875=VECTOR ( 'NONE', #47171, 1000.000000000000000 ) ;
#52891=ORIENTED_EDGE ( 'NONE', *, *, #40936, .T. ) ;
#52901=CARTESIAN_POINT ( 'NONE',  ( 23.15000000000000213, -9.599999999988845900, -143.8939691226524644 ) ) ;
#52919=CARTESIAN_POINT ( 'NONE',  ( -21.05000000000000071, -11.74999999998884448, -164.5000000000000000 ) ) ;
#52932=EDGE_CURVE ( 'NONE', #178186, #175143, #226245, .T. ) ;
#52959=EDGE_CURVE ( 'NONE', #36655, #52558, #84231, .T. ) ;
#52964=CIRCLE ( 'NONE', #169733, 0.5999999999999998668 ) ;
#52968=AXIS2_PLACEMENT_3D ( 'NONE', #193001, #52180, #95174 ) ;
#52998=DIRECTION ( 'NONE',  ( 0.000000000000000000, 0.000000000000000000, -1.000000000000000000 ) ) ;
#53011=DIRECTION ( 'NONE',  ( 0.000000000000000000, 0.7397360091702777085, -0.6728971962616808744 ) ) ;
#53015=CARTESIAN_POINT ( 'NONE',  ( 23.15000000000000213, -11.48912529306489994, -164.4000000000000057 ) ) ;
#53033=CIRCLE ( 'NONE', #33365, 0.09999999999999939493 ) ;
#53039=ADVANCED_FACE ( 'NONE', ( #29400 ), #48914, .T. ) ;
#53061=ORIENTED_EDGE ( 'NONE', *, *, #241362, .F. ) ;
#53063=LINE ( 'NONE', #187465, #197614 ) ;
#53092=AXIS2_PLACEMENT_3D ( 'NONE', #224360, #122720, #202237 ) ;
#53104=ORIENTED_EDGE ( 'NONE', *, *, #34104, .T. ) ;
#53166=AXIS2_PLACEMENT_3D ( 'NONE', #239534, #219961, #157462 ) ;
#53184=DIRECTION ( 'NONE',  ( 1.000000000000000000, 3.265361837132813093E-16, -0.000000000000000000 ) ) ;
#53192=DIRECTION ( 'NONE',  ( 0.000000000000000000, -0.8700118002898359348, 0.4930308989875165082 ) ) ;
#53202=FACE_OUTER_BOUND ( 'NONE', #144194, .T. ) ;
#53216=AXIS2_PLACEMENT_3D ( 'NONE', #24040, #246907, #184363 ) ;
#53234=DIRECTION ( 'NONE',  ( 0.000000000000000000, 0.000000000000000000, -1.000000000000000000 ) ) ;
#53241=AXIS2_PLACEMENT_3D ( 'NONE', #223442, #167367, #205157 ) ;
#53244=EDGE_CURVE ( 'NONE', #212047, #200852, #175510, .T. ) ;
#53256=DIRECTION ( 'NONE',  ( -0.9880948137434723000, 0.1538461538461483591, -0.000000000000000000 ) ) ;
#53288=AXIS2_PLACEMENT_3D ( 'NONE', #23330, #121150, #256723 ) ;
#53290=ORIENTED_EDGE ( 'NONE', *, *, #132832, .F. ) ;
#53343=ORIENTED_EDGE ( 'NONE', *, *, #218646, .T. ) ;
#53353=CARTESIAN_POINT ( 'NONE',  ( -20.15000000000000568, 9.291421356248463326, -155.2500000000000284 ) ) ;
#53360=ORIENTED_EDGE ( 'NONE', *, *, #46960, .F. ) ;
#53373=ORIENTED_EDGE ( 'NONE', *, *, #129460, .T. ) ;
#53460=CIRCLE ( 'NONE', #194940, 0.09999999999998898659 ) ;
#53476=DIRECTION ( 'NONE',  ( 0.000000000000000000, 0.000000000000000000, -1.000000000000000000 ) ) ;
#53516=ADVANCED_FACE ( 'NONE', ( #130721 ), #126878, .T. ) ;
#53532=CARTESIAN_POINT ( 'NONE',  ( -20.00857864376270001, 9.250000000011157297, -155.2500000000000284 ) ) ;
#53535=CARTESIAN_POINT ( 'NONE',  ( 20.94999999999997442, -1.263275465206102233, -175.4018646667464338 ) ) ;
#53575=FACE_OUTER_BOUND ( 'NONE', #211931, .T. ) ;
#53584=AXIS2_PLACEMENT_3D ( 'NONE', #86869, #26954, #106430 ) ;
#53590=VERTEX_POINT ( 'NONE', #160275 ) ;
#53592=( NAMED_UNIT ( * ) PLANE_ANGLE_UNIT ( ) SI_UNIT ( $, .RADIAN. ) );
#53594=DIRECTION ( 'NONE',  ( -0.000000000000000000, -0.000000000000000000, 1.000000000000000000 ) ) ;
#53616=FACE_OUTER_BOUND ( 'NONE', #209617, .T. ) ;
#53644=LINE ( 'NONE', #14541, #209674 ) ;
#53662=CYLINDRICAL_SURFACE ( 'NONE', #175436, 0.09999999999999939493 ) ;
#53667=ORIENTED_EDGE ( 'NONE', *, *, #73162, .T. ) ;
#53683=ORIENTED_EDGE ( 'NONE', *, *, #94418, .T. ) ;
#53685=VECTOR ( 'NONE', #201744, 1000.000000000000000 ) ;
#53688=DIRECTION ( 'NONE',  ( 0.000000000000000000, 0.000000000000000000, 1.000000000000000000 ) ) ;
#53711=ORIENTED_EDGE ( 'NONE', *, *, #38950, .F. ) ;
#53735=DIRECTION ( 'NONE',  ( -1.000000000000000000, 0.000000000000000000, 0.000000000000000000 ) ) ;
#53738=EDGE_CURVE ( 'NONE', #59872, #85212, #79961, .T. ) ;
#53767=CARTESIAN_POINT ( 'NONE',  ( 20.94999999999999574, 1.750000000011155743, -145.6695115579016715 ) ) ;
#53770=DIRECTION ( 'NONE',  ( 1.000000000000000000, 0.000000000000000000, 0.000000000000000000 ) ) ;
#53778=LINE ( 'NONE', #229850, #155871 ) ;
#53795=ORIENTED_EDGE ( 'NONE', *, *, #137043, .T. ) ;
#53811=DIRECTION ( 'NONE',  ( 0.000000000000000000, 0.000000000000000000, -1.000000000000000000 ) ) ;
#53821=VECTOR ( 'NONE', #66357, 1000.000000000000000 ) ;
#53835=CARTESIAN_POINT ( 'NONE',  ( -18.43569575749026157, -9.519327731081284938, -140.9729763765592452 ) ) ;
#53849=PLANE ( 'NONE',  #205997 ) ;
#53879=ADVANCED_FACE ( 'NONE', ( #33620 ), #50534, .F. ) ;
#53896=EDGE_CURVE ( 'NONE', #161970, #105589, #33069, .T. ) ;
#53958=CARTESIAN_POINT ( 'NONE',  ( 21.05000000000000071, 6.496686585778244982, -134.0146561185100325 ) ) ;
#53963=EDGE_CURVE ( 'NONE', #73323, #187889, #139278, .T. ) ;
#53968=ORIENTED_EDGE ( 'NONE', *, *, #20589, .F. ) ;
#53970=CARTESIAN_POINT ( 'NONE',  ( 21.05000000000000071, 10.72371710471867701, -146.1611902941274650 ) ) ;
#53976=AXIS2_PLACEMENT_3D ( 'NONE', #29411, #187183, #108900 ) ;
#53987=CARTESIAN_POINT ( 'NONE',  ( -23.24999999999999645, -9.599999999988845900, -174.1001893912220737 ) ) ;
#54015=ORIENTED_EDGE ( 'NONE', *, *, #63669, .T. ) ;
#54079=VECTOR ( 'NONE', #42614, 1000.000000000000000 ) ;
#54096=FACE_OUTER_BOUND ( 'NONE', #242265, .T. ) ;
#54108=CARTESIAN_POINT ( 'NONE',  ( 21.11747605621531321, 8.778708005504054057, -146.2445631697897852 ) ) ;
#54112=AXIS2_PLACEMENT_3D ( 'NONE', #51621, #129899, #128641 ) ;
#54116=VERTEX_POINT ( 'NONE', #3405 ) ;
#54202=VECTOR ( 'NONE', #116422, 1000.000000000000000 ) ;
#54206=CARTESIAN_POINT ( 'NONE',  ( 18.58725287972279361, -9.566626910681346629, -174.3225048057644244 ) ) ;
#54211=ORIENTED_EDGE ( 'NONE', *, *, #15932, .F. ) ;
#54238=DIRECTION ( 'NONE',  ( 0.000000000000000000, 0.000000000000000000, -1.000000000000000000 ) ) ;
#54241=ORIENTED_EDGE ( 'NONE', *, *, #160012, .F. ) ;
#54249=DIRECTION ( 'NONE',  ( 0.000000000000000000, -1.000000000000000000, 0.000000000000000000 ) ) ;
#54285=CARTESIAN_POINT ( 'NONE',  ( -20.96428641294271600, 11.75000000001149303, -160.6748931779414704 ) ) ;
#54290=CARTESIAN_POINT ( 'NONE',  ( -23.15000000000000213, -9.599999999988844124, -122.2500000000000284 ) ) ;
#54354=ADVANCED_FACE ( 'NONE', ( #17526 ), #137471, .F. ) ;
#54366=CARTESIAN_POINT ( 'NONE',  ( 20.95203847575071521, 10.50106053928516303, -141.5670713486235570 ) ) ;
#54392=CARTESIAN_POINT ( 'NONE',  ( -23.25000000000000000, 6.933893972137497030, -171.2856458343736108 ) ) ;
#54393=EDGE_LOOP ( 'NONE', ( #42196, #226035 ) ) ;
#54410=CARTESIAN_POINT ( 'NONE',  ( -21.07971444708686093, 0.08782343632898097219, -127.6702079183734924 ) ) ;
#54426=CIRCLE ( 'NONE', #29516, 0.09999999999998898659 ) ;
#54477=CARTESIAN_POINT ( 'NONE',  ( -20.54999999999999716, 2.000000000011154189, -154.2753780772379173 ) ) ;
#54496=CARTESIAN_POINT ( 'NONE',  ( 20.85000000000000142, 6.982009704867603972, -171.1961521182563217 ) ) ;
#54523=DIRECTION ( 'NONE',  ( 0.000000000000000000, 0.000000000000000000, -1.000000000000000000 ) ) ;
#54584=CARTESIAN_POINT ( 'NONE',  ( -21.07094088545304089, 6.320167221927643020, -133.9011062974477966 ) ) ;
#54586=ORIENTED_EDGE ( 'NONE', *, *, #40448, .F. ) ;
#54623=CARTESIAN_POINT ( 'NONE',  ( -20.54999999999999716, 1.115600667400684642E-11, -167.5000000000000284 ) ) ;
#54683=ORIENTED_EDGE ( 'NONE', *, *, #97080, .F. ) ;
#54691=ADVANCED_FACE ( 'NONE', ( #138440 ), #205420, .F. ) ;
#54714=AXIS2_PLACEMENT_3D ( 'NONE', #95001, #19318, #194132 ) ;
#54719=DIRECTION ( 'NONE',  ( 0.000000000000000000, 1.000000000000000000, 0.000000000000000000 ) ) ;
#54728=DIRECTION ( 'NONE',  ( 0.000000000000000000, -0.1298341882520124002, -0.9915357197604841577 ) ) ;
#54732=CARTESIAN_POINT ( 'NONE',  ( -23.25000000000000000, 4.150000000011156764, -155.2500000000000284 ) ) ;
#54748=CARTESIAN_POINT ( 'NONE',  ( -20.54999999999999716, 1.940186915899009490, -146.8291192110533530 ) ) ;
#54769=CIRCLE ( 'NONE', #175592, 0.09999999999999892308 ) ;
#54799=VECTOR ( 'NONE', #110265, 1000.000000000000000 ) ;
#54801=FACE_OUTER_BOUND ( 'NONE', #185118, .T. ) ;
#54817=AXIS2_PLACEMENT_3D ( 'NONE', #170643, #135289, #190165 ) ;
#54824=CARTESIAN_POINT ( 'NONE',  ( 21.04999999999999716, 8.872080675388993143, -142.5210474188322962 ) ) ;
#54863=VERTEX_POINT ( 'NONE', #242697 ) ;
#54877=DIRECTION ( 'NONE',  ( 1.000000000000000000, -0.000000000000000000, 0.000000000000000000 ) ) ;
#54893=ORIENTED_EDGE ( 'NONE', *, *, #69917, .T. ) ;
#54904=FACE_OUTER_BOUND ( 'NONE', #172598, .T. ) ;
#54908=ORIENTED_EDGE ( 'NONE', *, *, #157263, .F. ) ;
#54912=CARTESIAN_POINT ( 'NONE',  ( 20.04142135623730070, 11.65000000001115943, -122.2500000000000284 ) ) ;
#54921=ORIENTED_EDGE ( 'NONE', *, *, #72718, .F. ) ;
#54925=EDGE_LOOP ( 'NONE', ( #187718, #80126, #175524, #26727 ) ) ;
#54933=ORIENTED_EDGE ( 'NONE', *, *, #28896, .F. ) ;
#54945=EDGE_CURVE ( 'NONE', #87130, #7471, #159661, .T. ) ;
#54967=AXIS2_PLACEMENT_3D ( 'NONE', #89131, #172581, #153001 ) ;
#54980=ORIENTED_EDGE ( 'NONE', *, *, #122202, .F. ) ;
#54988=CARTESIAN_POINT ( 'NONE',  ( -23.25000000000000000, 11.75000000001115552, -160.4851942293460638 ) ) ;
#55052=AXIS2_PLACEMENT_3D ( 'NONE', #54477, #134014, #213548 ) ;
#55102=LINE ( 'NONE', #194683, #16382 ) ;
#55107=VERTEX_POINT ( 'NONE', #78175 ) ;
#55130=ORIENTED_EDGE ( 'NONE', *, *, #142404, .T. ) ;
#55158=FACE_OUTER_BOUND ( 'NONE', #119024, .T. ) ;
#55171=DIRECTION ( 'NONE',  ( 0.000000000000000000, 1.000000000000000000, 0.000000000000000000 ) ) ;
#55194=ADVANCED_FACE ( 'NONE', ( #95190 ), #254240, .F. ) ;
#55210=ORIENTED_EDGE ( 'NONE', *, *, #225840, .T. ) ;
#55214=CARTESIAN_POINT ( 'NONE',  ( 21.05000000000000071, 6.258847123090562015, -133.9682416469444775 ) ) ;
#55221=EDGE_LOOP ( 'NONE', ( #30578, #90418, #256985, #141711 ) ) ;
#55224=CARTESIAN_POINT ( 'NONE',  ( 21.07189867249812210, 10.72498027010430377, -146.2124514422767732 ) ) ;
#55262=DIRECTION ( 'NONE',  ( 1.000000000000000000, 0.000000000000000000, 0.000000000000000000 ) ) ;
#55270=EDGE_CURVE ( 'NONE', #116539, #153561, #105642, .T. ) ;
#55295=DIRECTION ( 'NONE',  ( -0.000000000000000000, 0.000000000000000000, 1.000000000000000000 ) ) ;
#55389=AXIS2_PLACEMENT_3D ( 'NONE', #229894, #51221, #130785 ) ;
#55395=LINE ( 'NONE', #176686, #162893 ) ;
#55396=CARTESIAN_POINT ( 'NONE',  ( -21.14999999999999858, -0.09999999998884338825, -122.3504291924552234 ) ) ;
#55401=EDGE_CURVE ( 'NONE', #51801, #22303, #101729, .T. ) ;
#55404=DIRECTION ( 'NONE',  ( 1.000000000000000000, 7.304098846218134667E-16, 0.000000000000000000 ) ) ;
#55412=CIRCLE ( 'NONE', #109605, 7.899999999999990585 ) ;
#55430=ORIENTED_EDGE ( 'NONE', *, *, #201077, .T. ) ;
#55462=ADVANCED_FACE ( 'NONE', ( #59230 ), #95814, .T. ) ;
#55490=DIRECTION ( 'NONE',  ( 0.000000000000000000, -1.000000000000000000, 0.000000000000000000 ) ) ;
#55507=( BOUNDED_CURVE ( )  B_SPLINE_CURVE ( 3, ( #28516, #70190, #225365, #8908 ),
 .UNSPECIFIED., .F., .T. ) 
 B_SPLINE_CURVE_WITH_KNOTS ( ( 4, 4 ),
 ( 3.141592653589793116, 4.712388980384689674 ),
 .UNSPECIFIED. ) 
 CURVE ( )  GEOMETRIC_REPRESENTATION_ITEM ( )  RATIONAL_B_SPLINE_CURVE ( ( 1.000000000000000000, 0.8047378541243649375, 0.8047378541243649375, 1.000000000000000000 ) ) 
 REPRESENTATION_ITEM ( '' )  );
#55511=ORIENTED_EDGE ( 'NONE', *, *, #69646, .F. ) ;
#55536=EDGE_CURVE ( 'NONE', #189870, #109393, #43497, .T. ) ;
#55542=TOROIDAL_SURFACE ( 'NONE', #163926, 11.70000000000000462, 0.1000000000000000056 ) ;
#55551=CARTESIAN_POINT ( 'NONE',  ( 21.05000000000000071, 1.115600667400684642E-11, -167.5000000000000284 ) ) ;
#55553=EDGE_CURVE ( 'NONE', #156063, #114275, #18862, .T. ) ;
#55571=DIRECTION ( 'NONE',  ( 0.000000000000000000, 0.000000000000000000, -1.000000000000000000 ) ) ;
#55607=ORIENTED_EDGE ( 'NONE', *, *, #146951, .T. ) ;
#55612=CARTESIAN_POINT ( 'NONE',  ( 21.05000000000000071, 1.115600667400684642E-11, -134.0000000000000000 ) ) ;
#55621=DIRECTION ( 'NONE',  ( 0.000000000000000000, 1.000000000000000000, 0.000000000000000000 ) ) ;
#55632=DIRECTION ( 'NONE',  ( 0.000000000000000000, -0.000000000000000000, 1.000000000000000000 ) ) ;
#55657=LINE ( 'NONE', #157407, #204968 ) ;
#55661=VERTEX_POINT ( 'NONE', #7008 ) ;
#55666=EDGE_LOOP ( 'NONE', ( #70397, #206194, #33099, #174214 ) ) ;
#55734=CARTESIAN_POINT ( 'NONE',  ( 18.59999999999999076, 6.450000000011156587, -144.0170271704400307 ) ) ;
#55736=EDGE_CURVE ( 'NONE', #140838, #41279, #114421, .T. ) ;
#55745=CARTESIAN_POINT ( 'NONE',  ( -23.25000000000000000, -1.736705739456431807, -179.0174225876237415 ) ) ;
#55755=ORIENTED_EDGE ( 'NONE', *, *, #90782, .F. ) ;
#55757=DIRECTION ( 'NONE',  ( 1.000000000000000000, 0.000000000000000000, -0.000000000000000000 ) ) ;
#55770=DIRECTION ( 'NONE',  ( 1.000000000000000000, 0.000000000000000000, -0.000000000000000000 ) ) ;
#55790=DIRECTION ( 'NONE',  ( -1.000000000000000000, -1.836970198721029934E-16, 0.000000000000000000 ) ) ;
#55804=ADVANCED_FACE ( 'NONE', ( #192092, #186964 ), #53849, .T. ) ;
#55822=AXIS2_PLACEMENT_3D ( 'NONE', #160595, #161871, #21082 ) ;
#55891=CARTESIAN_POINT ( 'NONE',  ( 18.49999999999999645, 5.950000000011100632, -144.3057023050348846 ) ) ;
#55895=ORIENTED_EDGE ( 'NONE', *, *, #229306, .F. ) ;
#55917=CARTESIAN_POINT ( 'NONE',  ( -20.64999999999999858, 2.500000000011154633, -154.2753780772379173 ) ) ;
#55945=EDGE_LOOP ( 'NONE', ( #192290, #38384, #79670, #56856 ) ) ;
#55967=DIRECTION ( 'NONE',  ( 1.000000000000000000, 0.000000000000000000, 0.000000000000000000 ) ) ;
#55998=ORIENTED_EDGE ( 'NONE', *, *, #93152, .F. ) ;
#56021=DIRECTION ( 'NONE',  ( -1.836970198721029934E-16, 1.000000000000000000, 0.000000000000000000 ) ) ;
#56026=CYLINDRICAL_SURFACE ( 'NONE', #238100, 0.09999999999999892308 ) ;
#56062=ADVANCED_FACE ( 'NONE', ( #246593 ), #147504, .F. ) ;
#56067=DIRECTION ( 'NONE',  ( 0.000000000000000000, 0.000000000000000000, -1.000000000000000000 ) ) ;
#56070=EDGE_CURVE ( 'NONE', #226085, #18582, #118531, .T. ) ;
#56113=CIRCLE ( 'NONE', #76976, 0.09999999999998898659 ) ;
#56114=DIRECTION ( 'NONE',  ( -0.000000000000000000, 0.1350103645451626311, 0.9908441862701635738 ) ) ;
#56118=VERTEX_POINT ( 'NONE', #50942 ) ;
#56119=DIRECTION ( 'NONE',  ( 0.000000000000000000, -1.000000000000000000, 0.000000000000000000 ) ) ;
#56124=TOROIDAL_SURFACE ( 'NONE', #81246, 0.2000000000000000111, 0.1000000000000000056 ) ;
#56190=FACE_OUTER_BOUND ( 'NONE', #13966, .T. ) ;
#56215=DIRECTION ( 'NONE',  ( -4.408576920032448588E-17, 0.1350103645451876666, -0.9908441862701600211 ) ) ;
#56245=ORIENTED_EDGE ( 'NONE', *, *, #165990, .F. ) ;
#56337=DIRECTION ( 'NONE',  ( 0.000000000000000000, 0.000000000000000000, 1.000000000000000000 ) ) ;
#56339=EDGE_CURVE ( 'NONE', #158124, #85588, #68812, .T. ) ;
#56341=EDGE_CURVE ( 'NONE', #155942, #23713, #106195, .T. ) ;
#56354=CARTESIAN_POINT ( 'NONE',  ( -23.15000000000000213, 2.500000000011156409, -147.2246219227621111 ) ) ;
#56361=DIRECTION ( 'NONE',  ( 0.000000000000000000, 0.000000000000000000, 1.000000000000000000 ) ) ;
#56406=CARTESIAN_POINT ( 'NONE',  ( -18.50000000000000000, 9.350000000011156942, -146.3500000000000227 ) ) ;
#56416=LINE ( 'NONE', #215506, #54202 ) ;
#56444=EDGE_LOOP ( 'NONE', ( #18727, #142381, #39869, #19324 ) ) ;
#56472=DIRECTION ( 'NONE',  ( 1.000000000000000000, 0.000000000000000000, 0.000000000000000000 ) ) ;
#56481=EDGE_CURVE ( 'NONE', #86831, #79296, #148103, .T. ) ;
#56508=DIRECTION ( 'NONE',  ( 1.000000000000000000, 0.000000000000000000, 0.000000000000000000 ) ) ;
#56523=CARTESIAN_POINT ( 'NONE',  ( -20.94999999999999929, 1.115600667400684642E-11, -167.5000000000000284 ) ) ;
#56551=CIRCLE ( 'NONE', #19176, 0.09999999999998898659 ) ;
#56581=AXIS2_PLACEMENT_3D ( 'NONE', #95091, #174684, #36432 ) ;
#56676=CARTESIAN_POINT ( 'NONE',  ( -18.59999999999999787, 1.115600667400684642E-11, -134.0000000000000000 ) ) ;
#56695=ORIENTED_EDGE ( 'NONE', *, *, #186012, .T. ) ;
#56701=DIRECTION ( 'NONE',  ( 0.000000000000000000, 1.000000000000000000, 2.891205793294679805E-16 ) ) ;
#56702=VERTEX_POINT ( 'NONE', #249017 ) ;
#56718=VERTEX_POINT ( 'NONE', #66514 ) ;
#56765=DIRECTION ( 'NONE',  ( 1.000000000000000000, 0.000000000000000000, 0.000000000000000000 ) ) ;
#56784=AXIS2_PLACEMENT_3D ( 'NONE', #16492, #12644, #92155 ) ;
#56825=CIRCLE ( 'NONE', #227543, 0.1000000000000028644 ) ;
#56839=DIRECTION ( 'NONE',  ( 0.000000000000000000, 0.000000000000000000, 1.000000000000000000 ) ) ;
#56840=ORIENTED_EDGE ( 'NONE', *, *, #52932, .T. ) ;
#56848=CARTESIAN_POINT ( 'NONE',  ( -22.00411653889213071, 0.09903810579707936212, -126.7465571323596123 ) ) ;
#56850=ORIENTED_EDGE ( 'NONE', *, *, #133450, .F. ) ;
#56856=ORIENTED_EDGE ( 'NONE', *, *, #38474, .F. ) ;
#56858=EDGE_CURVE ( 'NONE', #173723, #178019, #127253, .T. ) ;
#56860=CARTESIAN_POINT ( 'NONE',  ( -20.64999999999999858, 4.350000000011156054, -155.2500000000000284 ) ) ;
#56870=AXIS2_PLACEMENT_3D ( 'NONE', #144540, #222790, #1171 ) ;
#56916=CARTESIAN_POINT ( 'NONE',  ( 21.07928932188134397, 6.328516656404459262, -133.9011048543456184 ) ) ;
#56936=EDGE_CURVE ( 'NONE', #157661, #248851, #131529, .T. ) ;
#56956=AXIS2_PLACEMENT_3D ( 'NONE', #86929, #189913, #243458 ) ;
#56973=CIRCLE ( 'NONE', #90301, 4.000000000000003553 ) ;
#56984=DIRECTION ( 'NONE',  ( 0.000000000000000000, 1.000000000000000000, 0.000000000000000000 ) ) ;
#56989=ORIENTED_EDGE ( 'NONE', *, *, #253131, .F. ) ;
#56991=CARTESIAN_POINT ( 'NONE',  ( -23.25000000000000000, 1.115600667400684642E-11, -146.7750000000000057 ) ) ;
#57004=VECTOR ( 'NONE', #15310, 1000.000000000000000 ) ;
#57015=CARTESIAN_POINT ( 'NONE',  ( -18.59999999999999787, 9.250000000011157297, -155.2500000000000284 ) ) ;
#57026=ORIENTED_EDGE ( 'NONE', *, *, #13305, .F. ) ;
#57044=CIRCLE ( 'NONE', #202815, 0.09999999999999817368 ) ;
#57075=CARTESIAN_POINT ( 'NONE',  ( -23.25000000000000000, 1.115600667400684642E-11, -167.5000000000000284 ) ) ;
#57086=ORIENTED_EDGE ( 'NONE', *, *, #72256, .F. ) ;
#57128=ORIENTED_EDGE ( 'NONE', *, *, #98543, .T. ) ;
#57140=CARTESIAN_POINT ( 'NONE',  ( -23.15000000000000213, 11.65000000001115588, -160.4851942293460638 ) ) ;
#57196=ADVANCED_FACE ( 'NONE', ( #156028 ), #73932, .F. ) ;
#57202=ORIENTED_EDGE ( 'NONE', *, *, #182328, .T. ) ;
#57214=ORIENTED_EDGE ( 'NONE', *, *, #173074, .F. ) ;
#57232=DIRECTION ( 'NONE',  ( 0.000000000000000000, 0.000000000000000000, -1.000000000000000000 ) ) ;
#57254=CARTESIAN_POINT ( 'NONE',  ( -20.94999999999999929, -11.48912529306490349, -137.1000000000000227 ) ) ;
#57297=FACE_OUTER_BOUND ( 'NONE', #134683, .T. ) ;
#57303=CARTESIAN_POINT ( 'NONE',  ( -22.48660254037843131, 11.65000000001115588, -133.9500000000000455 ) ) ;
#57331=ORIENTED_EDGE ( 'NONE', *, *, #186388, .F. ) ;
#57337=FACE_OUTER_BOUND ( 'NONE', #49845, .T. ) ;
#57357=AXIS2_PLACEMENT_3D ( 'NONE', #57254, #172138, #138083 ) ;
#57394=CARTESIAN_POINT ( 'NONE',  ( 18.59999999999999787, -11.74999999998883737, -155.3500000000000227 ) ) ;
#57419=( LENGTH_UNIT ( ) NAMED_UNIT ( * ) SI_UNIT ( .MILLI., .METRE. ) );
#57428=ORIENTED_EDGE ( 'NONE', *, *, #117544, .T. ) ;
#57441=B_SPLINE_CURVE_WITH_KNOTS ( 'NONE', 3,
 ( #185356, #249191, #211343, #32743, #49695, #152682, #110954 ),
 .UNSPECIFIED., .F., .F.,
 ( 4, 3, 4 ),
 ( 0.000000000000000000, 3.357501770814691602E-05, 5.199112466349472097E-05 ),
 .UNSPECIFIED. ) ;
#57463=DIRECTION ( 'NONE',  ( 1.000000000000000000, 0.000000000000000000, 0.000000000000000000 ) ) ;
#57477=FACE_OUTER_BOUND ( 'NONE', #224965, .T. ) ;
#57543=VECTOR ( 'NONE', #250247, 1000.000000000000000 ) ;
#57544=ORIENTED_EDGE ( 'NONE', *, *, #228203, .F. ) ;
#57546=CARTESIAN_POINT ( 'NONE',  ( -21.14999999999999858, -11.64999999998884483, -136.9000000000000341 ) ) ;
#57592=EDGE_LOOP ( 'NONE', ( #46307, #224875, #176720, #170437 ) ) ;
#57632=AXIS2_PLACEMENT_3D ( 'NONE', #208336, #213437, #132634 ) ;
#57636=FACE_OUTER_BOUND ( 'NONE', #147692, .T. ) ;
#57652=CIRCLE ( 'NONE', #199329, 0.09999999999998898659 ) ;
#57709=CARTESIAN_POINT ( 'NONE',  ( -18.44448725179913851, -9.490081715472173940, -174.1289602940624945 ) ) ;
#57711=DIRECTION ( 'NONE',  ( 2.694716079187272946E-16, -1.000000000000000000, 0.000000000000000000 ) ) ;
#57747=EDGE_CURVE ( 'NONE', #53590, #161202, #40920, .T. ) ;
#57748=CARTESIAN_POINT ( 'NONE',  ( -18.50000000000000000, -1.135018845899022466, -175.2169768834323520 ) ) ;
#57754=AXIS2_PLACEMENT_3D ( 'NONE', #1200, #61200, #146811 ) ;
#57767=CARTESIAN_POINT ( 'NONE',  ( 21.14999999999999503, -0.09999999998884338825, -122.3504291924552234 ) ) ;
#57784=EDGE_LOOP ( 'NONE', ( #164355, #10617, #230839, #230418 ) ) ;
#57787=( BOUNDED_CURVE ( )  B_SPLINE_CURVE ( 3, ( #132792, #117060, #200443, #101282 ),
 .UNSPECIFIED., .F., .F. ) 
 B_SPLINE_CURVE_WITH_KNOTS ( ( 4, 4 ),
 ( 0.000000000000000000, 1.570796326794908992 ),
 .UNSPECIFIED. ) 
 CURVE ( )  GEOMETRIC_REPRESENTATION_ITEM ( )  RATIONAL_B_SPLINE_CURVE ( ( 1.000000000000000000, 0.8047378541243619399, 0.8047378541243619399, 1.000000000000000000 ) ) 
 REPRESENTATION_ITEM ( '' )  );
#57795=CARTESIAN_POINT ( 'NONE',  ( 21.07928932188134397, 6.328516656404468144, -133.9011048543456184 ) ) ;
#57803=EDGE_CURVE ( 'NONE', #99200, #37772, #201234, .T. ) ;
#57811=ORIENTED_EDGE ( 'NONE', *, *, #59122, .F. ) ;
#57813=EDGE_LOOP ( 'NONE', ( #169787, #242135, #215971, #77380 ) ) ;
#57818=LINE ( 'NONE', #61695, #2265 ) ;
#57847=AXIS2_PLACEMENT_3D ( 'NONE', #38283, #255982, #215616 ) ;
#57903=EDGE_CURVE ( 'NONE', #3992, #160216, #125559, .T. ) ;
#57956=CARTESIAN_POINT ( 'NONE',  ( 23.15000000000000213, -11.64999999998883595, -122.2500000000000284 ) ) ;
#57968=FACE_OUTER_BOUND ( 'NONE', #228042, .T. ) ;
#57999=CARTESIAN_POINT ( 'NONE',  ( -23.15000000000000213, 4.150000000011156764, -155.1500000000000057 ) ) ;
#58004=B_SPLINE_CURVE_WITH_KNOTS ( 'NONE', 3,
 ( #145102, #109827, #10750, #190696, #130683, #147690 ),
 .UNSPECIFIED., .F., .F.,
 ( 4, 2, 4 ),
 ( 1.138412281109779656E-18, 0.0001569047307838639788, 0.0003138094615677267650 ),
 .UNSPECIFIED. ) ;
#58009=DIRECTION ( 'NONE',  ( 0.000000000000000000, 3.469446951953995998E-14, 1.000000000000000000 ) ) ;
#58018=CARTESIAN_POINT ( 'NONE',  ( 23.14999999999999858, 5.600000000011153389, -155.0947339810869323 ) ) ;
#58074=DIRECTION ( 'NONE',  ( -1.000000000000000000, 0.000000000000000000, 0.000000000000000000 ) ) ;
#58075=DIRECTION ( 'NONE',  ( 0.000000000000000000, -0.000000000000000000, -1.000000000000000000 ) ) ;
#58102=DIRECTION ( 'NONE',  ( -0.7071067811865475727, -0.7071067811865475727, -0.000000000000000000 ) ) ;
#58106=CARTESIAN_POINT ( 'NONE',  ( -18.59999999999999787, 7.021664781911246322, -171.3335654018973173 ) ) ;
#58183=EDGE_CURVE ( 'NONE', #65123, #87825, #35486, .T. ) ;
#58222=CARTESIAN_POINT ( 'NONE',  ( -21.05000000000000071, -0.02110330804822888387, -127.6954836707355270 ) ) ;
#58227=ORIENTED_EDGE ( 'NONE', *, *, #110515, .T. ) ;
#58230=LINE ( 'NONE', #20426, #121079 ) ;
#58242=ORIENTED_EDGE ( 'NONE', *, *, #134470, .F. ) ;
#58290=DIRECTION ( 'NONE',  ( 0.000000000000000000, 0.000000000000000000, 1.000000000000000000 ) ) ;
#58291=DIRECTION ( 'NONE',  ( -1.000000000000000000, 0.000000000000000000, 0.000000000000000000 ) ) ;
#58351=EDGE_LOOP ( 'NONE', ( #101131, #114919, #43399, #3914, #196161, #180728, #165251 ) ) ;
#58357=UNCERTAINTY_MEASURE_WITH_UNIT (LENGTH_MEASURE( 1.000000000000000082E-05 ), #175355, 'distance_accuracy_value', 'NONE');
#58361=CARTESIAN_POINT ( 'NONE',  ( 22.39999999999999503, 11.75000000001116263, -134.1000000000000227 ) ) ;
#58372=ORIENTED_EDGE ( 'NONE', *, *, #44975, .F. ) ;
#58398=DIRECTION ( 'NONE',  ( -0.000000000000000000, -0.000000000000000000, 1.000000000000000000 ) ) ;
#58419=AXIS2_PLACEMENT_3D ( 'NONE', #49313, #169307, #229250 ) ;
#58434=CARTESIAN_POINT ( 'NONE',  ( 18.49999999999999289, 11.75000000001115907, -122.2500000000000284 ) ) ;
#58437=ORIENTED_EDGE ( 'NONE', *, *, #72415, .T. ) ;
#58448=AXIS2_PLACEMENT_3D ( 'NONE', #5507, #206310, #242855 ) ;
#58465=ORIENTED_EDGE ( 'NONE', *, *, #21564, .F. ) ;
#58500=ORIENTED_EDGE ( 'NONE', *, *, #28885, .F. ) ;
#58505=DIRECTION ( 'NONE',  ( 0.000000000000000000, -0.9654727137038715545, 0.2605042016806676242 ) ) ;
#58506=DIRECTION ( 'NONE',  ( 0.000000000000000000, 0.000000000000000000, -1.000000000000000000 ) ) ;
#58512=LINE ( 'NONE', #24567, #6597 ) ;
#58513=DIRECTION ( 'NONE',  ( 1.000000000000000000, 0.000000000000000000, -0.000000000000000000 ) ) ;
#58539=CARTESIAN_POINT ( 'NONE',  ( -18.50000000000000000, 9.350000000011156942, -155.1500000000000057 ) ) ;
#58545=DIRECTION ( 'NONE',  ( 0.000000000000000000, 1.000000000000000000, 0.000000000000000000 ) ) ;
#58580=DIRECTION ( 'NONE',  ( -1.000000000000000000, -0.000000000000000000, -0.000000000000000000 ) ) ;
#58590=CARTESIAN_POINT ( 'NONE',  ( -22.48660254037843131, 11.75000000001115374, -133.9500000000000171 ) ) ;
#58599=ADVANCED_FACE ( 'NONE', ( #187184 ), #102612, .T. ) ;
#58659=AXIS2_PLACEMENT_3D ( 'NONE', #61428, #121434, #237502 ) ;
#58694=EDGE_LOOP ( 'NONE', ( #87938, #177841, #206295, #150242 ) ) ;
#58706=VERTEX_POINT ( 'NONE', #175333 ) ;
#58728=FACE_OUTER_BOUND ( 'NONE', #230681, .T. ) ;
#58757=CARTESIAN_POINT ( 'NONE',  ( 23.14999999999999858, 1.115600667400684642E-11, -167.5000000000000284 ) ) ;
#58774=AXIS2_PLACEMENT_3D ( 'NONE', #229588, #210033, #7975 ) ;
#58782=AXIS2_PLACEMENT_3D ( 'NONE', #228945, #149424, #132409 ) ;
#58819=CARTESIAN_POINT ( 'NONE',  ( 23.14999999999999503, 11.65000000001116298, -160.4851942293460922 ) ) ;
#58821=ORIENTED_EDGE ( 'NONE', *, *, #152482, .F. ) ;
#58852=VERTEX_POINT ( 'NONE', #177888 ) ;
#58923=CIRCLE ( 'NONE', #204692, 1.900000000000012790 ) ;
#58929=CYLINDRICAL_SURFACE ( 'NONE', #256640, 0.1000000000000098310 ) ;
#58981=LINE ( 'NONE', #36923, #212011 ) ;
#58999=EDGE_LOOP ( 'NONE', ( #181965, #209421, #20166, #224001 ) ) ;
#59023=DIRECTION ( 'NONE',  ( 1.000000000000000000, 2.952720810173289112E-16, -0.000000000000000000 ) ) ;
#59043=EDGE_LOOP ( 'NONE', ( #246244, #193355, #75596, #145820 ) ) ;
#59046=ORIENTED_EDGE ( 'NONE', *, *, #117563, .T. ) ;
#59057=FACE_OUTER_BOUND ( 'NONE', #244461, .T. ) ;
#59063=CARTESIAN_POINT ( 'NONE',  ( 21.04999999999999716, 6.441084688482184184, -134.0177194333088835 ) ) ;
#59088=ORIENTED_EDGE ( 'NONE', *, *, #27307, .T. ) ;
#59122=EDGE_CURVE ( 'NONE', #109066, #225500, #251968, .T. ) ;
#59136=AXIS2_PLACEMENT_3D ( 'NONE', #12819, #31115, #190162 ) ;
#59221=AXIS2_PLACEMENT_3D ( 'NONE', #145961, #161712, #224215 ) ;
#59230=FACE_OUTER_BOUND ( 'NONE', #229083, .T. ) ;
#59247=EDGE_CURVE ( 'NONE', #221150, #222371, #112620, .T. ) ;
#59251=TOROIDAL_SURFACE ( 'NONE', #121855, 4.149999999999999467, 0.1000000000000000056 ) ;
#59276=EDGE_CURVE ( 'NONE', #113536, #227353, #99294, .T. ) ;
#59363=VERTEX_POINT ( 'NONE', #52173 ) ;
#59387=LINE ( 'NONE', #214643, #60351 ) ;
#59394=ORIENTED_EDGE ( 'NONE', *, *, #200460, .F. ) ;
#59399=FACE_OUTER_BOUND ( 'NONE', #24559, .T. ) ;
#59451=VERTEX_POINT ( 'NONE', #230849 ) ;
#59465=ORIENTED_EDGE ( 'NONE', *, *, #154566, .F. ) ;
#59481=CARTESIAN_POINT ( 'NONE',  ( 21.30740335185486245, 6.556657922039159203, -133.9010654742241684 ) ) ;
#59482=CARTESIAN_POINT ( 'NONE',  ( 21.05000000000000071, 1.115600667400684642E-11, -134.0000000000000000 ) ) ;
#59490=ADVANCED_FACE ( 'NONE', ( #57297 ), #159022, .F. ) ;
#59498=ADVANCED_FACE ( 'NONE', ( #61171 ), #256750, .F. ) ;
#59511=CARTESIAN_POINT ( 'NONE',  ( 20.12500000000000000, 9.750000000011153745, -142.1117712821142902 ) ) ;
#59522=CARTESIAN_POINT ( 'NONE',  ( -18.46946985241255490, -9.509317228700188807, -140.9866625654999552 ) ) ;
#59539=CARTESIAN_POINT ( 'NONE',  ( -20.64999999999999858, -8.730841121484171907, -143.5980747189843783 ) ) ;
#59575=CARTESIAN_POINT ( 'NONE',  ( -20.94999999999999929, 1.162701749949165642, -142.1000000000000227 ) ) ;
#59589=EDGE_LOOP ( 'NONE', ( #52891, #169898, #125948, #20037 ) ) ;
#59602=FACE_OUTER_BOUND ( 'NONE', #160322, .T. ) ;
#59625=DIRECTION ( 'NONE',  ( 0.000000000000000000, 0.000000000000000000, -1.000000000000000000 ) ) ;
#59646=VECTOR ( 'NONE', #147030, 1000.000000000000000 ) ;
#59654=CARTESIAN_POINT ( 'NONE',  ( 21.08750232978087524, 10.72486338602132250, -146.2288581729995940 ) ) ;
#59664=CARTESIAN_POINT ( 'NONE',  ( 18.59999999999999432, -1.135018845899022466, -175.2169768834323520 ) ) ;
#59665=CARTESIAN_POINT ( 'NONE',  ( -20.54999999999999716, -9.399999999988848387, -143.8939691226524644 ) ) ;
#59667=CIRCLE ( 'NONE', #159663, 4.299999999999970512 ) ;
#59674=ORIENTED_EDGE ( 'NONE', *, *, #28244, .F. ) ;
#59693=DIRECTION ( 'NONE',  ( 1.000000000000000000, 7.304098846218134667E-16, -0.000000000000000000 ) ) ;
#59703=CIRCLE ( 'NONE', #30713, 0.09999999999998898659 ) ;
#59718=VERTEX_POINT ( 'NONE', #67591 ) ;
#59759=ORIENTED_EDGE ( 'NONE', *, *, #149560, .T. ) ;
#59761=CIRCLE ( 'NONE', #113767, 0.1000000000000001860 ) ;
#59790=CARTESIAN_POINT ( 'NONE',  ( -23.15000000000000213, 1.115600667400684642E-11, -134.0000000000000000 ) ) ;
#59866=CIRCLE ( 'NONE', #151494, 0.09999999999998898659 ) ;
#59872=VERTEX_POINT ( 'NONE', #169304 ) ;
#59877=CYLINDRICAL_SURFACE ( 'NONE', #133279, 0.09999999999998898659 ) ;
#59907=CYLINDRICAL_SURFACE ( 'NONE', #100411, 0.09999999999999939493 ) ;
#59929=EDGE_LOOP ( 'NONE', ( #57202, #99509, #53667, #3982 ) ) ;
#59936=EDGE_CURVE ( 'NONE', #120136, #237128, #150231, .T. ) ;
#59963=DIRECTION ( 'NONE',  ( 0.000000000000000000, 6.505213034913742890E-15, -1.000000000000000000 ) ) ;
#59975=ORIENTED_EDGE ( 'NONE', *, *, #120735, .F. ) ;
#60055=DIRECTION ( 'NONE',  ( 1.000000000000000000, 0.000000000000000000, 0.000000000000000000 ) ) ;
#60070=EDGE_CURVE ( 'NONE', #27375, #242008, #71309, .T. ) ;
#60082=FACE_OUTER_BOUND ( 'NONE', #99176, .T. ) ;
#60099=VERTEX_POINT ( 'NONE', #108071 ) ;
#60110=VERTEX_POINT ( 'NONE', #250145 ) ;
#60114=DIRECTION ( 'NONE',  ( 0.000000000000000000, 0.9908441862701596881, 0.1350103645451904977 ) ) ;
#60138=CIRCLE ( 'NONE', #68353, 0.09999999999999491240 ) ;
#60139=DIRECTION ( 'NONE',  ( 0.000000000000000000, -0.9908441862701782288, -0.1350103645450542456 ) ) ;
#60187=CARTESIAN_POINT ( 'NONE',  ( 18.59999999999999076, 11.65000000001115943, -158.7500000000000284 ) ) ;
#60213=DIRECTION ( 'NONE',  ( 0.000000000000000000, 0.000000000000000000, -1.000000000000000000 ) ) ;
#60222=AXIS2_PLACEMENT_3D ( 'NONE', #52901, #132447, #249831 ) ;
#60230=ADVANCED_FACE ( 'NONE', ( #238266 ), #50410, .T. ) ;
#60243=CARTESIAN_POINT ( 'NONE',  ( 18.39999999999999858, -9.499999999988842703, -174.1001893912220737 ) ) ;
#60246=CIRCLE ( 'NONE', #226847, 12.87499999999999822 ) ;
#60280=CARTESIAN_POINT ( 'NONE',  ( -18.47690164073606667, -9.464844538001088381, -174.2013809398361559 ) ) ;
#60291=CIRCLE ( 'NONE', #101966, 0.09999999999998898659 ) ;
#60300=ADVANCED_FACE ( 'NONE', ( #114479 ), #234416, .T. ) ;
#60310=ORIENTED_EDGE ( 'NONE', *, *, #31490, .F. ) ;
#60348=ADVANCED_FACE ( 'NONE', ( #179609 ), #85575, .F. ) ;
#60351=VECTOR ( 'NONE', #136361, 1000.000000000000000 ) ;
#60352=ORIENTED_EDGE ( 'NONE', *, *, #56341, .F. ) ;
#60354=AXIS2_PLACEMENT_3D ( 'NONE', #158764, #195326, #139138 ) ;
#60356=ADVANCED_FACE ( 'NONE', ( #4769 ), #3502, .T. ) ;
#60364=ORIENTED_EDGE ( 'NONE', *, *, #20635, .T. ) ;
#60386=CIRCLE ( 'NONE', #106164, 0.09999999999998898659 ) ;
#60400=DIRECTION ( 'NONE',  ( 0.000000000000000000, -1.000000000000000000, 0.000000000000000000 ) ) ;
#60414=EDGE_LOOP ( 'NONE', ( #17683, #48901, #206743, #143988 ) ) ;
#60445=EDGE_CURVE ( 'NONE', #227344, #96734, #34098, .T. ) ;
#60446=AXIS2_PLACEMENT_3D ( 'NONE', #148481, #168085, #31136 ) ;
#60471=DIRECTION ( 'NONE',  ( 1.000000000000000000, 0.000000000000000000, 0.000000000000000000 ) ) ;
#60472=DIRECTION ( 'NONE',  ( 1.000000000000000000, 0.000000000000000000, 0.000000000000000000 ) ) ;
#60499=CARTESIAN_POINT ( 'NONE',  ( -18.59999999999999787, 1.162701749949165642, -142.0000000000000284 ) ) ;
#60502=EDGE_CURVE ( 'NONE', #157963, #158625, #171462, .T. ) ;
#60507=CARTESIAN_POINT ( 'NONE',  ( -21.14999999999999858, 11.65000000001115588, -134.1000000000000227 ) ) ;
#60508=ORIENTED_EDGE ( 'NONE', *, *, #142596, .F. ) ;
#60564=AXIS2_PLACEMENT_3D ( 'NONE', #215259, #160452, #61323 ) ;
#60594=CARTESIAN_POINT ( 'NONE',  ( 18.59999999999999432, -1.835859311432484375, -179.0044391687985410 ) ) ;
#60646=CARTESIAN_POINT ( 'NONE',  ( -20.64999999999999858, -8.999999999988844479, -157.6060308773475924 ) ) ;
#60656=AXIS2_PLACEMENT_3D ( 'NONE', #50784, #69109, #32572 ) ;
#60674=CARTESIAN_POINT ( 'NONE',  ( -18.50000000000000000, -1.835341550213255957, -145.5551512925629822 ) ) ;
#60695=CARTESIAN_POINT ( 'NONE',  ( -20.54999999999999716, 7.150000000011155876, -150.7500000000000284 ) ) ;
#60734=AXIS2_PLACEMENT_3D ( 'NONE', #79919, #115233, #236464 ) ;
#60756=ORIENTED_EDGE ( 'NONE', *, *, #62914, .F. ) ;
#60769=EDGE_CURVE ( 'NONE', #42519, #189870, #238236, .T. ) ;
#60780=DIRECTION ( 'NONE',  ( 0.000000000000000000, -1.000000000000000000, 0.000000000000000000 ) ) ;
#60797=CARTESIAN_POINT ( 'NONE',  ( -21.04999999999999716, 1.115177828553415134E-11, -127.4593430482987912 ) ) ;
#60822=ORIENTED_EDGE ( 'NONE', *, *, #95880, .F. ) ;
#60825=CARTESIAN_POINT ( 'NONE',  ( -18.49719636458551975, -9.446365359216901680, -141.0716138698831230 ) ) ;
#60838=EDGE_CURVE ( 'NONE', #175143, #8211, #150756, .T. ) ;
#60844=FACE_OUTER_BOUND ( 'NONE', #200029, .T. ) ;
#60862=CARTESIAN_POINT ( 'NONE',  ( 18.50000000000000000, -9.399999999988843058, -141.2972597596633193 ) ) ;
#60865=DIRECTION ( 'NONE',  ( 0.000000000000000000, 2.891205793294679805E-16, -1.000000000000000000 ) ) ;
#60929=DIRECTION ( 'NONE',  ( 0.000000000000000000, 0.000000000000000000, -1.000000000000000000 ) ) ;
#60973=ORIENTED_EDGE ( 'NONE', *, *, #248881, .T. ) ;
#60976=AXIS2_PLACEMENT_3D ( 'NONE', #191062, #107638, #127212 ) ;
#60984=CARTESIAN_POINT ( 'NONE',  ( 20.95512820512820440, 10.62384868372303615, -146.1500000000000341 ) ) ;
#60987=ORIENTED_EDGE ( 'NONE', *, *, #110695, .F. ) ;
#60993=LINE ( 'NONE', #988, #233773 ) ;
#61000=ORIENTED_EDGE ( 'NONE', *, *, #144793, .T. ) ;
#61010=CARTESIAN_POINT ( 'NONE',  ( 23.14999999999999858, 11.65000000001116298, -160.4851942293460922 ) ) ;
#61025=CARTESIAN_POINT ( 'NONE',  ( 20.94999999999999574, -1.349084418615859482, -141.9864989635455004 ) ) ;
#61038=EDGE_CURVE ( 'NONE', #220134, #41279, #190875, .T. ) ;
#61067=FACE_OUTER_BOUND ( 'NONE', #137510, .T. ) ;
#61075=DIRECTION ( 'NONE',  ( 0.000000000000000000, -0.000000000000000000, 1.000000000000000000 ) ) ;
#61093=VERTEX_POINT ( 'NONE', #236383 ) ;
#61114=FACE_OUTER_BOUND ( 'NONE', #238066, .T. ) ;
#61158=DIRECTION ( 'NONE',  ( -1.000000000000000000, -0.000000000000000000, -0.000000000000000000 ) ) ;
#61171=FACE_OUTER_BOUND ( 'NONE', #30295, .T. ) ;
#61186=ORIENTED_EDGE ( 'NONE', *, *, #112189, .F. ) ;
#61200=DIRECTION ( 'NONE',  ( -0.000000000000000000, -0.4791956752371546169, -0.8777080977375152360 ) ) ;
#61250=AXIS2_PLACEMENT_3D ( 'NONE', #83265, #24641, #147107 ) ;
#61260=CIRCLE ( 'NONE', #144429, 0.09999999999998898659 ) ;
#61323=DIRECTION ( 'NONE',  ( 1.000000000000000000, 0.000000000000000000, 0.000000000000000000 ) ) ;
#61376=CARTESIAN_POINT ( 'NONE',  ( 18.59999999999999076, -1.149570369564537842, -175.3159124845019790 ) ) ;
#61377=DIRECTION ( 'NONE',  ( 0.000000000000000000, 0.000000000000000000, -1.000000000000000000 ) ) ;
#61415=TOROIDAL_SURFACE ( 'NONE', #194532, 6.258578643762700899, 0.1000000000000000056 ) ;
#61420=VECTOR ( 'NONE', #141616, 1000.000000000000227 ) ;
#61427=ADVANCED_FACE ( 'NONE', ( #100056 ), #237035, .F. ) ;
#61428=CARTESIAN_POINT ( 'NONE',  ( -18.59999999999999787, 9.150000000011157653, -155.1500000000000057 ) ) ;
#61437=DIRECTION ( 'NONE',  ( 0.000000000000000000, 0.000000000000000000, -1.000000000000000000 ) ) ;
#61451=EDGE_LOOP ( 'NONE', ( #120511, #64943, #66868, #96115 ) ) ;
#61466=AXIS2_PLACEMENT_3D ( 'NONE', #76835, #18148, #114685 ) ;
#61496=AXIS2_PLACEMENT_3D ( 'NONE', #192278, #74914, #13629 ) ;
#61530=ORIENTED_EDGE ( 'NONE', *, *, #61941, .T. ) ;
#61536=ORIENTED_EDGE ( 'NONE', *, *, #149282, .T. ) ;
#61552=ORIENTED_EDGE ( 'NONE', *, *, #226747, .T. ) ;
#61577=ORIENTED_EDGE ( 'NONE', *, *, #244798, .F. ) ;
#61581=CARTESIAN_POINT ( 'NONE',  ( 20.94999999999999929, 11.63687328911507635, -160.6782407866756159 ) ) ;
#61609=FACE_OUTER_BOUND ( 'NONE', #59043, .T. ) ;
#61610=AXIS2_PLACEMENT_3D ( 'NONE', #132484, #33423, #95907 ) ;
#61620=DIRECTION ( 'NONE',  ( 0.000000000000000000, 0.1298341882520022694, 0.9915357197604852679 ) ) ;
#61644=ADVANCED_FACE ( 'NONE', ( #45248 ), #105171, .F. ) ;
#61649=ORIENTED_EDGE ( 'NONE', *, *, #124374, .F. ) ;
#61683=EDGE_CURVE ( 'NONE', #115258, #96658, #238613, .T. ) ;
#61688=EDGE_CURVE ( 'NONE', #92142, #184550, #34625, .T. ) ;
#61695=CARTESIAN_POINT ( 'NONE',  ( 21.05000000000000071, 6.650000000011155876, -143.8438220896831297 ) ) ;
#61703=EDGE_CURVE ( 'NONE', #157963, #190865, #248583, .T. ) ;
#61720=FACE_OUTER_BOUND ( 'NONE', #198829, .T. ) ;
#61733=DIRECTION ( 'NONE',  ( -0.000000000000000000, -2.891205793294679805E-16, 1.000000000000000000 ) ) ;
#61735=DIRECTION ( 'NONE',  ( 1.000000000000000000, -0.000000000000000000, -0.000000000000000000 ) ) ;
#61736=CARTESIAN_POINT ( 'NONE',  ( -23.15000000000000213, -11.48912529306489994, -164.5000000000000000 ) ) ;
#61787=CIRCLE ( 'NONE', #228399, 0.09999999999998898659 ) ;
#61794=ORIENTED_EDGE ( 'NONE', *, *, #164123, .F. ) ;
#61806=ADVANCED_FACE ( 'NONE', ( #112929 ), #155930, .T. ) ;
#61816=CIRCLE ( 'NONE', #74327, 0.09999999999999939493 ) ;
#61822=CARTESIAN_POINT ( 'NONE',  ( 18.59999999999998721, 6.933893972137497030, -171.2856458343736108 ) ) ;
#61836=AXIS2_PLACEMENT_3D ( 'NONE', #122803, #163207, #242718 ) ;
#61913=AXIS2_PLACEMENT_3D ( 'NONE', #25002, #201044, #22434 ) ;
#61931=VERTEX_POINT ( 'NONE', #237995 ) ;
#61937=CYLINDRICAL_SURFACE ( 'NONE', #137664, 4.000000000000003553 ) ;
#61941=EDGE_CURVE ( 'NONE', #246557, #171400, #59703, .T. ) ;
#61951=CARTESIAN_POINT ( 'NONE',  ( -18.59999999999999787, 11.65000000001115232, -146.1500000000000341 ) ) ;
#61963=CARTESIAN_POINT ( 'NONE',  ( -21.05000000000000071, 1.115600667400684642E-11, -134.0000000000000000 ) ) ;
#61969=CIRCLE ( 'NONE', #3505, 11.69999999999998863 ) ;
#61971=EDGE_LOOP ( 'NONE', ( #213406, #74581, #72085, #108327 ) ) ;
#61984=CIRCLE ( 'NONE', #254076, 0.09999999999998898659 ) ;
#62071=ORIENTED_EDGE ( 'NONE', *, *, #82288, .T. ) ;
#62102=EDGE_CURVE ( 'NONE', #135871, #52558, #214038, .T. ) ;
#62140=EDGE_CURVE ( 'NONE', #59451, #246280, #122466, .T. ) ;
#62159=CARTESIAN_POINT ( 'NONE',  ( 21.05000000000000071, 1.115600667400684642E-11, -169.5000000000000284 ) ) ;
#62206=CARTESIAN_POINT ( 'NONE',  ( 20.94999999999999929, 6.550000000011156231, -144.0170271704400307 ) ) ;
#62210=CARTESIAN_POINT ( 'NONE',  ( 21.00000000000000000, 9.750000000011153745, -155.2500000000000284 ) ) ;
#62282=CIRCLE ( 'NONE', #244876, 0.09999999999998898659 ) ;
#62292=CYLINDRICAL_SURFACE ( 'NONE', #240686, 0.1000000000000101225 ) ;
#62323=CARTESIAN_POINT ( 'NONE',  ( -20.94999999999999929, 10.29270135741298731, -172.9573618871519614 ) ) ;
#62363=CARTESIAN_POINT ( 'NONE',  ( -18.50000000000000000, -26.43935341558978891, -152.1415086075074896 ) ) ;
#62375=CARTESIAN_POINT ( 'NONE',  ( 21.14999999999999858, 11.65000000001115943, -146.1500000000000341 ) ) ;
#62377=CARTESIAN_POINT ( 'NONE',  ( -23.25000000000000000, 1.115600667400684642E-11, -134.0000000000000000 ) ) ;
#62393=ORIENTED_EDGE ( 'NONE', *, *, #112189, .T. ) ;
#62413=EDGE_CURVE ( 'NONE', #180058, #24563, #64193, .T. ) ;
#62418=DIRECTION ( 'NONE',  ( 1.000000000000000000, -0.000000000000000000, -0.000000000000000000 ) ) ;
#62426=CARTESIAN_POINT ( 'NONE',  ( -21.44999999999999929, 7.350000000011155166, -146.2500000000000284 ) ) ;
#62446=ORIENTED_EDGE ( 'NONE', *, *, #125154, .T. ) ;
#62460=CYLINDRICAL_SURFACE ( 'NONE', #102069, 0.09999999999998898659 ) ;
#62475=VECTOR ( 'NONE', #76542, 1000.000000000000000 ) ;
#62526=TOROIDAL_SURFACE ( 'NONE', #112415, 12.97499999999999609, 0.1000000000000000056 ) ;
#62527=ORIENTED_EDGE ( 'NONE', *, *, #235512, .F. ) ;
#62563=DIRECTION ( 'NONE',  ( 1.000000000000000000, 0.000000000000000000, 0.000000000000000000 ) ) ;
#62584=ORIENTED_EDGE ( 'NONE', *, *, #128872, .F. ) ;
#62601=ORIENTED_EDGE ( 'NONE', *, *, #217978, .F. ) ;
#62651=AXIS2_PLACEMENT_3D ( 'NONE', #76228, #194927, #117923 ) ;
#62671=EDGE_CURVE ( 'NONE', #27654, #200535, #126143, .T. ) ;
#62674=CARTESIAN_POINT ( 'NONE',  ( -20.85000000000000142, 11.65000000001115232, -167.5000000000000284 ) ) ;
#62700=CARTESIAN_POINT ( 'NONE',  ( -20.85000000000000142, -1.835859311432481045, -179.0044391687985410 ) ) ;
#62708=ADVANCED_FACE ( 'NONE', ( #213997 ), #96581, .T. ) ;
#62710=ORIENTED_EDGE ( 'NONE', *, *, #184880, .F. ) ;
#62756=CARTESIAN_POINT ( 'NONE',  ( 18.59999999999999076, 11.75000000001115907, -122.2500000000000284 ) ) ;
#62770=EDGE_CURVE ( 'NONE', #101205, #226140, #177465, .T. ) ;
#62775=VERTEX_POINT ( 'NONE', #161746 ) ;
#62780=EDGE_CURVE ( 'NONE', #64013, #31307, #222963, .T. ) ;
#62790=AXIS2_PLACEMENT_3D ( 'NONE', #145734, #8811, #46622 ) ;
#62792=EDGE_LOOP ( 'NONE', ( #78969, #20459, #72634, #138316 ) ) ;
#62811=ORIENTED_EDGE ( 'NONE', *, *, #63496, .F. ) ;
#62816=CARTESIAN_POINT ( 'NONE',  ( 20.95262331984771009, 10.50415726280093409, -141.5608883295933822 ) ) ;
#62832=LINE ( 'NONE', #8009, #149176 ) ;
#62859=DIRECTION ( 'NONE',  ( -0.000000000000000000, 0.000000000000000000, -1.000000000000000000 ) ) ;
#62895=CARTESIAN_POINT ( 'NONE',  ( 21.05000000000000071, 6.540656951712400691, -134.1000000000000227 ) ) ;
#62914=EDGE_CURVE ( 'NONE', #46944, #37340, #66471, .T. ) ;
#62937=CARTESIAN_POINT ( 'NONE',  ( -20.54999999999999716, 1.115600667400684642E-11, -154.6250000000000284 ) ) ;
#62978=EDGE_CURVE ( 'NONE', #217227, #207656, #142884, .T. ) ;
#63017=ORIENTED_EDGE ( 'NONE', *, *, #157408, .T. ) ;
#63021=CARTESIAN_POINT ( 'NONE',  ( -20.54999999999999716, 2.000000000011154189, -147.2246219227621111 ) ) ;
#63023=CARTESIAN_POINT ( 'NONE',  ( 20.50589344625199217, 10.48318793148705197, -141.5729949786710336 ) ) ;
#63036=AXIS2_PLACEMENT_3D ( 'NONE', #134292, #15682, #235968 ) ;
#63079=PLANE ( 'NONE',  #70248 ) ;
#63088=CARTESIAN_POINT ( 'NONE',  ( 20.94999999999999574, 6.550000000011159784, -143.8438220896831581 ) ) ;
#63089=EDGE_CURVE ( 'NONE', #61093, #228115, #36014, .T. ) ;
#63099=FACE_OUTER_BOUND ( 'NONE', #213776, .T. ) ;
#63101=CARTESIAN_POINT ( 'NONE',  ( -23.25000000000000000, 7.021664781911246322, -171.3335654018973173 ) ) ;
#63123=DIRECTION ( 'NONE',  ( -1.000000000000000000, 0.000000000000000000, 0.000000000000000000 ) ) ;
#63132=LINE ( 'NONE', #142664, #80073 ) ;
#63150=VECTOR ( 'NONE', #38793, 1000.000000000000000 ) ;
#63155=VERTEX_POINT ( 'NONE', #104912 ) ;
#63157=ORIENTED_EDGE ( 'NONE', *, *, #37997, .F. ) ;
#63180=CARTESIAN_POINT ( 'NONE',  ( 23.14999999999999858, 5.900000000011162093, -157.2809002353436654 ) ) ;
#63202=TOROIDAL_SURFACE ( 'NONE', #96518, 0.6000000000000004219, 0.1000000000000000056 ) ;
#63261=EDGE_CURVE ( 'NONE', #86414, #93478, #147379, .T. ) ;
#63318=ORIENTED_EDGE ( 'NONE', *, *, #120941, .T. ) ;
#63336=CARTESIAN_POINT ( 'NONE',  ( 19.99999999738043144, 11.75000000001116263, -158.6871719496316473 ) ) ;
#63340=VERTEX_POINT ( 'NONE', #51362 ) ;
#63350=TOROIDAL_SURFACE ( 'NONE', #150850, 4.149999999999999467, 0.1000000000000000056 ) ;
#63356=CARTESIAN_POINT ( 'NONE',  ( 21.14999999999999858, 6.540656951712400691, -134.0000000000000000 ) ) ;
#63359=ORIENTED_EDGE ( 'NONE', *, *, #101839, .T. ) ;
#63420=TOROIDAL_SURFACE ( 'NONE', #230020, 0.4000000000000003553, 0.1000000000000000056 ) ;
#63441=CARTESIAN_POINT ( 'NONE',  ( 21.93340585971691326, 7.324147022868161550, -134.0000000000000000 ) ) ;
#63452=FACE_OUTER_BOUND ( 'NONE', #15242, .T. ) ;
#63477=DIRECTION ( 'NONE',  ( -1.000000000000000000, 0.000000000000000000, 0.000000000000000000 ) ) ;
#63496=EDGE_CURVE ( 'NONE', #96104, #153822, #218094, .T. ) ;
#63497=AXIS2_PLACEMENT_3D ( 'NONE', #144247, #146821, #189824 ) ;
#63502=CIRCLE ( 'NONE', #163480, 7.791421356237338003 ) ;
#63504=LINE ( 'NONE', #157867, #66909 ) ;
#63520=SPHERICAL_SURFACE ( 'NONE', #210440, 0.1000000000000000056 ) ;
#63540=ORIENTED_EDGE ( 'NONE', *, *, #241944, .T. ) ;
#63555=CARTESIAN_POINT ( 'NONE',  ( 22.41477678272288188, 0.0008238657741001855503, -122.3504147154846180 ) ) ;
#63576=DIRECTION ( 'NONE',  ( -3.469446951953635015E-14, 1.000000000000000000, 0.000000000000000000 ) ) ;
#63579=AXIS2_PLACEMENT_3D ( 'NONE', #149407, #71150, #234043 ) ;
#63598=LINE ( 'NONE', #37973, #177807 ) ;
#63634=CARTESIAN_POINT ( 'NONE',  ( -18.59999999999999787, -1.851028230129704522, -145.6539132694225032 ) ) ;
#63639=FACE_OUTER_BOUND ( 'NONE', #180546, .T. ) ;
#63669=EDGE_CURVE ( 'NONE', #154183, #11174, #159869, .T. ) ;
#63722=CARTESIAN_POINT ( 'NONE',  ( 23.14999999999999858, 1.115600667400684642E-11, -167.5000000000000284 ) ) ;
#63728=VERTEX_POINT ( 'NONE', #108502 ) ;
#63747=ORIENTED_EDGE ( 'NONE', *, *, #178575, .T. ) ;
#63800=DIRECTION ( 'NONE',  ( 1.000000000000000000, 0.000000000000000000, 0.000000000000000000 ) ) ;
#63850=CARTESIAN_POINT ( 'NONE',  ( 20.94999999999999929, -1.835341550213257733, -145.5551512925629822 ) ) ;
#63864=ORIENTED_EDGE ( 'NONE', *, *, #68917, .T. ) ;
#63868=TOROIDAL_SURFACE ( 'NONE', #168534, 0.4000000000000015210, 0.1000000000000000056 ) ;
#63880=ORIENTED_EDGE ( 'NONE', *, *, #168658, .T. ) ;
#63950=CARTESIAN_POINT ( 'NONE',  ( -21.14999999999999858, 11.65000000001115588, -134.1000000000000227 ) ) ;
#63952=VERTEX_POINT ( 'NONE', #55917 ) ;
#63964=VECTOR ( 'NONE', #140768, 999.9999999999998863 ) ;
#63976=ORIENTED_EDGE ( 'NONE', *, *, #244823, .F. ) ;
#64013=VERTEX_POINT ( 'NONE', #40267 ) ;
#64055=DIRECTION ( 'NONE',  ( 0.000000000000000000, 1.000000000000000000, -6.308085367188393199E-16 ) ) ;
#64107=CARTESIAN_POINT ( 'NONE',  ( 21.05000000000000071, 10.68429367439815891, -141.5266739386365771 ) ) ;
#64138=CARTESIAN_POINT ( 'NONE',  ( -20.64999999999999858, 7.250000000011155521, -155.1500000000000057 ) ) ;
#64161=DIRECTION ( 'NONE',  ( 0.000000000000000000, -1.000000000000000000, 0.000000000000000000 ) ) ;
#64187=EDGE_CURVE ( 'NONE', #206030, #41545, #53063, .T. ) ;
#64193=CIRCLE ( 'NONE', #126556, 0.09999999999998898659 ) ;
#64220=DIRECTION ( 'NONE',  ( -1.000000000000000000, -0.000000000000000000, -0.000000000000000000 ) ) ;
#64230=DIRECTION ( 'NONE',  ( 1.000000000000000000, 0.000000000000000000, -0.000000000000000000 ) ) ;
#64235=CARTESIAN_POINT ( 'NONE',  ( 23.14999999999999858, -3.999999999988843147, -167.5000000000000284 ) ) ;
#64247=VERTEX_POINT ( 'NONE', #70095 ) ;
#64280=ORIENTED_EDGE ( 'NONE', *, *, #27656, .F. ) ;
#64298=DIRECTION ( 'NONE',  ( 0.000000000000000000, -0.8700118002898321601, 0.4930308989875230030 ) ) ;
#64315=AXIS2_PLACEMENT_3D ( 'NONE', #71608, #208549, #151136 ) ;
#64323=VECTOR ( 'NONE', #124431, 1000.000000000000000 ) ;
#64336=DIRECTION ( 'NONE',  ( 0.000000000000000000, -1.000000000000000000, 0.000000000000000000 ) ) ;
#64347=VERTEX_POINT ( 'NONE', #15243 ) ;
#64362=CIRCLE ( 'NONE', #76821, 0.4000000000000114575 ) ;
#64374=ORIENTED_EDGE ( 'NONE', *, *, #12428, .T. ) ;
#64382=CARTESIAN_POINT ( 'NONE',  ( 22.39999999999999503, 11.75000000001115552, -134.0000000000000284 ) ) ;
#64443=VECTOR ( 'NONE', #159919, 1000.000000000000000 ) ;
#64486=EDGE_CURVE ( 'NONE', #239010, #105589, #152043, .T. ) ;
#64496=CIRCLE ( 'NONE', #222682, 0.5000000000000004441 ) ;
#64504=CARTESIAN_POINT ( 'NONE',  ( -21.44999999999999929, 7.350000000011155166, -155.1500000000000057 ) ) ;
#64515=DIRECTION ( 'NONE',  ( -2.602085213965226419E-14, -0.000000000000000000, 1.000000000000000000 ) ) ;
#64542=DIRECTION ( 'NONE',  ( -0.000000000000000000, -0.000000000000000000, -1.000000000000000000 ) ) ;
#64547=CIRCLE ( 'NONE', #210315, 0.1000000000000000472 ) ;
#64557=ORIENTED_EDGE ( 'NONE', *, *, #67634, .F. ) ;
#64597=CARTESIAN_POINT ( 'NONE',  ( -23.15000000000000213, 2.000000000011154189, -154.2753780772379173 ) ) ;
#64607=ORIENTED_EDGE ( 'NONE', *, *, #23175, .F. ) ;
#64608=DIRECTION ( 'NONE',  ( -1.000000000000000000, 0.000000000000000000, 0.000000000000000000 ) ) ;
#64628=DIRECTION ( 'NONE',  ( 0.000000000000000000, -0.9915357197604971473, 0.1298341882519111479 ) ) ;
#64629=ORIENTED_EDGE ( 'NONE', *, *, #29689, .F. ) ;
#64633=CARTESIAN_POINT ( 'NONE',  ( 19.87657994471988232, 11.75000000001116263, -158.7657881246250611 ) ) ;
#64634=CARTESIAN_POINT ( 'NONE',  ( -18.59999999999999787, 9.150000000011157653, -122.2500000000000284 ) ) ;
#64644=DIRECTION ( 'NONE',  ( -1.000000000000000000, -2.952720810173289112E-16, 0.000000000000000000 ) ) ;
#64681=CARTESIAN_POINT ( 'NONE',  ( -21.05000000000000071, 11.75000000001115552, -160.4851942293460638 ) ) ;
#64704=EDGE_CURVE ( 'NONE', #206150, #85588, #72947, .T. ) ;
#64709=CARTESIAN_POINT ( 'NONE',  ( -22.39999999999999858, 1.115600667400684642E-11, -134.0000000000000000 ) ) ;
#64733=ADVANCED_FACE ( 'NONE', ( #118855 ), #140985, .F. ) ;
#64765=CYLINDRICAL_SURFACE ( 'NONE', #220582, 0.09999999999999939493 ) ;
#64784=CARTESIAN_POINT ( 'NONE',  ( 18.39999999999999858, -9.499999999988844479, -174.1001893912220737 ) ) ;
#64794=CYLINDRICAL_SURFACE ( 'NONE', #229251, 0.09999999999998898659 ) ;
#64807=VERTEX_POINT ( 'NONE', #48286 ) ;
#64837=ORIENTED_EDGE ( 'NONE', *, *, #173074, .T. ) ;
#64869=FACE_OUTER_BOUND ( 'NONE', #226495, .T. ) ;
#64935=EDGE_CURVE ( 'NONE', #171037, #241225, #135627, .T. ) ;
#64943=ORIENTED_EDGE ( 'NONE', *, *, #192464, .T. ) ;
#64980=ORIENTED_EDGE ( 'NONE', *, *, #17937, .F. ) ;
#64988=CARTESIAN_POINT ( 'NONE',  ( -18.59999999999999787, 1.162701749949165642, -142.1000000000000227 ) ) ;
#65002=EDGE_CURVE ( 'NONE', #152770, #54116, #93941, .T. ) ;
#65113=CARTESIAN_POINT ( 'NONE',  ( 23.14999999999999858, 6.650000000011155876, -146.3500000000000227 ) ) ;
#65114=CARTESIAN_POINT ( 'NONE',  ( 18.46947024752513045, -9.509297157144889212, -140.9866894486979731 ) ) ;
#65123=VERTEX_POINT ( 'NONE', #122389 ) ;
#65138=ORIENTED_EDGE ( 'NONE', *, *, #41193, .T. ) ;
#65154=LINE ( 'NONE', #166872, #221264 ) ;
#65182=EDGE_LOOP ( 'NONE', ( #252302, #233847, #133543, #42280 ) ) ;
#65203=ORIENTED_EDGE ( 'NONE', *, *, #159609, .F. ) ;
#65216=CIRCLE ( 'NONE', #40327, 0.09999999999998898659 ) ;
#65225=ORIENTED_EDGE ( 'NONE', *, *, #172471, .F. ) ;
#65227=DIRECTION ( 'NONE',  ( 0.000000000000000000, -0.9999176327611369874, 0.01283462868041984617 ) ) ;
#65301=DIRECTION ( 'NONE',  ( 1.000000000000000000, -0.000000000000000000, -0.000000000000000000 ) ) ;
#65311=FACE_OUTER_BOUND ( 'NONE', #236544, .T. ) ;
#65323=CARTESIAN_POINT ( 'NONE',  ( -21.07928932188134041, 1.115600667400684642E-11, -134.0000000000000000 ) ) ;
#65359=TOROIDAL_SURFACE ( 'NONE', #40460, 0.2000000000000000111, 0.1000000000000000056 ) ;
#65369=ORIENTED_EDGE ( 'NONE', *, *, #1134, .F. ) ;
#65381=DIRECTION ( 'NONE',  ( 1.000000000000000000, -0.000000000000000000, -0.000000000000000000 ) ) ;
#65398=CARTESIAN_POINT ( 'NONE',  ( 20.94999999999999929, 5.000000000011153745, -146.4052660189131245 ) ) ;
#65450=VECTOR ( 'NONE', #179547, 1000.000000000000000 ) ;
#65476=DIRECTION ( 'NONE',  ( -1.000000000000000000, 0.000000000000000000, 0.000000000000000000 ) ) ;
#65486=AXIS2_PLACEMENT_3D ( 'NONE', #207703, #29096, #181708 ) ;
#65487=DIRECTION ( 'NONE',  ( 0.000000000000000000, 0.4999999999999543698, 0.8660254037844650199 ) ) ;
#65489=VERTEX_POINT ( 'NONE', #37422 ) ;
#65495=CARTESIAN_POINT ( 'NONE',  ( -20.05000000000000426, 9.250000000011157297, -146.3500000000000227 ) ) ;
#65512=DIRECTION ( 'NONE',  ( 0.000000000000000000, 1.000000000000000000, 0.000000000000000000 ) ) ;
#65575=DIRECTION ( 'NONE',  ( 0.000000000000000000, 0.4930308989875230585, 0.8700118002898322711 ) ) ;
#65578=DIRECTION ( 'NONE',  ( 0.000000000000000000, 0.000000000000000000, -1.000000000000000000 ) ) ;
#65605=DIRECTION ( 'NONE',  ( 0.000000000000000000, -1.000000000000000000, -0.000000000000000000 ) ) ;
#65633=ORIENTED_EDGE ( 'NONE', *, *, #110515, .F. ) ;
#65640=ORIENTED_EDGE ( 'NONE', *, *, #206833, .T. ) ;
#65649=DIRECTION ( 'NONE',  ( 0.000000000000000000, -1.000000000000000000, -0.000000000000000000 ) ) ;
#65737=AXIS2_PLACEMENT_3D ( 'NONE', #76188, #38366, #137438 ) ;
#65761=ORIENTED_EDGE ( 'NONE', *, *, #203258, .F. ) ;
#65766=ORIENTED_EDGE ( 'NONE', *, *, #144477, .T. ) ;
#65768=ADVANCED_FACE ( 'NONE', ( #111499 ), #50219, .F. ) ;
#65816=DIRECTION ( 'NONE',  ( 0.000000000000000000, -1.000000000000000000, 0.000000000000000000 ) ) ;
#65838=DIRECTION ( 'NONE',  ( -7.304098846218134667E-16, -1.000000000000000000, 0.000000000000000000 ) ) ;
#65852=TOROIDAL_SURFACE ( 'NONE', #128229, 0.6000000000000013101, 0.1000000000000000056 ) ;
#65894=LINE ( 'NONE', #245823, #35997 ) ;
#65921=LINE ( 'NONE', #46337, #121278 ) ;
#65926=CARTESIAN_POINT ( 'NONE',  ( 19.97071067695831559, 11.72071067696947644, -158.6762534328032075 ) ) ;
#65934=CARTESIAN_POINT ( 'NONE',  ( 18.55807992284871233, 10.32898536001801659, -173.0826683222764757 ) ) ;
#65941=AXIS2_PLACEMENT_3D ( 'NONE', #197202, #38152, #180228 ) ;
#65944=CARTESIAN_POINT ( 'NONE',  ( -18.59999999999999787, -1.835341550213255957, -145.5551512925629822 ) ) ;
#65991=CARTESIAN_POINT ( 'NONE',  ( -18.40904629823843663, -9.499999999988851584, -174.1001895624823135 ) ) ;
#66023=DIRECTION ( 'NONE',  ( 0.000000000000000000, 0.1350103645451904977, -0.9908441862701596881 ) ) ;
#66028=CARTESIAN_POINT ( 'NONE',  ( 21.00023020733501866, 1.115539681028482333E-11, -127.6091307547316518 ) ) ;
#66034=AXIS2_PLACEMENT_3D ( 'NONE', #71127, #88068, #150645 ) ;
#66046=DIRECTION ( 'NONE',  ( -6.938893903907224433E-15, 1.000000000000000000, 0.000000000000000000 ) ) ;
#66058=AXIS2_PLACEMENT_3D ( 'NONE', #190177, #87190, #251421 ) ;
#66092=DIRECTION ( 'NONE',  ( 0.000000000000000000, 0.000000000000000000, -1.000000000000000000 ) ) ;
#66096=ORIENTED_EDGE ( 'NONE', *, *, #244084, .T. ) ;
#66103=AXIS2_PLACEMENT_3D ( 'NONE', #108821, #206650, #163677 ) ;
#66107=LINE ( 'NONE', #45263, #188158 ) ;
#66145=ORIENTED_EDGE ( 'NONE', *, *, #43515, .F. ) ;
#66166=ORIENTED_EDGE ( 'NONE', *, *, #66804, .T. ) ;
#66172=CARTESIAN_POINT ( 'NONE',  ( 20.46382478191415188, 10.59862044130854031, -141.6778144693454919 ) ) ;
#66237=CARTESIAN_POINT ( 'NONE',  ( 18.59999999999999787, -1.851028230129704522, -145.6539132694225032 ) ) ;
#66242=DIRECTION ( 'NONE',  ( 0.000000000000000000, 0.000000000000000000, -1.000000000000000000 ) ) ;
#66295=ORIENTED_EDGE ( 'NONE', *, *, #148533, .F. ) ;
#66317=CARTESIAN_POINT ( 'NONE',  ( -21.05000000000000071, 6.400000000011158541, -143.9304246300615944 ) ) ;
#66342=AXIS2_PLACEMENT_3D ( 'NONE', #226246, #183303, #64628 ) ;
#66348=CARTESIAN_POINT ( 'NONE',  ( 22.40000000000010516, 1.020945751984553285E-11, -122.3504291924549108 ) ) ;
#66351=ORIENTED_EDGE ( 'NONE', *, *, #41822, .F. ) ;
#66357=DIRECTION ( 'NONE',  ( -0.000000000000000000, -0.000000000000000000, -1.000000000000000000 ) ) ;
#66391=EDGE_LOOP ( 'NONE', ( #10539, #16585, #113755, #48285 ) ) ;
#66407=CARTESIAN_POINT ( 'NONE',  ( 18.40000000000000213, -9.519327731081279609, -140.9729763765593304 ) ) ;
#66410=CARTESIAN_POINT ( 'NONE',  ( -20.94999999999999929, -1.736257131586239844, -145.5686523290175387 ) ) ;
#66425=CARTESIAN_POINT ( 'NONE',  ( 21.05000000000000071, 0.05148288189266662929, -127.6998201820867820 ) ) ;
#66431=LINE ( 'NONE', #149832, #20336 ) ;
#66439=SPHERICAL_SURFACE ( 'NONE', #59221, 0.1000000000000000056 ) ;
#66446=EDGE_CURVE ( 'NONE', #231169, #101967, #52964, .T. ) ;
#66457=CARTESIAN_POINT ( 'NONE',  ( -22.59999999999999787, 1.115600667400684642E-11, -134.0000000000000000 ) ) ;
#66464=AXIS2_PLACEMENT_3D ( 'NONE', #102772, #243597, #145764 ) ;
#66471=LINE ( 'NONE', #9060, #138771 ) ;
#66514=CARTESIAN_POINT ( 'NONE',  ( 21.14999999999998082, -11.74999999998884448, -134.0000000000000000 ) ) ;
#66551=ADVANCED_FACE ( 'NONE', ( #116985 ), #118273, .T. ) ;
#66570=ORIENTED_EDGE ( 'NONE', *, *, #147901, .F. ) ;
#66597=CARTESIAN_POINT ( 'NONE',  ( -21.05000000000000071, 1.115600667400684642E-11, -167.5000000000000284 ) ) ;
#66599=CARTESIAN_POINT ( 'NONE',  ( 23.14999999999998437, 1.115600667400684642E-11, -134.0000000000000000 ) ) ;
#66625=LINE ( 'NONE', #230853, #120831 ) ;
#66628=CARTESIAN_POINT ( 'NONE',  ( -18.59999999999999787, 5.341242990002807112, -124.1933497935119988 ) ) ;
#66644=LINE ( 'NONE', #243982, #220080 ) ;
#66649=EDGE_CURVE ( 'NONE', #159384, #217170, #77843, .T. ) ;
#66674=EDGE_CURVE ( 'NONE', #65489, #159084, #94852, .T. ) ;
#66680=CARTESIAN_POINT ( 'NONE',  ( -20.94999999999999929, 1.115600667400684642E-11, -134.0000000000000000 ) ) ;
#66696=DIRECTION ( 'NONE',  ( 0.000000000000000000, 0.000000000000000000, 1.000000000000000000 ) ) ;
#66698=DIRECTION ( 'NONE',  ( 0.000000000000000000, -0.1568667991644863147, 0.9876197685951252359 ) ) ;
#66715=EDGE_CURVE ( 'NONE', #22303, #18611, #174014, .T. ) ;
#66718=CARTESIAN_POINT ( 'NONE',  ( 21.05000000000000071, 11.75000000001115907, -160.4851942293460638 ) ) ;
#66721=EDGE_CURVE ( 'NONE', #62775, #99917, #207306, .T. ) ;
#66733=ORIENTED_EDGE ( 'NONE', *, *, #47955, .F. ) ;
#66752=ADVANCED_FACE ( 'NONE', ( #144225 ), #94354, .T. ) ;
#66757=DIRECTION ( 'NONE',  ( -0.000000000000000000, -0.000000000000000000, -1.000000000000000000 ) ) ;
#66780=CARTESIAN_POINT ( 'NONE',  ( -23.25000000000000000, 1.115600667400684642E-11, -167.5000000000000284 ) ) ;
#66792=ORIENTED_EDGE ( 'NONE', *, *, #178030, .T. ) ;
#66797=ORIENTED_EDGE ( 'NONE', *, *, #172201, .F. ) ;
#66804=EDGE_CURVE ( 'NONE', #86414, #148410, #161517, .T. ) ;
#66805=AXIS2_PLACEMENT_3D ( 'NONE', #30113, #207458, #146175 ) ;
#66816=ORIENTED_EDGE ( 'NONE', *, *, #179929, .T. ) ;
#66823=EDGE_CURVE ( 'NONE', #92094, #121951, #46116, .T. ) ;
#66832=ORIENTED_EDGE ( 'NONE', *, *, #44470, .F. ) ;
#66851=ORIENTED_EDGE ( 'NONE', *, *, #94401, .T. ) ;
#66853=CARTESIAN_POINT ( 'NONE',  ( 21.05000000000000071, 11.65000000001116298, -134.0000000000000000 ) ) ;
#66865=DIRECTION ( 'NONE',  ( -1.836970198721029934E-16, 1.000000000000000000, 0.000000000000000000 ) ) ;
#66868=ORIENTED_EDGE ( 'NONE', *, *, #143262, .F. ) ;
#66872=CARTESIAN_POINT ( 'NONE',  ( 21.05000000000000071, -0.09999999998884512298, -127.5229536182101384 ) ) ;
#66876=CYLINDRICAL_SURFACE ( 'NONE', #190691, 0.1000000000000000472 ) ;
#66888=CARTESIAN_POINT ( 'NONE',  ( 20.74625933824108870, 8.882913521095431975, -142.5551710241120986 ) ) ;
#66909=VECTOR ( 'NONE', #36625, 1000.000000000000000 ) ;
#66918=CARTESIAN_POINT ( 'NONE',  ( -21.14999999999999858, 11.75000000001115552, -134.1000000000000227 ) ) ;
#66946=ORIENTED_EDGE ( 'NONE', *, *, #245462, .T. ) ;
#66983=ORIENTED_EDGE ( 'NONE', *, *, #124086, .T. ) ;
#67061=EDGE_CURVE ( 'NONE', #221635, #174969, #29171, .T. ) ;
#67073=CARTESIAN_POINT ( 'NONE',  ( 20.94999999999999574, -1.360870587180885716, -142.0729979270909951 ) ) ;
#67108=ORIENTED_EDGE ( 'NONE', *, *, #211240, .T. ) ;
#67133=LINE ( 'NONE', #226167, #8602 ) ;
#67169=DIRECTION ( 'NONE',  ( 0.000000000000000000, 0.000000000000000000, -1.000000000000000000 ) ) ;
#67175=CARTESIAN_POINT ( 'NONE',  ( -21.05000000000000071, 1.115600667400684642E-11, -155.8000000000000398 ) ) ;
#67186=AXIS2_PLACEMENT_3D ( 'NONE', #66457, #2618, #41787 ) ;
#67198=FACE_OUTER_BOUND ( 'NONE', #178613, .T. ) ;
#67207=VERTEX_POINT ( 'NONE', #253296 ) ;
#67237=CIRCLE ( 'NONE', #117321, 11.75000000000001066 ) ;
#67279=VECTOR ( 'NONE', #173604, 1000.000000000000000 ) ;
#67344=CIRCLE ( 'NONE', #158959, 0.1000000000000089567 ) ;
#67347=ADVANCED_FACE ( 'NONE', ( #2819 ), #184035, .F. ) ;
#67357=DIRECTION ( 'NONE',  ( 1.000000000000000000, -0.000000000000000000, 0.000000000000000000 ) ) ;
#67393=CYLINDRICAL_SURFACE ( 'NONE', #175704, 4.000000000000003553 ) ;
#67394=CARTESIAN_POINT ( 'NONE',  ( -20.92356734117541706, 10.31973158071402175, -173.0505334713354841 ) ) ;
#67427=FACE_OUTER_BOUND ( 'NONE', #126772, .T. ) ;
#67429=AXIS2_PLACEMENT_3D ( 'NONE', #248240, #134689, #188261 ) ;
#67484=ORIENTED_EDGE ( 'NONE', *, *, #212828, .F. ) ;
#67515=LINE ( 'NONE', #47945, #71943 ) ;
#67572=DIRECTION ( 'NONE',  ( 1.000000000000000000, 0.000000000000000000, 0.000000000000000000 ) ) ;
#67582=ORIENTED_EDGE ( 'NONE', *, *, #60502, .F. ) ;
#67583=CARTESIAN_POINT ( 'NONE',  ( -21.07928932188134041, 0.09889514566555068775, -127.6714833436067238 ) ) ;
#67591=CARTESIAN_POINT ( 'NONE',  ( 21.14999999999999503, -11.74999999998883560, -136.9000000000000341 ) ) ;
#67595=LINE ( 'NONE', #48025, #191503 ) ;
#67619=FACE_OUTER_BOUND ( 'NONE', #49704, .T. ) ;
#67634=EDGE_CURVE ( 'NONE', #42134, #42010, #15575, .T. ) ;
#67744=VERTEX_POINT ( 'NONE', #124447 ) ;
#67804=EDGE_LOOP ( 'NONE', ( #7594, #220224, #130201, #47080, #1257 ) ) ;
#67899=DIRECTION ( 'NONE',  ( -1.000000000000000000, 0.000000000000000000, 0.000000000000000000 ) ) ;
#67902=CIRCLE ( 'NONE', #176076, 11.75000000000001066 ) ;
#67903=CYLINDRICAL_SURFACE ( 'NONE', #170487, 0.09999999999999939493 ) ;
#67909=VECTOR ( 'NONE', #2630, 1000.000000000000000 ) ;
#67938=FACE_OUTER_BOUND ( 'NONE', #201904, .T. ) ;
#67960=EDGE_CURVE ( 'NONE', #148690, #133237, #100680, .T. ) ;
#67979=CIRCLE ( 'NONE', #242936, 0.09999999999998898659 ) ;
#68011=AXIS2_PLACEMENT_3D ( 'NONE', #81923, #100216, #217600 ) ;
#68016=CARTESIAN_POINT ( 'NONE',  ( 18.53691006697058796, 10.30215155716188669, -158.7021987172990976 ) ) ;
#68017=TOROIDAL_SURFACE ( 'NONE', #238706, 0.9750000000000019762, 0.1000000000000000056 ) ;
#68096=CARTESIAN_POINT ( 'NONE',  ( -18.59999999999999787, -1.835859311432481045, -179.0044391687985410 ) ) ;
#68156=DIRECTION ( 'NONE',  ( -1.000000000000000000, 0.000000000000000000, 0.000000000000000000 ) ) ;
#68162=ADVANCED_FACE ( 'NONE', ( #206241 ), #246636, .F. ) ;
#68174=CARTESIAN_POINT ( 'NONE',  ( 20.19326291201655721, 10.15606098791450229, -141.7618618076040775 ) ) ;
#68225=ORIENTED_EDGE ( 'NONE', *, *, #95201, .T. ) ;
#68236=DIRECTION ( 'NONE',  ( 0.000000000000000000, -1.734723475983309083E-15, 1.000000000000000000 ) ) ;
#68266=LINE ( 'NONE', #238897, #82718 ) ;
#68313=EDGE_CURVE ( 'NONE', #239914, #125623, #95018, .T. ) ;
#68353=AXIS2_PLACEMENT_3D ( 'NONE', #211400, #148872, #228407 ) ;
#68374=ORIENTED_EDGE ( 'NONE', *, *, #166826, .F. ) ;
#68378=AXIS2_PLACEMENT_3D ( 'NONE', #153090, #136018, #215575 ) ;
#68396=ORIENTED_EDGE ( 'NONE', *, *, #46126, .T. ) ;
#68397=DIRECTION ( 'NONE',  ( -0.000000000000000000, -0.000000000000000000, 1.000000000000000000 ) ) ;
#68423=CARTESIAN_POINT ( 'NONE',  ( -20.94999999999999929, 1.115600667400684642E-11, -167.5000000000000284 ) ) ;
#68467=CARTESIAN_POINT ( 'NONE',  ( -22.59999999999999787, 11.74956712350054744, -133.8991416309013118 ) ) ;
#68518=ORIENTED_EDGE ( 'NONE', *, *, #157408, .F. ) ;
#68526=ORIENTED_EDGE ( 'NONE', *, *, #70853, .F. ) ;
#68543=CARTESIAN_POINT ( 'NONE',  ( 23.14999999999999858, 5.000000000011153745, -155.0947339810869323 ) ) ;
#68561=CIRCLE ( 'NONE', #243328, 0.1999999999999996503 ) ;
#68570=FACE_OUTER_BOUND ( 'NONE', #8714, .T. ) ;
#68575=EDGE_CURVE ( 'NONE', #180198, #182048, #165785, .T. ) ;
#68577=CARTESIAN_POINT ( 'NONE',  ( 21.17356465864818205, 0.09891124102502621418, -127.5771968737582966 ) ) ;
#68607=CARTESIAN_POINT ( 'NONE',  ( -18.39999999999999858, -9.499999999988849808, -141.0320693966996828 ) ) ;
#68609=DIRECTION ( 'NONE',  ( -1.000000000000000000, 0.000000000000000000, 0.000000000000000000 ) ) ;
#68644=LINE ( 'NONE', #223837, #256087 ) ;
#68680=VERTEX_POINT ( 'NONE', #15449 ) ;
#68726=FACE_OUTER_BOUND ( 'NONE', #192592, .T. ) ;
#68733=VERTEX_POINT ( 'NONE', #220046 ) ;
#68742=CIRCLE ( 'NONE', #106130, 4.000000000000003553 ) ;
#68746=DIRECTION ( 'NONE',  ( 0.000000000000000000, 0.000000000000000000, -1.000000000000000000 ) ) ;
#68790=ORIENTED_EDGE ( 'NONE', *, *, #181041, .T. ) ;
#68812=LINE ( 'NONE', #128783, #231143 ) ;
#68818=DIRECTION ( 'NONE',  ( 0.000000000000000000, 1.000000000000000000, 0.000000000000000000 ) ) ;
#68821=CARTESIAN_POINT ( 'NONE',  ( -23.15000000000000213, 1.115600667400684642E-11, -134.0000000000000000 ) ) ;
#68863=CARTESIAN_POINT ( 'NONE',  ( -21.08621493067320429, 0.05619483948720575828, -127.6507057088280845 ) ) ;
#68888=DIRECTION ( 'NONE',  ( 0.000000000000000000, 0.000000000000000000, -1.000000000000000000 ) ) ;
#68889=CARTESIAN_POINT ( 'NONE',  ( -18.59999999999999787, -1.162701749926853712, -142.1000000000000227 ) ) ;
#68906=AXIS2_PLACEMENT_3D ( 'NONE', #173818, #74704, #154245 ) ;
#68907=VECTOR ( 'NONE', #226965, 1000.000000000000000 ) ;
#68917=EDGE_CURVE ( 'NONE', #220002, #11174, #137351, .T. ) ;
#68941=ORIENTED_EDGE ( 'NONE', *, *, #107932, .F. ) ;
#68964=CARTESIAN_POINT ( 'NONE',  ( 20.94999999999999574, 1.851028230152016674, -145.6539132694225032 ) ) ;
#68975=EDGE_CURVE ( 'NONE', #216709, #129965, #245704, .T. ) ;
#68997=FACE_OUTER_BOUND ( 'NONE', #56444, .T. ) ;
#68999=AXIS2_PLACEMENT_3D ( 'NONE', #224103, #123740, #45475 ) ;
#69011=DIRECTION ( 'NONE',  ( 1.000000000000000000, -0.000000000000000000, -0.000000000000000000 ) ) ;
#69109=DIRECTION ( 'NONE',  ( 1.000000000000000000, 0.000000000000000000, 0.000000000000000000 ) ) ;
#69110=ORIENTED_EDGE ( 'NONE', *, *, #205051, .T. ) ;
#69123=ORIENTED_EDGE ( 'NONE', *, *, #21819, .F. ) ;
#69149=EDGE_CURVE ( 'NONE', #220754, #72588, #85334, .T. ) ;
#69178=EDGE_LOOP ( 'NONE', ( #76425, #216861, #101081, #167606, #27049 ) ) ;
#69209=FACE_OUTER_BOUND ( 'NONE', #4984, .T. ) ;
#69218=CIRCLE ( 'NONE', #223118, 0.5000000000000013323 ) ;
#69227=AXIS2_PLACEMENT_3D ( 'NONE', #146149, #47036, #225664 ) ;
#69238=DIRECTION ( 'NONE',  ( 1.000000000000000000, 2.952720810173289112E-16, -0.000000000000000000 ) ) ;
#69255=FACE_OUTER_BOUND ( 'NONE', #75545, .T. ) ;
#69273=ORIENTED_EDGE ( 'NONE', *, *, #57747, .T. ) ;
#69286=CIRCLE ( 'NONE', #214998, 0.09999999999999939493 ) ;
#69291=AXIS2_PLACEMENT_3D ( 'NONE', #123831, #45570, #188933 ) ;
#69302=VERTEX_POINT ( 'NONE', #81473 ) ;
#69314=CARTESIAN_POINT ( 'NONE',  ( -20.94999999999999929, 6.846123162363745074, -171.2377262668498759 ) ) ;
#69318=CARTESIAN_POINT ( 'NONE',  ( 22.39999999999999503, 1.115600667400684642E-11, -126.2092204016266379 ) ) ;
#69414=DIRECTION ( 'NONE',  ( 2.952720810173289112E-16, -1.000000000000000000, 0.000000000000000000 ) ) ;
#69491=AXIS2_PLACEMENT_3D ( 'NONE', #160910, #180462, #85167 ) ;
#69493=CARTESIAN_POINT ( 'NONE',  ( -23.25000000000000000, 4.350000000011156054, -155.1500000000000057 ) ) ;
#69495=ADVANCED_FACE ( 'NONE', ( #58728 ), #105975, .F. ) ;
#69511=VECTOR ( 'NONE', #79696, 1000.000000000000000 ) ;
#69527=ORIENTED_EDGE ( 'NONE', *, *, #98543, .F. ) ;
#69534=DIRECTION ( 'NONE',  ( 0.000000000000000000, 0.9915357197604792727, -0.1298341882520475943 ) ) ;
#69543=DIRECTION ( 'NONE',  ( 1.000000000000000000, 0.000000000000000000, 0.000000000000000000 ) ) ;
#69592=VECTOR ( 'NONE', #82968, 1000.000000000000000 ) ;
#69601=ORIENTED_EDGE ( 'NONE', *, *, #82564, .T. ) ;
#69608=AXIS2_PLACEMENT_3D ( 'NONE', #46034, #107295, #162160 ) ;
#69633=ORIENTED_EDGE ( 'NONE', *, *, #63496, .T. ) ;
#69643=CARTESIAN_POINT ( 'NONE',  ( -18.50000000000000000, 10.29270135741298375, -172.9573618871519614 ) ) ;
#69646=EDGE_CURVE ( 'NONE', #153155, #253265, #101686, .T. ) ;
#69647=VECTOR ( 'NONE', #109634, 1000.000000000000000 ) ;
#69657=CARTESIAN_POINT ( 'NONE',  ( 19.58285714285715073, 9.015001489659738354, -142.4206528160817413 ) ) ;
#69689=ORIENTED_EDGE ( 'NONE', *, *, #227667, .T. ) ;
#69733=CARTESIAN_POINT ( 'NONE',  ( 23.15000000000000213, -9.499999999988844479, -157.6060308773475640 ) ) ;
#69737=DIRECTION ( 'NONE',  ( 0.000000000000000000, 0.9915357197604971473, -0.1298341882519111479 ) ) ;
#69739=ORIENTED_EDGE ( 'NONE', *, *, #247540, .T. ) ;
#69753=ADVANCED_FACE ( 'NONE', ( #71616 ), #213674, .T. ) ;
#69799=DIRECTION ( 'NONE',  ( -0.000000000000000000, 0.8660254037844411501, 0.4999999999999956701 ) ) ;
#69814=DIRECTION ( 'NONE',  ( 1.000000000000000000, -0.000000000000000000, -0.000000000000000000 ) ) ;
#69846=CARTESIAN_POINT ( 'NONE',  ( -21.14999999999999858, 6.540656951712397138, -134.0000000000000000 ) ) ;
#69850=CIRCLE ( 'NONE', #86358, 0.09999999999999939493 ) ;
#69866=CARTESIAN_POINT ( 'NONE',  ( -18.53317502108577131, 10.32263460347359540, -173.0605957968672328 ) ) ;
#69867=FACE_OUTER_BOUND ( 'NONE', #10612, .T. ) ;
#69868=CYLINDRICAL_SURFACE ( 'NONE', #63579, 0.09999999999998898659 ) ;
#69881=LINE ( 'NONE', #108971, #212723 ) ;
#69917=EDGE_CURVE ( 'NONE', #50997, #61093, #64496, .T. ) ;
#69946=LINE ( 'NONE', #167768, #122395 ) ;
#69991=DIRECTION ( 'NONE',  ( -1.000000000000000000, 0.000000000000000000, 0.000000000000000000 ) ) ;
#69993=ORIENTED_EDGE ( 'NONE', *, *, #110290, .F. ) ;
#69995=VECTOR ( 'NONE', #126758, 999.9999999999998863 ) ;
#70002=( BOUNDED_SURFACE ( )  B_SPLINE_SURFACE ( 3, 2, ( 
 ( #80005, #179172, #218243 ),
 ( #42207, #220828, #96993 ),
 ( #22663, #181714, #82570 ),
 ( #159586, #239120, #235254 ),
 ( #197412, #216963, #139989 ),
 ( #219536, #136129, #117872 ) ),
 .UNSPECIFIED., .F., .F., .F. ) 
 B_SPLINE_SURFACE_WITH_KNOTS ( ( 4, 2, 4 ),
 ( 3, 3 ),
 ( 1.570796326794895448, 2.356194490192343505, 3.141592653589791784 ),
 ( 0.000000000000000000, 1.000000000000000000 ),
 .UNSPECIFIED. ) 
 GEOMETRIC_REPRESENTATION_ITEM ( )  RATIONAL_B_SPLINE_SURFACE ( (
 ( 1.000000000000000000, 0.7071067811865352493, 1.000000000000000000),
 ( 1.000000000000000000, 0.6611148371775558141, 1.000000000000000000),
 ( 1.000000000000000000, 0.6092287576700777807, 1.000000000000000000),
 ( 1.000000000000000000, 0.5278258667052361242, 1.000000000000000000),
 ( 1.000000000000000000, 0.4993418825338509226, 1.000000000000000000),
 ( 1.000000000000000000, 0.5000000000000260902, 1.000000000000000000) ) ) 
 REPRESENTATION_ITEM ( '' )  SURFACE ( )  );
#70022=AXIS2_PLACEMENT_3D ( 'NONE', #196093, #174005, #16191 ) ;
#70069=ADVANCED_FACE ( 'NONE', ( #67427 ), #123557, .T. ) ;
#70083=CYLINDRICAL_SURFACE ( 'NONE', #15347, 0.09999999999998898659 ) ;
#70095=CARTESIAN_POINT ( 'NONE',  ( 18.39999999999999858, -9.499999999988842703, -141.0320693966996828 ) ) ;
#70100=ORIENTED_EDGE ( 'NONE', *, *, #149399, .T. ) ;
#70128=AXIS2_PLACEMENT_3D ( 'NONE', #121533, #143622, #203603 ) ;
#70147=AXIS2_PLACEMENT_3D ( 'NONE', #117960, #137505, #119264 ) ;
#70152=AXIS2_PLACEMENT_3D ( 'NONE', #164061, #23289, #27147 ) ;
#70156=DIRECTION ( 'NONE',  ( 1.000000000000000000, -0.000000000000000000, -0.000000000000000000 ) ) ;
#70158=CARTESIAN_POINT ( 'NONE',  ( -21.05000000000000071, -0.2561057920810652089, -133.9651035583277121 ) ) ;
#70159=DIRECTION ( 'NONE',  ( 0.000000000000000000, 0.4999999999999478195, -0.8660254037844686836 ) ) ;
#70190=CARTESIAN_POINT ( 'NONE',  ( -21.00857864376268935, 11.60000000001115161, -140.9282032302755852 ) ) ;
#70214=DIRECTION ( 'NONE',  ( -1.000000000000000000, -0.000000000000000000, -0.000000000000000000 ) ) ;
#70228=EDGE_CURVE ( 'NONE', #4224, #179208, #249921, .T. ) ;
#70248=AXIS2_PLACEMENT_3D ( 'NONE', #145177, #190455, #230863 ) ;
#70269=AXIS2_PLACEMENT_3D ( 'NONE', #50844, #144822, #204794 ) ;
#70288=CARTESIAN_POINT ( 'NONE',  ( 23.24999999999999645, 5.600000000011153389, -155.0947339810869323 ) ) ;
#70299=VERTEX_POINT ( 'NONE', #217187 ) ;
#70332=ORIENTED_EDGE ( 'NONE', *, *, #138813, .F. ) ;
#70366=DIRECTION ( 'NONE',  ( 0.000000000000000000, 0.000000000000000000, -1.000000000000000000 ) ) ;
#70367=DIRECTION ( 'NONE',  ( 0.000000000000000000, 0.000000000000000000, -1.000000000000000000 ) ) ;
#70384=CARTESIAN_POINT ( 'NONE',  ( -20.54999999999999716, 1.115600667400684642E-11, -169.4000000000000625 ) ) ;
#70392=CARTESIAN_POINT ( 'NONE',  ( -20.85000000000000142, 7.070967871809997973, -171.2465642218683115 ) ) ;
#70397=ORIENTED_EDGE ( 'NONE', *, *, #5441, .T. ) ;
#70405=ORIENTED_EDGE ( 'NONE', *, *, #21428, .F. ) ;
#70418=ORIENTED_EDGE ( 'NONE', *, *, #36955, .T. ) ;
#70496=DIRECTION ( 'NONE',  ( 0.000000000000000000, -0.1298341882520022694, -0.9915357197604853789 ) ) ;
#70510=VECTOR ( 'NONE', #181405, 1000.000000000000000 ) ;
#70515=DIRECTION ( 'NONE',  ( -1.000000000000000000, 0.000000000000000000, 0.000000000000000000 ) ) ;
#70516=ORIENTED_EDGE ( 'NONE', *, *, #195646, .F. ) ;
#70556=CARTESIAN_POINT ( 'NONE',  ( 21.04105312098506531, 8.875332623054768888, -146.3285067472120602 ) ) ;
#70571=SPHERICAL_SURFACE ( 'NONE', #138466, 0.1000000000000000056 ) ;
#70604=SPHERICAL_SURFACE ( 'NONE', #10146, 0.1000000000000000056 ) ;
#70605=AXIS2_PLACEMENT_3D ( 'NONE', #9168, #84812, #169572 ) ;
#70612=ADVANCED_FACE ( 'NONE', ( #95660 ), #19056, .T. ) ;
#70625=ORIENTED_EDGE ( 'NONE', *, *, #6367, .T. ) ;
#70632=VERTEX_POINT ( 'NONE', #216890 ) ;
#70666=DIRECTION ( 'NONE',  ( 1.000000000000000000, 0.000000000000000000, 0.000000000000000000 ) ) ;
#70699=AXIS2_PLACEMENT_3D ( 'NONE', #17077, #168805, #114871 ) ;
#70733=CARTESIAN_POINT ( 'NONE',  ( -21.05000000000000071, 14.05000000001115623, -139.5136950707610026 ) ) ;
#70742=EDGE_CURVE ( 'NONE', #47961, #199368, #248214, .T. ) ;
#70747=FACE_OUTER_BOUND ( 'NONE', #39926, .T. ) ;
#70770=EDGE_LOOP ( 'NONE', ( #165642, #239667, #114976, #203945 ) ) ;
#70796=CIRCLE ( 'NONE', #216511, 0.09999999999999820144 ) ;
#70853=EDGE_CURVE ( 'NONE', #201727, #123059, #9402, .T. ) ;
#70862=AXIS2_PLACEMENT_3D ( 'NONE', #185868, #144158, #202861 ) ;
#70880=ORIENTED_EDGE ( 'NONE', *, *, #218294, .F. ) ;
#70910=ORIENTED_EDGE ( 'NONE', *, *, #43515, .T. ) ;
#70949=CIRCLE ( 'NONE', #216662, 4.099999999999992539 ) ;
#70959=CARTESIAN_POINT ( 'NONE',  ( -20.05000000000000426, 9.250000000011157297, -155.2500000000000284 ) ) ;
#70997=DIRECTION ( 'NONE',  ( 0.000000000000000000, -1.000000000000000000, 0.000000000000000000 ) ) ;
#71001=VERTEX_POINT ( 'NONE', #87202 ) ;
#71015=CARTESIAN_POINT ( 'NONE',  ( 20.85000000000000142, 1.115600667400684642E-11, -167.5000000000000284 ) ) ;
#71025=CARTESIAN_POINT ( 'NONE',  ( -20.64999999999999858, 4.350000000011156054, -155.1500000000000057 ) ) ;
#71032=DIRECTION ( 'NONE',  ( 0.000000000000000000, 0.8660254037844384856, -0.5000000000000003331 ) ) ;
#71083=LINE ( 'NONE', #209281, #193736 ) ;
#71093=LINE ( 'NONE', #149354, #218427 ) ;
#71113=AXIS2_PLACEMENT_3D ( 'NONE', #168033, #44205, #247531 ) ;
#71127=CARTESIAN_POINT ( 'NONE',  ( -20.94999999999999929, -11.64999999998884306, -164.4000000000000057 ) ) ;
#71135=DIRECTION ( 'NONE',  ( -1.000000000000000000, -0.000000000000000000, -0.000000000000000000 ) ) ;
#71147=CARTESIAN_POINT ( 'NONE',  ( 21.05000000000000071, 1.115600667400684642E-11, -167.5000000000000284 ) ) ;
#71148=CARTESIAN_POINT ( 'NONE',  ( -18.50016250449483124, 10.29766095125282988, -172.9743663933276139 ) ) ;
#71150=DIRECTION ( 'NONE',  ( 1.000000000000000000, 0.000000000000000000, 0.000000000000000000 ) ) ;
#71161=TOROIDAL_SURFACE ( 'NONE', #25380, 0.4000000000000009104, 0.1000000000000000056 ) ;
#71192=ADVANCED_FACE ( 'NONE', ( #64869 ), #46577, .F. ) ;
#71240=CARTESIAN_POINT ( 'NONE',  ( -20.54999999999999716, 1.115600667400684642E-11, -146.9749999999999943 ) ) ;
#71303=EDGE_CURVE ( 'NONE', #125623, #46813, #248557, .T. ) ;
#71305=CARTESIAN_POINT ( 'NONE',  ( -21.14999999999999858, 11.75000000001115552, -134.0000000000000284 ) ) ;
#71309=CIRCLE ( 'NONE', #217009, 7.899999999999990585 ) ;
#71325=CARTESIAN_POINT ( 'NONE',  ( 23.15000000000000213, -8.596261682231833845, -143.4501275171502925 ) ) ;
#71335=EDGE_CURVE ( 'NONE', #91812, #106067, #165175, .T. ) ;
#71344=CARTESIAN_POINT ( 'NONE',  ( -23.15000000000000213, 1.115600667400684642E-11, -167.5000000000000284 ) ) ;
#71346=EDGE_CURVE ( 'NONE', #199368, #156063, #158558, .T. ) ;
#71393=ORIENTED_EDGE ( 'NONE', *, *, #9330, .F. ) ;
#71416=LINE ( 'NONE', #173113, #22644 ) ;
#71422=EDGE_LOOP ( 'NONE', ( #34132, #93622, #37467, #211239 ) ) ;
#71435=EDGE_CURVE ( 'NONE', #220754, #116282, #77664, .T. ) ;
#71448=LINE ( 'NONE', #169285, #41909 ) ;
#71454=VECTOR ( 'NONE', #14407, 1000.000000000000000 ) ;
#71515=( BOUNDED_SURFACE ( )  B_SPLINE_SURFACE ( 3, 2, ( 
 ( #57795, #158242, #156945 ),
 ( #36998, #115221, #55214 ),
 ( #95648, #137333, #93081 ),
 ( #153111, #59063, #254684 ),
 ( #233886, #53958, #214326 ),
 ( #255962, #35717, #176499 ) ),
 .UNSPECIFIED., .F., .F., .F. ) 
 B_SPLINE_SURFACE_WITH_KNOTS ( ( 4, 2, 4 ),
 ( 3, 3 ),
 ( 0.0001792624049599545865, 0.0003686986002124574124, 0.0005581347954649602382 ),
 ( 0.000000000000000000, 1.000000000000000000 ),
 .UNSPECIFIED. ) 
 GEOMETRIC_REPRESENTATION_ITEM ( )  RATIONAL_B_SPLINE_SURFACE ( (
 ( 1.000000000000000000, 0.9238795325112828527, 1.000000000000000000),
 ( 1.000000000000000000, 0.9229318695241007786, 1.000000000000000000),
 ( 1.000000000000000000, 0.8926288119227357987, 1.000000000000000000),
 ( 1.000000000000000000, 0.8123777807274511487, 1.000000000000000000),
 ( 1.000000000000000000, 0.7629087100929119458, 1.000000000000000000),
 ( 1.000000000000000000, 0.7071067811865475727, 1.000000000000000000) ) ) 
 REPRESENTATION_ITEM ( '' )  SURFACE ( )  );
#71535=EDGE_LOOP ( 'NONE', ( #191029, #241294, #22520, #22596 ) ) ;
#71579=CARTESIAN_POINT ( 'NONE',  ( -18.59999999999999787, 11.65000000001115232, -141.0148057706540214 ) ) ;
#71582=DIRECTION ( 'NONE',  ( 0.000000000000000000, 0.000000000000000000, -1.000000000000000000 ) ) ;
#71596=CARTESIAN_POINT ( 'NONE',  ( -20.64999999999999858, 7.150000000011155876, -146.3500000000000227 ) ) ;
#71607=CARTESIAN_POINT ( 'NONE',  ( -21.04999999999999716, 6.307425219576570541, -134.0168198683856815 ) ) ;
#71608=CARTESIAN_POINT ( 'NONE',  ( -20.94999999999999929, -12.41227409413852811, -164.5000000000000000 ) ) ;
#71609=ORIENTED_EDGE ( 'NONE', *, *, #42460, .T. ) ;
#71616=FACE_OUTER_BOUND ( 'NONE', #3724, .T. ) ;
#71651=DIRECTION ( 'NONE',  ( 0.000000000000000000, -1.000000000000000000, 0.000000000000000000 ) ) ;
#71655=TOROIDAL_SURFACE ( 'NONE', #4972, 0.2000000000000000111, 0.1000000000000000056 ) ;
#71656=ORIENTED_EDGE ( 'NONE', *, *, #167361, .F. ) ;
#71657=EDGE_CURVE ( 'NONE', #137714, #121616, #148624, .T. ) ;
#71667=CIRCLE ( 'NONE', #59136, 0.09999999999999178990 ) ;
#71683=EDGE_LOOP ( 'NONE', ( #78241, #27992, #80291, #89584 ) ) ;
#71730=AXIS2_PLACEMENT_3D ( 'NONE', #83293, #162888, #80733 ) ;
#71803=CYLINDRICAL_SURFACE ( 'NONE', #121195, 11.80000000000000426 ) ;
#71819=ORIENTED_EDGE ( 'NONE', *, *, #209243, .T. ) ;
#71825=DIRECTION ( 'NONE',  ( 1.000000000000000000, -0.000000000000000000, -0.000000000000000000 ) ) ;
#71839=AXIS2_PLACEMENT_3D ( 'NONE', #242874, #65512, #223295 ) ;
#71867=ADVANCED_FACE ( 'NONE', ( #104638 ), #123865, .T. ) ;
#71878=ORIENTED_EDGE ( 'NONE', *, *, #45512, .T. ) ;
#71886=CARTESIAN_POINT ( 'NONE',  ( 18.49999999999999289, 10.44006789215405639, -158.7671177488814465 ) ) ;
#71920=DIRECTION ( 'NONE',  ( -0.000000000000000000, 0.000000000000000000, 1.000000000000000000 ) ) ;
#71943=VECTOR ( 'NONE', #187490, 1000.000000000000000 ) ;
#71974=EDGE_LOOP ( 'NONE', ( #251773, #105357, #107370, #229864 ) ) ;
#72025=LINE ( 'NONE', #191987, #228280 ) ;
#72033=ORIENTED_EDGE ( 'NONE', *, *, #102296, .T. ) ;
#72064=ORIENTED_EDGE ( 'NONE', *, *, #136992, .F. ) ;
#72085=ORIENTED_EDGE ( 'NONE', *, *, #110445, .F. ) ;
#72116=ORIENTED_EDGE ( 'NONE', *, *, #256300, .F. ) ;
#72163=EDGE_CURVE ( 'NONE', #175143, #155422, #219126, .T. ) ;
#72168=DIRECTION ( 'NONE',  ( -2.252264143451594314E-15, -0.1298341882520124002, -0.9915357197604841577 ) ) ;
#72176=CIRCLE ( 'NONE', #1221, 0.09999999999999971412 ) ;
#72190=DIRECTION ( 'NONE',  ( 2.827886303505249259E-16, -0.8660254037844411501, -0.4999999999999956701 ) ) ;
#72205=VECTOR ( 'NONE', #175534, 1000.000000000000000 ) ;
#72256=EDGE_CURVE ( 'NONE', #161970, #109286, #31740, .T. ) ;
#72267=AXIS2_PLACEMENT_3D ( 'NONE', #94259, #212938, #12191 ) ;
#72271=ORIENTED_EDGE ( 'NONE', *, *, #55736, .T. ) ;
#72273=AXIS2_PLACEMENT_3D ( 'NONE', #254519, #193304, #14684 ) ;
#72285=CIRCLE ( 'NONE', #14033, 0.09999999999999439892 ) ;
#72289=DIRECTION ( 'NONE',  ( -1.000000000000000000, -0.000000000000000000, -0.000000000000000000 ) ) ;
#72324=ORIENTED_EDGE ( 'NONE', *, *, #63261, .F. ) ;
#72329=AXIS2_PLACEMENT_3D ( 'NONE', #146867, #67357, #105146 ) ;
#72363=DIRECTION ( 'NONE',  ( 0.000000000000000000, 0.1350103645451904977, 0.9908441862701596881 ) ) ;
#72396=ADVANCED_FACE ( 'NONE', ( #15231 ), #70083, .T. ) ;
#72415=EDGE_CURVE ( 'NONE', #9008, #117471, #152729, .T. ) ;
#72432=PLANE ( 'NONE',  #19971 ) ;
#72448=DIRECTION ( 'NONE',  ( 0.000000000000000000, 0.000000000000000000, -1.000000000000000000 ) ) ;
#72462=CYLINDRICAL_SURFACE ( 'NONE', #42509, 0.09999999999999881206 ) ;
#72476=CIRCLE ( 'NONE', #193275, 0.5000000000000004441 ) ;
#72478=VECTOR ( 'NONE', #158221, 1000.000000000000000 ) ;
#72487=DIRECTION ( 'NONE',  ( 1.000000000000000000, -0.000000000000000000, -0.000000000000000000 ) ) ;
#72512=DIRECTION ( 'NONE',  ( 0.000000000000000000, 7.993605777301153912E-15, -1.000000000000000000 ) ) ;
#72518=VECTOR ( 'NONE', #195720, 1000.000000000000000 ) ;
#72519=CARTESIAN_POINT ( 'NONE',  ( 18.59999999999999432, -9.480686695267811714, -174.4411151687578752 ) ) ;
#72539=PLANE ( 'NONE',  #120579 ) ;
#72560=ORIENTED_EDGE ( 'NONE', *, *, #241944, .F. ) ;
#72588=VERTEX_POINT ( 'NONE', #79007 ) ;
#72603=ORIENTED_EDGE ( 'NONE', *, *, #179540, .F. ) ;
#72614=ORIENTED_EDGE ( 'NONE', *, *, #71435, .F. ) ;
#72628=AXIS2_PLACEMENT_3D ( 'NONE', #92222, #114366, #34857 ) ;
#72634=ORIENTED_EDGE ( 'NONE', *, *, #87008, .T. ) ;
#72635=ORIENTED_EDGE ( 'NONE', *, *, #75259, .T. ) ;
#72640=AXIS2_PLACEMENT_3D ( 'NONE', #125451, #146278, #225797 ) ;
#72651=AXIS2_PLACEMENT_3D ( 'NONE', #7484, #206977, #88279 ) ;
#72685=CARTESIAN_POINT ( 'NONE',  ( -23.25000000000000000, -11.48912529306489994, -164.4000000000000057 ) ) ;
#72699=DIRECTION ( 'NONE',  ( 0.000000000000000000, 0.000000000000000000, -1.000000000000000000 ) ) ;
#72704=DIRECTION ( 'NONE',  ( 0.000000000000000000, 0.000000000000000000, 1.000000000000000000 ) ) ;
#72718=EDGE_CURVE ( 'NONE', #79888, #200654, #65894, .T. ) ;
#72759=DIRECTION ( 'NONE',  ( 1.000000000000000000, 3.265361837132813093E-16, -0.000000000000000000 ) ) ;
#72782=VERTEX_POINT ( 'NONE', #249677 ) ;
#72838=FACE_OUTER_BOUND ( 'NONE', #71535, .T. ) ;
#72846=VECTOR ( 'NONE', #105470, 1000.000000000000000 ) ;
#72857=DIRECTION ( 'NONE',  ( 0.000000000000000000, 0.1350103645451904977, -0.9908441862701596881 ) ) ;
#72873=LINE ( 'NONE', #87246, #117854 ) ;
#72891=DIRECTION ( 'NONE',  ( 0.000000000000000000, 0.000000000000000000, 1.000000000000000000 ) ) ;
#72928=AXIS2_PLACEMENT_3D ( 'NONE', #30382, #89040, #225955 ) ;
#72947=CIRCLE ( 'NONE', #218643, 0.09999999999999939493 ) ;
#72957=ORIENTED_EDGE ( 'NONE', *, *, #148933, .T. ) ;
#72970=EDGE_LOOP ( 'NONE', ( #166366, #35497, #174007, #199531 ) ) ;
#73001=CARTESIAN_POINT ( 'NONE',  ( 23.25000000000000000, -8.596261682231828516, -158.0498724828497359 ) ) ;
#73020=EDGE_CURVE ( 'NONE', #21693, #20940, #103407, .T. ) ;
#73074=AXIS2_PLACEMENT_3D ( 'NONE', #120932, #223828, #200440 ) ;
#73090=FACE_OUTER_BOUND ( 'NONE', #24757, .T. ) ;
#73136=VERTEX_POINT ( 'NONE', #87703 ) ;
#73145=ADVANCED_FACE ( 'NONE', ( #49875 ), #248077, .T. ) ;
#73156=FACE_OUTER_BOUND ( 'NONE', #214156, .T. ) ;
#73162=EDGE_CURVE ( 'NONE', #203670, #70299, #217918, .T. ) ;
#73194=CIRCLE ( 'NONE', #243838, 0.09999999999998898659 ) ;
#73199=CARTESIAN_POINT ( 'NONE',  ( 18.49505832270841310, -9.438028062771731896, -141.1984731748938771 ) ) ;
#73203=CARTESIAN_POINT ( 'NONE',  ( 20.85000000000000142, 7.021664781911246322, -171.3335654018973173 ) ) ;
#73215=EDGE_CURVE ( 'NONE', #204820, #190865, #102970, .T. ) ;
#73222=VERTEX_POINT ( 'NONE', #176277 ) ;
#73244=DIRECTION ( 'NONE',  ( 0.000000000000000000, 1.000000000000000000, 0.000000000000000000 ) ) ;
#73247=EDGE_CURVE ( 'NONE', #17738, #244686, #207241, .T. ) ;
#73273=AXIS2_PLACEMENT_3D ( 'NONE', #189083, #129111, #10451 ) ;
#73296=EDGE_LOOP ( 'NONE', ( #168482, #196756, #174304, #29440 ) ) ;
#73323=VERTEX_POINT ( 'NONE', #243916 ) ;
#73334=DIRECTION ( 'NONE',  ( 0.000000000000000000, 0.000000000000000000, -1.000000000000000000 ) ) ;
#73373=TOROIDAL_SURFACE ( 'NONE', #60656, 0.4000000000000017431, 0.1000000000000000056 ) ;
#73374=DIRECTION ( 'NONE',  ( -1.000000000000000000, -0.000000000000000000, -0.000000000000000000 ) ) ;
#73406=CARTESIAN_POINT ( 'NONE',  ( 18.49999999999999645, -1.637172712959225507, -145.5821533654720383 ) ) ;
#73448=CARTESIAN_POINT ( 'NONE',  ( -23.15000000000000213, 4.350000000011156054, -155.2500000000000284 ) ) ;
#73462=CARTESIAN_POINT ( 'NONE',  ( 20.94999999999999929, 1.115600667400684642E-11, -167.5000000000000284 ) ) ;
#73488=CARTESIAN_POINT ( 'NONE',  ( 18.59999999999999076, 14.05000000001116689, -139.5136950707610026 ) ) ;
#73496=DIRECTION ( 'NONE',  ( -1.000000000000000000, -2.952720810173289112E-16, 0.000000000000000000 ) ) ;
#73505=ORIENTED_EDGE ( 'NONE', *, *, #252470, .T. ) ;
#73509=CYLINDRICAL_SURFACE ( 'NONE', #162877, 0.5000000000000004441 ) ;
#73553=ADVANCED_FACE ( 'NONE', ( #157713 ), #78216, .F. ) ;
#73572=CARTESIAN_POINT ( 'NONE',  ( 21.05193202509564898, 10.72393601970834354, -146.1725346033257722 ) ) ;
#73585=FACE_OUTER_BOUND ( 'NONE', #166907, .T. ) ;
#73599=CIRCLE ( 'NONE', #219306, 0.09999999999999939493 ) ;
#73608=ORIENTED_EDGE ( 'NONE', *, *, #9246, .T. ) ;
#73681=DIRECTION ( 'NONE',  ( 0.000000000000000000, -1.000000000000000000, -5.551115123125777653E-14 ) ) ;
#73703=SPHERICAL_SURFACE ( 'NONE', #223088, 0.1000000000000000056 ) ;
#73710=CARTESIAN_POINT ( 'NONE',  ( 21.09706851349341861, 8.775842513484549912, -146.2355662163996612 ) ) ;
#73720=DIRECTION ( 'NONE',  ( 0.000000000000000000, -0.9915357197604853789, 0.1298341882520022694 ) ) ;
#73727=CARTESIAN_POINT ( 'NONE',  ( 21.12642695952774474, 0.09890328320052040045, -127.6243400779648596 ) ) ;
#73736=CARTESIAN_POINT ( 'NONE',  ( 22.50000000000000000, 1.115600667400684642E-11, -134.0000000000000000 ) ) ;
#73738=CIRCLE ( 'NONE', #61250, 0.09999999999998898659 ) ;
#73769=FACE_OUTER_BOUND ( 'NONE', #194177, .T. ) ;
#73806=AXIS2_PLACEMENT_3D ( 'NONE', #424, #203776, #22590 ) ;
#73834=VERTEX_POINT ( 'NONE', #149678 ) ;
#73866=( BOUNDED_SURFACE ( )  B_SPLINE_SURFACE ( 3, 2, ( 
 ( #165854, #8056, #227079 ),
 ( #191851, #189259, #250495 ),
 ( #68016, #146258, #187975 ),
 ( #9324, #167155, #88838 ),
 ( #249235, #71886, #32782 ),
 ( #48448, #130550, #168460 ) ),
 .UNSPECIFIED., .F., .F., .T. ) 
 B_SPLINE_SURFACE_WITH_KNOTS ( ( 4, 2, 4 ),
 ( 3, 3 ),
 ( 3.141592653589793116, 3.926990816987241395, 4.712388980384689674 ),
 ( 0.000000000000000000, 1.000000000000000000 ),
 .UNSPECIFIED. ) 
 GEOMETRIC_REPRESENTATION_ITEM ( )  RATIONAL_B_SPLINE_SURFACE ( (
 ( 1.000000000000000000, 0.9238795325112820755, 1.000000000000000000),
 ( 1.000000000000000000, 0.9240297172239489987, 1.000000000000000000),
 ( 1.000000000000000000, 0.9038128468044698272, 1.000000000000000000),
 ( 1.000000000000000000, 0.8282379607644166919, 1.000000000000000000),
 ( 1.000000000000000000, 0.7727932973495217350, 1.000000000000000000),
 ( 1.000000000000000000, 0.7071067811865475727, 1.000000000000000000) ) ) 
 REPRESENTATION_ITEM ( '' )  SURFACE ( )  );
#73872=ORIENTED_EDGE ( 'NONE', *, *, #153955, .T. ) ;
#73887=CARTESIAN_POINT ( 'NONE',  ( -20.85000000000000142, 11.65000000001115232, -160.7161343370219129 ) ) ;
#73910=ORIENTED_EDGE ( 'NONE', *, *, #192730, .T. ) ;
#73932=PLANE ( 'NONE',  #85691 ) ;
#73941=AXIS2_PLACEMENT_3D ( 'NONE', #171430, #226184, #69737 ) ;
#73971=CARTESIAN_POINT ( 'NONE',  ( 20.95017935633852346, 10.47548927963648246, -141.5774397973904968 ) ) ;
#73981=CARTESIAN_POINT ( 'NONE',  ( -20.94999999999999929, 14.05000000001115623, -161.9863049292391111 ) ) ;
#73993=CIRCLE ( 'NONE', #61496, 12.87499999999999822 ) ;
#73995=CARTESIAN_POINT ( 'NONE',  ( -21.04999999999999716, 0.01485563490459204140, -127.6556409579560949 ) ) ;
#74025=LINE ( 'NONE', #114397, #87386 ) ;
#74048=CARTESIAN_POINT ( 'NONE',  ( 20.94999999999999929, 1.115600667400684642E-11, -167.5000000000000284 ) ) ;
#74067=EDGE_CURVE ( 'NONE', #140417, #991, #25243, .T. ) ;
#74080=DIRECTION ( 'NONE',  ( 0.000000000000000000, 6.505213034913742890E-15, -1.000000000000000000 ) ) ;
#74113=TOROIDAL_SURFACE ( 'NONE', #190619, 0.2000000000000000111, 0.1000000000000000056 ) ;
#74127=CARTESIAN_POINT ( 'NONE',  ( -23.15000000000000213, 4.350000000011156054, -146.3500000000000227 ) ) ;
#74146=FACE_OUTER_BOUND ( 'NONE', #111235, .T. ) ;
#74187=LINE ( 'NONE', #115842, #141971 ) ;
#74246=CIRCLE ( 'NONE', #128379, 0.09999999999998898659 ) ;
#74327=AXIS2_PLACEMENT_3D ( 'NONE', #46560, #123554, #184800 ) ;
#74330=CARTESIAN_POINT ( 'NONE',  ( -23.25000000000000000, 2.000000000011154189, -154.2753780772379173 ) ) ;
#74399=EDGE_CURVE ( 'NONE', #159790, #220173, #110732, .T. ) ;
#74423=CARTESIAN_POINT ( 'NONE',  ( -18.59999999999999787, 1.115600667400684642E-11, -167.5000000000000284 ) ) ;
#74461=CYLINDRICAL_SURFACE ( 'NONE', #24351, 0.1000000000000028644 ) ;
#74474=ADVANCED_FACE ( 'NONE', ( #1016 ), #216236, .F. ) ;
#74543=SPHERICAL_SURFACE ( 'NONE', #84859, 0.1000000000000000056 ) ;
#74573=DIRECTION ( 'NONE',  ( 0.000000000000000000, -4.336808689942494997E-15, -1.000000000000000000 ) ) ;
#74580=CARTESIAN_POINT ( 'NONE',  ( -21.05000000000000071, -12.41227409413852811, -164.6000000000000227 ) ) ;
#74581=ORIENTED_EDGE ( 'NONE', *, *, #78318, .T. ) ;
#74599=CIRCLE ( 'NONE', #16317, 0.1999999999999996503 ) ;
#74613=ORIENTED_EDGE ( 'NONE', *, *, #144300, .F. ) ;
#74634=ORIENTED_EDGE ( 'NONE', *, *, #252470, .F. ) ;
#74641=CARTESIAN_POINT ( 'NONE',  ( -20.85000000000000142, 7.021664781911246322, -171.2335654018973230 ) ) ;
#74670=AXIS2_PLACEMENT_3D ( 'NONE', #89383, #230188, #48981 ) ;
#74704=DIRECTION ( 'NONE',  ( -1.000000000000000000, 0.000000000000000000, 0.000000000000000000 ) ) ;
#74728=CARTESIAN_POINT ( 'NONE',  ( -23.15000000000000213, 11.65000000001115588, -160.4851942293460638 ) ) ;
#74756=DIRECTION ( 'NONE',  ( -1.000000000000000000, -2.952720810173289112E-16, 0.000000000000000000 ) ) ;
#74761=DIRECTION ( 'NONE',  ( 0.000000000000000000, -1.000000000000000000, 0.000000000000000000 ) ) ;
#74813=CARTESIAN_POINT ( 'NONE',  ( 21.05000000000000071, 1.835341550235569663, -145.5551512925629822 ) ) ;
#74840=CIRCLE ( 'NONE', #228933, 0.1999999999999987899 ) ;
#74841=CARTESIAN_POINT ( 'NONE',  ( -23.25000000000000000, -1.851617760457748618, -179.1031897196036766 ) ) ;
#74844=ORIENTED_EDGE ( 'NONE', *, *, #214250, .F. ) ;
#74860=DIRECTION ( 'NONE',  ( 2.952720810173289112E-16, -1.000000000000000000, 0.000000000000000000 ) ) ;
#74914=DIRECTION ( 'NONE',  ( -1.000000000000000000, -0.000000000000000000, -0.000000000000000000 ) ) ;
#74916=CARTESIAN_POINT ( 'NONE',  ( -21.05000000000000071, 1.835341550235567887, -145.5551512925629822 ) ) ;
#74936=DIRECTION ( 'NONE',  ( 0.000000000000000000, 0.000000000000000000, -1.000000000000000000 ) ) ;
#74969=( BOUNDED_SURFACE ( )  B_SPLINE_SURFACE ( 3, 2, ( 
 ( #161587, #216395, #160307 ),
 ( #141987, #101552, #182427 ),
 ( #221513, #237254, #122445 ),
 ( #57303, #58590, #138126 ) ),
 .UNSPECIFIED., .F., .F., .F. ) 
 B_SPLINE_SURFACE_WITH_KNOTS ( ( 4, 4 ),
 ( 3, 3 ),
 ( 0.0006461284895273765793, 0.0007503702773986197947 ),
 ( 0.000000000000000000, 1.000000000000000000 ),
 .UNSPECIFIED. ) 
 GEOMETRIC_REPRESENTATION_ITEM ( )  RATIONAL_B_SPLINE_SURFACE ( (
 ( 1.000000000000000000, 0.7071067811865475727, 1.000000000000000000),
 ( 1.000000000000000000, 0.7076476444648808206, 1.000000000000000000),
 ( 1.000000000000000000, 0.7075727925191797052, 1.000000000000000000),
 ( 1.000000000000000000, 0.7071067811865581199, 1.000000000000000000) ) ) 
 REPRESENTATION_ITEM ( '' )  SURFACE ( )  );
#74975=ORIENTED_EDGE ( 'NONE', *, *, #50290, .T. ) ;
#75002=EDGE_CURVE ( 'NONE', #207677, #226065, #153844, .T. ) ;
#75021=CARTESIAN_POINT ( 'NONE',  ( -23.15000000000000213, 11.75000000001116263, -146.1500000000000341 ) ) ;
#75027=DIRECTION ( 'NONE',  ( 1.000000000000000000, 0.000000000000000000, 0.000000000000000000 ) ) ;
#75052=AXIS2_PLACEMENT_3D ( 'NONE', #31669, #80698, #216372 ) ;
#75054=FACE_OUTER_BOUND ( 'NONE', #55666, .T. ) ;
#75083=VECTOR ( 'NONE', #186270, 1000.000000000000000 ) ;
#75089=EDGE_CURVE ( 'NONE', #158190, #178251, #157937, .T. ) ;
#75090=CARTESIAN_POINT ( 'NONE',  ( 21.10320863425824811, 6.400277386470322405, -133.9749777487728579 ) ) ;
#75095=ORIENTED_EDGE ( 'NONE', *, *, #112576, .T. ) ;
#75096=CARTESIAN_POINT ( 'NONE',  ( 18.31325810956334266, -9.536388475996066205, -174.3684402063047969 ) ) ;
#75099=AXIS2_PLACEMENT_3D ( 'NONE', #124306, #40941, #81285 ) ;
#75109=CARTESIAN_POINT ( 'NONE',  ( -22.48660254037843487, 11.65000000001115588, -133.9500000000000455 ) ) ;
#75139=EDGE_CURVE ( 'NONE', #220244, #170581, #145580, .T. ) ;
#75172=DIRECTION ( 'NONE',  ( 0.000000000000000000, 0.000000000000000000, 1.000000000000000000 ) ) ;
#75183=AXIS2_PLACEMENT_3D ( 'NONE', #248793, #207097, #229231 ) ;
#75245=EDGE_CURVE ( 'NONE', #128128, #16470, #241459, .T. ) ;
#75254=CARTESIAN_POINT ( 'NONE',  ( 23.14999999999999503, 11.75000000001116263, -122.2500000000000284 ) ) ;
#75259=EDGE_CURVE ( 'NONE', #35508, #54116, #70796, .T. ) ;
#75265=CARTESIAN_POINT ( 'NONE',  ( 23.14999999999998792, 11.65000000001115588, -134.0000000000000000 ) ) ;
#75271=B_SPLINE_CURVE_WITH_KNOTS ( 'NONE', 3,
 ( #69318, #151425, #148855, #31492 ),
 .UNSPECIFIED., .F., .F.,
 ( 4, 4 ),
 ( 0.000000000000000000, 0.001767853679387121216 ),
 .UNSPECIFIED. ) ;
#75300=EDGE_CURVE ( 'NONE', #144444, #214790, #246059, .T. ) ;
#75306=CARTESIAN_POINT ( 'NONE',  ( -21.05000000000000071, 6.413662734880722027, -134.0855928633627911 ) ) ;
#75353=DIRECTION ( 'NONE',  ( 1.000000000000000000, -0.000000000000000000, -0.000000000000000000 ) ) ;
#75356=CARTESIAN_POINT ( 'NONE',  ( 18.59999999999999076, 7.120270961708750512, -171.1595630418393625 ) ) ;
#75373=CYLINDRICAL_SURFACE ( 'NONE', #243346, 0.5000000000000004441 ) ;
#75423=DIRECTION ( 'NONE',  ( 0.000000000000000000, 0.000000000000000000, 1.000000000000000000 ) ) ;
#75467=EDGE_CURVE ( 'NONE', #233607, #23909, #160787, .T. ) ;
#75470=CIRCLE ( 'NONE', #171167, 0.09999999999998898659 ) ;
#75473=CYLINDRICAL_SURFACE ( 'NONE', #54714, 0.09999999999999939493 ) ;
#75545=EDGE_LOOP ( 'NONE', ( #116498, #76618, #133524, #20824 ) ) ;
#75562=DIRECTION ( 'NONE',  ( -0.000000000000000000, -0.000000000000000000, 1.000000000000000000 ) ) ;
#75574=DIRECTION ( 'NONE',  ( -1.000000000000000000, 0.000000000000000000, 0.000000000000000000 ) ) ;
#75596=ORIENTED_EDGE ( 'NONE', *, *, #203419, .F. ) ;
#75638=ADVANCED_FACE ( 'NONE', ( #188033 ), #154208, .T. ) ;
#75650=DIRECTION ( 'NONE',  ( 1.000000000000000000, -0.000000000000000000, -0.000000000000000000 ) ) ;
#75719=CYLINDRICAL_SURFACE ( 'NONE', #86846, 0.09999999999999939493 ) ;
#75746=CIRCLE ( 'NONE', #46672, 11.80000000000000249 ) ;
#75749=DIRECTION ( 'NONE',  ( -1.000000000000000000, 0.000000000000000000, 0.000000000000000000 ) ) ;
#75803=ORIENTED_EDGE ( 'NONE', *, *, #10574, .F. ) ;
#75826=ORIENTED_EDGE ( 'NONE', *, *, #85609, .F. ) ;
#75857=ORIENTED_EDGE ( 'NONE', *, *, #253669, .F. ) ;
#75864=DIRECTION ( 'NONE',  ( 0.000000000000000000, 0.000000000000000000, 1.000000000000000000 ) ) ;
#75875=CIRCLE ( 'NONE', #167480, 0.09999999999998898659 ) ;
#75879=VERTEX_POINT ( 'NONE', #215288 ) ;
#75911=DIRECTION ( 'NONE',  ( 0.000000000000000000, -1.000000000000000000, -0.000000000000000000 ) ) ;
#75913=AXIS2_PLACEMENT_3D ( 'NONE', #221009, #106191, #183195 ) ;
#75915=AXIS2_PLACEMENT_3D ( 'NONE', #140650, #39007, #22007 ) ;
#75926=EDGE_CURVE ( 'NONE', #8049, #63952, #216866, .T. ) ;
#75944=CARTESIAN_POINT ( 'NONE',  ( -20.85000000000000142, 11.75000000001115552, -167.5000000000000284 ) ) ;
#75953=CARTESIAN_POINT ( 'NONE',  ( -20.64999999999999858, 2.400000000011155432, -147.2246219227621111 ) ) ;
#75971=CARTESIAN_POINT ( 'NONE',  ( 23.14999999999999503, 11.65000000001116298, -155.3500000000000227 ) ) ;
#75995=TOROIDAL_SURFACE ( 'NONE', #21826, 0.2000000000000000111, 0.1000000000000000056 ) ;
#75996=ORIENTED_EDGE ( 'NONE', *, *, #119405, .F. ) ;
#76075=EDGE_CURVE ( 'NONE', #224095, #170589, #241816, .T. ) ;
#76087=ORIENTED_EDGE ( 'NONE', *, *, #170281, .F. ) ;
#76101=ADVANCED_FACE ( 'NONE', ( #165607 ), #203440, .T. ) ;
#76123=ORIENTED_EDGE ( 'NONE', *, *, #150856, .F. ) ;
#76148=CARTESIAN_POINT ( 'NONE',  ( 18.59999999999999076, 6.400000000011158541, -143.9304246300615944 ) ) ;
#76161=CIRCLE ( 'NONE', #96975, 2.000000000000002665 ) ;
#76167=VECTOR ( 'NONE', #41581, 1000.000000000000000 ) ;
#76188=CARTESIAN_POINT ( 'NONE',  ( 21.97500000000000497, 9.750000000011153745, -146.3500000000000227 ) ) ;
#76206=ORIENTED_EDGE ( 'NONE', *, *, #163708, .T. ) ;
#76208=FACE_OUTER_BOUND ( 'NONE', #229924, .T. ) ;
#76209=SURFACE_STYLE_FILL_AREA ( #154517 ) ;
#76228=CARTESIAN_POINT ( 'NONE',  ( -18.59999999999999787, 1.162701749949165642, -142.1000000000000227 ) ) ;
#76264=CARTESIAN_POINT ( 'NONE',  ( 20.94999999999999574, 1.835341550235569663, -145.5551512925629822 ) ) ;
#76268=DIRECTION ( 'NONE',  ( -0.000000000000000000, 0.000000000000000000, -1.000000000000000000 ) ) ;
#76290=CARTESIAN_POINT ( 'NONE',  ( -22.24259225415828567, 7.491937870576586889, -133.9009341165471483 ) ) ;
#76311=FACE_OUTER_BOUND ( 'NONE', #221856, .T. ) ;
#76384=VECTOR ( 'NONE', #52254, 1000.000000000000000 ) ;
#76385=DIRECTION ( 'NONE',  ( -0.7071067811865388020, 0.7071067811865561215, 0.000000000000000000 ) ) ;
#76399=DIRECTION ( 'NONE',  ( -0.000000000000000000, 0.000000000000000000, -1.000000000000000000 ) ) ;
#76400=ORIENTED_EDGE ( 'NONE', *, *, #95880, .T. ) ;
#76417=CARTESIAN_POINT ( 'NONE',  ( -21.02374657821563630, 11.60000000083177696, -160.5717967701983184 ) ) ;
#76425=ORIENTED_EDGE ( 'NONE', *, *, #185104, .F. ) ;
#76428=EDGE_CURVE ( 'NONE', #246321, #4110, #221135, .T. ) ;
#76469=ORIENTED_EDGE ( 'NONE', *, *, #238486, .T. ) ;
#76490=ORIENTED_EDGE ( 'NONE', *, *, #119877, .T. ) ;
#76496=DIRECTION ( 'NONE',  ( 1.000000000000000000, 2.952720810173289112E-16, -0.000000000000000000 ) ) ;
#76497=FACE_OUTER_BOUND ( 'NONE', #29004, .T. ) ;
#76501=DIRECTION ( 'NONE',  ( -1.000000000000000000, -3.265361837132813093E-16, 0.000000000000000000 ) ) ;
#76507=DIRECTION ( 'NONE',  ( -0.000000000000000000, -0.9875055080513799322, 0.1575844902526464253 ) ) ;
#76513=CARTESIAN_POINT ( 'NONE',  ( -21.14999999999999503, 1.115524773248610657E-11, -127.4593430482987912 ) ) ;
#76523=LINE ( 'NONE', #115667, #31977 ) ;
#76526=ORIENTED_EDGE ( 'NONE', *, *, #32228, .F. ) ;
#76541=VERTEX_POINT ( 'NONE', #251210 ) ;
#76542=DIRECTION ( 'NONE',  ( 0.000000000000000000, 0.000000000000000000, 1.000000000000000000 ) ) ;
#76548=CARTESIAN_POINT ( 'NONE',  ( -21.07928932188134041, 6.328516656409861163, -133.9011048543453910 ) ) ;
#76564=DIRECTION ( 'NONE',  ( 0.000000000000000000, 0.000000000000000000, -1.000000000000000000 ) ) ;
#76575=CARTESIAN_POINT ( 'NONE',  ( 18.59999999999999076, 6.650000000011155876, -155.1500000000000057 ) ) ;
#76587=DIRECTION ( 'NONE',  ( 0.000000000000000000, 0.000000000000000000, -1.000000000000000000 ) ) ;
#76601=CARTESIAN_POINT ( 'NONE',  ( -18.59999999999999787, -1.851617760457748618, -179.1031897196036766 ) ) ;
#76615=VECTOR ( 'NONE', #203110, 1000.000000000000000 ) ;
#76618=ORIENTED_EDGE ( 'NONE', *, *, #192110, .T. ) ;
#76636=DIRECTION ( 'NONE',  ( -1.000000000000000000, -3.265361837132813093E-16, 0.000000000000000000 ) ) ;
#76642=EDGE_CURVE ( 'NONE', #180800, #98196, #212971, .T. ) ;
#76662=CARTESIAN_POINT ( 'NONE',  ( -20.94999999999999929, 1.360870587203197646, -142.0729979270909951 ) ) ;
#76667=EDGE_LOOP ( 'NONE', ( #2062, #58437, #145290, #88150, #122117 ) ) ;
#76689=CARTESIAN_POINT ( 'NONE',  ( 20.95443524775735256, 8.878554263883964737, -142.5337222756001552 ) ) ;
#76694=CARTESIAN_POINT ( 'NONE',  ( 22.39999999999999503, 7.790779598384535376, -134.0000000000000000 ) ) ;
#76704=TOROIDAL_SURFACE ( 'NONE', #1690, 0.2000000000000000111, 0.1000000000000000056 ) ;
#76724=EDGE_CURVE ( 'NONE', #56702, #196380, #246289, .T. ) ;
#76742=LINE ( 'NONE', #156323, #188869 ) ;
#76777=EDGE_LOOP ( 'NONE', ( #46930, #67108, #217572, #7207 ) ) ;
#76786=ORIENTED_EDGE ( 'NONE', *, *, #101478, .F. ) ;
#76795=DIRECTION ( 'NONE',  ( 1.000000000000000000, 0.000000000000000000, 0.000000000000000000 ) ) ;
#76819=DIRECTION ( 'NONE',  ( 1.000000000000000000, 0.000000000000000000, 0.000000000000000000 ) ) ;
#76821=AXIS2_PLACEMENT_3D ( 'NONE', #112109, #96351, #58506 ) ;
#76833=DIRECTION ( 'NONE',  ( 7.304098846218134667E-16, -1.000000000000000000, 0.000000000000000000 ) ) ;
#76835=CARTESIAN_POINT ( 'NONE',  ( -18.59999999999999787, 9.350000000011156942, -155.1500000000000057 ) ) ;
#76862=DIRECTION ( 'NONE',  ( 1.000000000000000000, -0.000000000000000000, -0.000000000000000000 ) ) ;
#76867=ORIENTED_EDGE ( 'NONE', *, *, #253669, .T. ) ;
#76878=CARTESIAN_POINT ( 'NONE',  ( -18.59999999999999787, 11.65000000001115232, -141.0148057706539930 ) ) ;
#76943=EDGE_CURVE ( 'NONE', #7645, #178157, #189672, .T. ) ;
#76947=DIRECTION ( 'NONE',  ( -0.7071067811865475727, -0.7071067811865475727, -0.000000000000000000 ) ) ;
#76949=DIRECTION ( 'NONE',  ( 0.000000000000000000, 0.000000000000000000, -1.000000000000000000 ) ) ;
#76955=VECTOR ( 'NONE', #222907, 1000.000000000000000 ) ;
#76974=DIRECTION ( 'NONE',  ( 0.000000000000000000, 0.000000000000000000, 1.000000000000000000 ) ) ;
#76976=AXIS2_PLACEMENT_3D ( 'NONE', #112278, #109678, #9306 ) ;
#76984=ORIENTED_EDGE ( 'NONE', *, *, #211034, .T. ) ;
#76992=EDGE_LOOP ( 'NONE', ( #225842, #53711, #252737, #227648 ) ) ;
#76995=EDGE_CURVE ( 'NONE', #236521, #63340, #191773, .T. ) ;
#77012=CARTESIAN_POINT ( 'NONE',  ( -23.25000000000000000, 1.115650265596050101E-11, -129.9500000000000171 ) ) ;
#77030=EDGE_CURVE ( 'NONE', #242592, #180754, #121033, .T. ) ;
#77033=ORIENTED_EDGE ( 'NONE', *, *, #171027, .F. ) ;
#77054=CARTESIAN_POINT ( 'NONE',  ( 18.59999999999999432, 1.162701749949165642, -142.1000000000000227 ) ) ;
#77063=AXIS2_PLACEMENT_3D ( 'NONE', #17540, #97046, #159642 ) ;
#77071=DIRECTION ( 'NONE',  ( 0.000000000000000000, -0.8777080977375715243, 0.4791956752370512551 ) ) ;
#77114=CARTESIAN_POINT ( 'NONE',  ( 21.14999999999999858, -11.74999999998884448, -146.2500000000000284 ) ) ;
#77137=CARTESIAN_POINT ( 'NONE',  ( 18.59999999999999787, 1.851028230152016674, -145.6539132694225032 ) ) ;
#77153=ORIENTED_EDGE ( 'NONE', *, *, #17203, .F. ) ;
#77160=CARTESIAN_POINT ( 'NONE',  ( -20.64999999999999858, -9.499999999988848032, -143.8939691226524644 ) ) ;
#77211=CARTESIAN_POINT ( 'NONE',  ( 20.85000000000000142, -1.835859311432481045, -179.1044391687985353 ) ) ;
#77239=CIRCLE ( 'NONE', #164745, 0.09999999999998898659 ) ;
#77272=ORIENTED_EDGE ( 'NONE', *, *, #120941, .F. ) ;
#77278=CARTESIAN_POINT ( 'NONE',  ( -18.39999999999999858, -9.499999999988849808, -174.1001893912220737 ) ) ;
#77315=CARTESIAN_POINT ( 'NONE',  ( -18.50000000000000000, 5.341242990002803559, -124.1933497935119988 ) ) ;
#77342=FACE_OUTER_BOUND ( 'NONE', #154941, .T. ) ;
#77365=DIRECTION ( 'NONE',  ( 0.000000000000000000, 0.000000000000000000, -1.000000000000000000 ) ) ;
#77366=ORIENTED_EDGE ( 'NONE', *, *, #178, .F. ) ;
#77374=ADVANCED_FACE ( 'NONE', ( #198014 ), #372, .F. ) ;
#77380=ORIENTED_EDGE ( 'NONE', *, *, #217623, .F. ) ;
#77384=DIRECTION ( 'NONE',  ( -0.000000000000000000, 0.8660254037844411501, 0.4999999999999956146 ) ) ;
#77398=CARTESIAN_POINT ( 'NONE',  ( 22.50000000000000000, 0.1000000000111554016, -122.3504291924552234 ) ) ;
#77427=ADVANCED_FACE ( 'NONE', ( #257948 ), #18101, .T. ) ;
#77475=VECTOR ( 'NONE', #239653, 999.9999999999998863 ) ;
#77498=ORIENTED_EDGE ( 'NONE', *, *, #216083, .T. ) ;
#77532=DIRECTION ( 'NONE',  ( -1.000000000000000000, 0.000000000000000000, 0.000000000000000000 ) ) ;
#77565=DIRECTION ( 'NONE',  ( 0.000000000000000000, 0.000000000000000000, -1.000000000000000000 ) ) ;
#77570=ORIENTED_EDGE ( 'NONE', *, *, #195398, .T. ) ;
#77572=CARTESIAN_POINT ( 'NONE',  ( 20.94999999999999574, 1.835341550235567887, -145.5551512925629822 ) ) ;
#77594=CARTESIAN_POINT ( 'NONE',  ( 21.05000000000000071, -1.835341550213257733, -145.5551512925629822 ) ) ;
#77602=ADVANCED_FACE ( 'NONE', ( #247409 ), #83175, .F. ) ;
#77625=CARTESIAN_POINT ( 'NONE',  ( 23.14999999999999503, 11.65000000001116298, -155.2500000000000284 ) ) ;
#77664=CIRCLE ( 'NONE', #173612, 0.09999999999998898659 ) ;
#77691=CARTESIAN_POINT ( 'NONE',  ( -20.85000000000000142, 7.021664781911246322, -171.3335654018973173 ) ) ;
#77696=ORIENTED_EDGE ( 'NONE', *, *, #236887, .T. ) ;
#77707=CARTESIAN_POINT ( 'NONE',  ( 20.94999999999999929, -8.730841121484166578, -157.9019252810156786 ) ) ;
#77728=CIRCLE ( 'NONE', #52794, 0.1000000000000043493 ) ;
#77737=CARTESIAN_POINT ( 'NONE',  ( 22.59999999999999432, 11.74987124438766273, -133.9345704089863318 ) ) ;
#77759=CARTESIAN_POINT ( 'NONE',  ( 18.59999999999999432, -1.162701749926853712, -142.1000000000000227 ) ) ;
#77764=ORIENTED_EDGE ( 'NONE', *, *, #75926, .T. ) ;
#77775=AXIS2_PLACEMENT_3D ( 'NONE', #232840, #235375, #77565 ) ;
#77808=CARTESIAN_POINT ( 'NONE',  ( -21.05000000000000071, 6.540656951712397138, -134.1000000000000227 ) ) ;
#77809=CARTESIAN_POINT ( 'NONE',  ( -21.14250536705909411, 1.115548662937858831E-11, -127.4818278231192608 ) ) ;
#77810=DIRECTION ( 'NONE',  ( 0.000000000000000000, 1.265107689135680095E-16, -1.000000000000000000 ) ) ;
#77816=DIRECTION ( 'NONE',  ( 0.000000000000000000, 0.000000000000000000, -1.000000000000000000 ) ) ;
#77820=ORIENTED_EDGE ( 'NONE', *, *, #80395, .T. ) ;
#77843=LINE ( 'NONE', #154853, #65450 ) ;
#77861=DIRECTION ( 'NONE',  ( 1.224646799147353207E-16, 1.000000000000000000, 0.000000000000000000 ) ) ;
#77914=CARTESIAN_POINT ( 'NONE',  ( -21.55000000000000071, 7.250000000011155521, -146.3500000000000227 ) ) ;
#78010=CARTESIAN_POINT ( 'NONE',  ( -21.59142135623730852, 7.850000000011158718, -146.2500000000000284 ) ) ;
#78013=DIRECTION ( 'NONE',  ( -3.265361837132813093E-16, 1.000000000000000000, 0.000000000000000000 ) ) ;
#78032=EDGE_CURVE ( 'NONE', #11174, #41773, #240270, .T. ) ;
#78040=ORIENTED_EDGE ( 'NONE', *, *, #195890, .T. ) ;
#78051=DIRECTION ( 'NONE',  ( 1.000000000000000000, -0.000000000000000000, -0.000000000000000000 ) ) ;
#78070=B_SPLINE_CURVE_WITH_KNOTS ( 'NONE', 3,
 ( #82850, #97275, #77737, #99854 ),
 .UNSPECIFIED., .F., .F.,
 ( 4, 4 ),
 ( 3.469446951953614189E-18, 0.0001058379652594581074 ),
 .UNSPECIFIED. ) ;
#78095=AXIS2_PLACEMENT_3D ( 'NONE', #216070, #119571, #180816 ) ;
#78102=DIRECTION ( 'NONE',  ( 0.000000000000000000, 0.000000000000000000, 1.000000000000000000 ) ) ;
#78175=CARTESIAN_POINT ( 'NONE',  ( -18.50000000000000000, 9.150000000011157653, -155.1500000000000057 ) ) ;
#78181=AXIS2_PLACEMENT_3D ( 'NONE', #231365, #189658, #16180 ) ;
#78196=DIRECTION ( 'NONE',  ( 1.000000000000000000, 0.000000000000000000, 0.000000000000000000 ) ) ;
#78216=TOROIDAL_SURFACE ( 'NONE', #57357, 0.2000000000000000111, 0.1000000000000000056 ) ;
#78232=DIRECTION ( 'NONE',  ( 0.000000000000000000, 0.000000000000000000, -1.000000000000000000 ) ) ;
#78241=ORIENTED_EDGE ( 'NONE', *, *, #28793, .T. ) ;
#78318=EDGE_CURVE ( 'NONE', #198298, #215317, #163719, .T. ) ;
#78337=EDGE_CURVE ( 'NONE', #200852, #140838, #15953, .T. ) ;
#78340=DIRECTION ( 'NONE',  ( 0.000000000000000000, 0.000000000000000000, -1.000000000000000000 ) ) ;
#78347=DIRECTION ( 'NONE',  ( 0.000000000000000000, 0.000000000000000000, 1.000000000000000000 ) ) ;
#78380=CARTESIAN_POINT ( 'NONE',  ( -18.50000000000000000, 11.65000000001115232, -146.1500000000000341 ) ) ;
#78388=EDGE_LOOP ( 'NONE', ( #184092, #133425, #5257, #79640, #101871 ) ) ;
#78428=CARTESIAN_POINT ( 'NONE',  ( -20.94999999999999929, 1.115600667400684642E-11, -134.0000000000000000 ) ) ;
#78433=EDGE_LOOP ( 'NONE', ( #246448, #83335, #213644, #124507 ) ) ;
#78441=CIRCLE ( 'NONE', #32522, 0.09999999999999992228 ) ;
#78475=CARTESIAN_POINT ( 'NONE',  ( 21.05000000000000071, 11.75000000001116263, -160.4851942293460638 ) ) ;
#78521=DIRECTION ( 'NONE',  ( 1.000000000000000000, -0.000000000000000000, -0.000000000000000000 ) ) ;
#78525=CIRCLE ( 'NONE', #91197, 0.09999999999998898659 ) ;
#78529=ORIENTED_EDGE ( 'NONE', *, *, #52296, .T. ) ;
#78533=DIRECTION ( 'NONE',  ( 1.000000000000000000, 0.000000000000000000, 0.000000000000000000 ) ) ;
#78558=CIRCLE ( 'NONE', #170192, 0.09999999999999939493 ) ;
#78630=ADVANCED_FACE ( 'NONE', ( #148721 ), #151446, .F. ) ;
#78639=EDGE_CURVE ( 'NONE', #86831, #137609, #52827, .T. ) ;
#78642=CARTESIAN_POINT ( 'NONE',  ( 20.94999999999999574, -1.162701749926853712, -142.1000000000000227 ) ) ;
#78659=ADVANCED_FACE ( 'NONE', ( #65311 ), #14078, .F. ) ;
#78685=CARTESIAN_POINT ( 'NONE',  ( -21.04999999999999716, -0.08574093702224233615, -127.5861737111870440 ) ) ;
#78694=AXIS2_PLACEMENT_3D ( 'NONE', #110879, #186581, #185285 ) ;
#78708=ADVANCED_FACE ( 'NONE', ( #127867 ), #9768, .T. ) ;
#78836=EDGE_CURVE ( 'NONE', #229356, #104833, #10743, .T. ) ;
#78846=LINE ( 'NONE', #243073, #178985 ) ;
#78881=ORIENTED_EDGE ( 'NONE', *, *, #172998, .F. ) ;
#78901=PLANE ( 'NONE',  #33917 ) ;
#78917=CARTESIAN_POINT ( 'NONE',  ( -20.64999999999999858, 1.940186915899009490, -146.8291192110533530 ) ) ;
#78945=DIRECTION ( 'NONE',  ( 0.000000000000000000, 0.000000000000000000, -1.000000000000000000 ) ) ;
#78969=ORIENTED_EDGE ( 'NONE', *, *, #131929, .F. ) ;
#79007=CARTESIAN_POINT ( 'NONE',  ( -23.25000000000000000, 11.65000000001115588, -160.4851942293460638 ) ) ;
#79016=( BOUNDED_CURVE ( )  B_SPLINE_CURVE ( 3, ( #64681, #28160, #184630, #124671 ),
 .UNSPECIFIED., .F., .F. ) 
 B_SPLINE_CURVE_WITH_KNOTS ( ( 4, 4 ),
 ( 3.141592653589791784, 4.712388980384688786 ),
 .UNSPECIFIED. ) 
 CURVE ( )  GEOMETRIC_REPRESENTATION_ITEM ( )  RATIONAL_B_SPLINE_CURVE ( ( 1.000000000000000000, 0.8047378541243649375, 0.8047378541243649375, 1.000000000000000000 ) ) 
 REPRESENTATION_ITEM ( '' )  );
#79017=EDGE_CURVE ( 'NONE', #141295, #200852, #222441, .T. ) ;
#79072=ORIENTED_EDGE ( 'NONE', *, *, #75467, .T. ) ;
#79097=CARTESIAN_POINT ( 'NONE',  ( -18.51991288638514277, -9.392436789662243157, -141.1432664039592169 ) ) ;
#79109=EDGE_CURVE ( 'NONE', #80663, #196636, #69218, .T. ) ;
#79132=ORIENTED_EDGE ( 'NONE', *, *, #156253, .T. ) ;
#79180=CARTESIAN_POINT ( 'NONE',  ( -20.94999999999999929, 1.115600667400684642E-11, -134.0000000000000000 ) ) ;
#79186=FACE_OUTER_BOUND ( 'NONE', #114695, .T. ) ;
#79226=ORIENTED_EDGE ( 'NONE', *, *, #193921, .T. ) ;
#79232=CIRCLE ( 'NONE', #75183, 0.09999999999999939493 ) ;
#79251=DIRECTION ( 'NONE',  ( 1.000000000000000000, 3.265361837132813093E-16, -0.000000000000000000 ) ) ;
#79277=ADVANCED_FACE ( 'NONE', ( #21427 ), #162220, .T. ) ;
#79287=DIRECTION ( 'NONE',  ( 1.000000000000000000, 3.265361837132813093E-16, -0.000000000000000000 ) ) ;
#79293=CARTESIAN_POINT ( 'NONE',  ( -18.50000000000000000, 9.250000000011157297, -155.3500000000000227 ) ) ;
#79296=VERTEX_POINT ( 'NONE', #201315 ) ;
#79345=EDGE_CURVE ( 'NONE', #68680, #118232, #177921, .T. ) ;
#79356=EDGE_CURVE ( 'NONE', #137609, #3992, #163479, .T. ) ;
#79366=VERTEX_POINT ( 'NONE', #143904 ) ;
#79369=VECTOR ( 'NONE', #162004, 1000.000000000000114 ) ;
#79385=EDGE_LOOP ( 'NONE', ( #57086, #98691, #100468, #241586 ) ) ;
#79399=ORIENTED_EDGE ( 'NONE', *, *, #117742, .F. ) ;
#79406=ORIENTED_EDGE ( 'NONE', *, *, #235385, .T. ) ;
#79412=CARTESIAN_POINT ( 'NONE',  ( 20.94999999999999574, 1.162701749949165642, -141.9000000000000341 ) ) ;
#79434=DIRECTION ( 'NONE',  ( 0.000000000000000000, 0.9274965247785529332, -0.3738317757009255171 ) ) ;
#79498=CARTESIAN_POINT ( 'NONE',  ( -21.05000000000000071, 1.835341550235567887, -145.5551512925629822 ) ) ;
#79545=CARTESIAN_POINT ( 'NONE',  ( 21.05000000000000071, 1.115600667400684642E-11, -146.8750000000000000 ) ) ;
#79562=ORIENTED_EDGE ( 'NONE', *, *, #48420, .F. ) ;
#79563=CARTESIAN_POINT ( 'NONE',  ( 20.94999675878240808, 10.29307482169070731, -172.9586421466940465 ) ) ;
#79588=TOROIDAL_SURFACE ( 'NONE', #225328, 0.2000000000000000111, 0.1000000000000000056 ) ;
#79603=CARTESIAN_POINT ( 'NONE',  ( -23.15000000000000213, 1.115600667400684642E-11, -167.5000000000000284 ) ) ;
#79604=EDGE_CURVE ( 'NONE', #200654, #212362, #57044, .T. ) ;
#79622=ORIENTED_EDGE ( 'NONE', *, *, #135713, .T. ) ;
#79640=ORIENTED_EDGE ( 'NONE', *, *, #38386, .F. ) ;
#79655=DIRECTION ( 'NONE',  ( 1.000000000000000000, -7.304098846218133681E-16, -2.111765289898285610E-31 ) ) ;
#79657=EDGE_CURVE ( 'NONE', #44689, #156098, #215290, .T. ) ;
#79670=ORIENTED_EDGE ( 'NONE', *, *, #237261, .F. ) ;
#79696=DIRECTION ( 'NONE',  ( -1.000000000000000000, -0.000000000000000000, -0.000000000000000000 ) ) ;
#79697=CARTESIAN_POINT ( 'NONE',  ( -20.00857864376270001, 9.350000000011156942, -146.2500000000000284 ) ) ;
#79702=AXIS2_PLACEMENT_3D ( 'NONE', #77572, #21503, #138820 ) ;
#79732=AXIS2_PLACEMENT_3D ( 'NONE', #50566, #72759, #210957 ) ;
#79738=EDGE_CURVE ( 'NONE', #119168, #64013, #6997, .T. ) ;
#79764=AXIS2_PLACEMENT_3D ( 'NONE', #122759, #223108, #245261 ) ;
#79773=ADVANCED_FACE ( 'NONE', ( #243983 ), #186606, .T. ) ;
#79795=VERTEX_POINT ( 'NONE', #84876 ) ;
#79878=DIRECTION ( 'NONE',  ( 0.000000000000000000, 0.000000000000000000, -1.000000000000000000 ) ) ;
#79888=VERTEX_POINT ( 'NONE', #246548 ) ;
#79899=EDGE_CURVE ( 'NONE', #174422, #154105, #126613, .T. ) ;
#79919=CARTESIAN_POINT ( 'NONE',  ( -18.59999999999999787, 9.350000000011156942, -146.3500000000000227 ) ) ;
#79961=CIRCLE ( 'NONE', #134148, 0.09999999999999999167 ) ;
#79995=ORIENTED_EDGE ( 'NONE', *, *, #771, .T. ) ;
#79999=CARTESIAN_POINT ( 'NONE',  ( 20.85000000000000142, -0.3238857010591806307, -167.4575895893140114 ) ) ;
#80005=CARTESIAN_POINT ( 'NONE',  ( -21.05000000000000071, 11.65000000001115055, -140.7838656629781724 ) ) ;
#80008=DIRECTION ( 'NONE',  ( 1.301042606982683418E-14, -0.8660254037844330455, 0.5000000000000096589 ) ) ;
#80015=DIRECTION ( 'NONE',  ( 0.000000000000000000, 0.000000000000000000, -1.000000000000000000 ) ) ;
#80046=CARTESIAN_POINT ( 'NONE',  ( -21.45000000000000284, 7.708578643773852157, -155.2500000000000284 ) ) ;
#80056=LINE ( 'NONE', #140048, #216642 ) ;
#80073=VECTOR ( 'NONE', #240502, 999.9999999999998863 ) ;
#80126=ORIENTED_EDGE ( 'NONE', *, *, #162341, .F. ) ;
#80155=ADVANCED_FACE ( 'NONE', ( #126297 ), #40553, .T. ) ;
#80261=ORIENTED_EDGE ( 'NONE', *, *, #219592, .F. ) ;
#80291=ORIENTED_EDGE ( 'NONE', *, *, #47896, .T. ) ;
#80355=AXIS2_PLACEMENT_3D ( 'NONE', #150813, #230343, #247338 ) ;
#80395=EDGE_CURVE ( 'NONE', #106574, #148927, #15367, .T. ) ;
#80397=ORIENTED_EDGE ( 'NONE', *, *, #242384, .T. ) ;
#80430=AXIS2_PLACEMENT_3D ( 'NONE', #113088, #252582, #15289 ) ;
#80450=EDGE_CURVE ( 'NONE', #189027, #37051, #203184, .T. ) ;
#80459=EDGE_CURVE ( 'NONE', #217297, #128950, #128184, .T. ) ;
#80525=CARTESIAN_POINT ( 'NONE',  ( 18.59999999999999076, 10.20857864377385127, -158.6500000000000057 ) ) ;
#80547=DIRECTION ( 'NONE',  ( 4.239556034732056743E-17, -0.1298341882520022694, -0.9915357197604852679 ) ) ;
#80588=ORIENTED_EDGE ( 'NONE', *, *, #148933, .F. ) ;
#80593=ORIENTED_EDGE ( 'NONE', *, *, #52716, .T. ) ;
#80594=ORIENTED_EDGE ( 'NONE', *, *, #176201, .T. ) ;
#80663=VERTEX_POINT ( 'NONE', #194678 ) ;
#80681=CARTESIAN_POINT ( 'NONE',  ( -18.59999999999999787, -1.162701749926853712, -142.1000000000000227 ) ) ;
#80694=VERTEX_POINT ( 'NONE', #215483 ) ;
#80696=AXIS2_PLACEMENT_3D ( 'NONE', #160382, #243737, #23442 ) ;
#80698=DIRECTION ( 'NONE',  ( 1.836970198721029934E-16, -1.000000000000000000, -0.000000000000000000 ) ) ;
#80732=ORIENTED_EDGE ( 'NONE', *, *, #152482, .T. ) ;
#80733=DIRECTION ( 'NONE',  ( 0.000000000000000000, 1.776356839400254803E-15, 1.000000000000000000 ) ) ;
#80788=EDGE_CURVE ( 'NONE', #94099, #246280, #82531, .T. ) ;
#80808=FACE_OUTER_BOUND ( 'NONE', #161369, .T. ) ;
#80811=CARTESIAN_POINT ( 'NONE',  ( -21.45000000000000284, 7.708578643773852157, -155.1500000000000057 ) ) ;
#80844=CARTESIAN_POINT ( 'NONE',  ( 20.84999999999998721, 10.33248238083634440, -173.0948465439131496 ) ) ;
#80859=ORIENTED_EDGE ( 'NONE', *, *, #147576, .T. ) ;
#80871=AXIS2_PLACEMENT_3D ( 'NONE', #236879, #234309, #257665 ) ;
#80878=DIRECTION ( 'NONE',  ( 1.000000000000000000, -0.000000000000000000, -0.000000000000000000 ) ) ;
#80900=CARTESIAN_POINT ( 'NONE',  ( -23.15000000000000213, 4.350000000011156054, -146.1500000000000341 ) ) ;
#80919=EDGE_CURVE ( 'NONE', #13549, #55661, #224208, .T. ) ;
#80996=ORIENTED_EDGE ( 'NONE', *, *, #241618, .F. ) ;
#81011=FACE_OUTER_BOUND ( 'NONE', #105696, .T. ) ;
#81019=DIRECTION ( 'NONE',  ( 0.000000000000000000, 0.000000000000000000, -1.000000000000000000 ) ) ;
#81023=ADVANCED_FACE ( 'NONE', ( #110948 ), #244027, .F. ) ;
#81030=EDGE_CURVE ( 'NONE', #140838, #116413, #45836, .T. ) ;
#81038=EDGE_CURVE ( 'NONE', #257964, #128012, #182740, .T. ) ;
#81079=CARTESIAN_POINT ( 'NONE',  ( -18.60000000000000853, -9.364240527579752893, -141.1802485818407717 ) ) ;
#81104=VERTEX_POINT ( 'NONE', #172254 ) ;
#81141=CARTESIAN_POINT ( 'NONE',  ( -21.37071067811865532, 8.070710678129811910, -155.2500000000000284 ) ) ;
#81159=DIRECTION ( 'NONE',  ( 1.000000000000000000, 0.000000000000000000, 0.000000000000000000 ) ) ;
#81169=ORIENTED_EDGE ( 'NONE', *, *, #24392, .F. ) ;
#81201=ORIENTED_EDGE ( 'NONE', *, *, #244399, .F. ) ;
#81246=AXIS2_PLACEMENT_3D ( 'NONE', #158823, #21858, #41438 ) ;
#81267=CARTESIAN_POINT ( 'NONE',  ( 21.05000000000000426, 0.03486800302426367598, -127.7299141363108816 ) ) ;
#81281=DIRECTION ( 'NONE',  ( -1.000000000000000000, -0.000000000000000000, -0.000000000000000000 ) ) ;
#81285=DIRECTION ( 'NONE',  ( 0.000000000000000000, 0.9999631594459053030, 0.008583690987162899758 ) ) ;
#81312=CIRCLE ( 'NONE', #68906, 0.09999999999998898659 ) ;
#81377=DIRECTION ( 'NONE',  ( 6.938893903907224433E-15, -1.000000000000000000, -2.891205793294679805E-16 ) ) ;
#81400=DIRECTION ( 'NONE',  ( -0.000000000000000000, -0.000000000000000000, 1.000000000000000000 ) ) ;
#81416=EDGE_CURVE ( 'NONE', #236893, #206400, #74599, .T. ) ;
#81453=ORIENTED_EDGE ( 'NONE', *, *, #146400, .F. ) ;
#81462=CARTESIAN_POINT ( 'NONE',  ( -23.25000000000000000, 11.75000000001115552, -122.2500000000000284 ) ) ;
#81469=ORIENTED_EDGE ( 'NONE', *, *, #225763, .T. ) ;
#81473=CARTESIAN_POINT ( 'NONE',  ( -20.85000000000000142, -1.736705739456431807, -179.0174225876237415 ) ) ;
#81482=EDGE_CURVE ( 'NONE', #154251, #180754, #57787, .T. ) ;
#81496=EDGE_CURVE ( 'NONE', #141490, #73323, #257789, .T. ) ;
#81519=DIRECTION ( 'NONE',  ( 0.000000000000000000, 1.000000000000000000, 0.000000000000000000 ) ) ;
#81539=EDGE_LOOP ( 'NONE', ( #192170, #103458, #118841, #50186, #223213 ) ) ;
#81574=ORIENTED_EDGE ( 'NONE', *, *, #243215, .T. ) ;
#81575=ORIENTED_EDGE ( 'NONE', *, *, #80395, .F. ) ;
#81581=EDGE_LOOP ( 'NONE', ( #116981, #20688, #56245, #30891 ) ) ;
#81649=CARTESIAN_POINT ( 'NONE',  ( -18.48550754432048748, -9.463399778548652108, -141.0487897524151322 ) ) ;
#81665=CARTESIAN_POINT ( 'NONE',  ( -18.41817142474042157, -9.498703066590927335, -174.1039654876370548 ) ) ;
#81667=CARTESIAN_POINT ( 'NONE',  ( 22.48660254037844197, 11.65000000001115588, -133.9500000000000171 ) ) ;
#81705=DIRECTION ( 'NONE',  ( -1.000000000000000000, 0.000000000000000000, 0.000000000000000000 ) ) ;
#81732=DIRECTION ( 'NONE',  ( 1.000000000000000000, 0.000000000000000000, 0.000000000000000000 ) ) ;
#81760=CARTESIAN_POINT ( 'NONE',  ( -23.25000000000000000, -11.74999999998884448, -134.0000000000000000 ) ) ;
#81777=DIRECTION ( 'NONE',  ( 0.000000000000000000, -0.000000000000000000, 1.000000000000000000 ) ) ;
#81822=CYLINDRICAL_SURFACE ( 'NONE', #112692, 0.09999999999999939493 ) ;
#81828=ORIENTED_EDGE ( 'NONE', *, *, #144866, .F. ) ;
#81883=CARTESIAN_POINT ( 'NONE',  ( 20.94999999999999929, 1.115600667400684642E-11, -169.4000000000000625 ) ) ;
#81886=ORIENTED_EDGE ( 'NONE', *, *, #204811, .F. ) ;
#81911=ORIENTED_EDGE ( 'NONE', *, *, #49390, .T. ) ;
#81922=ORIENTED_EDGE ( 'NONE', *, *, #8284, .F. ) ;
#81923=CARTESIAN_POINT ( 'NONE',  ( -21.05000000000000071, 1.162701749949165642, -142.1000000000000227 ) ) ;
#81935=AXIS2_PLACEMENT_3D ( 'NONE', #187108, #72289, #130966 ) ;
#81973=EDGE_CURVE ( 'NONE', #219363, #222383, #87192, .T. ) ;
#81987=FACE_OUTER_BOUND ( 'NONE', #81581, .T. ) ;
#81996=DIRECTION ( 'NONE',  ( 0.000000000000000000, -1.000000000000000000, 0.000000000000000000 ) ) ;
#81997=FACE_OUTER_BOUND ( 'NONE', #159066, .T. ) ;
#82036=DIRECTION ( 'NONE',  ( -0.7071067811865475727, -0.7071067811865475727, 0.000000000000000000 ) ) ;
#82038=CARTESIAN_POINT ( 'NONE',  ( -21.05000000000000071, 1.261786168576181755, -142.0864989635454947 ) ) ;
#82075=AXIS2_PLACEMENT_3D ( 'NONE', #132021, #192020, #133315 ) ;
#82118=ORIENTED_EDGE ( 'NONE', *, *, #203059, .T. ) ;
#82150=AXIS2_PLACEMENT_3D ( 'NONE', #175963, #92533, #136796 ) ;
#82203=VERTEX_POINT ( 'NONE', #43624 ) ;
#82271=EDGE_CURVE ( 'NONE', #118509, #197481, #33452, .T. ) ;
#82275=EDGE_LOOP ( 'NONE', ( #194552, #201179, #235036, #39011 ) ) ;
#82288=EDGE_CURVE ( 'NONE', #129965, #104663, #211703, .T. ) ;
#82402=DIRECTION ( 'NONE',  ( -1.000000000000000000, -2.952720810173289112E-16, 0.000000000000000000 ) ) ;
#82447=ORIENTED_EDGE ( 'NONE', *, *, #87305, .T. ) ;
#82456=ORIENTED_EDGE ( 'NONE', *, *, #174564, .F. ) ;
#82465=DIRECTION ( 'NONE',  ( -1.000000000000000000, 0.000000000000000000, 0.000000000000000000 ) ) ;
#82484=CIRCLE ( 'NONE', #11822, 0.4000000000000114575 ) ;
#82487=ORIENTED_EDGE ( 'NONE', *, *, #95201, .F. ) ;
#82520=VERTEX_POINT ( 'NONE', #203675 ) ;
#82531=CIRCLE ( 'NONE', #7553, 0.09999999999998898659 ) ;
#82563=EDGE_CURVE ( 'NONE', #92859, #98991, #206245, .T. ) ;
#82564=EDGE_CURVE ( 'NONE', #217227, #96734, #1610, .T. ) ;
#82568=ORIENTED_EDGE ( 'NONE', *, *, #169257, .F. ) ;
#82570=CARTESIAN_POINT ( 'NONE',  ( -21.12844524849339223, 11.75000000001115197, -140.9044134708424565 ) ) ;
#82634=EDGE_CURVE ( 'NONE', #7645, #18611, #237611, .T. ) ;
#82663=DIRECTION ( 'NONE',  ( 1.000000000000000000, -0.000000000000000000, -0.000000000000000000 ) ) ;
#82675=CARTESIAN_POINT ( 'NONE',  ( 22.39999999999999503, 11.65000000001116298, -133.9000000000000057 ) ) ;
#82679=EDGE_CURVE ( 'NONE', #163431, #115258, #179357, .T. ) ;
#82718=VECTOR ( 'NONE', #117656, 1000.000000000000000 ) ;
#82727=LINE ( 'NONE', #175056, #210071 ) ;
#82733=CIRCLE ( 'NONE', #145297, 0.1000000000000102612 ) ;
#82756=CARTESIAN_POINT ( 'NONE',  ( 18.49999999999998934, 6.550000000011156231, -155.2500000000000284 ) ) ;
#82764=EDGE_CURVE ( 'NONE', #7471, #56118, #63504, .T. ) ;
#82767=CIRCLE ( 'NONE', #78694, 0.09999999999998807065 ) ;
#82790=EDGE_CURVE ( 'NONE', #212843, #220745, #12782, .T. ) ;
#82794=ORIENTED_EDGE ( 'NONE', *, *, #97874, .T. ) ;
#82846=FACE_OUTER_BOUND ( 'NONE', #164337, .T. ) ;
#82850=CARTESIAN_POINT ( 'NONE',  ( 22.57320508075687115, 11.75000000001115552, -134.0000000000000000 ) ) ;
#82857=ADVANCED_FACE ( 'NONE', ( #165187 ), #64794, .F. ) ;
#82865=EDGE_LOOP ( 'NONE', ( #227946, #183309 ) ) ;
#82868=EDGE_LOOP ( 'NONE', ( #142846, #130663, #186239, #248180, #177933 ) ) ;
#82875=EDGE_CURVE ( 'NONE', #56118, #44033, #200191, .T. ) ;
#82878=CARTESIAN_POINT ( 'NONE',  ( 20.95575313997065336, 10.61455330328599089, -141.6212907019448437 ) ) ;
#82879=VERTEX_POINT ( 'NONE', #144305 ) ;
#82911=DIRECTION ( 'NONE',  ( 0.000000000000000000, 0.000000000000000000, -1.000000000000000000 ) ) ;
#82936=CARTESIAN_POINT ( 'NONE',  ( -18.52186455168995849, -9.481018481431584988, -141.0250164779142210 ) ) ;
#82947=ORIENTED_EDGE ( 'NONE', *, *, #170528, .F. ) ;
#82950=DIRECTION ( 'NONE',  ( 1.000000000000000000, 3.265361837132813093E-16, -0.000000000000000000 ) ) ;
#82952=CARTESIAN_POINT ( 'NONE',  ( 22.49533356619864222, 11.65000000631534149, -133.9348774196772069 ) ) ;
#82968=DIRECTION ( 'NONE',  ( 0.000000000000000000, 1.000000000000000000, -0.000000000000000000 ) ) ;
#82974=AXIS2_PLACEMENT_3D ( 'NONE', #256175, #241503, #62859 ) ;
#82979=CARTESIAN_POINT ( 'NONE',  ( 20.94999999999999929, 5.500000000011153745, -155.0947339810869323 ) ) ;
#83000=CIRCLE ( 'NONE', #237168, 0.09999999999998898659 ) ;
#83009=CARTESIAN_POINT ( 'NONE',  ( -23.15000000000000213, 1.115600667400684642E-11, -138.0500000000000114 ) ) ;
#83010=CARTESIAN_POINT ( 'NONE',  ( -20.94999999999999929, 1.736257131608553550, -145.5686523290175387 ) ) ;
#83016=DIRECTION ( 'NONE',  ( 1.000000000000000000, 0.000000000000000000, 0.000000000000000000 ) ) ;
#83018=DIRECTION ( 'NONE',  ( -1.000000000000000000, -3.265361837132813093E-16, 0.000000000000000000 ) ) ;
#83081=DIRECTION ( 'NONE',  ( 0.7071067811865487940, 0.000000000000000000, -0.7071067811865463515 ) ) ;
#83089=CARTESIAN_POINT ( 'NONE',  ( 21.05000000000000071, 8.776282895303632259, -146.1500000000000341 ) ) ;
#83099=AXIS2_PLACEMENT_3D ( 'NONE', #88710, #189123, #30077 ) ;
#83113=DIRECTION ( 'NONE',  ( 0.000000000000000000, 0.4999999999999348299, -0.8660254037844762331 ) ) ;
#83124=AXIS2_PLACEMENT_3D ( 'NONE', #14657, #216682, #194582 ) ;
#83138=DIRECTION ( 'NONE',  ( 0.000000000000000000, 0.4999999999999478195, -0.8660254037844686836 ) ) ;
#83171=VERTEX_POINT ( 'NONE', #20248 ) ;
#83175=CYLINDRICAL_SURFACE ( 'NONE', #237716, 0.09999999999998898659 ) ;
#83178=ORIENTED_EDGE ( 'NONE', *, *, #96936, .F. ) ;
#83182=VERTEX_POINT ( 'NONE', #256200 ) ;
#83190=CARTESIAN_POINT ( 'NONE',  ( -21.05000000000000071, -11.29603075032412463, -164.4521008403361577 ) ) ;
#83233=CIRCLE ( 'NONE', #75099, 0.09999999999999917288 ) ;
#83265=CARTESIAN_POINT ( 'NONE',  ( 20.94999999999999574, 1.835341550235567887, -145.5551512925629822 ) ) ;
#83270=CARTESIAN_POINT ( 'NONE',  ( 20.94999999999999929, 5.850000000011156942, -157.3675027757221017 ) ) ;
#83272=DIRECTION ( 'NONE',  ( 0.000000000000000000, 0.3738317757009345654, 0.9274965247785492695 ) ) ;
#83281=EDGE_CURVE ( 'NONE', #117646, #94122, #154442, .T. ) ;
#83293=CARTESIAN_POINT ( 'NONE',  ( -18.59999999999999787, 1.115600667400684642E-11, -134.0000000000000000 ) ) ;
#83308=FACE_OUTER_BOUND ( 'NONE', #184719, .T. ) ;
#83309=DIRECTION ( 'NONE',  ( 1.000000000000000000, -0.000000000000000000, -0.000000000000000000 ) ) ;
#83335=ORIENTED_EDGE ( 'NONE', *, *, #192730, .F. ) ;
#83348=ADVANCED_FACE ( 'NONE', ( #252119 ), #189600, .F. ) ;
#83364=ORIENTED_EDGE ( 'NONE', *, *, #151538, .T. ) ;
#83371=CARTESIAN_POINT ( 'NONE',  ( -21.70464131381649509, 7.095358018979010417, -134.0000000000000000 ) ) ;
#83379=ORIENTED_EDGE ( 'NONE', *, *, #198032, .T. ) ;
#83383=DIRECTION ( 'NONE',  ( -1.000000000000000000, 0.000000000000000000, 0.000000000000000000 ) ) ;
#83407=VERTEX_POINT ( 'NONE', #212996 ) ;
#83430=CARTESIAN_POINT ( 'NONE',  ( 21.05000000000000071, 1.115600667400684642E-11, -167.5000000000000284 ) ) ;
#83434=CARTESIAN_POINT ( 'NONE',  ( 20.94999999999999929, 1.115600667400684642E-11, -146.8750000000000000 ) ) ;
#83435=ORIENTED_EDGE ( 'NONE', *, *, #86688, .F. ) ;
#83486=EDGE_CURVE ( 'NONE', #240778, #189087, #8841, .T. ) ;
#83548=CARTESIAN_POINT ( 'NONE',  ( -20.64999999999999858, 1.940186915899004161, -154.6708807889467039 ) ) ;
#83573=AXIS2_PLACEMENT_3D ( 'NONE', #202152, #24827, #28694 ) ;
#83590=VECTOR ( 'NONE', #127863, 1000.000000000000000 ) ;
#83602=CARTESIAN_POINT ( 'NONE',  ( -20.64999999999999858, 2.000000000011154189, -154.2753780772379173 ) ) ;
#83610=VERTEX_POINT ( 'NONE', #224547 ) ;
#83614=CARTESIAN_POINT ( 'NONE',  ( -22.42253884134832020, 0.001932351146464877023, -122.3503943026515799 ) ) ;
#83645=CARTESIAN_POINT ( 'NONE',  ( -18.59999999999999787, 6.982009704867601307, -171.1961521182563217 ) ) ;
#83649=ORIENTED_EDGE ( 'NONE', *, *, #186029, .T. ) ;
#83651=VERTEX_POINT ( 'NONE', #42093 ) ;
#83722=EDGE_CURVE ( 'NONE', #44033, #158124, #8286, .T. ) ;
#83724=EDGE_LOOP ( 'NONE', ( #10469, #208501 ) ) ;
#83729=DIRECTION ( 'NONE',  ( 0.000000000000000000, 0.000000000000000000, -1.000000000000000000 ) ) ;
#83744=FACE_OUTER_BOUND ( 'NONE', #242806, .T. ) ;
#83765=ADVANCED_FACE ( 'NONE', ( #193151 ), #250535, .T. ) ;
#83777=DIRECTION ( 'NONE',  ( 0.000000000000000000, -1.000000000000000000, 0.000000000000000000 ) ) ;
#83803=CIRCLE ( 'NONE', #79732, 11.75000000000000000 ) ;
#83805=ORIENTED_EDGE ( 'NONE', *, *, #225628, .F. ) ;
#83817=DIRECTION ( 'NONE',  ( 0.000000000000000000, 0.000000000000000000, -1.000000000000000000 ) ) ;
#83823=DIRECTION ( 'NONE',  ( -0.000000000000000000, -0.000000000000000000, 1.000000000000000000 ) ) ;
#83835=CARTESIAN_POINT ( 'NONE',  ( 20.84451136049652575, 10.62014191481791947, -141.4939245595324167 ) ) ;
#83844=CARTESIAN_POINT ( 'NONE',  ( 20.94999999999999929, 6.550000000011156231, -146.2500000000000284 ) ) ;
#83912=CARTESIAN_POINT ( 'NONE',  ( -22.50000000000094147, 0.1008583691097610785, -122.2504328765106010 ) ) ;
#83917=CARTESIAN_POINT ( 'NONE',  ( 23.15000000000000213, -9.599999999988842347, -157.6060308773475640 ) ) ;
#84012=CARTESIAN_POINT ( 'NONE',  ( -21.14999999999999858, 6.257814610487270279, -133.9022097086912311 ) ) ;
#84031=CARTESIAN_POINT ( 'NONE',  ( 21.05000000000000071, 4.813084112160680661, -145.9415177565238366 ) ) ;
#84033=ORIENTED_EDGE ( 'NONE', *, *, #179730, .F. ) ;
#84056=LINE ( 'NONE', #243175, #202766 ) ;
#84067=CARTESIAN_POINT ( 'NONE',  ( -20.94999999999999929, -1.162701749926853712, -141.9000000000000341 ) ) ;
#84096=ADVANCED_FACE ( 'NONE', ( #230686 ), #52013, .T. ) ;
#84121=EDGE_LOOP ( 'NONE', ( #40210, #5614, #83649, #146784 ) ) ;
#84141=CARTESIAN_POINT ( 'NONE',  ( 19.75857864376269291, 11.75000000001116263, -158.8500000000000227 ) ) ;
#84147=ORIENTED_EDGE ( 'NONE', *, *, #73215, .F. ) ;
#84182=CARTESIAN_POINT ( 'NONE',  ( 22.50000000000000000, 7.750000000011162626, -133.9000000000000057 ) ) ;
#84196=CARTESIAN_POINT ( 'NONE',  ( -20.94999999999999929, -11.41227409413852811, -164.6000000000000227 ) ) ;
#84210=CARTESIAN_POINT ( 'NONE',  ( -18.49372193242244933, -9.442484523346822201, -174.2647812600350505 ) ) ;
#84231=CIRCLE ( 'NONE', #171820, 0.2000000000000057288 ) ;
#84261=CIRCLE ( 'NONE', #38354, 0.09999999999998898659 ) ;
#84276=CARTESIAN_POINT ( 'NONE',  ( -20.00857864376270001, 9.150000000011157653, -155.2500000000000284 ) ) ;
#84321=DIRECTION ( 'NONE',  ( 1.000000000000000000, 0.000000000000000000, 0.000000000000000000 ) ) ;
#84331=CIRCLE ( 'NONE', #230128, 0.09999999999998898659 ) ;
#84349=ADVANCED_FACE ( 'NONE', ( #222632 ), #81822, .T. ) ;
#84352=EDGE_CURVE ( 'NONE', #247600, #140944, #54426, .T. ) ;
#84359=EDGE_LOOP ( 'NONE', ( #197198, #3236, #42159, #70418, #178170, #163769, #147649, #163344, #98412, #92695, #101119 ) ) ;
#84440=ORIENTED_EDGE ( 'NONE', *, *, #182122, .F. ) ;
#84445=EDGE_CURVE ( 'NONE', #154130, #116413, #104469, .T. ) ;
#84451=EDGE_LOOP ( 'NONE', ( #120814, #172486, #127411, #216724, #165628, #86091, #127114 ) ) ;
#84477=CARTESIAN_POINT ( 'NONE',  ( -23.25000000000000000, -11.74999999998884448, -134.0000000000000000 ) ) ;
#84479=ORIENTED_EDGE ( 'NONE', *, *, #59936, .T. ) ;
#84494=AXIS2_PLACEMENT_3D ( 'NONE', #171572, #210663, #211964 ) ;
#84506=DIRECTION ( 'NONE',  ( 0.000000000000000000, -0.9908441862701782288, -0.1350103645450542456 ) ) ;
#84515=ORIENTED_EDGE ( 'NONE', *, *, #117544, .F. ) ;
#84555=ORIENTED_EDGE ( 'NONE', *, *, #129643, .T. ) ;
#84569=CARTESIAN_POINT ( 'NONE',  ( 18.49999999999999645, -1.866714910046153308, -145.7526752462820241 ) ) ;
#84586=VERTEX_POINT ( 'NONE', #186102 ) ;
#84632=ADVANCED_FACE ( 'NONE', ( #17406 ), #104640, .F. ) ;
#84639=DIRECTION ( 'NONE',  ( 0.000000000000000000, -0.000000000000000000, 1.000000000000000000 ) ) ;
#84644=ORIENTED_EDGE ( 'NONE', *, *, #56936, .T. ) ;
#84646=DIRECTION ( 'NONE',  ( -0.000000000000000000, 0.000000000000000000, 1.000000000000000000 ) ) ;
#84689=DIRECTION ( 'NONE',  ( 0.000000000000000000, 0.000000000000000000, -1.000000000000000000 ) ) ;
#84724=CARTESIAN_POINT ( 'NONE',  ( -21.14999999999999858, -0.09999999998884338825, -122.3504291924552234 ) ) ;
#84733=ORIENTED_EDGE ( 'NONE', *, *, #13514, .T. ) ;
#84812=DIRECTION ( 'NONE',  ( 1.000000000000000000, 0.000000000000000000, 0.000000000000000000 ) ) ;
#84838=CARTESIAN_POINT ( 'NONE',  ( 22.39999999999999503, 7.790779598384535376, -134.0000000000000000 ) ) ;
#84859=AXIS2_PLACEMENT_3D ( 'NONE', #77054, #134443, #196992 ) ;
#84860=DIRECTION ( 'NONE',  ( 0.000000000000000000, 0.1298341882520022972, 0.9915357197604853789 ) ) ;
#84861=VERTEX_POINT ( 'NONE', #211452 ) ;
#84876=CARTESIAN_POINT ( 'NONE',  ( -18.59999999999999787, 11.75000000001115197, -141.0148057706539930 ) ) ;
#84884=EDGE_CURVE ( 'NONE', #155087, #47711, #133709, .T. ) ;
#84901=CARTESIAN_POINT ( 'NONE',  ( -22.39999999999999858, 1.115600667400684642E-11, -122.3504291924552234 ) ) ;
#84904=ADVANCED_FACE ( 'NONE', ( #171090 ), #53662, .T. ) ;
#84910=FACE_OUTER_BOUND ( 'NONE', #220926, .T. ) ;
#84933=ORIENTED_EDGE ( 'NONE', *, *, #234291, .F. ) ;
#84936=AXIS2_PLACEMENT_3D ( 'NONE', #11907, #249218, #151412 ) ;
#84954=CARTESIAN_POINT ( 'NONE',  ( 21.05315837450969596, 11.75000000001116085, -160.6583560044166745 ) ) ;
#84967=ORIENTED_EDGE ( 'NONE', *, *, #28203, .T. ) ;
#84996=EDGE_CURVE ( 'NONE', #116221, #149669, #113229, .T. ) ;
#85011=ORIENTED_EDGE ( 'NONE', *, *, #12345, .T. ) ;
#85049=ORIENTED_EDGE ( 'NONE', *, *, #28306, .T. ) ;
#85053=EDGE_LOOP ( 'NONE', ( #131295, #84644, #92918, #250314 ) ) ;
#85055=VERTEX_POINT ( 'NONE', #45513 ) ;
#85070=ORIENTED_EDGE ( 'NONE', *, *, #156495, .T. ) ;
#85071=CARTESIAN_POINT ( 'NONE',  ( 22.47071067811865319, 7.720074744509199505, -133.9009075452974002 ) ) ;
#85081=ORIENTED_EDGE ( 'NONE', *, *, #12800, .F. ) ;
#85084=EDGE_LOOP ( 'NONE', ( #147634, #54015, #194399 ) ) ;
#85093=CARTESIAN_POINT ( 'NONE',  ( 20.85000000000000142, 1.115600667400684642E-11, -167.5000000000000284 ) ) ;
#85117=CIRCLE ( 'NONE', #110092, 0.09999999999998898659 ) ;
#85167=DIRECTION ( 'NONE',  ( 0.000000000000000000, -0.9908441862701782288, -0.1350103645450542456 ) ) ;
#85177=ORIENTED_EDGE ( 'NONE', *, *, #146951, .F. ) ;
#85179=FACE_OUTER_BOUND ( 'NONE', #202101, .T. ) ;
#85208=CARTESIAN_POINT ( 'NONE',  ( -22.60000000000094289, 0.1008583691096561485, -122.2504328765106010 ) ) ;
#85212=VERTEX_POINT ( 'NONE', #93625 ) ;
#85215=CARTESIAN_POINT ( 'NONE',  ( -23.15000000000000213, 11.65000000001115588, -146.2500000000000284 ) ) ;
#85222=EDGE_LOOP ( 'NONE', ( #30220, #35381, #242658, #51794 ) ) ;
#85236=CARTESIAN_POINT ( 'NONE',  ( 18.49999999999999289, 6.450000000011156587, -144.0170271704400307 ) ) ;
#85269=DIRECTION ( 'NONE',  ( 0.000000000000000000, 0.000000000000000000, 1.000000000000000000 ) ) ;
#85287=VERTEX_POINT ( 'NONE', #200427 ) ;
#85295=ORIENTED_EDGE ( 'NONE', *, *, #82764, .T. ) ;
#85305=EDGE_CURVE ( 'NONE', #158625, #192232, #221251, .T. ) ;
#85313=AXIS2_PLACEMENT_3D ( 'NONE', #159310, #217951, #98000 ) ;
#85334=LINE ( 'NONE', #124500, #230730 ) ;
#85381=EDGE_LOOP ( 'NONE', ( #172428, #170841, #139634, #190508, #228299, #182750, #165109, #178043, #11753, #197539, #121949 ) ) ;
#85390=ORIENTED_EDGE ( 'NONE', *, *, #62978, .T. ) ;
#85397=AXIS2_PLACEMENT_3D ( 'NONE', #55551, #135108, #214656 ) ;
#85435=CARTESIAN_POINT ( 'NONE',  ( -23.25000000000000000, -1.835859311432481045, -179.0044391687985410 ) ) ;
#85445=CYLINDRICAL_SURFACE ( 'NONE', #22654, 0.09999999999999939493 ) ;
#85449=DIRECTION ( 'NONE',  ( -0.000000000000000000, 0.000000000000000000, -1.000000000000000000 ) ) ;
#85488=DIRECTION ( 'NONE',  ( -0.000000000000000000, -1.000000000000000000, 6.308085367188393199E-16 ) ) ;
#85494=DIRECTION ( 'NONE',  ( -1.000000000000000000, -2.952720810173289112E-16, 0.000000000000000000 ) ) ;
#85509=DIRECTION ( 'NONE',  ( 0.000000000000000000, 0.000000000000000000, -1.000000000000000000 ) ) ;
#85516=CARTESIAN_POINT ( 'NONE',  ( -18.43459694179555441, -9.494210124986889099, -174.1170052026611188 ) ) ;
#85521=ORIENTED_EDGE ( 'NONE', *, *, #249770, .F. ) ;
#85527=AXIS2_PLACEMENT_3D ( 'NONE', #118023, #97132, #217102 ) ;
#85548=ORIENTED_EDGE ( 'NONE', *, *, #246349, .T. ) ;
#85574=DIRECTION ( 'NONE',  ( 0.000000000000000000, 0.000000000000000000, -1.000000000000000000 ) ) ;
#85575=CYLINDRICAL_SURFACE ( 'NONE', #113162, 0.09999999999998898659 ) ;
#85578=FACE_OUTER_BOUND ( 'NONE', #126675, .T. ) ;
#85588=VERTEX_POINT ( 'NONE', #11370 ) ;
#85596=CARTESIAN_POINT ( 'NONE',  ( 18.40916198585732388, -9.499999999988844479, -174.1001896318244349 ) ) ;
#85609=EDGE_CURVE ( 'NONE', #54116, #8349, #78070, .T. ) ;
#85610=DIRECTION ( 'NONE',  ( 0.000000000000000000, 0.000000000000000000, -1.000000000000000000 ) ) ;
#85614=DIRECTION ( 'NONE',  ( 0.000000000000000000, 1.224646799142185182E-16, 1.000000000000000000 ) ) ;
#85617=CARTESIAN_POINT ( 'NONE',  ( -23.25000000000000000, -1.164121893230052995, -175.4148480855716059 ) ) ;
#85639=ORIENTED_EDGE ( 'NONE', *, *, #32886, .F. ) ;
#85641=DIRECTION ( 'NONE',  ( 0.000000000000000000, 0.1568667991644863147, -0.9876197685951252359 ) ) ;
#85691=AXIS2_PLACEMENT_3D ( 'NONE', #234243, #92173, #252520 ) ;
#85712=CARTESIAN_POINT ( 'NONE',  ( 21.14999999999999858, -0.09999999998884338825, -122.3504291924552234 ) ) ;
#85831=CARTESIAN_POINT ( 'NONE',  ( 18.59999999999999076, 1.115600667400684642E-11, -167.5000000000000284 ) ) ;
#85868=CARTESIAN_POINT ( 'NONE',  ( 18.49999999999999645, 1.835341550235567887, -145.5551512925629822 ) ) ;
#85903=ORIENTED_EDGE ( 'NONE', *, *, #60070, .F. ) ;
#85932=CARTESIAN_POINT ( 'NONE',  ( 18.51997666896852479, -9.392332131507911797, -141.1434061874842030 ) ) ;
#85970=DIRECTION ( 'NONE',  ( 0.000000000000000000, 0.000000000000000000, 1.000000000000000000 ) ) ;
#85981=CARTESIAN_POINT ( 'NONE',  ( -22.00356870140485555, 7.254242362510171738, -134.0000000000000000 ) ) ;
#86006=DIRECTION ( 'NONE',  ( 1.000000000000000000, -0.000000000000000000, -0.000000000000000000 ) ) ;
#86017=EDGE_LOOP ( 'NONE', ( #47255, #53343, #158812, #143307 ) ) ;
#86064=FACE_OUTER_BOUND ( 'NONE', #178210, .T. ) ;
#86067=ORIENTED_EDGE ( 'NONE', *, *, #81038, .F. ) ;
#86074=DIRECTION ( 'NONE',  ( 0.000000000000000000, 1.000000000000000000, 0.000000000000000000 ) ) ;
#86091=ORIENTED_EDGE ( 'NONE', *, *, #238701, .T. ) ;
#86093=CARTESIAN_POINT ( 'NONE',  ( -20.85000000000000142, -1.164121893230052995, -175.4148480855716059 ) ) ;
#86105=VECTOR ( 'NONE', #245101, 1000.000000000000000 ) ;
#86135=LINE ( 'NONE', #242665, #68907 ) ;
#86136=DIRECTION ( 'NONE',  ( 0.000000000000000000, 0.000000000000000000, -1.000000000000000000 ) ) ;
#86149=CARTESIAN_POINT ( 'NONE',  ( -20.64999999999999858, -8.999999999988844479, -158.0060308773475981 ) ) ;
#86181=CARTESIAN_POINT ( 'NONE',  ( 23.24999999999999645, 1.115600667400684642E-11, -167.5000000000000284 ) ) ;
#86192=AXIS2_PLACEMENT_3D ( 'NONE', #230803, #130385, #106967 ) ;
#86195=CARTESIAN_POINT ( 'NONE',  ( -22.45372860728439690, 0.01492061955964466002, -122.3502028652961400 ) ) ;
#86244=CARTESIAN_POINT ( 'NONE',  ( -23.15000000000000213, 1.115600667400684642E-11, -167.5000000000000284 ) ) ;
#86285=EDGE_CURVE ( 'NONE', #155942, #205417, #5423, .T. ) ;
#86330=ORIENTED_EDGE ( 'NONE', *, *, #47896, .F. ) ;
#86358=AXIS2_PLACEMENT_3D ( 'NONE', #61010, #223924, #63576 ) ;
#86363=CARTESIAN_POINT ( 'NONE',  ( -23.15000000000000213, 11.75000000001115552, -160.4851942293460638 ) ) ;
#86395=CARTESIAN_POINT ( 'NONE',  ( -18.59999999999999787, 14.05000000001115623, -139.5136950707610026 ) ) ;
#86403=FACE_OUTER_BOUND ( 'NONE', #163746, .T. ) ;
#86414=VERTEX_POINT ( 'NONE', #2404 ) ;
#86443=DIRECTION ( 'NONE',  ( 0.000000000000000000, 1.000000000000000000, 1.734723475976807292E-15 ) ) ;
#86462=EDGE_CURVE ( 'NONE', #256904, #232714, #220198, .T. ) ;
#86552=AXIS2_PLACEMENT_3D ( 'NONE', #97007, #60472, #159600 ) ;
#86580=CIRCLE ( 'NONE', #128321, 0.2000000000000057288 ) ;
#86581=LINE ( 'NONE', #181866, #206071 ) ;
#86591=ORIENTED_EDGE ( 'NONE', *, *, #62780, .T. ) ;
#86597=B_SPLINE_CURVE_WITH_KNOTS ( 'NONE', 3,
 ( #23183, #240927, #63555, #183521, #121008, #200512, #257865, #162678, #102662, #123543, #203070, #21880, #143085, #222614, #24469, #103949 ),
 .UNSPECIFIED., .F., .F.,
 ( 4, 3, 3, 3, 3, 4 ),
 ( 0.000000000000000000, 2.209833635978077814E-05, 5.595056164119279336E-05, 8.979992002655381403E-05, 0.0001236482757198913553, 0.0001574984039362988268 ),
 .UNSPECIFIED. ) ;
#86610=CARTESIAN_POINT ( 'NONE',  ( -23.25000000000000000, 11.65000000001115588, -146.1500000000000341 ) ) ;
#86613=DIRECTION ( 'NONE',  ( -1.000000000000000000, -0.000000000000000000, -0.000000000000000000 ) ) ;
#86619=AXIS2_PLACEMENT_3D ( 'NONE', #248919, #111980, #170707 ) ;
#86621=CARTESIAN_POINT ( 'NONE',  ( -20.54999999999999716, -9.399999999988846611, -157.6060308773475924 ) ) ;
#86642=TOROIDAL_SURFACE ( 'NONE', #70147, 7.800000000000000711, 0.1000000000000000056 ) ;
#86659=EDGE_CURVE ( 'NONE', #155996, #11174, #72285, .T. ) ;
#86688=EDGE_CURVE ( 'NONE', #29064, #11395, #209653, .T. ) ;
#86709=EDGE_CURVE ( 'NONE', #200535, #197481, #210896, .T. ) ;
#86730=ORIENTED_EDGE ( 'NONE', *, *, #110135, .T. ) ;
#86754=CARTESIAN_POINT ( 'NONE',  ( 18.49999999999999289, 10.29270135741298731, -172.9573618871519614 ) ) ;
#86785=ORIENTED_EDGE ( 'NONE', *, *, #56070, .T. ) ;
#86793=LINE ( 'NONE', #15981, #251115 ) ;
#86818=CARTESIAN_POINT ( 'NONE',  ( -18.59999994787167310, -9.523637689750707125, -174.3824495347721779 ) ) ;
#86822=DIRECTION ( 'NONE',  ( 0.000000000000000000, 0.000000000000000000, -1.000000000000000000 ) ) ;
#86829=CARTESIAN_POINT ( 'NONE',  ( -20.94999999999999929, -11.74999999998884448, -164.4000000000000057 ) ) ;
#86831=VERTEX_POINT ( 'NONE', #63356 ) ;
#86840=ORIENTED_EDGE ( 'NONE', *, *, #217978, .T. ) ;
#86846=AXIS2_PLACEMENT_3D ( 'NONE', #234780, #50976, #14477 ) ;
#86851=ORIENTED_EDGE ( 'NONE', *, *, #71346, .T. ) ;
#86869=CARTESIAN_POINT ( 'NONE',  ( 20.94999999999999574, 1.250000000011155299, -141.9000000000000341 ) ) ;
#86876=DIRECTION ( 'NONE',  ( 1.000000000000000000, 1.734723475976817507E-14, 0.000000000000000000 ) ) ;
#86892=EDGE_CURVE ( 'NONE', #171186, #41545, #30599, .T. ) ;
#86896=CARTESIAN_POINT ( 'NONE',  ( 18.41815437325346849, -9.498709853130273828, -174.1039458388020194 ) ) ;
#86899=EDGE_CURVE ( 'NONE', #138896, #243619, #151404, .T. ) ;
#86929=CARTESIAN_POINT ( 'NONE',  ( 20.94999999999999929, -9.499999999988844479, -157.6060308773475640 ) ) ;
#86966=ORIENTED_EDGE ( 'NONE', *, *, #25651, .T. ) ;
#86969=CARTESIAN_POINT ( 'NONE',  ( 23.14999999999999503, 11.65000000001116298, -122.2500000000000284 ) ) ;
#86991=EDGE_CURVE ( 'NONE', #222371, #12431, #139059, .T. ) ;
#87008=EDGE_CURVE ( 'NONE', #25173, #212362, #1707, .T. ) ;
#87069=CARTESIAN_POINT ( 'NONE',  ( 22.48660254037844197, 11.65000000001116298, -133.9500000000000171 ) ) ;
#87086=DIRECTION ( 'NONE',  ( -1.000000000000000000, -2.952720810173289112E-16, 0.000000000000000000 ) ) ;
#87087=CIRCLE ( 'NONE', #120457, 0.09999999999998898659 ) ;
#87130=VERTEX_POINT ( 'NONE', #114038 ) ;
#87156=AXIS2_PLACEMENT_3D ( 'NONE', #123442, #223808, #20509 ) ;
#87157=VERTEX_POINT ( 'NONE', #95754 ) ;
#87167=ORIENTED_EDGE ( 'NONE', *, *, #126187, .F. ) ;
#87180=ORIENTED_EDGE ( 'NONE', *, *, #243426, .F. ) ;
#87190=DIRECTION ( 'NONE',  ( 0.000000000000000000, 0.4999999999999956701, -0.8660254037844411501 ) ) ;
#87192=CIRCLE ( 'NONE', #137278, 0.09999999999999907574 ) ;
#87194=CIRCLE ( 'NONE', #232979, 0.2000000000000057288 ) ;
#87202=CARTESIAN_POINT ( 'NONE',  ( -21.05000000000000071, 11.65000000001115588, -134.1000000000000227 ) ) ;
#87214=CIRCLE ( 'NONE', #220522, 0.2000000000000057288 ) ;
#87236=CARTESIAN_POINT ( 'NONE',  ( -22.39999999999999858, 0.1000000000111554016, -126.2092204016266379 ) ) ;
#87246=CARTESIAN_POINT ( 'NONE',  ( -21.05000000000000071, 1.835341550235567887, -145.6551512925629766 ) ) ;
#87247=CARTESIAN_POINT ( 'NONE',  ( 21.05000000000000071, 0.03201369319901656296, -127.7411572764626584 ) ) ;
#87250=DIRECTION ( 'NONE',  ( 1.000000000000000000, 0.000000000000000000, 0.000000000000000000 ) ) ;
#87251=CARTESIAN_POINT ( 'NONE',  ( 18.60000000000000142, -9.399999999988782662, -141.2972597596633193 ) ) ;
#87259=AXIS2_PLACEMENT_3D ( 'NONE', #256820, #194370, #78232 ) ;
#87264=DIRECTION ( 'NONE',  ( -0.000000000000000000, -2.891205793294679805E-16, 1.000000000000000000 ) ) ;
#87295=ORIENTED_EDGE ( 'NONE', *, *, #5749, .F. ) ;
#87305=EDGE_CURVE ( 'NONE', #116282, #241842, #158356, .T. ) ;
#87310=CARTESIAN_POINT ( 'NONE',  ( 20.94999999999999929, -9.499999999988844479, -157.6060308773475640 ) ) ;
#87311=ORIENTED_EDGE ( 'NONE', *, *, #104114, .F. ) ;
#87316=ORIENTED_EDGE ( 'NONE', *, *, #128591, .F. ) ;
#87342=DIRECTION ( 'NONE',  ( 0.000000000000000000, 0.000000000000000000, -1.000000000000000000 ) ) ;
#87347=CARTESIAN_POINT ( 'NONE',  ( -22.39999999999999858, 0.1000000000111554016, -126.2092204016266379 ) ) ;
#87386=VECTOR ( 'NONE', #174423, 1000.000000000000000 ) ;
#87414=EDGE_CURVE ( 'NONE', #23909, #56118, #114331, .T. ) ;
#87445=ORIENTED_EDGE ( 'NONE', *, *, #185104, .T. ) ;
#87446=DIRECTION ( 'NONE',  ( 0.000000000000000000, -1.000000000000000000, 0.000000000000000000 ) ) ;
#87451=EDGE_CURVE ( 'NONE', #229356, #187889, #53778, .T. ) ;
#87453=CARTESIAN_POINT ( 'NONE',  ( -20.94999999999999929, -11.74999999998884448, -137.1000000000000227 ) ) ;
#87493=CARTESIAN_POINT ( 'NONE',  ( -23.25000000000000000, 1.115600667400684642E-11, -134.0000000000000000 ) ) ;
#87512=CARTESIAN_POINT ( 'NONE',  ( 23.15000000000000213, -11.64999999998883595, -164.4000000000000057 ) ) ;
#87529=CIRCLE ( 'NONE', #29323, 0.09999999999999971412 ) ;
#87575=DIRECTION ( 'NONE',  ( 0.000000000000000000, 1.000000000000000000, 0.000000000000000000 ) ) ;
#87582=DIRECTION ( 'NONE',  ( 0.000000000000000000, 1.000000000000000000, 0.000000000000000000 ) ) ;
#87591=LINE ( 'NONE', #88873, #251881 ) ;
#87619=CARTESIAN_POINT ( 'NONE',  ( 20.94999999999999929, -8.999999999988844479, -143.8939691226524644 ) ) ;
#87623=CARTESIAN_POINT ( 'NONE',  ( -18.59999999999999787, 3.912899247244609580, -145.4818229730109920 ) ) ;
#87703=CARTESIAN_POINT ( 'NONE',  ( 18.59999999999999076, 7.070967871809997973, -171.2465642218683115 ) ) ;
#87704=CARTESIAN_POINT ( 'NONE',  ( -21.59142135623730852, 7.850000000011158718, -146.3500000000000227 ) ) ;
#87724=LINE ( 'NONE', #168621, #153958 ) ;
#87742=AXIS2_PLACEMENT_3D ( 'NONE', #46506, #145607, #169078 ) ;
#87745=DIRECTION ( 'NONE',  ( 1.000000000000000000, 7.304098846218133681E-16, -4.607487905232622991E-31 ) ) ;
#87761=EDGE_CURVE ( 'NONE', #11395, #63728, #94139, .T. ) ;
#87814=CARTESIAN_POINT ( 'NONE',  ( -18.39999999999999858, -9.682403433465239573, -174.1568433774127982 ) ) ;
#87818=ORIENTED_EDGE ( 'NONE', *, *, #218833, .F. ) ;
#87825=VERTEX_POINT ( 'NONE', #87453 ) ;
#87859=VERTEX_POINT ( 'NONE', #108324 ) ;
#87872=ORIENTED_EDGE ( 'NONE', *, *, #192110, .F. ) ;
#87901=EDGE_CURVE ( 'NONE', #140569, #206400, #92591, .T. ) ;
#87938=ORIENTED_EDGE ( 'NONE', *, *, #188443, .T. ) ;
#87952=CARTESIAN_POINT ( 'NONE',  ( 20.94999999999999929, 4.850467289730776344, -155.4657325909983570 ) ) ;
#87987=VECTOR ( 'NONE', #249580, 1000.000000000000000 ) ;
#87996=FACE_OUTER_BOUND ( 'NONE', #37776, .T. ) ;
#88068=DIRECTION ( 'NONE',  ( 1.000000000000000000, 1.836970198721029934E-16, 0.000000000000000000 ) ) ;
#88088=CARTESIAN_POINT ( 'NONE',  ( -18.50000324121759121, 10.29307482169070731, -172.9586421466940465 ) ) ;
#88111=CARTESIAN_POINT ( 'NONE',  ( -23.15000000000000213, 11.75000000001115552, -122.2500000000000284 ) ) ;
#88116=DIRECTION ( 'NONE',  ( 0.7071067811865487940, 8.659560562354918067E-17, 0.7071067811865463515 ) ) ;
#88132=FACE_OUTER_BOUND ( 'NONE', #78433, .T. ) ;
#88134=AXIS2_PLACEMENT_3D ( 'NONE', #230899, #49670, #194348 ) ;
#88150=ORIENTED_EDGE ( 'NONE', *, *, #159936, .F. ) ;
#88205=DIRECTION ( 'NONE',  ( 1.000000000000000000, 0.000000000000000000, 0.000000000000000000 ) ) ;
#88210=CARTESIAN_POINT ( 'NONE',  ( -20.85882249326303040, 10.33248238083634796, -173.0948465439131496 ) ) ;
#88223=EDGE_CURVE ( 'NONE', #59872, #13799, #77728, .T. ) ;
#88268=CARTESIAN_POINT ( 'NONE',  ( -23.25000000000000000, 6.933893972137497030, -171.2856458343736108 ) ) ;
#88279=DIRECTION ( 'NONE',  ( 1.000000000000000000, 0.000000000000000000, 0.000000000000000000 ) ) ;
#88285=CARTESIAN_POINT ( 'NONE',  ( -21.05000000000000071, -11.64999999998884483, -137.0000000000000000 ) ) ;
#88292=CARTESIAN_POINT ( 'NONE',  ( -20.64999999999999858, 2.000000000011154189, -147.2246219227621111 ) ) ;
#88329=DIRECTION ( 'NONE',  ( 0.000000000000000000, -0.1568667991644714932, 0.9876197685951274563 ) ) ;
#88350=CARTESIAN_POINT ( 'NONE',  ( -21.05000000000000071, 1.115600667400684642E-11, -134.0000000000000000 ) ) ;
#88357=CARTESIAN_POINT ( 'NONE',  ( 20.94999999999999929, -8.999999999988842703, -157.6060308773475640 ) ) ;
#88379=CARTESIAN_POINT ( 'NONE',  ( -21.08078803292166725, 0.07918598716886143807, -127.6669870355628973 ) ) ;
#88401=DIRECTION ( 'NONE',  ( 0.000000000000000000, -1.000000000000000000, 0.000000000000000000 ) ) ;
#88403=CARTESIAN_POINT ( 'NONE',  ( -22.42357213249529480, 0.09908696401271366305, -126.3270676136400965 ) ) ;
#88415=CARTESIAN_POINT ( 'NONE',  ( -21.05000000000000071, -11.48912529306490349, -136.9000000000000341 ) ) ;
#88418=ORIENTED_EDGE ( 'NONE', *, *, #30630, .F. ) ;
#88421=FACE_OUTER_BOUND ( 'NONE', #4901, .T. ) ;
#88425=ORIENTED_EDGE ( 'NONE', *, *, #146712, .F. ) ;
#88479=DIRECTION ( 'NONE',  ( -1.000000000000000000, -0.000000000000000000, -0.000000000000000000 ) ) ;
#88517=FACE_OUTER_BOUND ( 'NONE', #137197, .T. ) ;
#88525=VECTOR ( 'NONE', #185105, 1000.000000000000000 ) ;
#88549=DIRECTION ( 'NONE',  ( -1.000000000000000000, 0.000000000000000000, 0.000000000000000000 ) ) ;
#88572=AXIS2_PLACEMENT_3D ( 'NONE', #26891, #148098, #85509 ) ;
#88595=DIRECTION ( 'NONE',  ( 1.000000000000000000, 0.000000000000000000, 0.000000000000000000 ) ) ;
#88604=ORIENTED_EDGE ( 'NONE', *, *, #33601, .F. ) ;
#88607=SHAPE_REPRESENTATION ( 'Injection Molded Chain Links 5', ( #2425 ), #193986 ) ;
#88673=DIRECTION ( 'NONE',  ( -1.836970198721029934E-16, 1.000000000000000000, 0.000000000000000000 ) ) ;
#88705=CARTESIAN_POINT ( 'NONE',  ( 22.16821283564876666, 7.558973340791918183, -134.0000000000000000 ) ) ;
#88710=CARTESIAN_POINT ( 'NONE',  ( -21.29999999999995808, 1.115600667400684642E-11, -134.0000000000000000 ) ) ;
#88764=ORIENTED_EDGE ( 'NONE', *, *, #235884, .F. ) ;
#88838=CARTESIAN_POINT ( 'NONE',  ( 18.49999999999999289, 10.34378108836433263, -158.8284452778770230 ) ) ;
#88859=AXIS2_PLACEMENT_3D ( 'NONE', #26205, #126577, #223096 ) ;
#88873=CARTESIAN_POINT ( 'NONE',  ( -20.54999999999999716, 4.350000000011156054, -150.7500000000000284 ) ) ;
#88916=DIRECTION ( 'NONE',  ( 1.836970198721029934E-16, -1.000000000000000000, -0.000000000000000000 ) ) ;
#88940=FACE_OUTER_BOUND ( 'NONE', #210725, .T. ) ;
#88981=CARTESIAN_POINT ( 'NONE',  ( -21.10257677756355932, 6.398381742543874928, -133.9750492504320221 ) ) ;
#88987=VECTOR ( 'NONE', #94312, 1000.000000000000000 ) ;
#89005=VERTEX_POINT ( 'NONE', #63634 ) ;
#89011=AXIS2_PLACEMENT_3D ( 'NONE', #134380, #154022, #96534 ) ;
#89034=EDGE_CURVE ( 'NONE', #251858, #136324, #160364, .T. ) ;
#89040=DIRECTION ( 'NONE',  ( 1.000000000000000000, -7.304098846218134667E-16, -4.217023435051625732E-16 ) ) ;
#89046=ORIENTED_EDGE ( 'NONE', *, *, #81496, .T. ) ;
#89087=ORIENTED_EDGE ( 'NONE', *, *, #163574, .F. ) ;
#89091=EDGE_CURVE ( 'NONE', #17731, #251883, #221560, .T. ) ;
#89131=CARTESIAN_POINT ( 'NONE',  ( 21.00000000000000000, 9.750000000011153745, -146.2500000000000284 ) ) ;
#89152=FACE_OUTER_BOUND ( 'NONE', #226853, .T. ) ;
#89159=ORIENTED_EDGE ( 'NONE', *, *, #163935, .F. ) ;
#89162=EDGE_LOOP ( 'NONE', ( #231327, #64837, #254022, #201561 ) ) ;
#89229=DIRECTION ( 'NONE',  ( 0.000000000000000000, -0.4999999999999673039, -0.8660254037844573594 ) ) ;
#89240=CIRCLE ( 'NONE', #205771, 0.09999999999999939493 ) ;
#89270=EDGE_LOOP ( 'NONE', ( #215642, #70910, #127743, #62071 ) ) ;
#89292=CARTESIAN_POINT ( 'NONE',  ( -22.59999999999999787, 11.74987124438766273, -133.9345704089863318 ) ) ;
#89303=EDGE_CURVE ( 'NONE', #238843, #251548, #230587, .T. ) ;
#89304=TOROIDAL_SURFACE ( 'NONE', #43542, 11.90000000000000213, 0.1000000000000000056 ) ;
#89320=DIRECTION ( 'NONE',  ( -1.000000000000000000, 0.000000000000000000, 0.000000000000000000 ) ) ;
#89323=DIRECTION ( 'NONE',  ( 1.000000000000000000, 0.000000000000000000, 0.000000000000000000 ) ) ;
#89335=DIRECTION ( 'NONE',  ( 0.000000000000000000, 0.000000000000000000, 1.000000000000000000 ) ) ;
#89341=VECTOR ( 'NONE', #124469, 1000.000000000000000 ) ;
#89343=ORIENTED_EDGE ( 'NONE', *, *, #85305, .F. ) ;
#89383=CARTESIAN_POINT ( 'NONE',  ( 20.94999999999999574, 10.42338541492406279, -141.4920519238701218 ) ) ;
#89411=EDGE_LOOP ( 'NONE', ( #53104, #195543, #117130 ) ) ;
#89432=CIRCLE ( 'NONE', #205969, 6.258578643762724880 ) ;
#89433=LINE ( 'NONE', #96795, #130885 ) ;
#89479=ADVANCED_FACE ( 'NONE', ( #238264 ), #10180, .F. ) ;
#89497=VERTEX_POINT ( 'NONE', #161322 ) ;
#89511=FACE_OUTER_BOUND ( 'NONE', #12513, .T. ) ;
#89512=ADVANCED_FACE ( 'NONE', ( #19227 ), #103870, .T. ) ;
#89580=CARTESIAN_POINT ( 'NONE',  ( -22.50000000000000000, 11.75000000001115552, -134.0000000000000284 ) ) ;
#89584=ORIENTED_EDGE ( 'NONE', *, *, #62914, .T. ) ;
#89589=VERTEX_POINT ( 'NONE', #6067 ) ;
#89596=VECTOR ( 'NONE', #150815, 1000.000000000000000 ) ;
#89634=SPHERICAL_SURFACE ( 'NONE', #253268, 0.1000000000000000056 ) ;
#89641=LINE ( 'NONE', #107935, #130499 ) ;
#89647=DIRECTION ( 'NONE',  ( -0.000000000000000000, -0.1298341882519805091, -0.9915357197604881545 ) ) ;
#89697=EDGE_LOOP ( 'NONE', ( #6087, #64607, #51070, #213244 ) ) ;
#89701=DIRECTION ( 'NONE',  ( 0.000000000000000000, -1.000000000000000000, 0.000000000000000000 ) ) ;
#89732=EDGE_CURVE ( 'NONE', #28264, #41050, #251768, .T. ) ;
#89754=ORIENTED_EDGE ( 'NONE', *, *, #10705, .F. ) ;
#89770=FACE_OUTER_BOUND ( 'NONE', #85053, .T. ) ;
#89790=CARTESIAN_POINT ( 'NONE',  ( -18.59999999999999787, -1.164121893230052995, -175.4148480855716059 ) ) ;
#89813=FACE_OUTER_BOUND ( 'NONE', #57784, .T. ) ;
#89817=FACE_OUTER_BOUND ( 'NONE', #191901, .T. ) ;
#89841=CARTESIAN_POINT ( 'NONE',  ( -20.64999999999999858, -8.999999999988846255, -143.8939691226524644 ) ) ;
#89852=CARTESIAN_POINT ( 'NONE',  ( 18.49999999999999289, 6.650000000011155876, -155.3500000000000227 ) ) ;
#89878=AXIS2_PLACEMENT_3D ( 'NONE', #30440, #29187, #209061 ) ;
#89882=DIRECTION ( 'NONE',  ( 1.000000000000000000, 0.000000000000000000, 0.000000000000000000 ) ) ;
#89896=STYLED_ITEM ( 'NONE', ( #18810 ), #225623 ) ;
#89951=DIRECTION ( 'NONE',  ( -2.827886303505249259E-16, 0.8660254037844412611, 0.4999999999999956701 ) ) ;
#89977=EDGE_CURVE ( 'NONE', #68680, #179358, #209699, .T. ) ;
#89997=ORIENTED_EDGE ( 'NONE', *, *, #98701, .F. ) ;
#90006=EDGE_CURVE ( 'NONE', #44033, #85055, #56113, .T. ) ;
#90055=DIRECTION ( 'NONE',  ( -1.000000000000000000, 0.000000000000000000, 0.000000000000000000 ) ) ;
#90060=AXIS2_PLACEMENT_3D ( 'NONE', #21028, #114965, #15896 ) ;
#90067=CARTESIAN_POINT ( 'NONE',  ( 20.95512820512820440, 8.876151316299269567, -146.1500000000000341 ) ) ;
#90096=TOROIDAL_SURFACE ( 'NONE', #139967, 7.800000000000000711, 0.1000000000000000056 ) ;
#90139=EDGE_CURVE ( 'NONE', #70632, #116539, #99086, .T. ) ;
#90140=CARTESIAN_POINT ( 'NONE',  ( 21.05000000000000071, 6.257814610487280937, -133.9022097086912311 ) ) ;
#90145=VECTOR ( 'NONE', #154712, 1000.000000000000000 ) ;
#90157=DIRECTION ( 'NONE',  ( 0.000000000000000000, 0.000000000000000000, -1.000000000000000000 ) ) ;
#90195=DIRECTION ( 'NONE',  ( 2.952720810173289112E-16, -1.000000000000000000, -0.000000000000000000 ) ) ;
#90196=ORIENTED_EDGE ( 'NONE', *, *, #95897, .F. ) ;
#90218=CYLINDRICAL_SURFACE ( 'NONE', #153392, 11.75000000000001066 ) ;
#90246=FACE_OUTER_BOUND ( 'NONE', #89270, .T. ) ;
#90264=CARTESIAN_POINT ( 'NONE',  ( -21.13614978966382196, 6.499104701844944820, -134.0000000000000284 ) ) ;
#90271=DIRECTION ( 'NONE',  ( -0.7071067811865388020, 0.7071067811865561215, 0.000000000000000000 ) ) ;
#90276=AXIS2_PLACEMENT_3D ( 'NONE', #204821, #26219, #185282 ) ;
#90283=CARTESIAN_POINT ( 'NONE',  ( 20.97250901189795513, 10.62456803371303593, -141.6645457169670124 ) ) ;
#90284=AXIS2_PLACEMENT_3D ( 'NONE', #12274, #91789, #171373 ) ;
#90301=AXIS2_PLACEMENT_3D ( 'NONE', #120600, #237946, #41068 ) ;
#90359=DIRECTION ( 'NONE',  ( 7.304098846218134667E-16, -1.000000000000000000, 0.000000000000000000 ) ) ;
#90401=DIRECTION ( 'NONE',  ( 0.000000000000000000, -1.000000000000000000, 0.000000000000000000 ) ) ;
#90403=FACE_OUTER_BOUND ( 'NONE', #130196, .T. ) ;
#90410=CIRCLE ( 'NONE', #119465, 0.2000000000000005107 ) ;
#90417=CARTESIAN_POINT ( 'NONE',  ( -20.85000000000000142, -1.362429037182151470, -175.3888812479212334 ) ) ;
#90418=ORIENTED_EDGE ( 'NONE', *, *, #213710, .F. ) ;
#90426=VERTEX_POINT ( 'NONE', #51952 ) ;
#90466=ORIENTED_EDGE ( 'NONE', *, *, #57803, .T. ) ;
#90478=TOROIDAL_SURFACE ( 'NONE', #161237, 12.97499999999999787, 0.1000000000000000056 ) ;
#90479=EDGE_CURVE ( 'NONE', #251858, #14355, #14080, .T. ) ;
#90556=ORIENTED_EDGE ( 'NONE', *, *, #254163, .T. ) ;
#90566=( BOUNDED_SURFACE ( )  B_SPLINE_SURFACE ( 3, 2, ( 
 ( #164284, #243805, #224233 ),
 ( #185119, #85981, #15487 ),
 ( #132862, #250225, #110715 ),
 ( #214947, #114570, #54584 ) ),
 .UNSPECIFIED., .F., .F., .T. ) 
 B_SPLINE_SURFACE_WITH_KNOTS ( ( 4, 4 ),
 ( 3, 3 ),
 ( 0.04058434257139457990, 0.04256401539001584966 ),
 ( 0.000000000000000000, 1.000000000000000000 ),
 .UNSPECIFIED. ) 
 GEOMETRIC_REPRESENTATION_ITEM ( )  RATIONAL_B_SPLINE_SURFACE ( (
 ( 1.000000000000000000, 0.7103081912007872534, 1.000000000000000000),
 ( 1.000000000000000000, 0.7104998333556717949, 1.000000000000000000),
 ( 1.000000000000000000, 0.7107238315754015323, 1.000000000000000000),
 ( 1.000000000000000000, 0.7110073749539779220, 1.000000000000000000) ) ) 
 REPRESENTATION_ITEM ( '' )  SURFACE ( )  );
#90577=VECTOR ( 'NONE', #228415, 1000.000000000000000 ) ;
#90583=DIRECTION ( 'NONE',  ( 1.000000000000000000, 0.000000000000000000, 0.000000000000000000 ) ) ;
#90626=EDGE_CURVE ( 'NONE', #116221, #253858, #114188, .T. ) ;
#90635=ORIENTED_EDGE ( 'NONE', *, *, #17661, .T. ) ;
#90663=FACE_OUTER_BOUND ( 'NONE', #248731, .T. ) ;
#90676=CARTESIAN_POINT ( 'NONE',  ( 21.05000000000000071, 1.115649653272650466E-11, -163.5000000000000284 ) ) ;
#90677=CARTESIAN_POINT ( 'NONE',  ( -18.55121869061588669, 10.32747123227773045, -173.0774032850249569 ) ) ;
#90716=DIRECTION ( 'NONE',  ( 0.000000000000000000, 0.000000000000000000, 1.000000000000000000 ) ) ;
#90717=CARTESIAN_POINT ( 'NONE',  ( -20.54999999999999716, 9.350000000011156942, -155.1500000000000057 ) ) ;
#90720=LINE ( 'NONE', #175433, #251578 ) ;
#90742=AXIS2_PLACEMENT_3D ( 'NONE', #59539, #139075, #239507 ) ;
#90760=AXIS2_PLACEMENT_3D ( 'NONE', #48266, #148667, #127816 ) ;
#90762=EDGE_CURVE ( 'NONE', #12568, #82203, #89240, .T. ) ;
#90770=CARTESIAN_POINT ( 'NONE',  ( -22.49806830649814415, 11.64988965485023620, -133.9225356836745107 ) ) ;
#90782=EDGE_CURVE ( 'NONE', #142904, #119168, #130948, .T. ) ;
#90801=CARTESIAN_POINT ( 'NONE',  ( -18.59999999999999787, 1.866714910068465239, -145.7526752462820241 ) ) ;
#90804=ORIENTED_EDGE ( 'NONE', *, *, #104139, .F. ) ;
#90809=AXIS2_PLACEMENT_3D ( 'NONE', #66680, #101916, #43264 ) ;
#90828=EDGE_CURVE ( 'NONE', #173825, #12431, #85117, .T. ) ;
#90852=AXIS2_PLACEMENT_3D ( 'NONE', #87619, #147610, #186759 ) ;
#90855=DIRECTION ( 'NONE',  ( 0.000000000000000000, -1.265107689135680095E-16, 1.000000000000000000 ) ) ;
#90868=VECTOR ( 'NONE', #26525, 1000.000000000000000 ) ;
#90872=AXIS2_PLACEMENT_3D ( 'NONE', #144917, #165809, #22446 ) ;
#90908=DIRECTION ( 'NONE',  ( 0.000000000000000000, 0.000000000000000000, -1.000000000000000000 ) ) ;
#90946=EDGE_CURVE ( 'NONE', #100003, #54863, #218404, .T. ) ;
#90947=FACE_OUTER_BOUND ( 'NONE', #144268, .T. ) ;
#90968=CARTESIAN_POINT ( 'NONE',  ( -21.08134388332232589, 0.07581891751813471525, -127.6653194194820600 ) ) ;
#90997=CARTESIAN_POINT ( 'NONE',  ( 23.25000000000000000, -8.999999999988842703, -157.6060308773475640 ) ) ;
#91030=CARTESIAN_POINT ( 'NONE',  ( 18.59999999999999787, 1.115600667400684642E-11, -134.0000000000000000 ) ) ;
#91066=CARTESIAN_POINT ( 'NONE',  ( -23.25000000000000000, 11.75000000001115552, -167.5000000000000284 ) ) ;
#91096=VERTEX_POINT ( 'NONE', #86610 ) ;
#91115=SPHERICAL_SURFACE ( 'NONE', #225974, 0.1000000000000000056 ) ;
#91128=VERTEX_POINT ( 'NONE', #248285 ) ;
#91142=AXIS2_PLACEMENT_3D ( 'NONE', #21316, #23885, #239050 ) ;
#91146=CIRCLE ( 'NONE', #120410, 0.09999999999999939493 ) ;
#91167=CARTESIAN_POINT ( 'NONE',  ( 20.85000000000000142, 6.933893972137497030, -171.2856458343736108 ) ) ;
#91183=CARTESIAN_POINT ( 'NONE',  ( 18.52130828395271678, -9.481395502614628157, -141.0245067238836327 ) ) ;
#91197=AXIS2_PLACEMENT_3D ( 'NONE', #105534, #2609, #5156 ) ;
#91206=EDGE_CURVE ( 'NONE', #44801, #257362, #152012, .T. ) ;
#91213=DIRECTION ( 'NONE',  ( 0.000000000000000000, 0.9908441862701782288, -0.1350103645450542456 ) ) ;
#91229=( BOUNDED_SURFACE ( )  B_SPLINE_SURFACE ( 3, 2, ( 
 ( #64784, #223847, #45227 ),
 ( #85596, #165178, #106453 ),
 ( #86896, #127335, #206872 ),
 ( #107766, #75096, #193732 ),
 ( #154634, #15099, #234127 ),
 ( #132471, #94614, #112910 ),
 ( #131176, #153365, #210722 ),
 ( #150751, #171630, #54206 ),
 ( #133745, #214562, #12545 ),
 ( #11243, #35952, #213276 ) ),
 .UNSPECIFIED., .F., .F., .F. ) 
 B_SPLINE_SURFACE_WITH_KNOTS ( ( 4, 2, 2, 2, 4 ),
 ( 3, 3 ),
 ( 0.0001701955120502345899, 0.0002247052511886165759, 0.0002792149903269985889, 0.0003882344686037626151, 0.0006062734251572906132 ),
 ( 0.000000000000000000, 1.000000000000000000 ),
 .UNSPECIFIED. ) 
 GEOMETRIC_REPRESENTATION_ITEM ( )  RATIONAL_B_SPLINE_SURFACE ( (
 ( 1.000000000000000000, 0.2966190024560962923, 1.000000000000000000),
 ( 1.000000000000000000, 0.2964522492709221746, 1.000000000000000000),
 ( 1.000000000000000000, 0.3059923531885490600, 1.000000000000000000),
 ( 1.000000000000000000, 0.3355751146947310581, 1.000000000000000000),
 ( 1.000000000000000000, 0.3550672384961548467, 1.000000000000000000),
 ( 1.000000000000000000, 0.4157034672184251600, 1.000000000000000000),
 ( 1.000000000000000000, 0.4588031877658517166, 1.000000000000000000),
 ( 1.000000000000000000, 0.5771441759652446990, 1.000000000000000000),
 ( 1.000000000000000000, 0.6469377121778305817, 1.000000000000000000),
 ( 1.000000000000000000, 0.7071067811865524577, 1.000000000000000000) ) ) 
 REPRESENTATION_ITEM ( '' )  SURFACE ( )  );
#91237=ORIENTED_EDGE ( 'NONE', *, *, #145676, .T. ) ;
#91284=AXIS2_PLACEMENT_3D ( 'NONE', #98697, #177028, #134010 ) ;
#91365=DIRECTION ( 'NONE',  ( 0.000000000000000000, 2.891205793294679805E-16, -1.000000000000000000 ) ) ;
#91399=EDGE_CURVE ( 'NONE', #236473, #43709, #147894, .T. ) ;
#91408=CARTESIAN_POINT ( 'NONE',  ( 21.04999999999999716, 10.68430915749623367, -141.5266967903268664 ) ) ;
#91473=DIRECTION ( 'NONE',  ( -0.000000000000000000, -0.000000000000000000, 1.000000000000000000 ) ) ;
#91510=DIRECTION ( 'NONE',  ( 1.000000000000000000, 0.000000000000000000, 0.000000000000000000 ) ) ;
#91514=ORIENTED_EDGE ( 'NONE', *, *, #249128, .F. ) ;
#91532=ORIENTED_EDGE ( 'NONE', *, *, #186012, .F. ) ;
#91551=DIRECTION ( 'NONE',  ( 1.000000000000000000, 0.000000000000000000, -0.000000000000000000 ) ) ;
#91564=VECTOR ( 'NONE', #184638, 1000.000000000000000 ) ;
#91569=CARTESIAN_POINT ( 'NONE',  ( 20.94999999999999929, 10.29270135741298731, -172.9573618871519329 ) ) ;
#91577=DIRECTION ( 'NONE',  ( 1.734723475976817507E-14, 0.000000000000000000, -1.000000000000000000 ) ) ;
#91594=DIRECTION ( 'NONE',  ( 0.000000000000000000, 0.000000000000000000, -1.000000000000000000 ) ) ;
#91601=VERTEX_POINT ( 'NONE', #216212 ) ;
#91654=EDGE_CURVE ( 'NONE', #217170, #92859, #60386, .T. ) ;
#91663=ORIENTED_EDGE ( 'NONE', *, *, #189185, .T. ) ;
#91672=VECTOR ( 'NONE', #72190, 999.9999999999998863 ) ;
#91680=FACE_OUTER_BOUND ( 'NONE', #216612, .T. ) ;
#91682=DIRECTION ( 'NONE',  ( -1.000000000000000000, 0.000000000000000000, 0.000000000000000000 ) ) ;
#91688=AXIS2_PLACEMENT_3D ( 'NONE', #85868, #205848, #187594 ) ;
#91699=( BOUNDED_SURFACE ( )  B_SPLINE_SURFACE ( 3, 2, ( 
 ( #133852, #93431, #36054 ),
 ( #56848, #215942, #213381 ),
 ( #32212, #174320, #33519 ),
 ( #196388, #114289, #95994 ) ),
 .UNSPECIFIED., .F., .F., .F. ) 
 B_SPLINE_SURFACE_WITH_KNOTS ( ( 4, 4 ),
 ( 3, 3 ),
 ( 1.040834085586084257E-17, 0.001979672783031562362 ),
 ( 0.000000000000000000, 1.000000000000000000 ),
 .UNSPECIFIED. ) 
 GEOMETRIC_REPRESENTATION_ITEM ( )  RATIONAL_B_SPLINE_SURFACE ( (
 ( 1.000000000000000000, 0.7103081912008197829, 1.000000000000000000),
 ( 1.000000000000000000, 0.7104998333558716350, 1.000000000000000000),
 ( 1.000000000000000000, 0.7107238315755427527, 1.000000000000000000),
 ( 1.000000000000000000, 0.7110073749539292942, 1.000000000000000000) ) ) 
 REPRESENTATION_ITEM ( '' )  SURFACE ( )  );
#91724=CARTESIAN_POINT ( 'NONE',  ( -20.00857864376270001, 9.250000000011157297, -146.3500000000000227 ) ) ;
#91733=VERTEX_POINT ( 'NONE', #83089 ) ;
#91738=VECTOR ( 'NONE', #240109, 1000.000000000000114 ) ;
#91750=AXIS2_PLACEMENT_3D ( 'NONE', #223863, #21840, #45247 ) ;
#91789=DIRECTION ( 'NONE',  ( 0.000000000000000000, 0.9998779222360096863, -0.01562500000001061998 ) ) ;
#91812=VERTEX_POINT ( 'NONE', #226468 ) ;
#91864=CARTESIAN_POINT ( 'NONE',  ( 18.59999999999999076, 1.835341550235567887, -145.5551512925629822 ) ) ;
#91884=ORIENTED_EDGE ( 'NONE', *, *, #228711, .F. ) ;
#91895=ORIENTED_EDGE ( 'NONE', *, *, #115109, .T. ) ;
#91897=CARTESIAN_POINT ( 'NONE',  ( -20.94999999999999929, -1.360870587180885716, -142.0729979270909951 ) ) ;
#91961=DIRECTION ( 'NONE',  ( 0.000000000000000000, 0.008583690987124100932, -0.9999631594459055250 ) ) ;
#91973=CARTESIAN_POINT ( 'NONE',  ( 20.94999999999999929, 5.000000000011153745, -155.0947339810869323 ) ) ;
#91974=CARTESIAN_POINT ( 'NONE',  ( 21.59780538579342490, 0.09897866960914131207, -127.1529094700567839 ) ) ;
#91981=ORIENTED_EDGE ( 'NONE', *, *, #116819, .T. ) ;
#92006=CARTESIAN_POINT ( 'NONE',  ( -18.42554971533678199, -9.497159669426588735, -141.0398269135486942 ) ) ;
#92048=CARTESIAN_POINT ( 'NONE',  ( 18.46905048506370406, -9.473744257371240707, -174.1759862922554873 ) ) ;
#92061=ORIENTED_EDGE ( 'NONE', *, *, #180184, .T. ) ;
#92094=VERTEX_POINT ( 'NONE', #99787 ) ;
#92107=CARTESIAN_POINT ( 'NONE',  ( -23.25000000000000000, 1.115600667400684642E-11, -167.5000000000000284 ) ) ;
#92142=VERTEX_POINT ( 'NONE', #140203 ) ;
#92149=DIRECTION ( 'NONE',  ( -1.000000000000000000, -0.000000000000000000, -0.000000000000000000 ) ) ;
#92155=DIRECTION ( 'NONE',  ( -1.000000000000000000, 0.000000000000000000, 0.000000000000000000 ) ) ;
#92173=DIRECTION ( 'NONE',  ( -7.304098846218134667E-16, -1.000000000000000000, 0.000000000000000000 ) ) ;
#92183=DIRECTION ( 'NONE',  ( 0.000000000000000000, 0.9915357197604971473, -0.1298341882519111479 ) ) ;
#92203=CYLINDRICAL_SURFACE ( 'NONE', #136617, 0.1000000000000098310 ) ;
#92212=DIRECTION ( 'NONE',  ( 1.000000000000000000, -0.000000000000000000, -0.000000000000000000 ) ) ;
#92222=CARTESIAN_POINT ( 'NONE',  ( -20.94999999999999929, 1.115600667400684642E-11, -167.5000000000000284 ) ) ;
#92228=CARTESIAN_POINT ( 'NONE',  ( 23.14999999999998437, 1.115600667400684642E-11, -134.0000000000000000 ) ) ;
#92292=ORIENTED_EDGE ( 'NONE', *, *, #60502, .T. ) ;
#92309=VECTOR ( 'NONE', #76862, 1000.000000000000000 ) ;
#92382=DIRECTION ( 'NONE',  ( -7.304098846218134667E-16, -1.000000000000000000, 0.000000000000000000 ) ) ;
#92400=ORIENTED_EDGE ( 'NONE', *, *, #132380, .F. ) ;
#92402=ADVANCED_FACE ( 'NONE', ( #134762 ), #169129, .F. ) ;
#92419=DIRECTION ( 'NONE',  ( -1.000000000000000000, 0.000000000000000000, 0.000000000000000000 ) ) ;
#92430=CARTESIAN_POINT ( 'NONE',  ( 20.94999999999999574, -1.736257131586239844, -145.5686523290175387 ) ) ;
#92438=AXIS2_PLACEMENT_3D ( 'NONE', #123888, #1340, #125172 ) ;
#92488=CIRCLE ( 'NONE', #234132, 0.1999999999999996503 ) ;
#92525=CARTESIAN_POINT ( 'NONE',  ( -20.54999999999999716, 4.250000000011156409, -146.2500000000000284 ) ) ;
#92533=DIRECTION ( 'NONE',  ( -0.000000000000000000, 1.000000000000000000, 0.000000000000000000 ) ) ;
#92550=ORIENTED_EDGE ( 'NONE', *, *, #122202, .T. ) ;
#92556=DIRECTION ( 'NONE',  ( 1.000000000000000000, 0.000000000000000000, -0.000000000000000000 ) ) ;
#92591=LINE ( 'NONE', #150033, #235782 ) ;
#92596=DIRECTION ( 'NONE',  ( -1.000000000000000000, -2.952720810173289112E-16, 0.000000000000000000 ) ) ;
#92636=ORIENTED_EDGE ( 'NONE', *, *, #105928, .T. ) ;
#92661=AXIS2_PLACEMENT_3D ( 'NONE', #194973, #175417, #155845 ) ;
#92679=CARTESIAN_POINT ( 'NONE',  ( 21.05000000000000071, 8.926614585098249677, -142.4716830192231214 ) ) ;
#92684=CARTESIAN_POINT ( 'NONE',  ( 18.59999999999999076, 6.450000000011156587, -155.2500000000000284 ) ) ;
#92695=ORIENTED_EDGE ( 'NONE', *, *, #157097, .T. ) ;
#92719=DIRECTION ( 'NONE',  ( 0.000000000000000000, 0.000000000000000000, -1.000000000000000000 ) ) ;
#92757=CIRCLE ( 'NONE', #255007, 0.1000000000000002554 ) ;
#92824=ORIENTED_EDGE ( 'NONE', *, *, #76075, .T. ) ;
#92844=CARTESIAN_POINT ( 'NONE',  ( 21.05000000000000071, 5.400000000011154988, -155.0947339810869323 ) ) ;
#92852=FACE_OUTER_BOUND ( 'NONE', #163448, .T. ) ;
#92859=VERTEX_POINT ( 'NONE', #20753 ) ;
#92918=ORIENTED_EDGE ( 'NONE', *, *, #194473, .T. ) ;
#92931=VECTOR ( 'NONE', #140125, 1000.000000000000000 ) ;
#92932=ORIENTED_EDGE ( 'NONE', *, *, #126776, .F. ) ;
#92937=EDGE_CURVE ( 'NONE', #62775, #76541, #187533, .T. ) ;
#92955=LINE ( 'NONE', #192083, #28466 ) ;
#92958=FACE_OUTER_BOUND ( 'NONE', #23153, .T. ) ;
#92978=ADVANCED_FACE ( 'NONE', ( #145800 ), #252835, .T. ) ;
#93044=AXIS2_PLACEMENT_3D ( 'NONE', #85712, #2349, #183578 ) ;
#93049=CARTESIAN_POINT ( 'NONE',  ( -20.85000000000000142, -11.64999999998884483, -164.6000000000000227 ) ) ;
#93050=ORIENTED_EDGE ( 'NONE', *, *, #105230, .F. ) ;
#93054=LINE ( 'NONE', #228739, #87987 ) ;
#93061=VECTOR ( 'NONE', #126706, 1000.000000000000000 ) ;
#93068=EDGE_CURVE ( 'NONE', #105943, #149376, #11455, .T. ) ;
#93081=CARTESIAN_POINT ( 'NONE',  ( 21.05000000000000071, 6.304516329275452691, -134.0211033080591960 ) ) ;
#93101=DIRECTION ( 'NONE',  ( 0.000000000000000000, 0.000000000000000000, -1.000000000000000000 ) ) ;
#93103=DIRECTION ( 'NONE',  ( 0.000000000000000000, 0.000000000000000000, -1.000000000000000000 ) ) ;
#93117=CARTESIAN_POINT ( 'NONE',  ( -18.59999999999999787, 1.250000000011155299, -142.0000000000000284 ) ) ;
#93152=EDGE_CURVE ( 'NONE', #253265, #146973, #94805, .T. ) ;
#93154=AXIS2_PLACEMENT_3D ( 'NONE', #7926, #187855, #168317 ) ;
#93155=CYLINDRICAL_SURFACE ( 'NONE', #185153, 0.09999999999998898659 ) ;
#93161=ORIENTED_EDGE ( 'NONE', *, *, #85305, .T. ) ;
#93164=VECTOR ( 'NONE', #81705, 1000.000000000000000 ) ;
#93181=CARTESIAN_POINT ( 'NONE',  ( -20.07928932188135107, 9.220710678129810489, -155.2500000000000284 ) ) ;
#93185=AXIS2_PLACEMENT_3D ( 'NONE', #216415, #75650, #135580 ) ;
#93210=EDGE_CURVE ( 'NONE', #184016, #39881, #15548, .T. ) ;
#93231=DIRECTION ( 'NONE',  ( 0.000000000000000000, 0.6728971962617388280, 0.7397360091702248619 ) ) ;
#93240=DIRECTION ( 'NONE',  ( 0.000000000000000000, -0.9999631594459056361, -0.008583690987124413183 ) ) ;
#93289=ADVANCED_FACE ( 'NONE', ( #137783 ), #16595, .F. ) ;
#93290=CARTESIAN_POINT ( 'NONE',  ( -18.41353343127311604, -9.499999999988851584, -141.0320693966997396 ) ) ;
#93291=DIRECTION ( 'NONE',  ( -1.000000000000000000, 0.000000000000000000, 0.000000000000000000 ) ) ;
#93330=DIRECTION ( 'NONE',  ( 0.000000000000000000, 0.000000000000000000, -1.000000000000000000 ) ) ;
#93401=VECTOR ( 'NONE', #166000, 999.9999999999998863 ) ;
#93431=CARTESIAN_POINT ( 'NONE',  ( -22.47007471830799119, 1.115783626517291571E-11, -126.2792893480735330 ) ) ;
#93436=ORIENTED_EDGE ( 'NONE', *, *, #17685, .T. ) ;
#93469=CARTESIAN_POINT ( 'NONE',  ( -20.54999999999999716, 7.150000000011155876, -155.1500000000000057 ) ) ;
#93478=VERTEX_POINT ( 'NONE', #154528 ) ;
#93512=FACE_OUTER_BOUND ( 'NONE', #79385, .T. ) ;
#93527=AXIS2_PLACEMENT_3D ( 'NONE', #215568, #232602, #34399 ) ;
#93537=( BOUNDED_CURVE ( )  B_SPLINE_CURVE ( 3, ( #170072, #31830, #69657, #112623 ),
 .UNSPECIFIED., .F., .T. ) 
 B_SPLINE_CURVE_WITH_KNOTS ( ( 4, 4 ),
 ( 0.06456096931748307732, 3.077031684272310219 ),
 .UNSPECIFIED. ) 
 CURVE ( )  GEOMETRIC_REPRESENTATION_ITEM ( )  RATIONAL_B_SPLINE_CURVE ( ( 1.000000000000000000, 0.3763440860215093164, 0.3763440860215093164, 1.000000000000000000 ) ) 
 REPRESENTATION_ITEM ( '' )  );
#93549=CARTESIAN_POINT ( 'NONE',  ( -21.05000000000000071, 6.540656951712400691, -134.1000000000000227 ) ) ;
#93550=DIRECTION ( 'NONE',  ( 0.000000000000000000, -1.000000000000000000, -1.734723475976807292E-15 ) ) ;
#93555=ADVANCED_FACE ( 'NONE', ( #208065, #54096 ), #13688, .F. ) ;
#93570=ORIENTED_EDGE ( 'NONE', *, *, #200873, .T. ) ;
#93571=ADVANCED_FACE ( 'NONE', ( #131069 ), #111514, .F. ) ;
#93600=EDGE_CURVE ( 'NONE', #46556, #30259, #248950, .T. ) ;
#93603=EDGE_LOOP ( 'NONE', ( #219851, #61000, #116128, #186312 ) ) ;
#93609=DIRECTION ( 'NONE',  ( -1.000000000000000000, -0.000000000000000000, -0.000000000000000000 ) ) ;
#93622=ORIENTED_EDGE ( 'NONE', *, *, #82563, .F. ) ;
#93625=CARTESIAN_POINT ( 'NONE',  ( -21.14999999999999858, 1.115600667400684642E-11, -122.3504291924552234 ) ) ;
#93653=CARTESIAN_POINT ( 'NONE',  ( 21.05000000000000071, 1.115600667400684642E-11, -167.5000000000000284 ) ) ;
#93665=TOROIDAL_SURFACE ( 'NONE', #143555, 0.2000000000000000111, 0.1000000000000000056 ) ;
#93692=ADVANCED_FACE ( 'NONE', ( #196183 ), #237876, .T. ) ;
#93721=FACE_OUTER_BOUND ( 'NONE', #96809, .T. ) ;
#93808=CARTESIAN_POINT ( 'NONE',  ( -22.39999999999999858, -0.1008583690875579364, -122.2504328765106294 ) ) ;
#93829=DIRECTION ( 'NONE',  ( -0.000000000000000000, 1.000000000000000000, -1.224646799147352961E-16 ) ) ;
#93867=AXIS2_PLACEMENT_3D ( 'NONE', #20019, #77384, #156966 ) ;
#93874=AXIS2_PLACEMENT_3D ( 'NONE', #20277, #222280, #238016 ) ;
#93877=EDGE_CURVE ( 'NONE', #73136, #154872, #124051, .T. ) ;
#93908=CARTESIAN_POINT ( 'NONE',  ( -23.25000000000000000, 1.115600667400684642E-11, -167.5000000000000284 ) ) ;
#93910=DIRECTION ( 'NONE',  ( 0.000000000000000000, 0.000000000000000000, 1.000000000000000000 ) ) ;
#93941=CIRCLE ( 'NONE', #218822, 0.1999999999999987899 ) ;
#93965=CARTESIAN_POINT ( 'NONE',  ( -20.94999999999999929, 1.750000000011155743, -145.6695115579016715 ) ) ;
#93970=CARTESIAN_POINT ( 'NONE',  ( -20.54999999999999361, 11.65000000001115232, -155.3500000000000227 ) ) ;
#93982=DIRECTION ( 'NONE',  ( 0.000000000000000000, -4.163336342344333240E-14, -1.000000000000000000 ) ) ;
#93996=ORIENTED_EDGE ( 'NONE', *, *, #112672, .F. ) ;
#94048=VECTOR ( 'NONE', #10277, 1000.000000000000000 ) ;
#94059=ORIENTED_EDGE ( 'NONE', *, *, #82288, .F. ) ;
#94096=EDGE_CURVE ( 'NONE', #251548, #73136, #66644, .T. ) ;
#94099=VERTEX_POINT ( 'NONE', #45788 ) ;
#94109=EDGE_LOOP ( 'NONE', ( #192686, #229773, #114418, #168366 ) ) ;
#94122=VERTEX_POINT ( 'NONE', #240150 ) ;
#94127=CARTESIAN_POINT ( 'NONE',  ( 21.08479644141221954, 0.05855444257531394053, -127.6549613422681375 ) ) ;
#94139=CIRCLE ( 'NONE', #69227, 11.65000000000000036 ) ;
#94175=CARTESIAN_POINT ( 'NONE',  ( -23.15000000000000213, 1.115600667400684642E-11, -134.0000000000000000 ) ) ;
#94209=VECTOR ( 'NONE', #38862, 999.9999999999998863 ) ;
#94248=DIRECTION ( 'NONE',  ( -1.000000000000000000, 0.000000000000000000, 0.000000000000000000 ) ) ;
#94259=CARTESIAN_POINT ( 'NONE',  ( 18.59999999999999076, 11.65000000001115943, -167.5000000000000284 ) ) ;
#94286=ORIENTED_EDGE ( 'NONE', *, *, #229133, .T. ) ;
#94299=CARTESIAN_POINT ( 'NONE',  ( 21.05000000000000071, 10.72371710471867701, -146.1500000000000341 ) ) ;
#94312=DIRECTION ( 'NONE',  ( -1.000000000000000000, -1.836970198721029934E-16, 0.000000000000000000 ) ) ;
#94349=CIRCLE ( 'NONE', #77775, 0.09999999999998898659 ) ;
#94354=( BOUNDED_SURFACE ( )  B_SPLINE_SURFACE ( 3, 2, ( 
 ( #4712, #23043, #146790 ),
 ( #123403, #222472, #86818 ),
 ( #84210, #205491, #244620 ),
 ( #163821, #166412, #25594 ),
 ( #202932, #3436, #201649 ),
 ( #102513, #182100, #45144 ),
 ( #85516, #162548, #105075 ),
 ( #81665, #206789, #184647 ),
 ( #65991, #225042, #46415 ),
 ( #242054, #47696, #125953 ) ),
 .UNSPECIFIED., .F., .F., .F. ) 
 B_SPLINE_SURFACE_WITH_KNOTS ( ( 4, 2, 2, 2, 4 ),
 ( 3, 3 ),
 ( 0.0001836757140119304782, 0.0004000170051583701661, 0.0005081876507315899287, 0.0005622729735181998100, 0.0006163582963048097997 ),
 ( 0.000000000000000000, 1.000000000000000000 ),
 .UNSPECIFIED. ) 
 GEOMETRIC_REPRESENTATION_ITEM ( )  RATIONAL_B_SPLINE_SURFACE ( (
 ( 1.000000000000000000, 0.7071067811866005304, 1.000000000000000000),
 ( 1.000000000000000000, 0.6461995200062370381, 1.000000000000000000),
 ( 1.000000000000000000, 0.5776453529505152229, 1.000000000000000000),
 ( 1.000000000000000000, 0.4585233068373967824, 1.000000000000000000),
 ( 1.000000000000000000, 0.4154092989939170422, 1.000000000000000000),
 ( 1.000000000000000000, 0.3550093145836495379, 1.000000000000000000),
 ( 1.000000000000000000, 0.3354498651689102329, 1.000000000000000000),
 ( 1.000000000000000000, 0.3060347992252177574, 1.000000000000000000),
 ( 1.000000000000000000, 0.2963555829630397653, 1.000000000000000000),
 ( 1.000000000000000000, 0.2966190024560962923, 1.000000000000000000) ) ) 
 REPRESENTATION_ITEM ( '' )  SURFACE ( )  );
#94371=ORIENTED_EDGE ( 'NONE', *, *, #129588, .T. ) ;
#94401=EDGE_CURVE ( 'NONE', #47453, #91812, #253565, .T. ) ;
#94410=DIRECTION ( 'NONE',  ( -1.000000000000000000, -0.000000000000000000, -0.000000000000000000 ) ) ;
#94418=EDGE_CURVE ( 'NONE', #113685, #11797, #101573, .T. ) ;
#94452=CYLINDRICAL_SURFACE ( 'NONE', #235996, 0.09999999999999939493 ) ;
#94513=CARTESIAN_POINT ( 'NONE',  ( 21.12802099929860944, 8.780552590233368093, -146.2481899849316278 ) ) ;
#94573=CARTESIAN_POINT ( 'NONE',  ( -21.12642695952773764, 6.375659922046319927, -133.9010967168106276 ) ) ;
#94614=CARTESIAN_POINT ( 'NONE',  ( 18.33996824403499915, -9.569639859420224326, -174.3190656375171841 ) ) ;
#94625=CARTESIAN_POINT ( 'NONE',  ( -20.64999999999999858, 1.115600667400684642E-11, -165.5000000000000284 ) ) ;
#94649=FACE_OUTER_BOUND ( 'NONE', #99513, .T. ) ;
#94659=EDGE_CURVE ( 'NONE', #216916, #201029, #227867, .T. ) ;
#94662=AXIS2_PLACEMENT_3D ( 'NONE', #66780, #146305, #8099 ) ;
#94680=FACE_OUTER_BOUND ( 'NONE', #199228, .T. ) ;
#94702=ORIENTED_EDGE ( 'NONE', *, *, #78337, .T. ) ;
#94750=CIRCLE ( 'NONE', #78181, 11.80000000000000426 ) ;
#94772=DIRECTION ( 'NONE',  ( 0.000000000000000000, 0.000000000000000000, -1.000000000000000000 ) ) ;
#94792=CARTESIAN_POINT ( 'NONE',  ( 21.05000000000000071, 10.72371710471867701, -134.0000000000000000 ) ) ;
#94793=CARTESIAN_POINT ( 'NONE',  ( -18.59999999999999787, 1.750000000011155743, -145.6695115579016715 ) ) ;
#94805=CIRCLE ( 'NONE', #190524, 12.97499999999998721 ) ;
#94852=CIRCLE ( 'NONE', #90742, 0.09999999999999062417 ) ;
#94859=CYLINDRICAL_SURFACE ( 'NONE', #216831, 0.09999999999999939493 ) ;
#94875=EDGE_LOOP ( 'NONE', ( #183144, #75996, #14493, #198352 ) ) ;
#94889=TOROIDAL_SURFACE ( 'NONE', #190600, 3.899999999999999467, 0.1000000000000000056 ) ;
#94908=AXIS2_PLACEMENT_3D ( 'NONE', #257524, #238014, #663 ) ;
#94973=CONICAL_SURFACE ( 'NONE', #240731, 4.049999999999998046, 0.7853981633974604915 ) ;
#95001=CARTESIAN_POINT ( 'NONE',  ( -18.39999999999999858, -9.399999999988850163, -122.2500000000000284 ) ) ;
#95018=CIRCLE ( 'NONE', #174174, 12.77500000000000036 ) ;
#95033=DIRECTION ( 'NONE',  ( -0.000000000000000000, -0.000000000000000000, -1.000000000000000000 ) ) ;
#95036=CIRCLE ( 'NONE', #107503, 0.5000000000000004441 ) ;
#95062=EDGE_CURVE ( 'NONE', #93478, #180230, #145034, .T. ) ;
#95076=CARTESIAN_POINT ( 'NONE',  ( 20.94999999999999929, -8.663551401858002876, -143.5241011180673070 ) ) ;
#95091=CARTESIAN_POINT ( 'NONE',  ( 18.59999999999997655, 1.115600667400684642E-11, -167.5000000000000284 ) ) ;
#95114=ADVANCED_FACE ( 'NONE', ( #254585 ), #160682, .T. ) ;
#95174=DIRECTION ( 'NONE',  ( 0.000000000000000000, 0.000000000000000000, -1.000000000000000000 ) ) ;
#95189=ADVANCED_FACE ( 'NONE', ( #40740 ), #253189, .T. ) ;
#95190=FACE_OUTER_BOUND ( 'NONE', #137395, .T. ) ;
#95199=LINE ( 'NONE', #13109, #71454 ) ;
#95201=EDGE_CURVE ( 'NONE', #246321, #221635, #62832, .T. ) ;
#95209=EDGE_CURVE ( 'NONE', #244686, #142904, #28380, .T. ) ;
#95251=DIRECTION ( 'NONE',  ( 0.000000000000000000, 0.000000000000000000, 1.000000000000000000 ) ) ;
#95252=EDGE_LOOP ( 'NONE', ( #225272, #218665, #77820, #125919 ) ) ;
#95296=ADVANCED_FACE ( 'NONE', ( #4134 ), #94973, .F. ) ;
#95323=VERTEX_POINT ( 'NONE', #151378 ) ;
#95399=EDGE_CURVE ( 'NONE', #106067, #169023, #249300, .T. ) ;
#95425=AXIS2_PLACEMENT_3D ( 'NONE', #20673, #169828, #178471 ) ;
#95443=DIRECTION ( 'NONE',  ( 0.000000000000000000, 0.000000000000000000, 1.000000000000000000 ) ) ;
#95478=VECTOR ( 'NONE', #66046, 1000.000000000000000 ) ;
#95548=CIRCLE ( 'NONE', #195536, 0.09999999999998898659 ) ;
#95559=DIRECTION ( 'NONE',  ( 0.000000000000000000, -0.9915357197604971473, 0.1298341882519111479 ) ) ;
#95614=CARTESIAN_POINT ( 'NONE',  ( 20.95512840106819752, 10.62384869378447583, -146.2024792207988924 ) ) ;
#95627=TOROIDAL_SURFACE ( 'NONE', #83124, 0.2000000000000000111, 0.1000000000000000056 ) ;
#95648=CARTESIAN_POINT ( 'NONE',  ( 21.09096482362069835, 6.363544365415761739, -133.9605517212259542 ) ) ;
#95649=ORIENTED_EDGE ( 'NONE', *, *, #169480, .F. ) ;
#95653=ORIENTED_EDGE ( 'NONE', *, *, #200460, .T. ) ;
#95660=FACE_OUTER_BOUND ( 'NONE', #49891, .T. ) ;
#95672=ORIENTED_EDGE ( 'NONE', *, *, #164694, .T. ) ;
#95683=LINE ( 'NONE', #93117, #13829 ) ;
#95693=EDGE_CURVE ( 'NONE', #150597, #135871, #209745, .T. ) ;
#95694=DIRECTION ( 'NONE',  ( 0.000000000000000000, -1.000000000000000000, 0.000000000000000000 ) ) ;
#95754=CARTESIAN_POINT ( 'NONE',  ( 20.04142135623730070, 11.75000000001115907, -155.3500000000000227 ) ) ;
#95767=EDGE_CURVE ( 'NONE', #232714, #13799, #137044, .T. ) ;
#95786=DIRECTION ( 'NONE',  ( 0.000000000000000000, 0.7397360091702755991, -0.6728971962616832059 ) ) ;
#95788=CARTESIAN_POINT ( 'NONE',  ( 21.06600267594171783, 8.775166069211060460, -146.2042627823747409 ) ) ;
#95810=CIRCLE ( 'NONE', #16747, 0.09999999999998898659 ) ;
#95811=FACE_OUTER_BOUND ( 'NONE', #23651, .T. ) ;
#95814=CYLINDRICAL_SURFACE ( 'NONE', #239125, 0.09999999999998898659 ) ;
#95816=FACE_OUTER_BOUND ( 'NONE', #76992, .T. ) ;
#95818=CARTESIAN_POINT ( 'NONE',  ( -22.57848426163147693, -0.004264329271961140103, -122.2499416931096619 ) ) ;
#95820=DIRECTION ( 'NONE',  ( -1.000000000000000000, 0.000000000000000000, 0.000000000000000000 ) ) ;
#95825=DIRECTION ( 'NONE',  ( 0.000000000000000000, -1.000000000000000000, 0.000000000000000000 ) ) ;
#95837=ORIENTED_EDGE ( 'NONE', *, *, #123579, .T. ) ;
#95840=AXIS2_PLACEMENT_3D ( 'NONE', #195875, #120208, #81019 ) ;
#95858=ORIENTED_EDGE ( 'NONE', *, *, #168853, .F. ) ;
#95880=EDGE_CURVE ( 'NONE', #129556, #241225, #232925, .T. ) ;
#95897=EDGE_CURVE ( 'NONE', #226140, #222619, #97458, .T. ) ;
#95900=AXIS2_PLACEMENT_3D ( 'NONE', #182287, #21928, #181006 ) ;
#95907=DIRECTION ( 'NONE',  ( 0.000000000000000000, 0.000000000000000000, -1.000000000000000000 ) ) ;
#95912=DIRECTION ( 'NONE',  ( -0.000000000000000000, 1.000000000000000000, -0.000000000000000000 ) ) ;
#95932=ORIENTED_EDGE ( 'NONE', *, *, #188464, .F. ) ;
#95974=CARTESIAN_POINT ( 'NONE',  ( -20.99551997958390714, 11.75000000001129052, -160.6516591376896201 ) ) ;
#95975=AXIS2_PLACEMENT_3D ( 'NONE', #215561, #59023, #257210 ) ;
#95988=VERTEX_POINT ( 'NONE', #161333 ) ;
#95993=VERTEX_POINT ( 'NONE', #45213 ) ;
#95994=CARTESIAN_POINT ( 'NONE',  ( -21.00023020733502577, 1.115539681028482333E-11, -127.6091307547316518 ) ) ;
#96000=ORIENTED_EDGE ( 'NONE', *, *, #111258, .F. ) ;
#96002=FACE_OUTER_BOUND ( 'NONE', #255714, .T. ) ;
#96049=CARTESIAN_POINT ( 'NONE',  ( 20.95052659398289308, 10.47982436779105875, -141.5752387558655983 ) ) ;
#96050=ORIENTED_EDGE ( 'NONE', *, *, #30530, .F. ) ;
#96079=ORIENTED_EDGE ( 'NONE', *, *, #148192, .T. ) ;
#96085=ORIENTED_EDGE ( 'NONE', *, *, #228913, .T. ) ;
#96096=LINE ( 'NONE', #255131, #62475 ) ;
#96100=ORIENTED_EDGE ( 'NONE', *, *, #62140, .F. ) ;
#96102=CARTESIAN_POINT ( 'NONE',  ( -21.04999999999999361, 6.300179817925542380, -133.9485171181182466 ) ) ;
#96104=VERTEX_POINT ( 'NONE', #30816 ) ;
#96115=ORIENTED_EDGE ( 'NONE', *, *, #223309, .T. ) ;
#96133=DIRECTION ( 'NONE',  ( 1.000000000000000000, 0.000000000000000000, -0.000000000000000000 ) ) ;
#96153=DIRECTION ( 'NONE',  ( -0.000000000000000000, -1.000000000000000000, 6.308085367188393199E-16 ) ) ;
#96162=SPHERICAL_SURFACE ( 'NONE', #54817, 0.1000000000000000056 ) ;
#96183=DIRECTION ( 'NONE',  ( 7.589415207398576792E-15, -1.000000000000000000, -0.000000000000000000 ) ) ;
#96186=VECTOR ( 'NONE', #8663, 1000.000000000000000 ) ;
#96210=EDGE_CURVE ( 'NONE', #190865, #52387, #237666, .T. ) ;
#96252=ORIENTED_EDGE ( 'NONE', *, *, #222466, .T. ) ;
#96283=ORIENTED_EDGE ( 'NONE', *, *, #89977, .F. ) ;
#96312=VECTOR ( 'NONE', #7675, 1000.000000000000000 ) ;
#96329=ORIENTED_EDGE ( 'NONE', *, *, #27656, .T. ) ;
#96342=ORIENTED_EDGE ( 'NONE', *, *, #25337, .F. ) ;
#96351=DIRECTION ( 'NONE',  ( -1.000000000000000000, -0.000000000000000000, -0.000000000000000000 ) ) ;
#96361=DIRECTION ( 'NONE',  ( -1.836970198721029934E-16, 1.000000000000000000, 0.000000000000000000 ) ) ;
#96381=CIRCLE ( 'NONE', #133989, 0.2000000000000057288 ) ;
#96413=CARTESIAN_POINT ( 'NONE',  ( 19.75857864376268935, 11.75000000001115907, -158.8500000000000227 ) ) ;
#96429=CARTESIAN_POINT ( 'NONE',  ( -18.50000000000000000, 11.75000000001115197, -122.2500000000000284 ) ) ;
#96468=ADVANCED_FACE ( 'NONE', ( #121381 ), #138307, .T. ) ;
#96481=AXIS2_PLACEMENT_3D ( 'NONE', #244652, #66023, #145548 ) ;
#96518=AXIS2_PLACEMENT_3D ( 'NONE', #107008, #186578, #7936 ) ;
#96521=CARTESIAN_POINT ( 'NONE',  ( -18.59999999999999787, 1.162701749949165642, -142.1000000000000227 ) ) ;
#96534=DIRECTION ( 'NONE',  ( 0.000000000000000000, 0.000000000000000000, -1.000000000000000000 ) ) ;
#96539=( NAMED_UNIT ( * ) SI_UNIT ( $, .STERADIAN. ) SOLID_ANGLE_UNIT ( ) );
#96581=SPHERICAL_SURFACE ( 'NONE', #196897, 0.1000000000000000056 ) ;
#96601=VERTEX_POINT ( 'NONE', #123920 ) ;
#96636=ORIENTED_EDGE ( 'NONE', *, *, #156273, .T. ) ;
#96640=EDGE_LOOP ( 'NONE', ( #39460, #122415, #216104, #145041 ) ) ;
#96650=EDGE_LOOP ( 'NONE', ( #50148, #214414, #112258 ) ) ;
#96658=VERTEX_POINT ( 'NONE', #70384 ) ;
#96683=DIRECTION ( 'NONE',  ( 0.000000000000000000, -1.000000000000000000, 0.000000000000000000 ) ) ;
#96710=CARTESIAN_POINT ( 'NONE',  ( -21.52071067811865746, 7.779289321892505882, -155.2500000000000284 ) ) ;
#96721=CARTESIAN_POINT ( 'NONE',  ( 21.05000000000000071, -11.48912529306490349, -136.9000000000000341 ) ) ;
#96734=VERTEX_POINT ( 'NONE', #53353 ) ;
#96742=VECTOR ( 'NONE', #232565, 1000.000000000000000 ) ;
#96776=EDGE_CURVE ( 'NONE', #30259, #46556, #199963, .T. ) ;
#96795=CARTESIAN_POINT ( 'NONE',  ( -21.05000000000000071, 1.736257131608553550, -145.5686523290175387 ) ) ;
#96804=AXIS2_PLACEMENT_3D ( 'NONE', #154881, #191449, #132740 ) ;
#96805=ORIENTED_EDGE ( 'NONE', *, *, #117314, .T. ) ;
#96809=EDGE_LOOP ( 'NONE', ( #37326, #7498, #135176, #49298 ) ) ;
#96823=CARTESIAN_POINT ( 'NONE',  ( -20.64999999999999858, 1.115600667400684642E-11, -134.0000000000000000 ) ) ;
#96865=CARTESIAN_POINT ( 'NONE',  ( 21.09793522318412684, 10.72462451022393282, -146.2392908709771575 ) ) ;
#96869=DIRECTION ( 'NONE',  ( 0.000000000000000000, 0.008583690987124100932, -0.9999631594459055250 ) ) ;
#96896=VECTOR ( 'NONE', #160467, 1000.000000000000000 ) ;
#96902=DIRECTION ( 'NONE',  ( 1.000000000000000000, 0.000000000000000000, 0.000000000000000000 ) ) ;
#96925=DIRECTION ( 'NONE',  ( -0.7071067811865389130, 8.659560562355038861E-17, -0.7071067811865561215 ) ) ;
#96936=EDGE_CURVE ( 'NONE', #246557, #200447, #12718, .T. ) ;
#96952=CARTESIAN_POINT ( 'NONE',  ( 18.59999999999999787, 5.900000000011102586, -144.2190997646564483 ) ) ;
#96975=AXIS2_PLACEMENT_3D ( 'NONE', #101196, #105046, #120842 ) ;
#96980=FACE_OUTER_BOUND ( 'NONE', #247701, .T. ) ;
#96993=CARTESIAN_POINT ( 'NONE',  ( -21.14999999893415250, 11.75000000001115197, -140.8444953435266314 ) ) ;
#97007=CARTESIAN_POINT ( 'NONE',  ( 21.05000000000000071, 5.000000000011153745, -146.4052660189131245 ) ) ;
#97033=DIRECTION ( 'NONE',  ( 1.000000000000000000, 0.000000000000000000, 0.000000000000000000 ) ) ;
#97046=DIRECTION ( 'NONE',  ( 0.000000000000000000, -0.9908441862701600211, -0.1350103645451876666 ) ) ;
#97058=AXIS2_PLACEMENT_3D ( 'NONE', #92107, #114241, #150798 ) ;
#97074=AXIS2_PLACEMENT_3D ( 'NONE', #215892, #58102, #76385 ) ;
#97080=EDGE_CURVE ( 'NONE', #2800, #197139, #47893, .T. ) ;
#97081=CARTESIAN_POINT ( 'NONE',  ( 21.05000000000000071, 8.815452279208711772, -142.4203925526142882 ) ) ;
#97099=TOROIDAL_SURFACE ( 'NONE', #255308, 0.2000000000000000111, 0.1000000000000000056 ) ;
#97103=VERTEX_POINT ( 'NONE', #12657 ) ;
#97107=CARTESIAN_POINT ( 'NONE',  ( -21.65000000000000213, 7.708578643773852157, -146.3500000000000227 ) ) ;
#97132=DIRECTION ( 'NONE',  ( 2.840903330521633255E-16, -0.8700118002898322711, 0.4930308989875231696 ) ) ;
#97133=ADVANCED_FACE ( 'NONE', ( #96002 ), #45999, .T. ) ;
#97141=CARTESIAN_POINT ( 'NONE',  ( 21.08078803292165659, 6.333012964448272442, -133.9208140128422144 ) ) ;
#97142=EDGE_CURVE ( 'NONE', #139646, #208712, #150085, .T. ) ;
#97160=VECTOR ( 'NONE', #55632, 1000.000000000000000 ) ;
#97196=ORIENTED_EDGE ( 'NONE', *, *, #249679, .F. ) ;
#97206=DIRECTION ( 'NONE',  ( 1.000000000000000000, 0.000000000000000000, 0.000000000000000000 ) ) ;
#97243=DIRECTION ( 'NONE',  ( 0.000000000000000000, -0.4791956752371546169, -0.8777080977375152360 ) ) ;
#97275=CARTESIAN_POINT ( 'NONE',  ( 22.59080734064467677, 11.75000000001115552, -133.9692502919029380 ) ) ;
#97276=CIRCLE ( 'NONE', #193015, 11.80000000000000426 ) ;
#97277=VECTOR ( 'NONE', #150861, 1000.000000000000000 ) ;
#97310=CARTESIAN_POINT ( 'NONE',  ( 20.95512820512820440, 10.62384868372303615, -141.6649135690876165 ) ) ;
#97326=CARTESIAN_POINT ( 'NONE',  ( 21.76363531954645936, 7.012936547882880234, -133.9009981257005961 ) ) ;
#97346=EDGE_LOOP ( 'NONE', ( #148400, #244388, #27681, #164866 ) ) ;
#97353=DIRECTION ( 'NONE',  ( 0.000000000000000000, -0.1495327102803792052, -0.9887567792719320625 ) ) ;
#97359=ORIENTED_EDGE ( 'NONE', *, *, #255932, .T. ) ;
#97377=DIRECTION ( 'NONE',  ( 0.000000000000000000, -0.9908441862701782288, -0.1350103645450539402 ) ) ;
#97389=DIRECTION ( 'NONE',  ( 0.000000000000000000, 0.000000000000000000, 1.000000000000000000 ) ) ;
#97396=ADVANCED_FACE ( 'NONE', ( #108544 ), #142506, .F. ) ;
#97421=AXIS2_PLACEMENT_3D ( 'NONE', #145778, #221452, #46676 ) ;
#97425=AXIS2_PLACEMENT_3D ( 'NONE', #200413, #118319, #197835 ) ;
#97434=EDGE_CURVE ( 'NONE', #97103, #140176, #50918, .T. ) ;
#97458=LINE ( 'NONE', #77914, #157939 ) ;
#97517=EDGE_CURVE ( 'NONE', #33482, #15173, #236186, .T. ) ;
#97596=ORIENTED_EDGE ( 'NONE', *, *, #63261, .T. ) ;
#97621=ORIENTED_EDGE ( 'NONE', *, *, #210214, .T. ) ;
#97700=CARTESIAN_POINT ( 'NONE',  ( -23.25000000000000000, 1.115600667400684642E-11, -167.5000000000000284 ) ) ;
#97706=CIRCLE ( 'NONE', #243467, 11.64999999999999325 ) ;
#97770=DIRECTION ( 'NONE',  ( 1.000000000000000000, -0.000000000000000000, -0.000000000000000000 ) ) ;
#97791=DIRECTION ( 'NONE',  ( -3.265361837132813093E-16, 1.000000000000000000, 0.000000000000000000 ) ) ;
#97792=CARTESIAN_POINT ( 'NONE',  ( 20.02499999999999858, 9.750000000011153745, -155.2500000000000000 ) ) ;
#97798=DIRECTION ( 'NONE',  ( 0.000000000000000000, 0.000000000000000000, 1.000000000000000000 ) ) ;
#97812=DIRECTION ( 'NONE',  ( 0.000000000000000000, 1.000000000000000000, -1.224646799147353207E-16 ) ) ;
#97874=EDGE_CURVE ( 'NONE', #87157, #50799, #196867, .T. ) ;
#97875=DIRECTION ( 'NONE',  ( 0.000000000000000000, 0.000000000000000000, 1.000000000000000000 ) ) ;
#97943=DIRECTION ( 'NONE',  ( 0.000000000000000000, 0.000000000000000000, -1.000000000000000000 ) ) ;
#97958=DIRECTION ( 'NONE',  ( 0.000000000000000000, 0.000000000000000000, -1.000000000000000000 ) ) ;
#97973=ORIENTED_EDGE ( 'NONE', *, *, #112198, .F. ) ;
#97981=CARTESIAN_POINT ( 'NONE',  ( -20.94999999999999929, 1.115600667400684642E-11, -134.0000000000000000 ) ) ;
#97997=CARTESIAN_POINT ( 'NONE',  ( 23.14999999999999858, 2.000000000011158630, -167.5000000000000284 ) ) ;
#98000=DIRECTION ( 'NONE',  ( 0.000000000000000000, -0.9915357197604971473, 0.1298341882519111479 ) ) ;
#98015=EDGE_CURVE ( 'NONE', #92859, #236521, #72176, .T. ) ;
#98025=ORIENTED_EDGE ( 'NONE', *, *, #193338, .T. ) ;
#98029=DIRECTION ( 'NONE',  ( -1.000000000000000000, 0.000000000000000000, 0.000000000000000000 ) ) ;
#98064=ORIENTED_EDGE ( 'NONE', *, *, #135200, .F. ) ;
#98076=CYLINDRICAL_SURFACE ( 'NONE', #255752, 4.000000000000003553 ) ;
#98140=EDGE_CURVE ( 'NONE', #159384, #98991, #217874, .T. ) ;
#98196=VERTEX_POINT ( 'NONE', #46644 ) ;
#98206=FACE_OUTER_BOUND ( 'NONE', #30742, .T. ) ;
#98216=EDGE_CURVE ( 'NONE', #165316, #8049, #204440, .T. ) ;
#98233=EDGE_LOOP ( 'NONE', ( #172728, #74613, #185942, #132864 ) ) ;
#98239=AXIS2_PLACEMENT_3D ( 'NONE', #122326, #104013, #23252 ) ;
#98249=CARTESIAN_POINT ( 'NONE',  ( -21.55000000000000071, 7.150000000011155876, -155.2500000000000284 ) ) ;
#98260=AXIS2_PLACEMENT_3D ( 'NONE', #129933, #110385, #8726 ) ;
#98270=EDGE_CURVE ( 'NONE', #202658, #201029, #113059, .T. ) ;
#98275=CIRCLE ( 'NONE', #106682, 3.899999999999999467 ) ;
#98353=AXIS2_PLACEMENT_3D ( 'NONE', #256388, #118229, #38700 ) ;
#98372=LINE ( 'NONE', #203942, #191889 ) ;
#98383=DIRECTION ( 'NONE',  ( 0.000000000000000000, 0.000000000000000000, -1.000000000000000000 ) ) ;
#98385=DIRECTION ( 'NONE',  ( 0.000000000000000000, -1.000000000000000000, 0.000000000000000000 ) ) ;
#98396=CARTESIAN_POINT ( 'NONE',  ( 22.39999999999999858, 7.790779598384538929, -133.9000000000000057 ) ) ;
#98412=ORIENTED_EDGE ( 'NONE', *, *, #204734, .T. ) ;
#98423=FACE_OUTER_BOUND ( 'NONE', #50421, .T. ) ;
#98425=CARTESIAN_POINT ( 'NONE',  ( 21.07933241753356768, 6.328645948390904330, -133.9066204095807109 ) ) ;
#98452=ORIENTED_EDGE ( 'NONE', *, *, #17685, .F. ) ;
#98468=ORIENTED_EDGE ( 'NONE', *, *, #136510, .T. ) ;
#98492=CARTESIAN_POINT ( 'NONE',  ( 20.94999999999999574, 1.115600667400684642E-11, -134.0000000000000000 ) ) ;
#98543=EDGE_CURVE ( 'NONE', #154251, #149928, #104624, .T. ) ;
#98563=EDGE_LOOP ( 'NONE', ( #147709, #206943, #128381, #232082, #212462, #81575 ) ) ;
#98592=LINE ( 'NONE', #240722, #64443 ) ;
#98640=FACE_OUTER_BOUND ( 'NONE', #257499, .T. ) ;
#98650=CIRCLE ( 'NONE', #144453, 2.000000000000001776 ) ;
#98691=ORIENTED_EDGE ( 'NONE', *, *, #53896, .T. ) ;
#98692=CARTESIAN_POINT ( 'NONE',  ( 23.15000000000000213, -8.999999999988842703, -158.1060308773475640 ) ) ;
#98697=CARTESIAN_POINT ( 'NONE',  ( -20.94999999999999929, -1.835341550213255957, -145.5551512925629822 ) ) ;
#98700=CARTESIAN_POINT ( 'NONE',  ( 18.49999999999999645, 1.736257131608553550, -145.5686523290175387 ) ) ;
#98701=EDGE_CURVE ( 'NONE', #101967, #41050, #65921, .T. ) ;
#98702=AXIS2_PLACEMENT_3D ( 'NONE', #6581, #209945, #250335 ) ;
#98743=CARTESIAN_POINT ( 'NONE',  ( 18.59999999999999076, 6.550000000011156231, -155.2500000000000284 ) ) ;
#98747=CIRCLE ( 'NONE', #256960, 0.2000000000000057288 ) ;
#98768=CARTESIAN_POINT ( 'NONE',  ( 21.09696443733127325, 10.72400988392963228, -146.2347775270482373 ) ) ;
#98770=EDGE_CURVE ( 'NONE', #27502, #65123, #46563, .T. ) ;
#98810=ORIENTED_EDGE ( 'NONE', *, *, #3507, .T. ) ;
#98817=CIRCLE ( 'NONE', #73941, 0.09999999999999864553 ) ;
#98850=DIRECTION ( 'NONE',  ( 1.000000000000000000, 0.000000000000000000, -0.000000000000000000 ) ) ;
#98852=ADVANCED_FACE ( 'NONE', ( #137427 ), #70002, .T. ) ;
#98866=ORIENTED_EDGE ( 'NONE', *, *, #207477, .T. ) ;
#98891=AXIS2_PLACEMENT_3D ( 'NONE', #111601, #72487, #30803 ) ;
#98904=DIRECTION ( 'NONE',  ( 1.000000000000000000, -0.000000000000000000, 0.000000000000000000 ) ) ;
#98942=EDGE_CURVE ( 'NONE', #239387, #231425, #147727, .T. ) ;
#98991=VERTEX_POINT ( 'NONE', #44773 ) ;
#99015=DIRECTION ( 'NONE',  ( -0.000000000000000000, -0.000000000000000000, -1.000000000000000000 ) ) ;
#99028=PLANE ( 'NONE',  #134040 ) ;
#99054=ORIENTED_EDGE ( 'NONE', *, *, #124575, .F. ) ;
#99086=LINE ( 'NONE', #178688, #181052 ) ;
#99089=EDGE_CURVE ( 'NONE', #64247, #106553, #159043, .T. ) ;
#99121=ORIENTED_EDGE ( 'NONE', *, *, #184730, .F. ) ;
#99125=ADVANCED_FACE ( 'NONE', ( #192961 ), #153880, .T. ) ;
#99155=ORIENTED_EDGE ( 'NONE', *, *, #51606, .T. ) ;
#99169=DIRECTION ( 'NONE',  ( 0.000000000000000000, 0.000000000000000000, 1.000000000000000000 ) ) ;
#99176=EDGE_LOOP ( 'NONE', ( #162684, #235322, #60822, #118982 ) ) ;
#99190=ORIENTED_EDGE ( 'NONE', *, *, #239232, .F. ) ;
#99200=VERTEX_POINT ( 'NONE', #20750 ) ;
#99202=CARTESIAN_POINT ( 'NONE',  ( -18.59999999999999787, 1.115600667400684642E-11, -167.5000000000000284 ) ) ;
#99208=TOROIDAL_SURFACE ( 'NONE', #153443, 0.6000000000000009770, 0.1000000000000000056 ) ;
#99218=AXIS2_PLACEMENT_3D ( 'NONE', #63101, #243029, #222162 ) ;
#99246=ORIENTED_EDGE ( 'NONE', *, *, #234795, .T. ) ;
#99253=VECTOR ( 'NONE', #199989, 1000.000000000000114 ) ;
#99260=CARTESIAN_POINT ( 'NONE',  ( 20.94999999999999929, -1.162701749926853712, -141.9000000000000341 ) ) ;
#99261=CARTESIAN_POINT ( 'NONE',  ( -18.59999999999999787, -1.135018845899022466, -175.2169768834323520 ) ) ;
#99264=DIRECTION ( 'NONE',  ( -0.000000000000000000, 0.8660254037844383745, -0.5000000000000003331 ) ) ;
#99281=CARTESIAN_POINT ( 'NONE',  ( 21.14999999999999858, 11.75000000001116263, -134.1000000000000227 ) ) ;
#99294=LINE ( 'NONE', #240126, #12681 ) ;
#99303=EDGE_LOOP ( 'NONE', ( #124602, #133365, #126576, #29135 ) ) ;
#99312=DIRECTION ( 'NONE',  ( 0.000000000000000000, -0.4930308989874653269, -0.8700118002898649117 ) ) ;
#99347=AXIS2_PLACEMENT_3D ( 'NONE', #5400, #221886, #66698 ) ;
#99366=CARTESIAN_POINT ( 'NONE',  ( -21.05000000000000071, -1.162701749926853712, -142.1000000000000227 ) ) ;
#99391=EDGE_CURVE ( 'NONE', #175914, #59363, #32313, .T. ) ;
#99406=ORIENTED_EDGE ( 'NONE', *, *, #76428, .T. ) ;
#99424=AXIS2_PLACEMENT_3D ( 'NONE', #58434, #79287, #78013 ) ;
#99456=CIRCLE ( 'NONE', #253028, 0.1000000000000008937 ) ;
#99500=LINE ( 'NONE', #2983, #224362 ) ;
#99509=ORIENTED_EDGE ( 'NONE', *, *, #228588, .T. ) ;
#99513=EDGE_LOOP ( 'NONE', ( #175610, #57026, #241062, #10333 ) ) ;
#99517=VERTEX_POINT ( 'NONE', #37436 ) ;
#99534=ADVANCED_FACE ( 'NONE', ( #116955 ), #71161, .F. ) ;
#99562=CARTESIAN_POINT ( 'NONE',  ( 18.49999999999998934, 10.25000000001115552, -158.6500000000000057 ) ) ;
#99595=VECTOR ( 'NONE', #123046, 1000.000000000000000 ) ;
#99633=DIRECTION ( 'NONE',  ( -0.000000000000000000, -0.000000000000000000, -1.000000000000000000 ) ) ;
#99675=AXIS2_PLACEMENT_3D ( 'NONE', #235953, #209995, #31388 ) ;
#99737=VECTOR ( 'NONE', #183998, 1000.000000000000000 ) ;
#99781=EDGE_LOOP ( 'NONE', ( #37152, #227510, #189019, #211782 ) ) ;
#99787=CARTESIAN_POINT ( 'NONE',  ( -18.59999999999999787, 10.33248238083634440, -173.0948465439131496 ) ) ;
#99799=VERTEX_POINT ( 'NONE', #206758 ) ;
#99822=DIRECTION ( 'NONE',  ( 1.000000000000000000, 0.000000000000000000, -0.000000000000000000 ) ) ;
#99854=CARTESIAN_POINT ( 'NONE',  ( 22.60000000000000142, 11.74956712350054744, -133.8991416309013118 ) ) ;
#99879=CARTESIAN_POINT ( 'NONE',  ( 20.95561247346651967, 10.59500736521470721, -141.5937827669816613 ) ) ;
#99910=AXIS2_PLACEMENT_3D ( 'NONE', #27871, #180495, #103496 ) ;
#99917=VERTEX_POINT ( 'NONE', #211910 ) ;
#99938=CARTESIAN_POINT ( 'NONE',  ( -18.40000000000000568, -9.499999999988851584, -140.9993620971801533 ) ) ;
#99942=DIRECTION ( 'NONE',  ( 0.000000000000000000, 0.9908441862701782288, 0.1350103645450542456 ) ) ;
#99998=DIRECTION ( 'NONE',  ( 0.000000000000000000, 0.000000000000000000, -1.000000000000000000 ) ) ;
#100003=VERTEX_POINT ( 'NONE', #157069 ) ;
#100039=DIRECTION ( 'NONE',  ( 1.000000000000000000, -0.000000000000000000, 0.000000000000000000 ) ) ;
#100056=FACE_OUTER_BOUND ( 'NONE', #218720, .T. ) ;
#100069=DIRECTION ( 'NONE',  ( 0.000000000000000000, 6.308085367183347448E-16, 1.000000000000000000 ) ) ;
#100098=FACE_OUTER_BOUND ( 'NONE', #154899, .T. ) ;
#100111=AXIS2_PLACEMENT_3D ( 'NONE', #200694, #20787, #258044 ) ;
#100128=DIRECTION ( 'NONE',  ( 1.000000000000000000, 0.000000000000000000, 0.000000000000000000 ) ) ;
#100200=ORIENTED_EDGE ( 'NONE', *, *, #163107, .T. ) ;
#100216=DIRECTION ( 'NONE',  ( 1.000000000000000000, 0.000000000000000000, 0.000000000000000000 ) ) ;
#100225=AXIS2_PLACEMENT_3D ( 'NONE', #31423, #50916, #30123 ) ;
#100235=DIRECTION ( 'NONE',  ( 0.000000000000000000, 0.000000000000000000, -1.000000000000000000 ) ) ;
#100321=ORIENTED_EDGE ( 'NONE', *, *, #249016, .T. ) ;
#100393=AXIS2_PLACEMENT_3D ( 'NONE', #129601, #172628, #134710 ) ;
#100395=CARTESIAN_POINT ( 'NONE',  ( 20.85000000000000142, 7.070967871809997973, -171.2465642218683115 ) ) ;
#100411=AXIS2_PLACEMENT_3D ( 'NONE', #122488, #139450, #202016 ) ;
#100445=DIRECTION ( 'NONE',  ( -0.000000000000000000, 1.000000000000000000, 1.734723475976807292E-15 ) ) ;
#100449=ADVANCED_FACE ( 'NONE', ( #195621 ), #15706, .T. ) ;
#100455=( BOUNDED_SURFACE ( )  B_SPLINE_SURFACE ( 3, 2, ( 
 ( #208763, #225717, #167093 ),
 ( #129218, #246583, #147495 ),
 ( #70556, #105769, #164504 ),
 ( #165795, #228321, #30135 ),
 ( #28880, #189197, #206184 ),
 ( #90067, #169671, #187914 ) ),
 .UNSPECIFIED., .F., .F., .T. ) 
 B_SPLINE_SURFACE_WITH_KNOTS ( ( 4, 2, 4 ),
 ( 3, 3 ),
 ( 0.0001381104793128107321, 0.0002947094729387620326, 0.0004513084665647133873 ),
 ( 0.000000000000000000, 1.000000000000000000 ),
 .UNSPECIFIED. ) 
 GEOMETRIC_REPRESENTATION_ITEM ( )  RATIONAL_B_SPLINE_SURFACE ( (
 ( 1.000000000000000000, 0.7071067811865475727, 1.000000000000000000),
 ( 1.000000000000000000, 0.6919563088099242032, 1.000000000000000000),
 ( 1.000000000000000000, 0.6959445945717356308, 1.000000000000000000),
 ( 1.000000000000000000, 0.7137882985313203088, 1.000000000000000000),
 ( 1.000000000000000000, 0.7257496306096423710, 1.000000000000000000),
 ( 1.000000000000000000, 0.7250110520819876836, 1.000000000000000000) ) ) 
 REPRESENTATION_ITEM ( '' )  SURFACE ( )  );
#100468=ORIENTED_EDGE ( 'NONE', *, *, #64486, .F. ) ;
#100481=EDGE_LOOP ( 'NONE', ( #148252, #42688, #225497, #235347, #63157 ) ) ;
#100490=ORIENTED_EDGE ( 'NONE', *, *, #141251, .T. ) ;
#100529=FACE_OUTER_BOUND ( 'NONE', #239252, .T. ) ;
#100542=ADVANCED_FACE ( 'NONE', ( #1220, #23410 ), #99028, .F. ) ;
#100559=DIRECTION ( 'NONE',  ( 1.000000000000000000, 0.000000000000000000, -0.000000000000000000 ) ) ;
#100573=LINE ( 'NONE', #202283, #99737 ) ;
#100597=AXIS2_PLACEMENT_3D ( 'NONE', #85435, #4634, #146705 ) ;
#100680=LINE ( 'NONE', #180262, #198889 ) ;
#100717=CARTESIAN_POINT ( 'NONE',  ( 21.14999999999999858, 11.65000000001116298, -146.1500000000000341 ) ) ;
#100736=AXIS2_PLACEMENT_3D ( 'NONE', #82675, #145243, #123135 ) ;
#100769=EDGE_LOOP ( 'NONE', ( #1081, #40689 ) ) ;
#100774=ORIENTED_EDGE ( 'NONE', *, *, #137461, .F. ) ;
#100787=ORIENTED_EDGE ( 'NONE', *, *, #45538, .F. ) ;
#100855=CARTESIAN_POINT ( 'NONE',  ( -18.59999999999999787, 7.120270961708750512, -171.1595630418393625 ) ) ;
#100874=SHAPE_REPRESENTATION_RELATIONSHIP ( 'NONE' , 'NONE' ,  #88607, #225623 ) ;
#100879=ORIENTED_EDGE ( 'NONE', *, *, #246539, .T. ) ;
#100930=CARTESIAN_POINT ( 'NONE',  ( 23.14999999999999503, 11.65000000001116298, -155.3500000000000227 ) ) ;
#100934=DIRECTION ( 'NONE',  ( -1.000000000000000000, 0.000000000000000000, 0.000000000000000000 ) ) ;
#100941=VERTEX_POINT ( 'NONE', #170009 ) ;
#100944=CIRCLE ( 'NONE', #188477, 4.049999999999998046 ) ;
#100970=CYLINDRICAL_SURFACE ( 'NONE', #163628, 0.09999999999999939493 ) ;
#100990=CARTESIAN_POINT ( 'NONE',  ( 22.60000000000000142, 1.115600667400684642E-11, -134.0000000000000000 ) ) ;
#100996=TOROIDAL_SURFACE ( 'NONE', #221655, 4.099999999999999645, 0.1000000000000000056 ) ;
#101003=ADVANCED_FACE ( 'NONE', ( #12198 ), #132123, .T. ) ;
#101022=LINE ( 'NONE', #180619, #117604 ) ;
#101079=EDGE_CURVE ( 'NONE', #120967, #141295, #109453, .T. ) ;
#101081=ORIENTED_EDGE ( 'NONE', *, *, #79899, .T. ) ;
#101119=ORIENTED_EDGE ( 'NONE', *, *, #120735, .T. ) ;
#101131=ORIENTED_EDGE ( 'NONE', *, *, #159609, .T. ) ;
#101165=VERTEX_POINT ( 'NONE', #116418 ) ;
#101196=CARTESIAN_POINT ( 'NONE',  ( 23.14999999999999858, 1.115600667400684642E-11, -167.5000000000000284 ) ) ;
#101205=VERTEX_POINT ( 'NONE', #64138 ) ;
#101217=DIRECTION ( 'NONE',  ( -0.000000000000000000, 0.1350103645451649625, -0.9908441862701631297 ) ) ;
#101220=FACE_OUTER_BOUND ( 'NONE', #14910, .T. ) ;
#101227=ORIENTED_EDGE ( 'NONE', *, *, #154890, .T. ) ;
#101271=CARTESIAN_POINT ( 'NONE',  ( -23.15000000000000213, 1.115600667400684642E-11, -163.5000000000000284 ) ) ;
#101277=DIRECTION ( 'NONE',  ( 1.000000000000000000, -0.000000000000000000, -0.000000000000000000 ) ) ;
#101282=CARTESIAN_POINT ( 'NONE',  ( 19.75857864376268935, 11.75000000001115907, -158.8500000000000227 ) ) ;
#101304=ADVANCED_FACE ( 'NONE', ( #122841 ), #201074, .T. ) ;
#101329=CARTESIAN_POINT ( 'NONE',  ( -22.50000000000000000, 0.1000000000111554016, -134.0000000000000000 ) ) ;
#101349=CARTESIAN_POINT ( 'NONE',  ( 22.57320508075688537, 11.65000000001115588, -134.0000000000000000 ) ) ;
#101393=DIRECTION ( 'NONE',  ( 0.000000000000000000, -0.1350103645451876666, -0.9908441862701600211 ) ) ;
#101401=DIRECTION ( 'NONE',  ( 0.000000000000000000, -1.000000000000000000, 0.000000000000000000 ) ) ;
#101426=DIRECTION ( 'NONE',  ( 0.000000000000000000, -1.000000000000000000, -2.891205793294679805E-16 ) ) ;
#101430=ORIENTED_EDGE ( 'NONE', *, *, #59247, .F. ) ;
#101478=EDGE_CURVE ( 'NONE', #229990, #85055, #43031, .T. ) ;
#101489=LINE ( 'NONE', #118558, #24888 ) ;
#101503=ORIENTED_EDGE ( 'NONE', *, *, #2597, .F. ) ;
#101524=ORIENTED_EDGE ( 'NONE', *, *, #25067, .T. ) ;
#101525=EDGE_LOOP ( 'NONE', ( #50606, #199460, #95672, #248686, #223048, #89046, #50383 ) ) ;
#101542=DIRECTION ( 'NONE',  ( 0.000000000000000000, 0.000000000000000000, -1.000000000000000000 ) ) ;
#101552=CARTESIAN_POINT ( 'NONE',  ( -22.50014994444008209, 11.74971973190334040, -133.9169198432812777 ) ) ;
#101555=AXIS2_PLACEMENT_3D ( 'NONE', #252156, #202476, #1686 ) ;
#101573=LINE ( 'NONE', #187260, #103539 ) ;
#101622=VECTOR ( 'NONE', #135695, 1000.000000000000000 ) ;
#101659=CIRCLE ( 'NONE', #159982, 0.09999999999998898659 ) ;
#101661=CARTESIAN_POINT ( 'NONE',  ( -20.94999999999999929, 5.850000000011105428, -144.1324972242779836 ) ) ;
#101670=DIRECTION ( 'NONE',  ( 1.000000000000000000, -0.000000000000000000, -0.000000000000000000 ) ) ;
#101675=CARTESIAN_POINT ( 'NONE',  ( 18.50000000000000000, -9.399999999988843058, -140.9992856778388841 ) ) ;
#101677=CARTESIAN_POINT ( 'NONE',  ( 20.87600722750343252, 10.33112638556969465, -173.0901228926974795 ) ) ;
#101686=CIRCLE ( 'NONE', #180844, 0.09999999999999062417 ) ;
#101729=CIRCLE ( 'NONE', #197419, 0.09999999999999344136 ) ;
#101749=VERTEX_POINT ( 'NONE', #200767 ) ;
#101753=CARTESIAN_POINT ( 'NONE',  ( 20.94999999999999929, 11.65000000001115943, -167.5000000000000284 ) ) ;
#101772=ORIENTED_EDGE ( 'NONE', *, *, #39366, .T. ) ;
#101783=CARTESIAN_POINT ( 'NONE',  ( 22.47071067811865319, 1.115600667400684642E-11, -134.0000000000000000 ) ) ;
#101839=EDGE_CURVE ( 'NONE', #67744, #58852, #134752, .T. ) ;
#101852=CARTESIAN_POINT ( 'NONE',  ( -18.59999999999999787, 11.65000000001115232, -141.0148057706539930 ) ) ;
#101871=ORIENTED_EDGE ( 'NONE', *, *, #97434, .F. ) ;
#101911=DIRECTION ( 'NONE',  ( 0.000000000000000000, 0.000000000000000000, -1.000000000000000000 ) ) ;
#101913=FACE_OUTER_BOUND ( 'NONE', #228429, .T. ) ;
#101916=DIRECTION ( 'NONE',  ( -1.000000000000000000, -0.000000000000000000, -0.000000000000000000 ) ) ;
#101966=AXIS2_PLACEMENT_3D ( 'NONE', #28375, #128727, #223951 ) ;
#101967=VERTEX_POINT ( 'NONE', #196595 ) ;
#101978=CARTESIAN_POINT ( 'NONE',  ( -21.44999999999999929, 7.150000000011155876, -146.3500000000000227 ) ) ;
#101979=EDGE_CURVE ( 'NONE', #221635, #37340, #201411, .T. ) ;
#101981=VECTOR ( 'NONE', #252494, 1000.000000000000000 ) ;
#102014=ADVANCED_FACE ( 'NONE', ( #12858 ), #230860, .T. ) ;
#102024=EDGE_CURVE ( 'NONE', #227883, #96658, #234930, .T. ) ;
#102027=DIRECTION ( 'NONE',  ( 4.336808689942128177E-15, 0.8660254037844330455, -0.5000000000000096589 ) ) ;
#102054=EDGE_CURVE ( 'NONE', #240530, #231902, #35049, .T. ) ;
#102061=AXIS2_PLACEMENT_3D ( 'NONE', #102677, #183533, #148247 ) ;
#102069=AXIS2_PLACEMENT_3D ( 'NONE', #186261, #45452, #247507 ) ;
#102083=DIRECTION ( 'NONE',  ( 0.000000000000000000, -0.000000000000000000, -1.000000000000000000 ) ) ;
#102097=EDGE_CURVE ( 'NONE', #82879, #216709, #43944, .T. ) ;
#102163=DIRECTION ( 'NONE',  ( 0.000000000000000000, 1.734723475976997999E-14, -1.000000000000000000 ) ) ;
#102200=VECTOR ( 'NONE', #120425, 1000.000000000000000 ) ;
#102203=AXIS2_PLACEMENT_3D ( 'NONE', #105926, #124250, #83777 ) ;
#102205=CARTESIAN_POINT ( 'NONE',  ( -22.50875500270928953, -0.1008579137641102963, -122.2504328726021328 ) ) ;
#102233=FACE_OUTER_BOUND ( 'NONE', #155372, .T. ) ;
#102236=FACE_OUTER_BOUND ( 'NONE', #257798, .T. ) ;
#102245=CARTESIAN_POINT ( 'NONE',  ( 23.14999999999999858, 5.600000000011153389, -155.0947339810869323 ) ) ;
#102257=DIRECTION ( 'NONE',  ( -1.000000000000000000, 0.000000000000000000, 0.000000000000000000 ) ) ;
#102281=CIRCLE ( 'NONE', #15422, 0.09999999999998898659 ) ;
#102288=DIRECTION ( 'NONE',  ( 1.000000000000000000, 0.000000000000000000, 0.000000000000000000 ) ) ;
#102294=EDGE_CURVE ( 'NONE', #155996, #154183, #122511, .T. ) ;
#102296=EDGE_CURVE ( 'NONE', #89589, #197727, #155830, .T. ) ;
#102312=DIRECTION ( 'NONE',  ( 1.000000000000000000, -0.000000000000000000, -0.000000000000000000 ) ) ;
#102325=EDGE_CURVE ( 'NONE', #242592, #146074, #212025, .T. ) ;
#102388=ORIENTED_EDGE ( 'NONE', *, *, #87008, .F. ) ;
#102433=ADVANCED_FACE ( 'NONE', ( #61609 ), #22505, .T. ) ;
#102442=CARTESIAN_POINT ( 'NONE',  ( 19.83283456528358002, 11.75000000001116263, -158.8499999994178040 ) ) ;
#102447=CARTESIAN_POINT ( 'NONE',  ( 20.85000000000000142, -1.851617760457748618, -179.1031897196036766 ) ) ;
#102451=CARTESIAN_POINT ( 'NONE',  ( 18.50000324121758055, 10.29307482169091870, -172.9586421466939896 ) ) ;
#102459=DIRECTION ( 'NONE',  ( -0.000000000000000000, 1.000000000000000000, -1.224646799147352961E-16 ) ) ;
#102462=AXIS2_PLACEMENT_3D ( 'NONE', #233385, #11768, #249087 ) ;
#102513=CARTESIAN_POINT ( 'NONE',  ( -18.44204374631832977, -9.491036389587206301, -174.1262012702210598 ) ) ;
#102519=DIRECTION ( 'NONE',  ( 2.710505431213777355E-16, -1.000000000000000000, 0.000000000000000000 ) ) ;
#102521=AXIS2_PLACEMENT_3D ( 'NONE', #231526, #55404, #134946 ) ;
#102547=EDGE_LOOP ( 'NONE', ( #240244, #170537, #78529, #29803 ) ) ;
#102612=TOROIDAL_SURFACE ( 'NONE', #31778, 0.6000000000000009770, 0.1000000000000000056 ) ;
#102651=ORIENTED_EDGE ( 'NONE', *, *, #173799, .T. ) ;
#102662=CARTESIAN_POINT ( 'NONE',  ( 22.47110162079220785, 0.02879741281384913879, -122.3500640633156991 ) ) ;
#102667=DIRECTION ( 'NONE',  ( 0.000000000000000000, -0.000000000000000000, 1.000000000000000000 ) ) ;
#102669=ORIENTED_EDGE ( 'NONE', *, *, #204734, .F. ) ;
#102670=CIRCLE ( 'NONE', #190205, 0.09999999999998898659 ) ;
#102677=CARTESIAN_POINT ( 'NONE',  ( 18.59999999999999076, 6.450000000011156587, -144.0170271704400307 ) ) ;
#102697=LINE ( 'NONE', #79293, #14770 ) ;
#102734=DIRECTION ( 'NONE',  ( 1.000000000000000000, 3.265361837132813093E-16, -0.000000000000000000 ) ) ;
#102765=DIRECTION ( 'NONE',  ( -0.000000000000000000, -0.000000000000000000, 1.000000000000000000 ) ) ;
#102772=CARTESIAN_POINT ( 'NONE',  ( -18.59999999999999787, -1.866714910046153308, -145.7526752462820241 ) ) ;
#102808=DIRECTION ( 'NONE',  ( 0.000000000000000000, -1.000000000000000000, 0.000000000000000000 ) ) ;
#102819=DIRECTION ( 'NONE',  ( -0.000000000000000000, 0.000000000000000000, 1.000000000000000000 ) ) ;
#102823=DIRECTION ( 'NONE',  ( -1.000000000000000000, -0.000000000000000000, -0.000000000000000000 ) ) ;
#102830=VERTEX_POINT ( 'NONE', #178718 ) ;
#102870=ORIENTED_EDGE ( 'NONE', *, *, #242159, .T. ) ;
#102895=CARTESIAN_POINT ( 'NONE',  ( 20.04142135623730070, 11.65000000001115943, -155.3500000000000227 ) ) ;
#102906=ORIENTED_EDGE ( 'NONE', *, *, #185888, .T. ) ;
#102944=CARTESIAN_POINT ( 'NONE',  ( -22.16821283564876666, 7.558973340791935058, -134.0000000000000000 ) ) ;
#102970=CIRCLE ( 'NONE', #3010, 0.09999999999998898659 ) ;
#103018=CARTESIAN_POINT ( 'NONE',  ( 21.05000000000000071, -11.48912529306489994, -164.6000000000000227 ) ) ;
#103028=EDGE_LOOP ( 'NONE', ( #234614, #65138 ) ) ;
#103029=DIRECTION ( 'NONE',  ( 0.000000000000000000, 0.000000000000000000, -1.000000000000000000 ) ) ;
#103138=CIRCLE ( 'NONE', #248917, 4.299999999999970512 ) ;
#103191=CYLINDRICAL_SURFACE ( 'NONE', #196168, 0.09999999999999939493 ) ;
#103192=EDGE_CURVE ( 'NONE', #5925, #87825, #73194, .T. ) ;
#103199=CARTESIAN_POINT ( 'NONE',  ( -22.49510344025093644, 0.06712767820541534758, -122.3500298948857647 ) ) ;
#103232=ORIENTED_EDGE ( 'NONE', *, *, #235663, .F. ) ;
#103233=CIRCLE ( 'NONE', #249015, 0.9750000000000036415 ) ;
#103241=PLANE ( 'NONE',  #38824 ) ;
#103245=CARTESIAN_POINT ( 'NONE',  ( 20.87155475150661132, 11.75000000001115907, -160.5955865291576572 ) ) ;
#103277=DIRECTION ( 'NONE',  ( 0.000000000000000000, -0.000000000000000000, 1.000000000000000000 ) ) ;
#103286=CARTESIAN_POINT ( 'NONE',  ( 21.05000000000000071, 6.477067021135912483, -134.1000000000000227 ) ) ;
#103316=CARTESIAN_POINT ( 'NONE',  ( -23.15000000000000213, -8.596261682231835621, -143.4501275171502925 ) ) ;
#103331=CYLINDRICAL_SURFACE ( 'NONE', #90852, 0.5000000000000004441 ) ;
#103371=DIRECTION ( 'NONE',  ( -1.000000000000000000, 0.000000000000000000, 0.000000000000000000 ) ) ;
#103396=CARTESIAN_POINT ( 'NONE',  ( -23.25000000000000000, 6.982009704867601307, -171.1961521182563217 ) ) ;
#103406=CARTESIAN_POINT ( 'NONE',  ( -18.59999999999999787, 1.340746217944851715, -123.7271374945788409 ) ) ;
#103407=LINE ( 'NONE', #4316, #236077 ) ;
#103458=ORIENTED_EDGE ( 'NONE', *, *, #28620, .T. ) ;
#103478=DIRECTION ( 'NONE',  ( 0.000000000000000000, 0.000000000000000000, -1.000000000000000000 ) ) ;
#103484=DIRECTION ( 'NONE',  ( 0.000000000000000000, -1.000000000000000000, -0.000000000000000000 ) ) ;
#103493=ORIENTED_EDGE ( 'NONE', *, *, #178275, .T. ) ;
#103494=EDGE_CURVE ( 'NONE', #20283, #42426, #135497, .T. ) ;
#103496=DIRECTION ( 'NONE',  ( 1.000000000000000000, 0.000000000000000000, 0.000000000000000000 ) ) ;
#103513=FACE_OUTER_BOUND ( 'NONE', #140367, .T. ) ;
#103539=VECTOR ( 'NONE', #226341, 1000.000000000000000 ) ;
#103540=DIRECTION ( 'NONE',  ( 0.000000000000000000, 0.000000000000000000, -1.000000000000000000 ) ) ;
#103558=DIRECTION ( 'NONE',  ( -4.391705002472929091E-16, 1.000000000000000000, 0.000000000000000000 ) ) ;
#103560=ORIENTED_EDGE ( 'NONE', *, *, #168853, .T. ) ;
#103568=EDGE_LOOP ( 'NONE', ( #195373, #250369, #80588, #30162 ) ) ;
#103571=DIRECTION ( 'NONE',  ( 0.000000000000000000, -1.000000000000000000, 0.000000000000000000 ) ) ;
#103584=ORIENTED_EDGE ( 'NONE', *, *, #21819, .T. ) ;
#103621=DIRECTION ( 'NONE',  ( -1.000000000000000000, -0.000000000000000000, -0.000000000000000000 ) ) ;
#103679=DIRECTION ( 'NONE',  ( -0.7071067811865475727, -0.7071067811865475727, 0.000000000000000000 ) ) ;
#103764=EDGE_CURVE ( 'NONE', #83171, #226085, #21563, .T. ) ;
#103824=AXIS2_PLACEMENT_3D ( 'NONE', #49719, #129261, #174855 ) ;
#103843=VECTOR ( 'NONE', #34986, 1000.000000000000000 ) ;
#103850=CARTESIAN_POINT ( 'NONE',  ( 21.53752568622130781, 0.09897446127749356948, -127.2131921254514566 ) ) ;
#103870=CYLINDRICAL_SURFACE ( 'NONE', #210095, 0.8750000000000007772 ) ;
#103872=DIRECTION ( 'NONE',  ( 0.000000000000000000, 0.000000000000000000, 1.000000000000000000 ) ) ;
#103912=ORIENTED_EDGE ( 'NONE', *, *, #149399, .F. ) ;
#103923=CARTESIAN_POINT ( 'NONE',  ( -18.50000000000000000, 1.835341550235567887, -145.5551512925629822 ) ) ;
#103940=ADVANCED_FACE ( 'NONE', ( #34422 ), #256048, .F. ) ;
#103949=CARTESIAN_POINT ( 'NONE',  ( 22.50000000000000000, 0.1000000000111554016, -122.3504291924552234 ) ) ;
#103965=CARTESIAN_POINT ( 'NONE',  ( 23.24999999999999289, 6.650000000011155876, -155.1500000000000057 ) ) ;
#103973=ORIENTED_EDGE ( 'NONE', *, *, #90626, .T. ) ;
#103989=DIRECTION ( 'NONE',  ( 0.000000000000000000, -1.000000000000000000, 0.000000000000000000 ) ) ;
#103991=CARTESIAN_POINT ( 'NONE',  ( -23.15000000000000213, -11.74999999998884448, -134.0000000000000000 ) ) ;
#104003=AXIS2_PLACEMENT_3D ( 'NONE', #97700, #192994, #252942 ) ;
#104013=DIRECTION ( 'NONE',  ( 1.000000000000000000, -0.000000000000000000, -0.000000000000000000 ) ) ;
#104026=CYLINDRICAL_SURFACE ( 'NONE', #107730, 0.1000000000000000472 ) ;
#104041=ORIENTED_EDGE ( 'NONE', *, *, #178777, .T. ) ;
#104044=DIRECTION ( 'NONE',  ( -0.000000000000000000, -0.1350103645451876666, 0.9908441862701600211 ) ) ;
#104048=EDGE_CURVE ( 'NONE', #104618, #69302, #60291, .T. ) ;
#104065=AXIS2_PLACEMENT_3D ( 'NONE', #32675, #31386, #14378 ) ;
#104068=EDGE_LOOP ( 'NONE', ( #111306, #160381, #82456, #17862, #118404 ) ) ;
#104085=DIRECTION ( 'NONE',  ( -1.000000000000000000, 9.012599976028471648E-15, 6.882867235861662930E-14 ) ) ;
#104087=VERTEX_POINT ( 'NONE', #204388 ) ;
#104114=EDGE_CURVE ( 'NONE', #231902, #64347, #247368, .T. ) ;
#104119=DIRECTION ( 'NONE',  ( 1.000000000000000000, 0.000000000000000000, 0.000000000000000000 ) ) ;
#104125=EDGE_CURVE ( 'NONE', #226085, #79888, #6192, .T. ) ;
#104139=EDGE_CURVE ( 'NONE', #139646, #95988, #114463, .T. ) ;
#104156=EDGE_CURVE ( 'NONE', #253143, #4110, #126940, .T. ) ;
#104164=CARTESIAN_POINT ( 'NONE',  ( 22.59999954896768770, -0.008828232233025335232, -122.2494913259320128 ) ) ;
#104168=CARTESIAN_POINT ( 'NONE',  ( -21.05000000000000071, 1.115653327213047955E-11, -129.7000000000000455 ) ) ;
#104219=CIRCLE ( 'NONE', #100111, 0.09999999999999939493 ) ;
#104251=EDGE_LOOP ( 'NONE', ( #2411, #126358, #182695, #12335 ) ) ;
#104289=DIRECTION ( 'NONE',  ( 0.000000000000000000, 0.000000000000000000, -1.000000000000000000 ) ) ;
#104344=CIRCLE ( 'NONE', #233571, 0.1999999999999999833 ) ;
#104395=AXIS2_PLACEMENT_3D ( 'NONE', #29770, #93550, #149707 ) ;
#104439=ADVANCED_FACE ( 'NONE', ( #183256 ), #241930, .T. ) ;
#104465=ADVANCED_FACE ( 'NONE', ( #244503 ), #156374, .T. ) ;
#104469=CIRCLE ( 'NONE', #196084, 0.1999999999999996503 ) ;
#104477=DIRECTION ( 'NONE',  ( 0.000000000000000000, 0.000000000000000000, -1.000000000000000000 ) ) ;
#104502=DIRECTION ( 'NONE',  ( -0.000000000000000000, -0.8700118002898321601, 0.4930308989875230030 ) ) ;
#104504=CARTESIAN_POINT ( 'NONE',  ( -20.94999999999999929, 1.162701749949165642, -142.0000000000000284 ) ) ;
#104518=LINE ( 'NONE', #207523, #215865 ) ;
#104535=AXIS2_PLACEMENT_3D ( 'NONE', #1821, #103484, #138739 ) ;
#104556=AXIS2_PLACEMENT_3D ( 'NONE', #86181, #11840, #169650 ) ;
#104597=ADVANCED_FACE ( 'NONE', ( #154439 ), #218860, .T. ) ;
#104601=FACE_OUTER_BOUND ( 'NONE', #46089, .T. ) ;
#104618=VERTEX_POINT ( 'NONE', #116559 ) ;
#104624=CIRCLE ( 'NONE', #212826, 0.09999999999999939493 ) ;
#104638=FACE_OUTER_BOUND ( 'NONE', #198300, .T. ) ;
#104640=TOROIDAL_SURFACE ( 'NONE', #171371, 1.900000000000002576, 0.1000000000000000056 ) ;
#104648=CARTESIAN_POINT ( 'NONE',  ( -21.05000000000000071, 0.03363273534480443888, -127.7411828053185161 ) ) ;
#104663=VERTEX_POINT ( 'NONE', #96952 ) ;
#104674=CARTESIAN_POINT ( 'NONE',  ( 23.14999999999999147, -4.149999999988843058, -134.0000000000000000 ) ) ;
#104676=DIRECTION ( 'NONE',  ( 0.000000000000000000, -0.1350103645451876944, -0.9908441862701601321 ) ) ;
#104694=CARTESIAN_POINT ( 'NONE',  ( -18.59999999999999787, 1.736257131608553550, -145.5686523290175387 ) ) ;
#104704=ORIENTED_EDGE ( 'NONE', *, *, #246349, .F. ) ;
#104709=CARTESIAN_POINT ( 'NONE',  ( -22.39999999999999858, 11.65000000001115588, -134.1000000000000227 ) ) ;
#104758=ADVANCED_FACE ( 'NONE', ( #61720 ), #202316, .T. ) ;
#104763=ORIENTED_EDGE ( 'NONE', *, *, #17851, .F. ) ;
#104773=FACE_OUTER_BOUND ( 'NONE', #141906, .T. ) ;
#104777=AXIS2_PLACEMENT_3D ( 'NONE', #253776, #103679, #240650 ) ;
#104833=VERTEX_POINT ( 'NONE', #162123 ) ;
#104859=CARTESIAN_POINT ( 'NONE',  ( -21.05000000000000071, 1.115600667400684642E-11, -134.0000000000000000 ) ) ;
#104880=TOROIDAL_SURFACE ( 'NONE', #109579, 4.099999999999999645, 0.1000000000000000056 ) ;
#104912=CARTESIAN_POINT ( 'NONE',  ( 18.49999999999999289, 6.450000000011156587, -155.1500000000000057 ) ) ;
#104924=ORIENTED_EDGE ( 'NONE', *, *, #228069, .T. ) ;
#104934=EDGE_LOOP ( 'NONE', ( #181771, #200545, #128806 ) ) ;
#104965=ADVANCED_FACE ( 'NONE', ( #90246 ), #169853, .F. ) ;
#104998=CARTESIAN_POINT ( 'NONE',  ( 19.96984138294323685, 11.75000000001116263, -158.7245720712021750 ) ) ;
#105031=VECTOR ( 'NONE', #156222, 1000.000000000000000 ) ;
#105046=DIRECTION ( 'NONE',  ( 1.000000000000000000, 2.952720810173289112E-16, -0.000000000000000000 ) ) ;
#105049=DIRECTION ( 'NONE',  ( 0.000000000000000000, 1.000000000000000000, 0.000000000000000000 ) ) ;
#105065=EDGE_CURVE ( 'NONE', #218711, #83651, #127481, .T. ) ;
#105075=CARTESIAN_POINT ( 'NONE',  ( -18.46919391072055561, -9.670724388266535243, -174.1738035317996491 ) ) ;
#105078=EDGE_CURVE ( 'NONE', #148410, #159233, #206595, .T. ) ;
#105083=CYLINDRICAL_SURFACE ( 'NONE', #129120, 0.09999999999998898659 ) ;
#105146=DIRECTION ( 'NONE',  ( 0.000000000000000000, 0.000000000000000000, -1.000000000000000000 ) ) ;
#105166=ADVANCED_FACE ( 'NONE', ( #202213 ), #242602, .T. ) ;
#105167=DIRECTION ( 'NONE',  ( 0.000000000000000000, 0.000000000000000000, -1.000000000000000000 ) ) ;
#105171=CYLINDRICAL_SURFACE ( 'NONE', #26242, 0.09999999999998898659 ) ;
#105178=CARTESIAN_POINT ( 'NONE',  ( -23.15000000000000213, -9.599999999988845900, -157.6060308773475924 ) ) ;
#105187=CARTESIAN_POINT ( 'NONE',  ( -20.88420186297724257, 10.33025634372637391, -173.0870929282638997 ) ) ;
#105208=DIRECTION ( 'NONE',  ( 1.000000000000000000, 0.000000000000000000, 0.000000000000000000 ) ) ;
#105210=CARTESIAN_POINT ( 'NONE',  ( 21.05000000000000071, -11.29603075032412995, -137.0478991596638991 ) ) ;
#105212=CARTESIAN_POINT ( 'NONE',  ( -18.59999999999999787, -1.835859311432481045, -179.1044391687985353 ) ) ;
#105230=EDGE_CURVE ( 'NONE', #100941, #128950, #31843, .T. ) ;
#105239=AXIS2_PLACEMENT_3D ( 'NONE', #48883, #207982, #67169 ) ;
#105297=DIRECTION ( 'NONE',  ( 0.000000000000000000, -0.9908441862701596881, -0.1350103645451904977 ) ) ;
#105313=CARTESIAN_POINT ( 'NONE',  ( -20.54999999999999716, 2.400000000011155432, -157.6060308773475924 ) ) ;
#105357=ORIENTED_EDGE ( 'NONE', *, *, #157689, .F. ) ;
#105370=DIRECTION ( 'NONE',  ( 0.000000000000000000, 1.000000000000000000, 0.000000000000000000 ) ) ;
#105437=AXIS2_PLACEMENT_3D ( 'NONE', #91864, #102734, #227515 ) ;
#105455=DIRECTION ( 'NONE',  ( 0.000000000000000000, 0.000000000000000000, -1.000000000000000000 ) ) ;
#105470=DIRECTION ( 'NONE',  ( -0.000000000000000000, 0.000000000000000000, 1.000000000000000000 ) ) ;
#105493=CARTESIAN_POINT ( 'NONE',  ( 18.49999999999998579, -9.321008403350155902, -141.2359382490778899 ) ) ;
#105505=ORIENTED_EDGE ( 'NONE', *, *, #191605, .T. ) ;
#105532=VERTEX_POINT ( 'NONE', #1098 ) ;
#105534=CARTESIAN_POINT ( 'NONE',  ( -18.59999999999999787, 7.021664781911246322, -171.1335654018973003 ) ) ;
#105580=VECTOR ( 'NONE', #2639, 1000.000000000000000 ) ;
#105589=VERTEX_POINT ( 'NONE', #221430 ) ;
#105602=ADVANCED_FACE ( 'NONE', ( #16234 ), #94452, .F. ) ;
#105610=ORIENTED_EDGE ( 'NONE', *, *, #152861, .T. ) ;
#105642=CIRCLE ( 'NONE', #168260, 11.64999999999999325 ) ;
#105677=ORIENTED_EDGE ( 'NONE', *, *, #37064, .F. ) ;
#105682=CARTESIAN_POINT ( 'NONE',  ( -20.64999999999999858, 2.000000000011154189, -154.7753780772379173 ) ) ;
#105696=EDGE_LOOP ( 'NONE', ( #228099, #127467, #244087, #59975 ) ) ;
#105716=AXIS2_PLACEMENT_3D ( 'NONE', #54912, #97875, #60055 ) ;
#105729=ORIENTED_EDGE ( 'NONE', *, *, #190258, .F. ) ;
#105769=CARTESIAN_POINT ( 'NONE',  ( 21.09546886439553859, 8.878553113026075749, -146.2370938505546860 ) ) ;
#105800=AXIS2_PLACEMENT_3D ( 'NONE', #154049, #54877, #134406 ) ;
#105809=AXIS2_PLACEMENT_3D ( 'NONE', #8834, #128789, #66242 ) ;
#105831=ADVANCED_FACE ( 'NONE', ( #96980 ), #256042, .T. ) ;
#105854=AXIS2_PLACEMENT_3D ( 'NONE', #173637, #134426, #152766 ) ;
#105873=DIRECTION ( 'NONE',  ( 1.000000000000000000, -0.000000000000000000, -0.000000000000000000 ) ) ;
#105891=EDGE_CURVE ( 'NONE', #240051, #95993, #215331, .T. ) ;
#105909=ORIENTED_EDGE ( 'NONE', *, *, #13110, .T. ) ;
#105926=CARTESIAN_POINT ( 'NONE',  ( -23.25000000000000000, -11.64999999998884483, -137.1000000000000227 ) ) ;
#105928=EDGE_CURVE ( 'NONE', #114955, #240778, #15447, .T. ) ;
#105940=ORIENTED_EDGE ( 'NONE', *, *, #28203, .F. ) ;
#105943=VERTEX_POINT ( 'NONE', #23938 ) ;
#105952=AXIS2_PLACEMENT_3D ( 'NONE', #121312, #101670, #202096 ) ;
#105973=DIRECTION ( 'NONE',  ( 0.000000000000000000, 0.9908441862701596881, -0.1350103645451904977 ) ) ;
#105975=TOROIDAL_SURFACE ( 'NONE', #172689, 7.791421356237316687, 0.1000000000000000056 ) ;
#105977=EDGE_CURVE ( 'NONE', #174669, #89497, #161168, .T. ) ;
#105980=ORIENTED_EDGE ( 'NONE', *, *, #54945, .T. ) ;
#105987=CARTESIAN_POINT ( 'NONE',  ( 20.52683494730037239, 8.980530818312608687, -142.5052527225372216 ) ) ;
#106051=CYLINDRICAL_SURFACE ( 'NONE', #53241, 0.09999999999998898659 ) ;
#106053=CARTESIAN_POINT ( 'NONE',  ( -20.85000000000000142, 7.021664781911246322, -171.3335654018973173 ) ) ;
#106067=VERTEX_POINT ( 'NONE', #74641 ) ;
#106113=CARTESIAN_POINT ( 'NONE',  ( -23.15000000000000213, -11.74999999998884448, -164.4000000000000057 ) ) ;
#106130=AXIS2_PLACEMENT_3D ( 'NONE', #706, #39897, #119412 ) ;
#106164=AXIS2_PLACEMENT_3D ( 'NONE', #158845, #238349, #33785 ) ;
#106191=DIRECTION ( 'NONE',  ( 1.000000000000000000, 0.000000000000000000, 0.000000000000000000 ) ) ;
#106195=CIRCLE ( 'NONE', #127066, 0.09999999999998898659 ) ;
#106315=CARTESIAN_POINT ( 'NONE',  ( 18.56579813702275317, 10.33025634372637924, -173.0870929282638997 ) ) ;
#106318=CARTESIAN_POINT ( 'NONE',  ( -20.94999999999999929, 7.031312794766356511, -171.1091509382273159 ) ) ;
#106326=ORIENTED_EDGE ( 'NONE', *, *, #150629, .F. ) ;
#106340=EDGE_CURVE ( 'NONE', #18611, #176425, #110848, .T. ) ;
#106400=DIRECTION ( 'NONE',  ( -0.000000000000000000, -0.000000000000000000, 1.000000000000000000 ) ) ;
#106402=CARTESIAN_POINT ( 'NONE',  ( -20.94999999999999929, 11.60000000001115161, -140.9282032302755852 ) ) ;
#106409=ORIENTED_EDGE ( 'NONE', *, *, #176494, .F. ) ;
#106411=CARTESIAN_POINT ( 'NONE',  ( -20.54999999999999716, 7.150000000011155876, -155.1500000000000057 ) ) ;
#106413=CARTESIAN_POINT ( 'NONE',  ( 21.93340585898238260, 1.115541036281197940E-11, -126.6758529778678763 ) ) ;
#106418=ADVANCED_FACE ( 'NONE', ( #130405 ), #94889, .T. ) ;
#106430=DIRECTION ( 'NONE',  ( 0.000000000000000000, 0.000000000000000000, -1.000000000000000000 ) ) ;
#106434=DIRECTION ( 'NONE',  ( 1.000000000000000000, 0.000000000000000000, 0.000000000000000000 ) ) ;
#106453=CARTESIAN_POINT ( 'NONE',  ( 18.41832399655377372, -9.682403266662264585, -174.1568436200283543 ) ) ;
#106486=VECTOR ( 'NONE', #7502, 1000.000000000000000 ) ;
#106553=VERTEX_POINT ( 'NONE', #243631 ) ;
#106568=ORIENTED_EDGE ( 'NONE', *, *, #75926, .F. ) ;
#106574=VERTEX_POINT ( 'NONE', #27192 ) ;
#106605=CARTESIAN_POINT ( 'NONE',  ( -18.60000000000000142, -9.523954320741635726, -174.3820170568273795 ) ) ;
#106640=ORIENTED_EDGE ( 'NONE', *, *, #228069, .F. ) ;
#106655=VECTOR ( 'NONE', #127388, 1000.000000000000000 ) ;
#106661=DIRECTION ( 'NONE',  ( -3.265361837132813093E-16, 1.000000000000000000, 0.000000000000000000 ) ) ;
#106677=CARTESIAN_POINT ( 'NONE',  ( -1.820710678118658388, -9.929289321870186313, -158.6500000000000057 ) ) ;
#106682=AXIS2_PLACEMENT_3D ( 'NONE', #12363, #231398, #189693 ) ;
#106684=CIRCLE ( 'NONE', #139991, 0.09999999999999939493 ) ;
#106723=CARTESIAN_POINT ( 'NONE',  ( -18.50000000000000000, -1.164121893230052995, -175.4148480855716059 ) ) ;
#106765=CARTESIAN_POINT ( 'NONE',  ( 22.39999999999999503, 7.790779598384535376, -133.9000000000000057 ) ) ;
#106785=ORIENTED_EDGE ( 'NONE', *, *, #256861, .T. ) ;
#106802=DIRECTION ( 'NONE',  ( 1.000000000000000000, 0.000000000000000000, -0.000000000000000000 ) ) ;
#106809=ORIENTED_EDGE ( 'NONE', *, *, #120012, .T. ) ;
#106812=AXIS2_PLACEMENT_3D ( 'NONE', #180088, #86074, #165670 ) ;
#106889=EDGE_CURVE ( 'NONE', #178019, #9008, #220169, .T. ) ;
#106920=DIRECTION ( 'NONE',  ( -2.978066053179067751E-16, 1.000000000000000000, 0.000000000000000000 ) ) ;
#106937=VECTOR ( 'NONE', #138664, 1000.000000000000000 ) ;
#106967=DIRECTION ( 'NONE',  ( 0.000000000000000000, 0.000000000000000000, 1.000000000000000000 ) ) ;
#106982=EDGE_CURVE ( 'NONE', #84861, #256406, #190969, .T. ) ;
#107001=ADVANCED_FACE ( 'NONE', ( #42548 ), #141653, .F. ) ;
#107008=CARTESIAN_POINT ( 'NONE',  ( -23.15000000000000213, -8.999999999988844479, -157.6060308773475924 ) ) ;
#107009=DIRECTION ( 'NONE',  ( 1.000000000000000000, 0.000000000000000000, 0.000000000000000000 ) ) ;
#107035=ORIENTED_EDGE ( 'NONE', *, *, #147076, .T. ) ;
#107096=ADVANCED_FACE ( 'NONE', ( #251000 ), #28159, .T. ) ;
#107152=CARTESIAN_POINT ( 'NONE',  ( -21.55000000000000426, 7.750000000011159074, -155.1500000000000057 ) ) ;
#107162=LINE ( 'NONE', #31522, #52875 ) ;
#107186=CARTESIAN_POINT ( 'NONE',  ( -20.94999999999999929, 1.115600667400684642E-11, -155.7000000000000455 ) ) ;
#107193=AXIS2_PLACEMENT_3D ( 'NONE', #96823, #193411, #229947 ) ;
#107215=VERTEX_POINT ( 'NONE', #220575 ) ;
#107230=EDGE_CURVE ( 'NONE', #52558, #38015, #87529, .T. ) ;
#107240=ORIENTED_EDGE ( 'NONE', *, *, #82875, .F. ) ;
#107250=ORIENTED_EDGE ( 'NONE', *, *, #155424, .F. ) ;
#107273=CARTESIAN_POINT ( 'NONE',  ( -21.12230431290520727, 6.457566653304159132, -133.9947901483110400 ) ) ;
#107295=DIRECTION ( 'NONE',  ( -0.000000000000000000, 0.000000000000000000, -1.000000000000000000 ) ) ;
#107322=CYLINDRICAL_SURFACE ( 'NONE', #72928, 0.09999999999999939493 ) ;
#107341=EDGE_LOOP ( 'NONE', ( #61577, #230770, #82568, #117219 ) ) ;
#107370=ORIENTED_EDGE ( 'NONE', *, *, #230854, .F. ) ;
#107387=DIRECTION ( 'NONE',  ( 0.000000000000000000, 0.000000000000000000, -1.000000000000000000 ) ) ;
#107393=ADVANCED_FACE ( 'NONE', ( #40226 ), #218816, .F. ) ;
#107409=CARTESIAN_POINT ( 'NONE',  ( 20.94999999999999929, -11.48912529306489994, -164.4000000000000057 ) ) ;
#107436=ORIENTED_EDGE ( 'NONE', *, *, #25806, .T. ) ;
#107467=AXIS2_PLACEMENT_3D ( 'NONE', #226642, #88401, #168007 ) ;
#107475=DIRECTION ( 'NONE',  ( -0.000000000000000000, -0.000000000000000000, 1.000000000000000000 ) ) ;
#107489=CARTESIAN_POINT ( 'NONE',  ( -20.54999999999999716, 1.115600667400684642E-11, -167.5000000000000284 ) ) ;
#107503=AXIS2_PLACEMENT_3D ( 'NONE', #182110, #204220, #144233 ) ;
#107572=AXIS2_PLACEMENT_3D ( 'NONE', #52223, #71825, #195632 ) ;
#107593=VECTOR ( 'NONE', #206690, 1000.000000000000000 ) ;
#107625=CARTESIAN_POINT ( 'NONE',  ( -23.25000000000000000, 2.600000000011156054, -147.2246219227621111 ) ) ;
#107635=DIRECTION ( 'NONE',  ( -0.000000000000000000, 0.000000000000000000, 1.000000000000000000 ) ) ;
#107638=DIRECTION ( 'NONE',  ( 0.000000000000000000, -0.8660254037844411501, -0.4999999999999956146 ) ) ;
#107644=ADVANCED_FACE ( 'NONE', ( #164084 ), #4503, .T. ) ;
#107692=EDGE_LOOP ( 'NONE', ( #251133, #164864, #207053, #131372, #197074, #228783, #42431, #22882 ) ) ;
#107726=CARTESIAN_POINT ( 'NONE',  ( 21.05000000000000071, 1.115600667400684642E-11, -167.5000000000000284 ) ) ;
#107727=DIRECTION ( 'NONE',  ( -1.000000000000000000, 0.000000000000000000, 0.000000000000000000 ) ) ;
#107729=AXIS2_PLACEMENT_3D ( 'NONE', #2130, #202910, #240768 ) ;
#107730=AXIS2_PLACEMENT_3D ( 'NONE', #187461, #203151, #105297 ) ;
#107744=ORIENTED_EDGE ( 'NONE', *, *, #237204, .F. ) ;
#107766=CARTESIAN_POINT ( 'NONE',  ( 18.43466021071413863, -9.494190690445385883, -174.1170615601278939 ) ) ;
#107771=AXIS2_PLACEMENT_3D ( 'NONE', #66597, #65301, #27511 ) ;
#107795=DIRECTION ( 'NONE',  ( 1.000000000000000000, -0.000000000000000000, -0.000000000000000000 ) ) ;
#107801=CARTESIAN_POINT ( 'NONE',  ( -20.89192007715128341, 10.32898536001801304, -173.0826683222764757 ) ) ;
#107802=CYLINDRICAL_SURFACE ( 'NONE', #256648, 0.09999999999999817368 ) ;
#107833=EDGE_CURVE ( 'NONE', #197727, #180754, #58230, .T. ) ;
#107922=CARTESIAN_POINT ( 'NONE',  ( -23.15000000000000213, 1.115600667400684642E-11, -134.0000000000000000 ) ) ;
#107932=EDGE_CURVE ( 'NONE', #79795, #246557, #106684, .T. ) ;
#107935=CARTESIAN_POINT ( 'NONE',  ( -21.05000000000000071, -11.48912529306490349, -137.0000000000000000 ) ) ;
#107976=DIRECTION ( 'NONE',  ( 0.000000000000000000, 1.776356839400199780E-15, -1.000000000000000000 ) ) ;
#108040=ORIENTED_EDGE ( 'NONE', *, *, #10208, .F. ) ;
#108071=CARTESIAN_POINT ( 'NONE',  ( -21.55000000000000071, 7.350000000011155166, -146.3500000000000227 ) ) ;
#108091=CIRCLE ( 'NONE', #207489, 4.000000000000003553 ) ;
#108103=DIRECTION ( 'NONE',  ( 0.000000000000000000, 0.000000000000000000, 1.000000000000000000 ) ) ;
#108104=DIRECTION ( 'NONE',  ( -0.000000000000000000, 0.9876197685951279004, -0.1568667991644694115 ) ) ;
#108105=CARTESIAN_POINT ( 'NONE',  ( 18.46082813848004989, -9.480749650896274972, -141.0843701027156669 ) ) ;
#108137=DIRECTION ( 'NONE',  ( -3.469446951953605354E-14, 1.000000000000000000, 0.000000000000000000 ) ) ;
#108154=CARTESIAN_POINT ( 'NONE',  ( 21.14999999999999858, 8.786607556611267356, -146.2500000000000284 ) ) ;
#108164=CIRCLE ( 'NONE', #249803, 0.09999999999998898659 ) ;
#108208=ORIENTED_EDGE ( 'NONE', *, *, #226747, .F. ) ;
#108240=CYLINDRICAL_SURFACE ( 'NONE', #224113, 12.87499999999999822 ) ;
#108242=ORIENTED_EDGE ( 'NONE', *, *, #6164, .F. ) ;
#108247=CARTESIAN_POINT ( 'NONE',  ( -20.64999999999999858, 2.000000000011154189, -154.2753780772379173 ) ) ;
#108253=ORIENTED_EDGE ( 'NONE', *, *, #223786, .T. ) ;
#108261=ADVANCED_FACE ( 'NONE', ( #141331 ), #205133, .F. ) ;
#108324=CARTESIAN_POINT ( 'NONE',  ( 18.59999999999999076, 10.49142135624846439, -158.7500000000000284 ) ) ;
#108327=ORIENTED_EDGE ( 'NONE', *, *, #156572, .T. ) ;
#108338=EDGE_CURVE ( 'NONE', #171037, #188779, #98650, .T. ) ;
#108357=CARTESIAN_POINT ( 'NONE',  ( -21.45000000000000284, 7.708578643773852157, -146.2500000000000284 ) ) ;
#108371=CARTESIAN_POINT ( 'NONE',  ( -18.50000000000000000, 11.75000000001115197, -155.3500000000000227 ) ) ;
#108384=CARTESIAN_POINT ( 'NONE',  ( -20.64999999999999858, 7.150000000011155876, -155.1500000000000057 ) ) ;
#108441=ORIENTED_EDGE ( 'NONE', *, *, #167570, .T. ) ;
#108454=CYLINDRICAL_SURFACE ( 'NONE', #30652, 0.09999999999998898659 ) ;
#108502=CARTESIAN_POINT ( 'NONE',  ( 23.25000000000000000, -11.64999999998884483, -134.0000000000000000 ) ) ;
#108508=DIRECTION ( 'NONE',  ( 2.952720810173289112E-16, -1.000000000000000000, -0.000000000000000000 ) ) ;
#108530=DIRECTION ( 'NONE',  ( 0.000000000000000000, 0.000000000000000000, -1.000000000000000000 ) ) ;
#108544=FACE_OUTER_BOUND ( 'NONE', #202165, .T. ) ;
#108610=CYLINDRICAL_SURFACE ( 'NONE', #124527, 0.09999999999999939493 ) ;
#108615=DIRECTION ( 'NONE',  ( 0.000000000000000000, 0.000000000000000000, -1.000000000000000000 ) ) ;
#108645=AXIS2_PLACEMENT_3D ( 'NONE', #42304, #103540, #100934 ) ;
#108730=EDGE_LOOP ( 'NONE', ( #240037, #143730, #1168, #14931 ) ) ;
#108754=TOROIDAL_SURFACE ( 'NONE', #121277, 7.800000000000000711, 0.1000000000000000056 ) ;
#108788=DIRECTION ( 'NONE',  ( -1.000000000000000000, -0.000000000000000000, -0.000000000000000000 ) ) ;
#108821=CARTESIAN_POINT ( 'NONE',  ( 20.85000000000000142, -11.64999999998883595, -164.6000000000000227 ) ) ;
#108879=ORIENTED_EDGE ( 'NONE', *, *, #41535, .F. ) ;
#108890=CARTESIAN_POINT ( 'NONE',  ( -23.25000000000000000, -1.835859311432481045, -179.0044391687985410 ) ) ;
#108900=DIRECTION ( 'NONE',  ( 0.000000000000000000, -0.1455152366551721865, -0.9893560106964475187 ) ) ;
#108912=ORIENTED_EDGE ( 'NONE', *, *, #163781, .T. ) ;
#108917=DIRECTION ( 'NONE',  ( 0.000000000000000000, 8.673617379884087537E-15, -1.000000000000000000 ) ) ;
#108923=ADVANCED_FACE ( 'NONE', ( #196511 ), #178272, .F. ) ;
#108967=DIRECTION ( 'NONE',  ( -4.239556034732056743E-17, 0.1298341882520022694, 0.9915357197604853789 ) ) ;
#108969=DIRECTION ( 'NONE',  ( -0.000000000000000000, -0.9887567792719339499, -0.1495327102803676589 ) ) ;
#108971=CARTESIAN_POINT ( 'NONE',  ( 19.99999999999998934, 11.65000000001115943, -155.2500000000000284 ) ) ;
#109000=CARTESIAN_POINT ( 'NONE',  ( 18.59999999999999432, 1.728086936805619311, -120.8844350051678020 ) ) ;
#109002=CIRCLE ( 'NONE', #159118, 0.09999999999998898659 ) ;
#109061=CARTESIAN_POINT ( 'NONE',  ( 21.05000000000000071, 1.115600667400684642E-11, -134.0000000000000000 ) ) ;
#109066=VERTEX_POINT ( 'NONE', #4713 ) ;
#109067=DIRECTION ( 'NONE',  ( 0.000000000000000000, 0.5000000000000004441, 0.8660254037844384856 ) ) ;
#109081=DIRECTION ( 'NONE',  ( -2.978066053179067751E-16, 1.000000000000000000, 0.000000000000000000 ) ) ;
#109089=DIRECTION ( 'NONE',  ( 0.000000000000000000, 0.000000000000000000, -1.000000000000000000 ) ) ;
#109110=CIRCLE ( 'NONE', #13277, 2.000000000000002665 ) ;
#109135=ORIENTED_EDGE ( 'NONE', *, *, #79604, .F. ) ;
#109167=ADVANCED_FACE ( 'NONE', ( #69867 ), #72432, .F. ) ;
#109194=CARTESIAN_POINT ( 'NONE',  ( -23.15000000000000213, -4.831324760611774849, -150.9696969421987660 ) ) ;
#109242=FACE_OUTER_BOUND ( 'NONE', #39313, .T. ) ;
#109248=ORIENTED_EDGE ( 'NONE', *, *, #255694, .T. ) ;
#109281=CARTESIAN_POINT ( 'NONE',  ( 20.94999999999999929, 8.776282895303632259, -155.2500000000000284 ) ) ;
#109286=VERTEX_POINT ( 'NONE', #237897 ) ;
#109300=DIRECTION ( 'NONE',  ( 1.000000000000000000, 2.952720810173289112E-16, -0.000000000000000000 ) ) ;
#109323=DIRECTION ( 'NONE',  ( 1.000000000000000000, -0.000000000000000000, -0.000000000000000000 ) ) ;
#109351=CARTESIAN_POINT ( 'NONE',  ( 21.14999999999999858, 10.71339244341104013, -146.3500000000000227 ) ) ;
#109355=DIRECTION ( 'NONE',  ( 0.000000000000000000, 1.000000000000000000, 0.000000000000000000 ) ) ;
#109393=VERTEX_POINT ( 'NONE', #180505 ) ;
#109405=DIRECTION ( 'NONE',  ( 1.000000000000000000, 0.000000000000000000, 0.000000000000000000 ) ) ;
#109415=DIRECTION ( 'NONE',  ( 0.000000000000000000, -1.000000000000000000, 0.000000000000000000 ) ) ;
#109438=CARTESIAN_POINT ( 'NONE',  ( 18.59999999999999787, -1.835341550213255957, -145.6551512925629766 ) ) ;
#109453=CIRCLE ( 'NONE', #205306, 11.89999999999999858 ) ;
#109457=ADVANCED_FACE ( 'NONE', ( #201342 ), #220000, .T. ) ;
#109472=ADVANCED_FACE ( 'NONE', ( #163503 ), #5680, .F. ) ;
#109482=DIRECTION ( 'NONE',  ( 0.000000000000000000, -0.01283462868042125823, -0.9999176327611367654 ) ) ;
#109488=EDGE_CURVE ( 'NONE', #180800, #224095, #53460, .T. ) ;
#109490=ADVANCED_FACE ( 'NONE', ( #104773 ), #149151, .T. ) ;
#109491=AXIS2_PLACEMENT_3D ( 'NONE', #113393, #75574, #233366 ) ;
#109496=ORIENTED_EDGE ( 'NONE', *, *, #70742, .F. ) ;
#109555=ORIENTED_EDGE ( 'NONE', *, *, #218833, .T. ) ;
#109575=AXIS2_PLACEMENT_3D ( 'NONE', #117625, #233733, #36840 ) ;
#109579=AXIS2_PLACEMENT_3D ( 'NONE', #32147, #176786, #114225 ) ;
#109605=AXIS2_PLACEMENT_3D ( 'NONE', #175387, #179233, #237893 ) ;
#109634=DIRECTION ( 'NONE',  ( -1.000000000000000000, 0.000000000000000000, 0.000000000000000000 ) ) ;
#109667=AXIS2_PLACEMENT_3D ( 'NONE', #160626, #255796, #56337 ) ;
#109668=DIRECTION ( 'NONE',  ( 1.000000000000000000, 0.000000000000000000, 0.000000000000000000 ) ) ;
#109676=DIRECTION ( 'NONE',  ( 0.000000000000000000, 0.000000000000000000, -1.000000000000000000 ) ) ;
#109678=DIRECTION ( 'NONE',  ( 0.000000000000000000, -1.000000000000000000, 0.000000000000000000 ) ) ;
#109693=CARTESIAN_POINT ( 'NONE',  ( 18.59999999999999787, -1.835859311432481045, -179.0044391687985410 ) ) ;
#109701=CIRCLE ( 'NONE', #238710, 11.80000000000000426 ) ;
#109710=LINE ( 'NONE', #107152, #152335 ) ;
#109788=ORIENTED_EDGE ( 'NONE', *, *, #189571, .T. ) ;
#109796=DIRECTION ( 'NONE',  ( -1.000000000000000000, 0.000000000000000000, 0.000000000000000000 ) ) ;
#109813=DIRECTION ( 'NONE',  ( 0.000000000000000000, 0.000000000000000000, -1.000000000000000000 ) ) ;
#109818=ORIENTED_EDGE ( 'NONE', *, *, #187097, .F. ) ;
#109827=CARTESIAN_POINT ( 'NONE',  ( 22.59999999999999787, 0.04781839071596408891, -122.2499775809528160 ) ) ;
#109838=DIRECTION ( 'NONE',  ( -0.000000000000000000, 0.000000000000000000, 1.000000000000000000 ) ) ;
#109840=CARTESIAN_POINT ( 'NONE',  ( 23.15000000000000213, -8.663551401857999323, -157.9758988819327215 ) ) ;
#109867=DIRECTION ( 'NONE',  ( 0.000000000000000000, -0.9999176327611369874, 0.01283462868041987913 ) ) ;
#109882=EDGE_CURVE ( 'NONE', #153561, #24271, #193844, .T. ) ;
#109885=DIRECTION ( 'NONE',  ( 0.000000000000000000, -0.000000000000000000, -1.000000000000000000 ) ) ;
#109928=ADVANCED_FACE ( 'NONE', ( #241456 ), #124084, .T. ) ;
#109929=AXIS2_PLACEMENT_3D ( 'NONE', #88350, #182693, #180119 ) ;
#109995=ORIENTED_EDGE ( 'NONE', *, *, #163935, .T. ) ;
#110013=ORIENTED_EDGE ( 'NONE', *, *, #129643, .F. ) ;
#110045=ORIENTED_EDGE ( 'NONE', *, *, #14067, .F. ) ;
#110075=ORIENTED_EDGE ( 'NONE', *, *, #17769, .F. ) ;
#110092=AXIS2_PLACEMENT_3D ( 'NONE', #146887, #166507, #85614 ) ;
#110103=DIRECTION ( 'NONE',  ( 0.000000000000000000, 1.000000000000000000, 0.000000000000000000 ) ) ;
#110108=DIRECTION ( 'NONE',  ( -1.000000000000000000, 0.000000000000000000, 0.000000000000000000 ) ) ;
#110125=DIRECTION ( 'NONE',  ( 1.000000000000000000, -0.000000000000000000, -0.000000000000000000 ) ) ;
#110135=EDGE_CURVE ( 'NONE', #175804, #206030, #215158, .T. ) ;
#110168=ORIENTED_EDGE ( 'NONE', *, *, #126178, .F. ) ;
#110194=CARTESIAN_POINT ( 'NONE',  ( 23.15000000000000213, -8.999999999988842703, -157.6060308773475640 ) ) ;
#110236=AXIS2_PLACEMENT_3D ( 'NONE', #135730, #14538, #193169 ) ;
#110245=CARTESIAN_POINT ( 'NONE',  ( -18.50000972452446035, 10.29326151435326508, -172.9592822510415147 ) ) ;
#110246=DIRECTION ( 'NONE',  ( 0.000000000000000000, -0.1298341882520022694, -0.9915357197604853789 ) ) ;
#110254=CARTESIAN_POINT ( 'NONE',  ( 22.47071067811865319, 0.09909245471376171288, -126.2799252555019649 ) ) ;
#110265=DIRECTION ( 'NONE',  ( -0.7071067811865389130, 0.000000000000000000, 0.7071067811865561215 ) ) ;
#110282=DIRECTION ( 'NONE',  ( 1.000000000000000000, 0.000000000000000000, 0.000000000000000000 ) ) ;
#110290=EDGE_CURVE ( 'NONE', #141516, #61931, #183740, .T. ) ;
#110325=CARTESIAN_POINT ( 'NONE',  ( -21.05000000000000071, 1.162701749949165642, -141.9000000000000341 ) ) ;
#110352=LINE ( 'NONE', #49090, #27737 ) ;
#110364=PLANE ( 'NONE',  #56956 ) ;
#110385=DIRECTION ( 'NONE',  ( 0.000000000000000000, -1.000000000000000000, 0.000000000000000000 ) ) ;
#110387=EDGE_LOOP ( 'NONE', ( #171246, #157220, #201391, #230082 ) ) ;
#110418=ORIENTED_EDGE ( 'NONE', *, *, #225831, .T. ) ;
#110423=VECTOR ( 'NONE', #241617, 1000.000000000000000 ) ;
#110445=EDGE_CURVE ( 'NONE', #46944, #215317, #236985, .T. ) ;
#110508=EDGE_LOOP ( 'NONE', ( #40735, #63359, #188259, #137379 ) ) ;
#110515=EDGE_CURVE ( 'NONE', #117707, #67207, #158104, .T. ) ;
#110536=ORIENTED_EDGE ( 'NONE', *, *, #130062, .T. ) ;
#110557=DIRECTION ( 'NONE',  ( 0.000000000000000000, -1.000000000000000000, 0.000000000000000000 ) ) ;
#110580=DIRECTION ( 'NONE',  ( -0.000000000000000000, -0.000000000000000000, 1.000000000000000000 ) ) ;
#110590=AXIS2_PLACEMENT_3D ( 'NONE', #71325, #53011, #150836 ) ;
#110606=AXIS2_PLACEMENT_3D ( 'NONE', #122886, #42074, #81159 ) ;
#110613=EDGE_CURVE ( 'NONE', #126714, #140417, #83000, .T. ) ;
#110661=EDGE_CURVE ( 'NONE', #175518, #95323, #149710, .T. ) ;
#110665=CARTESIAN_POINT ( 'NONE',  ( 18.47073956224757296, -9.471729412460623720, -141.1086857528176779 ) ) ;
#110695=EDGE_CURVE ( 'NONE', #170246, #165391, #245546, .T. ) ;
#110715=CARTESIAN_POINT ( 'NONE',  ( -21.53752568617681007, 6.786807874514923178, -133.9010255387155723 ) ) ;
#110732=LINE ( 'NONE', #190291, #57543 ) ;
#110741=DIRECTION ( 'NONE',  ( 0.000000000000000000, 0.1568667991644863147, -0.9876197685951252359 ) ) ;
#110751=VERTEX_POINT ( 'NONE', #147393 ) ;
#110756=ORIENTED_EDGE ( 'NONE', *, *, #200873, .F. ) ;
#110774=CARTESIAN_POINT ( 'NONE',  ( 21.03675099975492202, 8.875180032795963569, -146.3255421367780968 ) ) ;
#110779=FACE_OUTER_BOUND ( 'NONE', #207838, .T. ) ;
#110782=ORIENTED_EDGE ( 'NONE', *, *, #10208, .T. ) ;
#110848=LINE ( 'NONE', #187844, #232299 ) ;
#110873=DIRECTION ( 'NONE',  ( 1.000000000000000000, -0.000000000000000000, -0.000000000000000000 ) ) ;
#110876=ORIENTED_EDGE ( 'NONE', *, *, #134126, .F. ) ;
#110879=CARTESIAN_POINT ( 'NONE',  ( 20.85000000000000142, -1.135018845899022466, -175.2169768834323520 ) ) ;
#110880=CYLINDRICAL_SURFACE ( 'NONE', #33162, 0.1000000000000101918 ) ;
#110889=CIRCLE ( 'NONE', #256374, 0.1999999999999996503 ) ;
#110944=CARTESIAN_POINT ( 'NONE',  ( -18.59999999999999787, 1.162701749949165642, -142.1000000000000227 ) ) ;
#110948=FACE_OUTER_BOUND ( 'NONE', #187127, .T. ) ;
#110954=CARTESIAN_POINT ( 'NONE',  ( 22.48660254037844197, 11.65000000001116298, -133.9500000000000171 ) ) ;
#110965=CARTESIAN_POINT ( 'NONE',  ( 21.05000000000000071, 8.776282895303630482, -142.5586289951409640 ) ) ;
#110977=FACE_OUTER_BOUND ( 'NONE', #55221, .T. ) ;
#110983=DIRECTION ( 'NONE',  ( 1.000000000000000000, 0.000000000000000000, 0.000000000000000000 ) ) ;
#110986=ORIENTED_EDGE ( 'NONE', *, *, #175310, .T. ) ;
#111004=VERTEX_POINT ( 'NONE', #155447 ) ;
#111013=TOROIDAL_SURFACE ( 'NONE', #115119, 1.900000000000002576, 0.1000000000000000056 ) ;
#111047=ORIENTED_EDGE ( 'NONE', *, *, #186666, .F. ) ;
#111055=VECTOR ( 'NONE', #230873, 1000.000000000000000 ) ;
#111070=ORIENTED_EDGE ( 'NONE', *, *, #138586, .F. ) ;
#111082=EDGE_CURVE ( 'NONE', #58852, #136758, #211680, .T. ) ;
#111087=ORIENTED_EDGE ( 'NONE', *, *, #25337, .T. ) ;
#111105=ORIENTED_EDGE ( 'NONE', *, *, #6773, .F. ) ;
#111112=CIRCLE ( 'NONE', #177773, 0.2000000000000057288 ) ;
#111115=VERTEX_POINT ( 'NONE', #79697 ) ;
#111135=CARTESIAN_POINT ( 'NONE',  ( -21.09610168723073542, 6.378955715235934854, -133.9664104931085546 ) ) ;
#111163=CARTESIAN_POINT ( 'NONE',  ( 18.54148534481893407, 10.32532329027886675, -173.0699343018359855 ) ) ;
#111168=DIRECTION ( 'NONE',  ( 0.000000000000000000, -1.000000000000000000, 0.000000000000000000 ) ) ;
#111172=CIRCLE ( 'NONE', #214634, 0.2000000000000057288 ) ;
#111201=ORIENTED_EDGE ( 'NONE', *, *, #199696, .F. ) ;
#111221=CIRCLE ( 'NONE', #82150, 0.09999999999998898659 ) ;
#111231=CARTESIAN_POINT ( 'NONE',  ( -23.15000000000000213, 11.75000000001115552, -146.2500000000000284 ) ) ;
#111235=EDGE_LOOP ( 'NONE', ( #91663, #250856, #158935, #231166 ) ) ;
#111239=CARTESIAN_POINT ( 'NONE',  ( 23.14999999999999503, 6.650000000011155876, -155.2500000000000284 ) ) ;
#111258=EDGE_CURVE ( 'NONE', #128012, #121012, #124543, .T. ) ;
#111265=CARTESIAN_POINT ( 'NONE',  ( -21.05000000000000071, 1.115600667400684642E-11, -134.0000000000000000 ) ) ;
#111275=AXIS2_PLACEMENT_3D ( 'NONE', #28674, #229401, #166886 ) ;
#111306=ORIENTED_EDGE ( 'NONE', *, *, #29312, .T. ) ;
#111315=AXIS2_PLACEMENT_3D ( 'NONE', #228684, #129572, #125706 ) ;
#111327=EDGE_CURVE ( 'NONE', #104663, #185781, #112147, .T. ) ;
#111354=DIRECTION ( 'NONE',  ( -1.000000000000000000, -0.000000000000000000, -0.000000000000000000 ) ) ;
#111380=DIRECTION ( 'NONE',  ( 1.000000000000000000, 2.952720810173289112E-16, -0.000000000000000000 ) ) ;
#111387=AXIS2_PLACEMENT_3D ( 'NONE', #254932, #178049, #235417 ) ;
#111397=DIRECTION ( 'NONE',  ( -1.000000000000000000, 0.000000000000000000, 0.000000000000000000 ) ) ;
#111414=ORIENTED_EDGE ( 'NONE', *, *, #45538, .T. ) ;
#111440=DIRECTION ( 'NONE',  ( 1.000000000000000000, -0.000000000000000000, -0.000000000000000000 ) ) ;
#111467=DIRECTION ( 'NONE',  ( 1.000000000000000000, -0.000000000000000000, -0.000000000000000000 ) ) ;
#111496=LINE ( 'NONE', #96710, #189405 ) ;
#111499=FACE_OUTER_BOUND ( 'NONE', #41005, .T. ) ;
#111514=SPHERICAL_SURFACE ( 'NONE', #186413, 0.1000000000000000056 ) ;
#111526=CARTESIAN_POINT ( 'NONE',  ( -21.05000000000000071, 1.162701749949165642, -142.0000000000000284 ) ) ;
#111538=CARTESIAN_POINT ( 'NONE',  ( -18.50596464788227635, 10.30632246271647112, -173.0041836778896140 ) ) ;
#111544=ADVANCED_FACE ( 'NONE', ( #2420 ), #41169, .T. ) ;
#111584=LINE ( 'NONE', #11200, #162207 ) ;
#111595=CARTESIAN_POINT ( 'NONE',  ( -18.59999999999999787, 11.65000000001115232, -155.3500000000000227 ) ) ;
#111601=CARTESIAN_POINT ( 'NONE',  ( 20.94999999999999929, 1.115600667400684642E-11, -167.5000000000000284 ) ) ;
#111608=DIRECTION ( 'NONE',  ( 1.734723475976817507E-14, -1.000000000000000000, 0.000000000000000000 ) ) ;
#111616=CARTESIAN_POINT ( 'NONE',  ( -23.15000000000000213, 4.150000000011156764, -146.3500000000000227 ) ) ;
#111622=CARTESIAN_POINT ( 'NONE',  ( 18.49505816908823519, -9.437872553199978753, -174.2776572016709054 ) ) ;
#111626=DIRECTION ( 'NONE',  ( -1.000000000000000000, -7.304098846218134667E-16, 0.000000000000000000 ) ) ;
#111651=CARTESIAN_POINT ( 'NONE',  ( -20.85000000000000142, 11.65000000001115232, -167.5000000000000284 ) ) ;
#111700=LINE ( 'NONE', #210799, #13541 ) ;
#111708=VERTEX_POINT ( 'NONE', #47974 ) ;
#111725=DIRECTION ( 'NONE',  ( -1.000000000000000000, 0.000000000000000000, 0.000000000000000000 ) ) ;
#111734=EDGE_LOOP ( 'NONE', ( #129241, #125176, #33321, #87818 ) ) ;
#111769=AXIS2_PLACEMENT_3D ( 'NONE', #65113, #28617, #123818 ) ;
#111786=ORIENTED_EDGE ( 'NONE', *, *, #244732, .F. ) ;
#111799=AXIS2_PLACEMENT_3D ( 'NONE', #87512, #208777, #206199 ) ;
#111813=DIRECTION ( 'NONE',  ( 1.000000000000000000, -0.000000000000000000, -0.000000000000000000 ) ) ;
#111832=DIRECTION ( 'NONE',  ( 0.000000000000000000, 2.664535259100430523E-15, -1.000000000000000000 ) ) ;
#111845=CARTESIAN_POINT ( 'NONE',  ( -21.14999999999999858, 6.540656951712399803, -134.0000000000000284 ) ) ;
#111855=CARTESIAN_POINT ( 'NONE',  ( 23.14999999999999858, 1.115600667400684642E-11, -146.8750000000000000 ) ) ;
#111874=AXIS2_PLACEMENT_3D ( 'NONE', #242063, #102519, #42585 ) ;
#111920=VERTEX_POINT ( 'NONE', #30380 ) ;
#111978=VERTEX_POINT ( 'NONE', #149046 ) ;
#111980=DIRECTION ( 'NONE',  ( 1.000000000000000000, -0.000000000000000000, -0.000000000000000000 ) ) ;
#112006=EDGE_LOOP ( 'NONE', ( #238034, #221388, #245469, #136768 ) ) ;
#112009=ADVANCED_FACE ( 'NONE', ( #172496 ), #251973, .T. ) ;
#112046=VECTOR ( 'NONE', #65605, 1000.000000000000000 ) ;
#112051=EDGE_CURVE ( 'NONE', #33915, #228115, #4092, .T. ) ;
#112099=VECTOR ( 'NONE', #37834, 1000.000000000000114 ) ;
#112109=CARTESIAN_POINT ( 'NONE',  ( -20.54999999999999716, 2.000000000011154189, -154.2753780772379173 ) ) ;
#112110=EDGE_LOOP ( 'NONE', ( #118187, #130655, #80593, #211874 ) ) ;
#112119=AXIS2_PLACEMENT_3D ( 'NONE', #255292, #79251, #136668 ) ;
#112122=DIRECTION ( 'NONE',  ( -0.000000000000000000, 1.265107689135680095E-16, -1.000000000000000000 ) ) ;
#112123=EDGE_CURVE ( 'NONE', #170589, #169023, #133322, .T. ) ;
#112147=LINE ( 'NONE', #156420, #24610 ) ;
#112186=PLANE ( 'NONE',  #133325 ) ;
#112188=VECTOR ( 'NONE', #140455, 1000.000000000000000 ) ;
#112189=EDGE_CURVE ( 'NONE', #87130, #156098, #108164, .T. ) ;
#112198=EDGE_CURVE ( 'NONE', #85212, #105589, #100573, .T. ) ;
#112202=AXIS2_PLACEMENT_3D ( 'NONE', #218834, #37673, #131938 ) ;
#112205=CIRCLE ( 'NONE', #29021, 4.099999999999992539 ) ;
#112221=PRODUCT_CONTEXT ( 'NONE', #52359, 'mechanical' ) ;
#112258=ORIENTED_EDGE ( 'NONE', *, *, #164978, .F. ) ;
#112278=CARTESIAN_POINT ( 'NONE',  ( -23.15000000000000213, -8.999999999988844479, -158.2060308773475867 ) ) ;
#112348=EDGE_CURVE ( 'NONE', #87859, #172414, #50063, .T. ) ;
#112379=ORIENTED_EDGE ( 'NONE', *, *, #214107, .F. ) ;
#112389=EDGE_CURVE ( 'NONE', #40580, #159384, #66625, .T. ) ;
#112415=AXIS2_PLACEMENT_3D ( 'NONE', #29853, #11563, #151062 ) ;
#112453=CARTESIAN_POINT ( 'NONE',  ( 20.86036036209916134, 10.62104277658212048, -141.6663484185077664 ) ) ;
#112467=CARTESIAN_POINT ( 'NONE',  ( 18.49999999999999645, 1.637172712981537659, -145.5821533654720383 ) ) ;
#112496=CIRCLE ( 'NONE', #145784, 2.000000000000002665 ) ;
#112505=CARTESIAN_POINT ( 'NONE',  ( 18.59999999999996945, 7.021664781911246322, -171.3335654018973173 ) ) ;
#112522=LINE ( 'NONE', #132079, #42975 ) ;
#112525=ORIENTED_EDGE ( 'NONE', *, *, #248374, .F. ) ;
#112554=ORIENTED_EDGE ( 'NONE', *, *, #97517, .F. ) ;
#112557=DIRECTION ( 'NONE',  ( -1.000000000000000000, -7.304098846218134667E-16, 0.000000000000000000 ) ) ;
#112570=ORIENTED_EDGE ( 'NONE', *, *, #4389, .T. ) ;
#112576=EDGE_CURVE ( 'NONE', #171400, #200447, #187455, .T. ) ;
#112600=CARTESIAN_POINT ( 'NONE',  ( -18.59999999999999787, 11.60000000001115872, -140.9282032302755852 ) ) ;
#112620=CIRCLE ( 'NONE', #95840, 0.09999999999998898659 ) ;
#112623=CARTESIAN_POINT ( 'NONE',  ( 20.94999999999999574, 8.926614585098251453, -142.4716830192231498 ) ) ;
#112639=EDGE_CURVE ( 'NONE', #52565, #220745, #104219, .T. ) ;
#112657=ORIENTED_EDGE ( 'NONE', *, *, #125868, .T. ) ;
#112672=EDGE_CURVE ( 'NONE', #178157, #17731, #25151, .T. ) ;
#112684=ORIENTED_EDGE ( 'NONE', *, *, #230608, .T. ) ;
#112685=CYLINDRICAL_SURFACE ( 'NONE', #116104, 0.09999999999998898659 ) ;
#112692=AXIS2_PLACEMENT_3D ( 'NONE', #123559, #145672, #223918 ) ;
#112751=CARTESIAN_POINT ( 'NONE',  ( 20.94999999999999574, -11.64999999998883595, -137.1000000000000227 ) ) ;
#112812=CARTESIAN_POINT ( 'NONE',  ( 21.05543885634738288, 8.775771046858691804, -146.1843844707147184 ) ) ;
#112814=ORIENTED_EDGE ( 'NONE', *, *, #155124, .T. ) ;
#112822=CARTESIAN_POINT ( 'NONE',  ( -18.56579813702276027, 10.33025634372637569, -173.0870929282638997 ) ) ;
#112883=CYLINDRICAL_SURFACE ( 'NONE', #98891, 12.87499999999999822 ) ;
#112893=TOROIDAL_SURFACE ( 'NONE', #167094, 1.900000000000002576, 0.1000000000000000056 ) ;
#112910=CARTESIAN_POINT ( 'NONE',  ( 18.52326479938695059, -9.642364444904258036, -174.2147574134058061 ) ) ;
#112929=FACE_OUTER_BOUND ( 'NONE', #89162, .T. ) ;
#112934=VERTEX_POINT ( 'NONE', #3442 ) ;
#112944=AXIS2_PLACEMENT_3D ( 'NONE', #52506, #235020, #252002 ) ;
#112984=ORIENTED_EDGE ( 'NONE', *, *, #242156, .F. ) ;
#112986=ORIENTED_EDGE ( 'NONE', *, *, #186678, .F. ) ;
#113059=LINE ( 'NONE', #154779, #226060 ) ;
#113088=CARTESIAN_POINT ( 'NONE',  ( 20.85000000000000142, -1.835859311432481045, -179.0044391687985410 ) ) ;
#113105=CARTESIAN_POINT ( 'NONE',  ( -21.05000000000000071, 1.250000000011155299, -142.0000000000000284 ) ) ;
#113140=CARTESIAN_POINT ( 'NONE',  ( -20.64999999999999858, 4.350000000011156054, -146.2500000000000284 ) ) ;
#113162=AXIS2_PLACEMENT_3D ( 'NONE', #182164, #101277, #183448 ) ;
#113183=EDGE_CURVE ( 'NONE', #198238, #207656, #34593, .T. ) ;
#113198=DIRECTION ( 'NONE',  ( 1.000000000000000000, -7.304098846218133681E-16, 4.607487905232622991E-31 ) ) ;
#113209=ORIENTED_EDGE ( 'NONE', *, *, #67960, .F. ) ;
#113212=DIRECTION ( 'NONE',  ( 0.000000000000000000, 0.000000000000000000, -1.000000000000000000 ) ) ;
#113213=VECTOR ( 'NONE', #202555, 1000.000000000000000 ) ;
#113229=CIRCLE ( 'NONE', #25750, 0.2000000000000057288 ) ;
#113233=B_SPLINE_CURVE_WITH_KNOTS ( 'NONE', 3,
 ( #80844, #138251, #178724, #101677, #118731, #156596, #40498, #160439, #120030, #142119, #237380, #199561, #2602, #216523, #37916, #157889, #79563, #159150, #238659 ),
 .UNSPECIFIED., .F., .F.,
 ( 4, 3, 3, 3, 3, 3, 4 ),
 ( 1.387778780781445676E-17, 2.646747978908746348E-05, 5.271166642127513550E-05, 9.008788829882962801E-05, 0.0001426648776560695663, 0.0001897378458659517613, 0.0001917382627806230261 ),
 .UNSPECIFIED. ) ;
#113250=CARTESIAN_POINT ( 'NONE',  ( 21.05000000000000071, 10.72371710471867701, -141.6649135690876165 ) ) ;
#113264=ORIENTED_EDGE ( 'NONE', *, *, #121609, .F. ) ;
#113280=LINE ( 'NONE', #192828, #19888 ) ;
#113293=CARTESIAN_POINT ( 'NONE',  ( -23.15000000000000213, 1.115600667400684642E-11, -146.8750000000000000 ) ) ;
#113321=CIRCLE ( 'NONE', #121718, 0.6000000000000015321 ) ;
#113353=ORIENTED_EDGE ( 'NONE', *, *, #41193, .F. ) ;
#113393=CARTESIAN_POINT ( 'NONE',  ( -21.05000000000000071, 1.115600667400684642E-11, -167.5000000000000284 ) ) ;
#113405=DIRECTION ( 'NONE',  ( 0.000000000000000000, 0.000000000000000000, -1.000000000000000000 ) ) ;
#113416=CIRCLE ( 'NONE', #9348, 0.09999999999999817368 ) ;
#113418=CARTESIAN_POINT ( 'NONE',  ( 20.94999999999999929, -1.835859311432481045, -179.0044391687985410 ) ) ;
#113424=DIRECTION ( 'NONE',  ( 0.000000000000000000, -0.9915357197604971473, 0.1298341882519111479 ) ) ;
#113445=CARTESIAN_POINT ( 'NONE',  ( 23.14999999999999503, 6.450000000011156587, -155.1500000000000057 ) ) ;
#113476=CARTESIAN_POINT ( 'NONE',  ( 18.50000000000000000, -9.499999999988842703, -122.2500000000000284 ) ) ;
#113482=ORIENTED_EDGE ( 'NONE', *, *, #37249, .T. ) ;
#113496=DIRECTION ( 'NONE',  ( 0.000000000000000000, -1.224646799142185182E-16, 1.000000000000000000 ) ) ;
#113507=CARTESIAN_POINT ( 'NONE',  ( -18.59999999999999787, 9.350000000011156942, -155.1500000000000057 ) ) ;
#113526=EDGE_CURVE ( 'NONE', #109066, #156163, #187999, .T. ) ;
#113534=EDGE_CURVE ( 'NONE', #163189, #153155, #204722, .T. ) ;
#113536=VERTEX_POINT ( 'NONE', #198152 ) ;
#113574=CARTESIAN_POINT ( 'NONE',  ( 18.39999999999999858, -9.499999999988842703, -141.0320693966996828 ) ) ;
#113575=ORIENTED_EDGE ( 'NONE', *, *, #61688, .F. ) ;
#113586=DIRECTION ( 'NONE',  ( 1.000000000000000000, 0.000000000000000000, 0.000000000000000000 ) ) ;
#113591=ORIENTED_EDGE ( 'NONE', *, *, #59122, .T. ) ;
#113603=VERTEX_POINT ( 'NONE', #125050 ) ;
#113633=ADVANCED_FACE ( 'NONE', ( #1215 ), #221541, .T. ) ;
#113634=CARTESIAN_POINT ( 'NONE',  ( 23.15000000000000213, -12.41227409413852811, -164.4000000000000057 ) ) ;
#113675=CARTESIAN_POINT ( 'NONE',  ( -22.59999999999999787, 11.74956712350054744, -133.8991416309013118 ) ) ;
#113685=VERTEX_POINT ( 'NONE', #239863 ) ;
#113728=ORIENTED_EDGE ( 'NONE', *, *, #177607, .T. ) ;
#113755=ORIENTED_EDGE ( 'NONE', *, *, #86892, .T. ) ;
#113758=EDGE_CURVE ( 'NONE', #218074, #231169, #71667, .T. ) ;
#113767=AXIS2_PLACEMENT_3D ( 'NONE', #213694, #31258, #110741 ) ;
#113804=CARTESIAN_POINT ( 'NONE',  ( -18.52139480978222963, -9.481358845055737561, -141.0245565671190491 ) ) ;
#113875=DIRECTION ( 'NONE',  ( 2.952720810173289112E-16, -1.000000000000000000, 0.000000000000000000 ) ) ;
#113906=CARTESIAN_POINT ( 'NONE',  ( 18.59999999999999076, 11.75000000001115907, -158.8500000000000227 ) ) ;
#113913=CARTESIAN_POINT ( 'NONE',  ( 20.94999999999999929, 1.115600667400684642E-11, -167.5000000000000284 ) ) ;
#113916=CARTESIAN_POINT ( 'NONE',  ( 23.15000000000000213, -11.64999999998883595, -164.5000000000000000 ) ) ;
#113943=ADVANCED_FACE ( 'NONE', ( #53202 ), #234393, .T. ) ;
#113973=VERTEX_POINT ( 'NONE', #195310 ) ;
#113976=AXIS2_PLACEMENT_3D ( 'NONE', #926, #123482, #60929 ) ;
#113986=EDGE_CURVE ( 'NONE', #235252, #51770, #134174, .T. ) ;
#114021=LINE ( 'NONE', #93181, #155928 ) ;
#114038=CARTESIAN_POINT ( 'NONE',  ( -20.64999999999999858, -8.999999999988844479, -158.1060308773475924 ) ) ;
#114077=CARTESIAN_POINT ( 'NONE',  ( 21.05095171578076574, 8.776179878782192745, -146.1658732766379103 ) ) ;
#114087=ORIENTED_EDGE ( 'NONE', *, *, #198811, .F. ) ;
#114101=VECTOR ( 'NONE', #100445, 1000.000000000000000 ) ;
#114135=CYLINDRICAL_SURFACE ( 'NONE', #124773, 0.09999999999999939493 ) ;
#114166=AXIS2_PLACEMENT_3D ( 'NONE', #24376, #225093, #226375 ) ;
#114188=CIRCLE ( 'NONE', #222502, 0.1000000000000089567 ) ;
#114194=DIRECTION ( 'NONE',  ( -1.000000000000000000, 0.000000000000000000, 0.000000000000000000 ) ) ;
#114200=CARTESIAN_POINT ( 'NONE',  ( -22.49436431346200038, 11.64995094766461392, -133.9330964702777749 ) ) ;
#114204=ADVANCED_FACE ( 'NONE', ( #169029 ), #100996, .F. ) ;
#114207=DIRECTION ( 'NONE',  ( 0.000000000000000000, 1.000000000000000000, 0.000000000000000000 ) ) ;
#114210=CARTESIAN_POINT ( 'NONE',  ( 21.14999999999999858, 6.550000000011156231, -146.1500000000000341 ) ) ;
#114225=DIRECTION ( 'NONE',  ( 0.000000000000000000, 0.000000000000000000, 1.000000000000000000 ) ) ;
#114241=DIRECTION ( 'NONE',  ( 1.000000000000000000, 0.000000000000000000, -0.000000000000000000 ) ) ;
#114252=ORIENTED_EDGE ( 'NONE', *, *, #188753, .F. ) ;
#114275=VERTEX_POINT ( 'NONE', #227669 ) ;
#114289=CARTESIAN_POINT ( 'NONE',  ( -21.07016717457010557, 1.115297090792388540E-11, -127.6790591618991044 ) ) ;
#114331=CIRCLE ( 'NONE', #234965, 12.87499999999999822 ) ;
#114339=ORIENTED_EDGE ( 'NONE', *, *, #241021, .F. ) ;
#114366=DIRECTION ( 'NONE',  ( -1.000000000000000000, 0.000000000000000000, 0.000000000000000000 ) ) ;
#114382=ADVANCED_FACE ( 'NONE', ( #73769 ), #231542, .F. ) ;
#114387=DIRECTION ( 'NONE',  ( 1.000000000000000000, 0.000000000000000000, 0.000000000000000000 ) ) ;
#114397=CARTESIAN_POINT ( 'NONE',  ( -20.94999999999999929, 1.250000000011155299, -142.0000000000000284 ) ) ;
#114404=CARTESIAN_POINT ( 'NONE',  ( -21.04999999999999716, 6.497017786442110143, -134.0145456905664503 ) ) ;
#114418=ORIENTED_EDGE ( 'NONE', *, *, #222621, .F. ) ;
#114421=CIRCLE ( 'NONE', #18559, 0.09999999999998898659 ) ;
#114451=ORIENTED_EDGE ( 'NONE', *, *, #82271, .T. ) ;
#114456=CARTESIAN_POINT ( 'NONE',  ( -23.15000000000000213, 4.350000000011156054, -155.3500000000000227 ) ) ;
#114463=CIRCLE ( 'NONE', #27014, 0.1000000000000043493 ) ;
#114465=ORIENTED_EDGE ( 'NONE', *, *, #159451, .F. ) ;
#114466=CARTESIAN_POINT ( 'NONE',  ( 20.12500000000000000, 9.750000000011153745, -142.1117712821142902 ) ) ;
#114479=FACE_OUTER_BOUND ( 'NONE', #58999, .T. ) ;
#114502=DIRECTION ( 'NONE',  ( 0.000000000000000000, 0.000000000000000000, -1.000000000000000000 ) ) ;
#114506=CIRCLE ( 'NONE', #2054, 12.77500000000000924 ) ;
#114563=CARTESIAN_POINT ( 'NONE',  ( -20.64999999999999858, 4.350000000011156054, -155.1500000000000057 ) ) ;
#114566=CARTESIAN_POINT ( 'NONE',  ( -18.59999999999999787, 5.900000000011102586, -144.2190997646564483 ) ) ;
#114570=CARTESIAN_POINT ( 'NONE',  ( -21.07016717456945543, 6.320940838111416049, -134.0000000000000000 ) ) ;
#114606=FACE_OUTER_BOUND ( 'NONE', #48282, .T. ) ;
#114676=EDGE_LOOP ( 'NONE', ( #42814, #220346, #125137, #8732 ) ) ;
#114685=DIRECTION ( 'NONE',  ( 0.000000000000000000, 0.000000000000000000, 1.000000000000000000 ) ) ;
#114695=EDGE_LOOP ( 'NONE', ( #158689, #70405, #207315, #87167 ) ) ;
#114723=AXIS2_PLACEMENT_3D ( 'NONE', #179111, #177815, #218170 ) ;
#114764=DIRECTION ( 'NONE',  ( -4.801466763864313332E-15, -0.2605042016806672911, -0.9654727137038716656 ) ) ;
#114816=CARTESIAN_POINT ( 'NONE',  ( 20.95512820512820440, 8.876151316299273120, -142.5586289951409640 ) ) ;
#114871=DIRECTION ( 'NONE',  ( -1.000000000000000000, 0.000000000000000000, 0.000000000000000000 ) ) ;
#114876=CARTESIAN_POINT ( 'NONE',  ( -22.39999999999999858, 1.115600667400684642E-11, -122.3504291924552234 ) ) ;
#114903=EDGE_LOOP ( 'NONE', ( #24160, #126505, #164903, #240822, #64557 ) ) ;
#114905=( BOUNDED_CURVE ( )  B_SPLINE_CURVE ( 3, ( #185923, #47676, #206776, #78475 ),
 .UNSPECIFIED., .F., .F. ) 
 B_SPLINE_CURVE_WITH_KNOTS ( ( 4, 4 ),
 ( 4.712388980384690562, 6.283185307179586232 ),
 .UNSPECIFIED. ) 
 CURVE ( )  GEOMETRIC_REPRESENTATION_ITEM ( )  RATIONAL_B_SPLINE_CURVE ( ( 1.000000000000000000, 0.8047378541243652705, 0.8047378541243652705, 1.000000000000000000 ) ) 
 REPRESENTATION_ITEM ( '' )  );
#114919=ORIENTED_EDGE ( 'NONE', *, *, #87451, .T. ) ;
#114930=VECTOR ( 'NONE', #108508, 1000.000000000000000 ) ;
#114955=VERTEX_POINT ( 'NONE', #92430 ) ;
#114959=ORIENTED_EDGE ( 'NONE', *, *, #3146, .F. ) ;
#114965=DIRECTION ( 'NONE',  ( -1.000000000000000000, -2.952720810173289112E-16, 0.000000000000000000 ) ) ;
#114976=ORIENTED_EDGE ( 'NONE', *, *, #229883, .F. ) ;
#115013=FACE_OUTER_BOUND ( 'NONE', #215278, .T. ) ;
#115025=ADVANCED_FACE ( 'NONE', ( #213678 ), #51316, .F. ) ;
#115055=ADVANCED_FACE ( 'NONE', ( #235797 ), #41479, .T. ) ;
#115068=EDGE_CURVE ( 'NONE', #148396, #219363, #178430, .T. ) ;
#115109=EDGE_CURVE ( 'NONE', #112934, #247963, #209182, .T. ) ;
#115113=DIRECTION ( 'NONE',  ( 1.000000000000000000, -0.000000000000000000, -0.000000000000000000 ) ) ;
#115116=DIRECTION ( 'NONE',  ( -2.827886303505248766E-16, 0.8660254037844411501, 0.4999999999999956146 ) ) ;
#115119=AXIS2_PLACEMENT_3D ( 'NONE', #257549, #97206, #78945 ) ;
#115122=AXIS2_PLACEMENT_3D ( 'NONE', #233056, #252583, #34863 ) ;
#115130=DIRECTION ( 'NONE',  ( 0.000000000000000000, 0.000000000000000000, -1.000000000000000000 ) ) ;
#115139=CARTESIAN_POINT ( 'NONE',  ( -23.15000000000000213, 1.115600667400684642E-11, -167.5000000000000284 ) ) ;
#115180=AXIS2_PLACEMENT_3D ( 'NONE', #68889, #166720, #6315 ) ;
#115185=EDGE_LOOP ( 'NONE', ( #195511, #188348, #130710 ) ) ;
#115189=CARTESIAN_POINT ( 'NONE',  ( 23.15000000000000213, -11.48912529306489994, -164.4000000000000057 ) ) ;
#115207=CARTESIAN_POINT ( 'NONE',  ( 21.30000000000002558, 1.115600667400684642E-11, -134.0000000000000000 ) ) ;
#115221=CARTESIAN_POINT ( 'NONE',  ( 21.05000000000000071, 6.300183336278856849, -133.9486725676586616 ) ) ;
#115227=ADVANCED_FACE ( 'NONE', ( #136039 ), #71515, .T. ) ;
#115233=DIRECTION ( 'NONE',  ( -1.000000000000000000, 0.000000000000000000, 0.000000000000000000 ) ) ;
#115258=VERTEX_POINT ( 'NONE', #252151 ) ;
#115271=DIRECTION ( 'NONE',  ( 0.000000000000000000, 0.000000000000000000, 1.000000000000000000 ) ) ;
#115283=AXIS2_PLACEMENT_3D ( 'NONE', #77691, #239355, #159834 ) ;
#115322=ADVANCED_FACE ( 'NONE', ( #202470 ), #251445, .T. ) ;
#115339=ADVANCED_FACE ( 'NONE', ( #179083 ), #42129, .T. ) ;
#115372=AXIS2_PLACEMENT_3D ( 'NONE', #150297, #168613, #91594 ) ;
#115389=AXIS2_PLACEMENT_3D ( 'NONE', #126847, #145107, #205077 ) ;
#115429=TOROIDAL_SURFACE ( 'NONE', #86192, 11.65000000000000036, 0.1000000000000000056 ) ;
#115450=AXIS2_PLACEMENT_3D ( 'NONE', #9466, #109838, #130692 ) ;
#115458=CARTESIAN_POINT ( 'NONE',  ( 21.09316766718127667, 6.370153312485567376, -133.9607365976853259 ) ) ;
#115486=CARTESIAN_POINT ( 'NONE',  ( 21.05000000000000071, 8.876614585098254295, -142.3850804788447135 ) ) ;
#115533=ORIENTED_EDGE ( 'NONE', *, *, #147826, .T. ) ;
#115541=CARTESIAN_POINT ( 'NONE',  ( -20.94999999999999929, 1.115600667400684642E-11, -167.5000000000000284 ) ) ;
#115579=CIRCLE ( 'NONE', #228212, 0.09999999999999363565 ) ;
#115616=VERTEX_POINT ( 'NONE', #117494 ) ;
#115645=DIRECTION ( 'NONE',  ( 1.000000000000000000, -0.000000000000000000, -0.000000000000000000 ) ) ;
#115648=CARTESIAN_POINT ( 'NONE',  ( -18.59999999999999787, -1.835859311432484375, -179.0044391687985410 ) ) ;
#115652=ORIENTED_EDGE ( 'NONE', *, *, #126168, .F. ) ;
#115667=CARTESIAN_POINT ( 'NONE',  ( 18.59999999999999076, 1.750000000011155743, -145.6695115579016715 ) ) ;
#115673=EDGE_CURVE ( 'NONE', #236893, #154872, #217724, .T. ) ;
#115687=ORIENTED_EDGE ( 'NONE', *, *, #43134, .T. ) ;
#115691=CARTESIAN_POINT ( 'NONE',  ( -21.05000000000000071, 6.344723404101401343, -133.9852821434760699 ) ) ;
#115715=( BOUNDED_SURFACE ( )  B_SPLINE_SURFACE ( 3, 2, ( 
 ( #207216, #105493, #149814 ),
 ( #7727, #229342, #26004 ),
 ( #185064, #85932, #165520 ),
 ( #110665, #28618, #50664 ),
 ( #108105, #130210, #45559 ),
 ( #209771, #243756, #65114 ),
 ( #125112, #190213, #164236 ),
 ( #245042, #204615, #66407 ) ),
 .UNSPECIFIED., .F., .F., .T. ) 
 B_SPLINE_SURFACE_WITH_KNOTS ( ( 4, 2, 2, 4 ),
 ( 3, 3 ),
 ( 0.0001704874539069909148, 0.0003809798300636642191, 0.0004862260181420008441, 0.0005914722062203374691 ),
 ( 0.000000000000000000, 1.000000000000000000 ),
 .UNSPECIFIED. ) 
 GEOMETRIC_REPRESENTATION_ITEM ( )  RATIONAL_B_SPLINE_SURFACE ( (
 ( 1.000000000000000000, 0.7071067811864942820, 1.000000000000000000),
 ( 1.000000000000000000, 0.7670648383576345042, 1.000000000000000000),
 ( 1.000000000000000000, 0.8204820770252110318, 1.000000000000000000),
 ( 1.000000000000000000, 0.8877218296113941198, 1.000000000000000000),
 ( 1.000000000000000000, 0.9080815932663666157, 1.000000000000000000),
 ( 1.000000000000000000, 0.9395541505863373999, 1.000000000000000000),
 ( 1.000000000000000000, 0.9506520335377883768, 1.000000000000000000),
 ( 1.000000000000000000, 0.9504532311154454405, 1.000000000000000000) ) ) 
 REPRESENTATION_ITEM ( '' )  SURFACE ( )  );
#115723=CARTESIAN_POINT ( 'NONE',  ( 18.59999999999999076, 11.65000000001115943, -158.8500000000000227 ) ) ;
#115740=DIRECTION ( 'NONE',  ( 0.000000000000000000, 0.000000000000000000, -1.000000000000000000 ) ) ;
#115793=CARTESIAN_POINT ( 'NONE',  ( 21.14999999999999858, 6.257814610487280937, -133.9022097086912311 ) ) ;
#115813=EDGE_LOOP ( 'NONE', ( #102651, #66570, #226519, #193076 ) ) ;
#115825=EDGE_LOOP ( 'NONE', ( #223095, #54893, #7205, #60973 ) ) ;
#115829=EDGE_LOOP ( 'NONE', ( #227152, #241589, #4811, #8967, #52411 ) ) ;
#115830=CARTESIAN_POINT ( 'NONE',  ( 20.94999999999999574, 8.926614585098251453, -142.4716830192231498 ) ) ;
#115842=CARTESIAN_POINT ( 'NONE',  ( -23.25000000000000000, -1.149570369564537842, -175.3159124845019790 ) ) ;
#115850=CARTESIAN_POINT ( 'NONE',  ( -20.94999999999999929, 11.75000000001115552, -141.0148057706540214 ) ) ;
#115869=EDGE_LOOP ( 'NONE', ( #111201, #200048, #15699 ) ) ;
#115895=AXIS2_PLACEMENT_3D ( 'NONE', #50161, #210540, #249670 ) ;
#115914=CIRCLE ( 'NONE', #132668, 2.100000000000002309 ) ;
#115946=DIRECTION ( 'NONE',  ( 0.000000000000000000, -0.8660254037844411501, -0.4999999999999956146 ) ) ;
#115955=FACE_OUTER_BOUND ( 'NONE', #147019, .T. ) ;
#115992=VERTEX_POINT ( 'NONE', #55891 ) ;
#116000=DIRECTION ( 'NONE',  ( 0.000000000000000000, 0.000000000000000000, -1.000000000000000000 ) ) ;
#116011=ORIENTED_EDGE ( 'NONE', *, *, #210476, .T. ) ;
#116089=DIRECTION ( 'NONE',  ( 1.000000000000000000, -0.000000000000000000, -0.000000000000000000 ) ) ;
#116104=AXIS2_PLACEMENT_3D ( 'NONE', #53987, #193516, #255985 ) ;
#116128=ORIENTED_EDGE ( 'NONE', *, *, #176955, .F. ) ;
#116136=VERTEX_POINT ( 'NONE', #23244 ) ;
#116164=FACE_OUTER_BOUND ( 'NONE', #94875, .T. ) ;
#116207=CARTESIAN_POINT ( 'NONE',  ( 20.94999999999999929, 1.835341550235569663, -145.5551512925629822 ) ) ;
#116221=VERTEX_POINT ( 'NONE', #46600 ) ;
#116224=ORIENTED_EDGE ( 'NONE', *, *, #192144, .T. ) ;
#116258=EDGE_LOOP ( 'NONE', ( #178714, #195249, #123893, #172756 ) ) ;
#116269=CIRCLE ( 'NONE', #16319, 0.09999999999999939493 ) ;
#116282=VERTEX_POINT ( 'NONE', #183576 ) ;
#116283=CARTESIAN_POINT ( 'NONE',  ( 21.13614978966381841, 1.115456470629326115E-11, -127.5008952981661565 ) ) ;
#116292=CIRCLE ( 'NONE', #99675, 6.329289321881370611 ) ;
#116294=CARTESIAN_POINT ( 'NONE',  ( -21.05000000000000071, -1.261786168553869603, -142.0864989635454947 ) ) ;
#116297=CARTESIAN_POINT ( 'NONE',  ( 18.59999999999999076, 11.75000000001115907, -142.1000000000000227 ) ) ;
#116342=ORIENTED_EDGE ( 'NONE', *, *, #19366, .F. ) ;
#116346=ORIENTED_EDGE ( 'NONE', *, *, #142950, .T. ) ;
#116370=ORIENTED_EDGE ( 'NONE', *, *, #74399, .T. ) ;
#116413=VERTEX_POINT ( 'NONE', #193848 ) ;
#116417=EDGE_LOOP ( 'NONE', ( #162367, #156882, #227243, #60756 ) ) ;
#116418=CARTESIAN_POINT ( 'NONE',  ( -18.59999999999999787, -9.321008403350132809, -141.2359382490778899 ) ) ;
#116422=DIRECTION ( 'NONE',  ( 0.000000000000000000, -1.000000000000000000, -0.000000000000000000 ) ) ;
#116498=ORIENTED_EDGE ( 'NONE', *, *, #224582, .T. ) ;
#116505=CIRCLE ( 'NONE', #191547, 4.099999999999992539 ) ;
#116527=ORIENTED_EDGE ( 'NONE', *, *, #226682, .T. ) ;
#116539=VERTEX_POINT ( 'NONE', #196397 ) ;
#116542=CARTESIAN_POINT ( 'NONE',  ( 21.14999999999999858, 6.540656951712400691, -134.1000000000000227 ) ) ;
#116554=CARTESIAN_POINT ( 'NONE',  ( -21.05000000000000071, -1.360870587180885716, -142.0729979270909951 ) ) ;
#116557=ORIENTED_EDGE ( 'NONE', *, *, #115673, .F. ) ;
#116558=DIRECTION ( 'NONE',  ( 1.000000000000000000, 2.952720810173289112E-16, -0.000000000000000000 ) ) ;
#116559=CARTESIAN_POINT ( 'NONE',  ( -20.85000000000000142, -1.835859311432481045, -179.1044391687985353 ) ) ;
#116564=ORIENTED_EDGE ( 'NONE', *, *, #149056, .T. ) ;
#116569=CARTESIAN_POINT ( 'NONE',  ( -22.57320508075687115, 11.65000000001115588, -134.0000000000000568 ) ) ;
#116583=FACE_OUTER_BOUND ( 'NONE', #45033, .T. ) ;
#116644=CARTESIAN_POINT ( 'NONE',  ( -22.39999999999999858, 7.790779598384560245, -133.9000000000000057 ) ) ;
#116679=CARTESIAN_POINT ( 'NONE',  ( 21.14999999999999858, 1.115600667400684642E-11, -146.1500000000000341 ) ) ;
#116694=DIRECTION ( 'NONE',  ( 0.000000000000000000, 0.000000000000000000, -1.000000000000000000 ) ) ;
#116695=FACE_OUTER_BOUND ( 'NONE', #72970, .T. ) ;
#116706=ORIENTED_EDGE ( 'NONE', *, *, #2542, .F. ) ;
#116715=CARTESIAN_POINT ( 'NONE',  ( 20.94999999999999929, 10.72371710471867701, -155.2500000000000284 ) ) ;
#116729=ORIENTED_EDGE ( 'NONE', *, *, #21564, .T. ) ;
#116738=AXIS2_PLACEMENT_3D ( 'NONE', #71344, #210837, #55571 ) ;
#116778=AXIS2_PLACEMENT_3D ( 'NONE', #128784, #136443, #210876 ) ;
#116781=AXIS2_PLACEMENT_3D ( 'NONE', #169761, #71920, #9350 ) ;
#116804=FACE_OUTER_BOUND ( 'NONE', #191231, .T. ) ;
#116819=EDGE_CURVE ( 'NONE', #99517, #201727, #209237, .T. ) ;
#116843=AXIS2_PLACEMENT_3D ( 'NONE', #93049, #237707, #56472 ) ;
#116849=CARTESIAN_POINT ( 'NONE',  ( -22.50000000000000000, 1.115600667400684642E-11, -134.0000000000000000 ) ) ;
#116870=CIRCLE ( 'NONE', #4432, 0.5000000000000013323 ) ;
#116880=CARTESIAN_POINT ( 'NONE',  ( -20.54999999999999716, 7.250000000011155521, -155.1500000000000057 ) ) ;
#116893=ORIENTED_EDGE ( 'NONE', *, *, #78639, .F. ) ;
#116905=EDGE_LOOP ( 'NONE', ( #216601, #189949, #37655, #257944 ) ) ;
#116930=TOROIDAL_SURFACE ( 'NONE', #133675, 0.2000000000000000111, 0.1000000000000000056 ) ;
#116932=CARTESIAN_POINT ( 'NONE',  ( -21.05000000000000071, -1.835341550213255957, -145.6551512925629766 ) ) ;
#116946=CIRCLE ( 'NONE', #58659, 0.09999999999999939493 ) ;
#116955=FACE_OUTER_BOUND ( 'NONE', #162372, .T. ) ;
#116958=CARTESIAN_POINT ( 'NONE',  ( -23.15000000000000213, 1.910280373842930812, -154.8686321448010972 ) ) ;
#116981=ORIENTED_EDGE ( 'NONE', *, *, #118735, .T. ) ;
#116982=CARTESIAN_POINT ( 'NONE',  ( -20.94999999999999929, 1.835341550235569663, -145.5551512925629822 ) ) ;
#116984=ORIENTED_EDGE ( 'NONE', *, *, #87414, .T. ) ;
#116985=FACE_OUTER_BOUND ( 'NONE', #641, .T. ) ;
#116987=CARTESIAN_POINT ( 'NONE',  ( 22.59066674512266104, 11.75000000001115552, -133.9694958763694217 ) ) ;
#117006=DIRECTION ( 'NONE',  ( -1.000000000000000000, -0.000000000000000000, 0.000000000000000000 ) ) ;
#117023=LINE ( 'NONE', #57015, #124590 ) ;
#117031=ORIENTED_EDGE ( 'NONE', *, *, #83486, .T. ) ;
#117043=DIRECTION ( 'NONE',  ( -1.000000000000000000, 0.000000000000000000, 0.000000000000000000 ) ) ;
#117060=CARTESIAN_POINT ( 'NONE',  ( 20.04142135623731136, 11.75000000001116085, -158.7671572875253787 ) ) ;
#117130=ORIENTED_EDGE ( 'NONE', *, *, #191058, .T. ) ;
#117206=DIRECTION ( 'NONE',  ( 0.7070776581708965169, 0.000000000000000000, 0.7071359030027827286 ) ) ;
#117208=TOROIDAL_SURFACE ( 'NONE', #37942, 0.2000000000000000111, 0.1000000000000000056 ) ;
#117219=ORIENTED_EDGE ( 'NONE', *, *, #147826, .F. ) ;
#117220=VECTOR ( 'NONE', #169649, 1000.000000000000000 ) ;
#117248=TOROIDAL_SURFACE ( 'NONE', #146276, 11.90000000000000391, 0.1000000000000000056 ) ;
#117263=EDGE_CURVE ( 'NONE', #8049, #235252, #64362, .T. ) ;
#117303=DIRECTION ( 'NONE',  ( -1.000000000000000000, 0.000000000000000000, 0.000000000000000000 ) ) ;
#117314=EDGE_CURVE ( 'NONE', #246557, #96104, #175940, .T. ) ;
#117321=AXIS2_PLACEMENT_3D ( 'NONE', #126605, #208729, #225672 ) ;
#117354=CARTESIAN_POINT ( 'NONE',  ( 20.94999999999999929, 5.000000000011153745, -155.4947339810869380 ) ) ;
#117376=CARTESIAN_POINT ( 'NONE',  ( -18.59999999999999787, 1.115600667400684642E-11, -175.4000000000000341 ) ) ;
#117390=FACE_OUTER_BOUND ( 'NONE', #12643, .T. ) ;
#117405=EDGE_LOOP ( 'NONE', ( #203056, #136004, #105980, #85295, #215854, #256172 ) ) ;
#117447=CARTESIAN_POINT ( 'NONE',  ( -23.15000000000000213, 5.900000000011162093, -157.2809002353436654 ) ) ;
#117471=VERTEX_POINT ( 'NONE', #66237 ) ;
#117489=ORIENTED_EDGE ( 'NONE', *, *, #167132, .F. ) ;
#117494=CARTESIAN_POINT ( 'NONE',  ( -23.25000000000000000, 1.115649040949250830E-11, -163.6000000000000512 ) ) ;
#117544=EDGE_CURVE ( 'NONE', #245081, #33915, #60246, .T. ) ;
#117563=EDGE_CURVE ( 'NONE', #189870, #39562, #229232, .T. ) ;
#117581=EDGE_CURVE ( 'NONE', #257362, #11797, #245780, .T. ) ;
#117604=VECTOR ( 'NONE', #43678, 1000.000000000000000 ) ;
#117625=CARTESIAN_POINT ( 'NONE',  ( -20.64999999999999858, 1.115600667400684642E-11, -167.5000000000000284 ) ) ;
#117646=VERTEX_POINT ( 'NONE', #255075 ) ;
#117654=CARTESIAN_POINT ( 'NONE',  ( -20.85000000000000142, 1.115600667400684642E-11, -167.5000000000000284 ) ) ;
#117656=DIRECTION ( 'NONE',  ( -0.000000000000000000, 0.000000000000000000, 1.000000000000000000 ) ) ;
#117707=VERTEX_POINT ( 'NONE', #212176 ) ;
#117719=VECTOR ( 'NONE', #226335, 1000.000000000000000 ) ;
#117727=EDGE_CURVE ( 'NONE', #184550, #92142, #195914, .T. ) ;
#117742=EDGE_CURVE ( 'NONE', #157963, #70299, #166712, .T. ) ;
#117745=ORIENTED_EDGE ( 'NONE', *, *, #117727, .F. ) ;
#117764=AXIS2_PLACEMENT_3D ( 'NONE', #75356, #53192, #229277 ) ;
#117818=ORIENTED_EDGE ( 'NONE', *, *, #125154, .F. ) ;
#117824=ORIENTED_EDGE ( 'NONE', *, *, #213954, .T. ) ;
#117854=VECTOR ( 'NONE', #69011, 1000.000000000000000 ) ;
#117872=CARTESIAN_POINT ( 'NONE',  ( -20.94999999999999929, 11.75000000001115197, -141.0148057706540214 ) ) ;
#117899=ORIENTED_EDGE ( 'NONE', *, *, #63089, .F. ) ;
#117906=SURFACE_STYLE_USAGE ( .BOTH. , #234008 ) ;
#117914=EDGE_CURVE ( 'NONE', #148927, #41773, #232949, .T. ) ;
#117915=DIRECTION ( 'NONE',  ( 0.000000000000000000, 0.000000000000000000, -1.000000000000000000 ) ) ;
#117920=DIRECTION ( 'NONE',  ( 0.000000000000000000, 0.000000000000000000, -1.000000000000000000 ) ) ;
#117923=DIRECTION ( 'NONE',  ( 1.000000000000000000, 0.000000000000000000, 0.000000000000000000 ) ) ;
#117929=AXIS2_PLACEMENT_3D ( 'NONE', #41669, #122483, #2503 ) ;
#117932=ORIENTED_EDGE ( 'NONE', *, *, #155045, .F. ) ;
#117960=CARTESIAN_POINT ( 'NONE',  ( -20.85000000000000142, 1.115600667400684642E-11, -167.5000000000000284 ) ) ;
#117970=DIRECTION ( 'NONE',  ( -3.469446951953677298E-14, -0.9908441862701782288, -0.1350103645450542456 ) ) ;
#117971=CARTESIAN_POINT ( 'NONE',  ( 21.05000000000000071, 8.876614585098254295, -142.3850804788447135 ) ) ;
#117991=VECTOR ( 'NONE', #161414, 1000.000000000000000 ) ;
#117996=FACE_OUTER_BOUND ( 'NONE', #65182, .T. ) ;
#118023=CARTESIAN_POINT ( 'NONE',  ( 18.59999999999999787, -10.35479209691423996, -161.2565409830737906 ) ) ;
#118048=FACE_OUTER_BOUND ( 'NONE', #201412, .T. ) ;
#118069=DIRECTION ( 'NONE',  ( 1.000000000000000000, -0.000000000000000000, -0.000000000000000000 ) ) ;
#118072=DIRECTION ( 'NONE',  ( 0.000000000000000000, 0.000000000000000000, -1.000000000000000000 ) ) ;
#118107=AXIS2_PLACEMENT_3D ( 'NONE', #76662, #72857, #217441 ) ;
#118113=ORIENTED_EDGE ( 'NONE', *, *, #256337, .F. ) ;
#118115=CARTESIAN_POINT ( 'NONE',  ( 20.94999999999999929, -8.999999999988842703, -157.6060308773475640 ) ) ;
#118134=CARTESIAN_POINT ( 'NONE',  ( -23.25000000000000000, 4.250000000011156409, -146.1500000000000341 ) ) ;
#118187=ORIENTED_EDGE ( 'NONE', *, *, #129444, .T. ) ;
#118214=CARTESIAN_POINT ( 'NONE',  ( 22.14074124539698829, 7.390077851054901892, -133.9009471041559607 ) ) ;
#118221=ORIENTED_EDGE ( 'NONE', *, *, #134470, .T. ) ;
#118229=DIRECTION ( 'NONE',  ( 0.000000000000000000, -0.000000000000000000, 1.000000000000000000 ) ) ;
#118232=VERTEX_POINT ( 'NONE', #174693 ) ;
#118240=ADVANCED_FACE ( 'NONE', ( #232064 ), #128702, .F. ) ;
#118250=CARTESIAN_POINT ( 'NONE',  ( -18.43599941264915998, -9.519327428583796546, -140.9729767895211126 ) ) ;
#118258=VECTOR ( 'NONE', #223984, 1000.000000000000227 ) ;
#118262=ADVANCED_FACE ( 'NONE', ( #213766 ), #24672, .T. ) ;
#118270=ORIENTED_EDGE ( 'NONE', *, *, #237370, .F. ) ;
#118273=PLANE ( 'NONE',  #78095 ) ;
#118276=DIRECTION ( 'NONE',  ( -1.000000000000000000, 3.469446951953635015E-14, 0.000000000000000000 ) ) ;
#118319=DIRECTION ( 'NONE',  ( 1.000000000000000000, 6.938893903907222067E-15, 0.000000000000000000 ) ) ;
#118322=DIRECTION ( 'NONE',  ( 1.000000000000000000, 0.000000000000000000, 0.000000000000000000 ) ) ;
#118404=ORIENTED_EDGE ( 'NONE', *, *, #233841, .F. ) ;
#118422=CARTESIAN_POINT ( 'NONE',  ( 21.14999999999999858, 6.650000000011155876, -146.1500000000000341 ) ) ;
#118440=DIRECTION ( 'NONE',  ( 0.000000000000000000, 1.000000000000000000, 0.000000000000000000 ) ) ;
#118495=CARTESIAN_POINT ( 'NONE',  ( 21.05000000000000071, 5.000000000011153745, -155.5947339810869323 ) ) ;
#118509=VERTEX_POINT ( 'NONE', #179167 ) ;
#118523=EDGE_LOOP ( 'NONE', ( #124925, #200425, #205915, #151547, #160335 ) ) ;
#118526=DIRECTION ( 'NONE',  ( 4.377807931758638789E-15, 0.2605042016806672911, 0.9654727137038716656 ) ) ;
#118531=CIRCLE ( 'NONE', #10379, 0.09999999999998898659 ) ;
#118558=CARTESIAN_POINT ( 'NONE',  ( -21.05000000000000071, -11.64999999998884483, -137.0000000000000000 ) ) ;
#118563=DIRECTION ( 'NONE',  ( 0.000000000000000000, 2.891205793294679805E-16, -1.000000000000000000 ) ) ;
#118569=DIRECTION ( 'NONE',  ( 1.000000000000000000, 0.000000000000000000, 0.000000000000000000 ) ) ;
#118612=ORIENTED_EDGE ( 'NONE', *, *, #246019, .T. ) ;
#118644=CIRCLE ( 'NONE', #247608, 0.1000000000000001027 ) ;
#118731=CARTESIAN_POINT ( 'NONE',  ( 20.88420186297724257, 10.33025634372637391, -173.0870929282638997 ) ) ;
#118735=EDGE_CURVE ( 'NONE', #253862, #116539, #83233, .T. ) ;
#118774=DIRECTION ( 'NONE',  ( 0.000000000000000000, 0.000000000000000000, -1.000000000000000000 ) ) ;
#118791=ORIENTED_EDGE ( 'NONE', *, *, #179458, .F. ) ;
#118801=AXIS2_PLACEMENT_3D ( 'NONE', #189867, #172918, #252385 ) ;
#118814=AXIS2_PLACEMENT_3D ( 'NONE', #18737, #115271, #37047 ) ;
#118841=ORIENTED_EDGE ( 'NONE', *, *, #202095, .T. ) ;
#118843=CYLINDRICAL_SURFACE ( 'NONE', #173717, 0.1000000000000000472 ) ;
#118855=FACE_OUTER_BOUND ( 'NONE', #52181, .T. ) ;
#118857=CARTESIAN_POINT ( 'NONE',  ( -18.59999999999999787, -9.480686695267820596, -174.4411151687578752 ) ) ;
#118869=ORIENTED_EDGE ( 'NONE', *, *, #249633, .T. ) ;
#118920=CARTESIAN_POINT ( 'NONE',  ( -20.85000000000000142, 7.120270961708750512, -171.1595630418393625 ) ) ;
#118929=CIRCLE ( 'NONE', #127290, 11.80000000000000426 ) ;
#118930=CARTESIAN_POINT ( 'NONE',  ( -18.59999999999999787, -1.164121893230052995, -175.4148480855716059 ) ) ;
#118961=AXIS2_PLACEMENT_3D ( 'NONE', #90801, #248606, #85641 ) ;
#118971=DIRECTION ( 'NONE',  ( 0.000000000000000000, 0.000000000000000000, -1.000000000000000000 ) ) ;
#118978=CARTESIAN_POINT ( 'NONE',  ( -18.59999999999999787, 11.65000000001115232, -155.2500000000000284 ) ) ;
#118982=ORIENTED_EDGE ( 'NONE', *, *, #130062, .F. ) ;
#118997=AXIS2_PLACEMENT_3D ( 'NONE', #143808, #203789, #6872 ) ;
#119024=EDGE_LOOP ( 'NONE', ( #72560, #173351, #219332, #71819 ) ) ;
#119030=ORIENTED_EDGE ( 'NONE', *, *, #155424, .T. ) ;
#119062=TOROIDAL_SURFACE ( 'NONE', #164845, 6.258578643762712446, 0.1000000000000000056 ) ;
#119091=ORIENTED_EDGE ( 'NONE', *, *, #79657, .F. ) ;
#119132=DIRECTION ( 'NONE',  ( 0.000000000000000000, 0.000000000000000000, -1.000000000000000000 ) ) ;
#119168=VERTEX_POINT ( 'NONE', #167019 ) ;
#119203=EDGE_CURVE ( 'NONE', #64247, #113685, #228250, .T. ) ;
#119220=ADVANCED_FACE ( 'NONE', ( #10484 ), #158486, .F. ) ;
#119264=DIRECTION ( 'NONE',  ( 0.000000000000000000, 0.000000000000000000, 1.000000000000000000 ) ) ;
#119301=CARTESIAN_POINT ( 'NONE',  ( 18.59999999999997655, 1.115600667400684642E-11, -167.5000000000000284 ) ) ;
#119338=AXIS2_PLACEMENT_3D ( 'NONE', #235264, #237843, #80015 ) ;
#119342=DIRECTION ( 'NONE',  ( 0.000000000000000000, -0.9908441862701411473, 0.1350103645453267498 ) ) ;
#119388=ORIENTED_EDGE ( 'NONE', *, *, #9151, .F. ) ;
#119395=ORIENTED_EDGE ( 'NONE', *, *, #119416, .T. ) ;
#119405=EDGE_CURVE ( 'NONE', #82203, #11722, #44174, .T. ) ;
#119411=CIRCLE ( 'NONE', #186043, 0.09999999999999939493 ) ;
#119412=DIRECTION ( 'NONE',  ( 0.000000000000000000, 0.000000000000000000, -1.000000000000000000 ) ) ;
#119416=EDGE_CURVE ( 'NONE', #217031, #163189, #196066, .T. ) ;
#119423=ORIENTED_EDGE ( 'NONE', *, *, #92937, .T. ) ;
#119440=ORIENTED_EDGE ( 'NONE', *, *, #121490, .T. ) ;
#119450=EDGE_CURVE ( 'NONE', #137714, #52387, #75470, .T. ) ;
#119465=AXIS2_PLACEMENT_3D ( 'NONE', #42596, #60865, #161278 ) ;
#119493=EDGE_LOOP ( 'NONE', ( #196375, #173370, #189717, #9590 ) ) ;
#119540=CARTESIAN_POINT ( 'NONE',  ( 20.12500000000000355, 9.258049272928479567, -142.3633388371424644 ) ) ;
#119550=ORIENTED_EDGE ( 'NONE', *, *, #22225, .T. ) ;
#119552=DIRECTION ( 'NONE',  ( -1.000000000000000000, -8.673617379884087537E-15, 0.000000000000000000 ) ) ;
#119556=CARTESIAN_POINT ( 'NONE',  ( -18.59999999999999787, 1.637172712981537659, -145.5821533654720383 ) ) ;
#119570=ORIENTED_EDGE ( 'NONE', *, *, #225399, .F. ) ;
#119571=DIRECTION ( 'NONE',  ( 0.000000000000000000, 2.891205793294679805E-16, -1.000000000000000000 ) ) ;
#119589=CARTESIAN_POINT ( 'NONE',  ( -23.25000000000000000, -8.999999999988846255, -143.8939691226524644 ) ) ;
#119596=ADVANCED_FACE ( 'NONE', ( #27200 ), #190095, .F. ) ;
#119607=CARTESIAN_POINT ( 'NONE',  ( -21.05000000000000071, 1.115600667400684642E-11, -163.5000000000000284 ) ) ;
#119629=DIRECTION ( 'NONE',  ( 1.000000000000000000, 0.000000000000000000, 0.000000000000000000 ) ) ;
#119650=DIRECTION ( 'NONE',  ( 0.000000000000000000, 0.000000000000000000, 1.000000000000000000 ) ) ;
#119703=CARTESIAN_POINT ( 'NONE',  ( 21.05000000000000071, -11.74999999998883560, -164.6000000000000227 ) ) ;
#119707=DIRECTION ( 'NONE',  ( 0.000000000000000000, -1.000000000000000000, 0.000000000000000000 ) ) ;
#119738=ADVANCED_FACE ( 'NONE', ( #173145 ), #108754, .T. ) ;
#119740=EDGE_LOOP ( 'NONE', ( #130887, #159898, #161138, #11267 ) ) ;
#119749=DIRECTION ( 'NONE',  ( 0.000000000000000000, 0.9908441862701782288, -0.1350103645450542456 ) ) ;
#119753=CIRCLE ( 'NONE', #178204, 0.09999999999998898659 ) ;
#119797=ORIENTED_EDGE ( 'NONE', *, *, #104125, .T. ) ;
#119818=ORIENTED_EDGE ( 'NONE', *, *, #199284, .T. ) ;
#119853=EDGE_LOOP ( 'NONE', ( #19910, #228188, #190370, #38361 ) ) ;
#119877=EDGE_CURVE ( 'NONE', #18582, #34631, #40033, .T. ) ;
#119878=CIRCLE ( 'NONE', #228576, 0.1000000000000000472 ) ;
#119894=DIRECTION ( 'NONE',  ( 1.000000000000000000, -7.304098846218134667E-16, 0.000000000000000000 ) ) ;
#119895=ADVANCED_FACE ( 'NONE', ( #2138 ), #179530, .T. ) ;
#119922=DIRECTION ( 'NONE',  ( 1.000000000000000000, 0.000000000000000000, 0.000000000000000000 ) ) ;
#119928=CIRCLE ( 'NONE', #48961, 0.09999999999999939493 ) ;
#119945=TOROIDAL_SURFACE ( 'NONE', #86552, 0.4000000000000012990, 0.1000000000000000056 ) ;
#119968=CIRCLE ( 'NONE', #194958, 0.09999999999999939493 ) ;
#120012=EDGE_CURVE ( 'NONE', #40935, #4681, #114905, .T. ) ;
#120013=DIRECTION ( 'NONE',  ( 0.000000000000000000, -0.4999999999999348299, 0.8660254037844762331 ) ) ;
#120018=EDGE_CURVE ( 'NONE', #52387, #140944, #178914, .T. ) ;
#120030=CARTESIAN_POINT ( 'NONE',  ( 20.91682497891422798, 10.32263460347359363, -173.0605957968672328 ) ) ;
#120041=FACE_OUTER_BOUND ( 'NONE', #134880, .T. ) ;
#120067=DIRECTION ( 'NONE',  ( 0.000000000000000000, -1.000000000000000000, 0.000000000000000000 ) ) ;
#120083=EDGE_CURVE ( 'NONE', #186823, #169023, #146339, .T. ) ;
#120109=CIRCLE ( 'NONE', #7656, 0.09999999999999892308 ) ;
#120136=VERTEX_POINT ( 'NONE', #41957 ) ;
#120157=CARTESIAN_POINT ( 'NONE',  ( -22.39999999999999858, 7.790779598384560245, -134.0000000000000000 ) ) ;
#120178=ORIENTED_EDGE ( 'NONE', *, *, #106889, .F. ) ;
#120208=DIRECTION ( 'NONE',  ( 0.000000000000000000, -1.000000000000000000, 0.000000000000000000 ) ) ;
#120242=EDGE_CURVE ( 'NONE', #155996, #229458, #67237, .T. ) ;
#120248=DIRECTION ( 'NONE',  ( 0.000000000000000000, 0.000000000000000000, -1.000000000000000000 ) ) ;
#120281=DIRECTION ( 'NONE',  ( 0.000000000000000000, 1.000000000000000000, 0.000000000000000000 ) ) ;
#120342=VERTEX_POINT ( 'NONE', #251687 ) ;
#120346=DIRECTION ( 'NONE',  ( 1.000000000000000000, 0.000000000000000000, 0.000000000000000000 ) ) ;
#120361=FACE_OUTER_BOUND ( 'NONE', #122300, .T. ) ;
#120375=ADVANCED_FACE ( 'NONE', ( #178604 ), #56026, .T. ) ;
#120395=DIRECTION ( 'NONE',  ( 0.000000000000000000, 0.000000000000000000, -1.000000000000000000 ) ) ;
#120410=AXIS2_PLACEMENT_3D ( 'NONE', #27004, #28295, #123511 ) ;
#120425=DIRECTION ( 'NONE',  ( 1.000000000000000000, 0.000000000000000000, 0.000000000000000000 ) ) ;
#120457=AXIS2_PLACEMENT_3D ( 'NONE', #138419, #75911, #133319 ) ;
#120490=ORIENTED_EDGE ( 'NONE', *, *, #141257, .F. ) ;
#120511=ORIENTED_EDGE ( 'NONE', *, *, #98770, .T. ) ;
#120546=DIRECTION ( 'NONE',  ( 1.000000000000000000, 0.000000000000000000, -0.000000000000000000 ) ) ;
#120574=ORIENTED_EDGE ( 'NONE', *, *, #36357, .F. ) ;
#120579=AXIS2_PLACEMENT_3D ( 'NONE', #153386, #109067, #33435 ) ;
#120600=CARTESIAN_POINT ( 'NONE',  ( 21.05000000000000071, 1.115600667400684642E-11, -167.5000000000000284 ) ) ;
#120612=EDGE_CURVE ( 'NONE', #101165, #89005, #184124, .T. ) ;
#120633=CIRCLE ( 'NONE', #145539, 0.09999999999999749367 ) ;
#120658=DIRECTION ( 'NONE',  ( 0.000000000000000000, -1.000000000000000000, -0.000000000000000000 ) ) ;
#120665=AXIS2_PLACEMENT_3D ( 'NONE', #123991, #88673, #44456 ) ;
#120728=EDGE_LOOP ( 'NONE', ( #90635, #193520, #178260, #232854 ) ) ;
#120734=EDGE_LOOP ( 'NONE', ( #238119, #161297, #65225, #77366 ) ) ;
#120735=EDGE_CURVE ( 'NONE', #178254, #50042, #138315, .T. ) ;
#120745=ORIENTED_EDGE ( 'NONE', *, *, #112051, .T. ) ;
#120790=CARTESIAN_POINT ( 'NONE',  ( 20.95556889135987788, 10.62194358774625336, -141.6423942218575291 ) ) ;
#120809=CIRCLE ( 'NONE', #249960, 12.87499999999999822 ) ;
#120814=ORIENTED_EDGE ( 'NONE', *, *, #151538, .F. ) ;
#120831=VECTOR ( 'NONE', #187872, 1000.000000000000000 ) ;
#120835=ADVANCED_FACE ( 'NONE', ( #236955 ), #75995, .F. ) ;
#120842=DIRECTION ( 'NONE',  ( 0.000000000000000000, -1.000000000000000000, 0.000000000000000000 ) ) ;
#120893=CARTESIAN_POINT ( 'NONE',  ( 21.07094088545304089, 6.320167221927651013, -133.9011062974477966 ) ) ;
#120906=FACE_OUTER_BOUND ( 'NONE', #34699, .T. ) ;
#120912=CARTESIAN_POINT ( 'NONE',  ( -21.05000000000000071, 11.65000000001115232, -140.7838656629781724 ) ) ;
#120929=VECTOR ( 'NONE', #236255, 1000.000000000000000 ) ;
#120931=TOROIDAL_SURFACE ( 'NONE', #179193, 12.77499999999999858, 0.1000000000000000056 ) ;
#120932=CARTESIAN_POINT ( 'NONE',  ( 23.25000000000000000, -11.74999999998883560, -122.2500000000000284 ) ) ;
#120941=EDGE_CURVE ( 'NONE', #73222, #195640, #30210, .T. ) ;
#120953=( BOUNDED_SURFACE ( )  B_SPLINE_SURFACE ( 3, 2, ( 
 ( #13158, #92679, #251757 ),
 ( #210079, #133103, #233503 ),
 ( #31464, #54824, #213912 ),
 ( #110965, #35321, #114816 ) ),
 .UNSPECIFIED., .F., .F., .F. ) 
 B_SPLINE_SURFACE_WITH_KNOTS ( ( 4, 4 ),
 ( 3, 3 ),
 ( 0.0002700421466196751283, 0.0004789321604330810467 ),
 ( 0.000000000000000000, 1.000000000000000000 ),
 .UNSPECIFIED. ) 
 GEOMETRIC_REPRESENTATION_ITEM ( )  RATIONAL_B_SPLINE_SURFACE ( (
 ( 1.000000000000000000, 0.7071067811865475727, 1.000000000000000000),
 ( 1.000000000000000000, 0.7163411249511765222, 1.000000000000000000),
 ( 1.000000000000000000, 0.7221957104841898456, 1.000000000000000000),
 ( 1.000000000000000000, 0.7250110520819876836, 1.000000000000000000) ) ) 
 REPRESENTATION_ITEM ( '' )  SURFACE ( )  );
#120967=VERTEX_POINT ( 'NONE', #124716 ) ;
#120993=CIRCLE ( 'NONE', #91750, 4.000000000000003553 ) ;
#121002=CARTESIAN_POINT ( 'NONE',  ( -21.05000000000000071, 1.115600667400684642E-11, -138.2999999999999829 ) ) ;
#121008=CARTESIAN_POINT ( 'NONE',  ( 22.43288208788031568, 0.004899854896538679595, -122.3503481562809441 ) ) ;
#121012=VERTEX_POINT ( 'NONE', #106402 ) ;
#121033=CIRCLE ( 'NONE', #179292, 0.09999999999998898659 ) ;
#121037=DIRECTION ( 'NONE',  ( -4.336808689942053235E-15, -0.8660254037844482555, -0.4999999999999836797 ) ) ;
#121039=ORIENTED_EDGE ( 'NONE', *, *, #129744, .T. ) ;
#121052=EDGE_LOOP ( 'NONE', ( #27699, #96079, #55895, #157842 ) ) ;
#121054=CARTESIAN_POINT ( 'NONE',  ( 20.94999999999999929, -1.835341550213257733, -145.5551512925629822 ) ) ;
#121079=VECTOR ( 'NONE', #180774, 1000.000000000000000 ) ;
#121083=AXIS2_PLACEMENT_3D ( 'NONE', #150878, #15240, #92183 ) ;
#121120=ADVANCED_FACE ( 'NONE', ( #133692 ), #234070, .F. ) ;
#121150=DIRECTION ( 'NONE',  ( 0.7071067811865475727, 0.7071067811865475727, 2.044391222244500083E-16 ) ) ;
#121195=AXIS2_PLACEMENT_3D ( 'NONE', #196854, #213865, #93910 ) ;
#121231=EDGE_CURVE ( 'NONE', #146973, #238921, #255175, .T. ) ;
#121239=ORIENTED_EDGE ( 'NONE', *, *, #251543, .F. ) ;
#121249=CARTESIAN_POINT ( 'NONE',  ( 20.94999999999999929, -1.349153571964892606, -175.2874973355899044 ) ) ;
#121251=DIRECTION ( 'NONE',  ( 1.000000000000000000, 0.000000000000000000, 0.000000000000000000 ) ) ;
#121266=CYLINDRICAL_SURFACE ( 'NONE', #31161, 7.899999999999990585 ) ;
#121271=EDGE_CURVE ( 'NONE', #223519, #6309, #219639, .T. ) ;
#121273=ORIENTED_EDGE ( 'NONE', *, *, #102097, .F. ) ;
#121277=AXIS2_PLACEMENT_3D ( 'NONE', #37451, #214777, #174428 ) ;
#121278=VECTOR ( 'NONE', #185860, 1000.000000000000000 ) ;
#121287=DIRECTION ( 'NONE',  ( -1.000000000000000000, 0.000000000000000000, 0.000000000000000000 ) ) ;
#121312=CARTESIAN_POINT ( 'NONE',  ( -20.85000000000000142, 1.115600667400684642E-11, -167.5000000000000284 ) ) ;
#121313=AXIS2_PLACEMENT_3D ( 'NONE', #83602, #178929, #60213 ) ;
#121329=CARTESIAN_POINT ( 'NONE',  ( 23.15000000000000213, -8.999999999988844479, -143.8939691226524644 ) ) ;
#121339=ORIENTED_EDGE ( 'NONE', *, *, #247152, .T. ) ;
#121357=AXIS2_PLACEMENT_3D ( 'NONE', #187379, #243480, #105208 ) ;
#121360=CARTESIAN_POINT ( 'NONE',  ( 23.14999999999999858, 1.115600667400684642E-11, -167.5000000000000284 ) ) ;
#121363=FACE_OUTER_BOUND ( 'NONE', #231050, .T. ) ;
#121381=FACE_OUTER_BOUND ( 'NONE', #140584, .T. ) ;
#121428=FACE_OUTER_BOUND ( 'NONE', #237981, .T. ) ;
#121434=DIRECTION ( 'NONE',  ( -0.000000000000000000, -0.000000000000000000, 1.000000000000000000 ) ) ;
#121441=LINE ( 'NONE', #221759, #70510 ) ;
#121443=CARTESIAN_POINT ( 'NONE',  ( 18.59999999999999076, 6.650000000011155876, -155.3500000000000227 ) ) ;
#121470=ORIENTED_EDGE ( 'NONE', *, *, #117914, .F. ) ;
#121475=DIRECTION ( 'NONE',  ( 1.000000000000000000, 0.000000000000000000, 0.000000000000000000 ) ) ;
#121490=EDGE_CURVE ( 'NONE', #83182, #160572, #205319, .T. ) ;
#121507=ADVANCED_FACE ( 'NONE', ( #170003 ), #233794, .F. ) ;
#121524=AXIS2_PLACEMENT_3D ( 'NONE', #87493, #187908, #143627 ) ;
#121533=CARTESIAN_POINT ( 'NONE',  ( -20.64999999999999858, 2.400000000011155432, -154.2753780772379173 ) ) ;
#121609=EDGE_CURVE ( 'NONE', #111978, #237934, #67979, .T. ) ;
#121616=VERTEX_POINT ( 'NONE', #21184 ) ;
#121658=PLANE ( 'NONE',  #230575 ) ;
#121685=AXIS2_PLACEMENT_3D ( 'NONE', #1075, #117206, #18096 ) ;
#121718=AXIS2_PLACEMENT_3D ( 'NONE', #243315, #85494, #217641 ) ;
#121719=ORIENTED_EDGE ( 'NONE', *, *, #132347, .F. ) ;
#121776=DIRECTION ( 'NONE',  ( 4.026293107431335996E-15, -0.8700118002898359348, 0.4930308989875165082 ) ) ;
#121786=CARTESIAN_POINT ( 'NONE',  ( -23.15000000000000213, 1.115600667400684642E-11, -167.5000000000000284 ) ) ;
#121824=CARTESIAN_POINT ( 'NONE',  ( -22.50047199487803695, 0.04490605193026415975, -122.2499525810811321 ) ) ;
#121827=B_SPLINE_CURVE_WITH_KNOTS ( 'NONE', 3,
 ( #154592, #94573, #252356, #170321, #11203, #230241, #249814, #35918, #76290, #235367 ),
 .UNSPECIFIED., .F., .F.,
 ( 4, 3, 3, 4 ),
 ( 0.000000000000000000, 0.0002000000000008585893, 0.001000000000082977483, 0.001967863649483336721 ),
 .UNSPECIFIED. ) ;
#121855=AXIS2_PLACEMENT_3D ( 'NONE', #146083, #169560, #5268 ) ;
#121875=AXIS2_PLACEMENT_3D ( 'NONE', #36222, #209706, #11519 ) ;
#121908=CARTESIAN_POINT ( 'NONE',  ( 23.25000000000000000, -11.64999999998883595, -164.4000000000000057 ) ) ;
#121927=ORIENTED_EDGE ( 'NONE', *, *, #66715, .T. ) ;
#121949=ORIENTED_EDGE ( 'NONE', *, *, #129135, .T. ) ;
#121951=VERTEX_POINT ( 'NONE', #69643 ) ;
#122039=FACE_OUTER_BOUND ( 'NONE', #76667, .T. ) ;
#122049=CARTESIAN_POINT ( 'NONE',  ( 19.90621891164687440, 11.75000000001116263, -158.8284452778770230 ) ) ;
#122050=CARTESIAN_POINT ( 'NONE',  ( 20.95545211741311320, 10.58641331155510379, -141.5861468595883252 ) ) ;
#122054=EDGE_CURVE ( 'NONE', #207209, #40580, #218101, .T. ) ;
#122055=DIRECTION ( 'NONE',  ( 0.000000000000000000, 0.000000000000000000, -1.000000000000000000 ) ) ;
#122117=ORIENTED_EDGE ( 'NONE', *, *, #56858, .T. ) ;
#122118=ORIENTED_EDGE ( 'NONE', *, *, #113758, .T. ) ;
#122141=LINE ( 'NONE', #180833, #69592 ) ;
#122147=ORIENTED_EDGE ( 'NONE', *, *, #94659, .F. ) ;
#122160=VECTOR ( 'NONE', #195447, 999.9999999999998863 ) ;
#122180=EDGE_CURVE ( 'NONE', #238921, #217031, #130878, .T. ) ;
#122202=EDGE_CURVE ( 'NONE', #140944, #192232, #126604, .T. ) ;
#122214=VECTOR ( 'NONE', #168862, 1000.000000000000000 ) ;
#122224=AXIS2_PLACEMENT_3D ( 'NONE', #254704, #93103, #111397 ) ;
#122234=CARTESIAN_POINT ( 'NONE',  ( 21.10642757222115051, 10.72315628916975250, -146.2406975237852294 ) ) ;
#122240=CARTESIAN_POINT ( 'NONE',  ( -20.94999999999999929, 1.115600667400684642E-11, -167.5000000000000284 ) ) ;
#122245=ADVANCED_FACE ( 'NONE', ( #30208 ), #76704, .T. ) ;
#122259=CARTESIAN_POINT ( 'NONE',  ( 21.13461538461538325, 10.61458296203669249, -146.3500000000000227 ) ) ;
#122297=DIRECTION ( 'NONE',  ( -0.000000000000000000, 1.000000000000000000, 0.000000000000000000 ) ) ;
#122300=EDGE_LOOP ( 'NONE', ( #230756, #41485, #89087, #63880 ) ) ;
#122303=CARTESIAN_POINT ( 'NONE',  ( 18.59999999999999432, 1.736257131608553550, -145.5686523290175387 ) ) ;
#122314=EDGE_CURVE ( 'NONE', #17731, #176425, #60138, .T. ) ;
#122326=CARTESIAN_POINT ( 'NONE',  ( -23.25000000000000000, -1.835859311432481045, -179.0044391687985410 ) ) ;
#122339=DIRECTION ( 'NONE',  ( 0.000000000000000000, 0.000000000000000000, -1.000000000000000000 ) ) ;
#122349=ADVANCED_FACE ( 'NONE', ( #116164 ), #154043, .T. ) ;
#122375=CARTESIAN_POINT ( 'NONE',  ( 18.39999999999999858, -9.399999999988843058, -122.2500000000000284 ) ) ;
#122376=ORIENTED_EDGE ( 'NONE', *, *, #18429, .T. ) ;
#122389=CARTESIAN_POINT ( 'NONE',  ( 20.94999999999999574, -11.74999999998883560, -137.1000000000000227 ) ) ;
#122395=VECTOR ( 'NONE', #204283, 1000.000000000000000 ) ;
#122401=ORIENTED_EDGE ( 'NONE', *, *, #44759, .F. ) ;
#122404=AXIS2_PLACEMENT_3D ( 'NONE', #8081, #87582, #221946 ) ;
#122415=ORIENTED_EDGE ( 'NONE', *, *, #167361, .T. ) ;
#122445=CARTESIAN_POINT ( 'NONE',  ( -22.59066674512252249, 11.75000000001115552, -133.9694958763695070 ) ) ;
#122451=EDGE_CURVE ( 'NONE', #173825, #18380, #176145, .T. ) ;
#122460=DIRECTION ( 'NONE',  ( 0.000000000000000000, 0.000000000000000000, -1.000000000000000000 ) ) ;
#122466=CIRCLE ( 'NONE', #226477, 0.2000000000000057288 ) ;
#122473=ORIENTED_EDGE ( 'NONE', *, *, #210214, .F. ) ;
#122479=( BOUNDED_SURFACE ( )  B_SPLINE_SURFACE ( 3, 2, ( 
 ( #165023, #221128, #84141 ),
 ( #125882, #22976, #102442 ),
 ( #241987, #64633, #122049 ),
 ( #124618, #104998, #245847 ),
 ( #65926, #63336, #224970 ),
 ( #21671, #205415, #26827 ) ),
 .UNSPECIFIED., .F., .F., .F. ) 
 B_SPLINE_SURFACE_WITH_KNOTS ( ( 4, 2, 4 ),
 ( 3, 3 ),
 ( 4.712388980384689674, 5.497787143782137953, 6.283185307179586232 ),
 ( 0.000000000000000000, 1.000000000000000000 ),
 .UNSPECIFIED. ) 
 GEOMETRIC_REPRESENTATION_ITEM ( )  RATIONAL_B_SPLINE_SURFACE ( (
 ( 1.000000000000000000, 0.7071067811865536790, 1.000000000000000000),
 ( 1.000000000000000000, 0.7727932973495903468, 1.000000000000000000),
 ( 1.000000000000000000, 0.8282379607643433062, 1.000000000000000000),
 ( 1.000000000000000000, 0.9038128468045532049, 1.000000000000000000),
 ( 1.000000000000000000, 0.9240297172239071433, 1.000000000000000000),
 ( 1.000000000000000000, 0.9238795325112914014, 1.000000000000000000) ) ) 
 REPRESENTATION_ITEM ( '' )  SURFACE ( )  );
#122483=DIRECTION ( 'NONE',  ( 1.000000000000000000, -0.000000000000000000, -0.000000000000000000 ) ) ;
#122488=CARTESIAN_POINT ( 'NONE',  ( 23.15000000000000213, -11.74999999998883737, -155.3500000000000227 ) ) ;
#122511=CIRCLE ( 'NONE', #126768, 0.09999999999998898659 ) ;
#122546=VECTOR ( 'NONE', #256199, 1000.000000000000000 ) ;
#122563=CARTESIAN_POINT ( 'NONE',  ( 21.14999999999999503, 1.115488181425289271E-11, -127.4593430482987912 ) ) ;
#122610=CARTESIAN_POINT ( 'NONE',  ( -18.59999999999999787, -1.835341550213255957, -145.5551512925629822 ) ) ;
#122614=FACE_OUTER_BOUND ( 'NONE', #60414, .T. ) ;
#122637=ADVANCED_FACE ( 'NONE', ( #250216 ), #63868, .F. ) ;
#122649=ORIENTED_EDGE ( 'NONE', *, *, #170777, .T. ) ;
#122693=DIRECTION ( 'NONE',  ( -1.000000000000000000, -0.000000000000000000, -0.000000000000000000 ) ) ;
#122710=DIRECTION ( 'NONE',  ( 0.000000000000000000, -1.000000000000000000, 0.000000000000000000 ) ) ;
#122717=DIRECTION ( 'NONE',  ( 0.000000000000000000, -1.000000000000000000, 0.000000000000000000 ) ) ;
#122720=DIRECTION ( 'NONE',  ( -1.000000000000000000, 0.000000000000000000, 0.000000000000000000 ) ) ;
#122723=DIRECTION ( 'NONE',  ( 0.000000000000000000, -0.1350103645451904977, 0.9908441862701596881 ) ) ;
#122736=DIRECTION ( 'NONE',  ( -1.000000000000000000, -2.952720810173289112E-16, 0.000000000000000000 ) ) ;
#122759=CARTESIAN_POINT ( 'NONE',  ( -20.64999999999999858, -8.999999999988844479, -157.6060308773475924 ) ) ;
#122803=CARTESIAN_POINT ( 'NONE',  ( -22.50000000000000000, 1.115600667400684642E-11, -134.0000000000000000 ) ) ;
#122812=CARTESIAN_POINT ( 'NONE',  ( 21.05000000000000071, 10.56271494673980271, -141.4568021056454654 ) ) ;
#122831=CARTESIAN_POINT ( 'NONE',  ( 20.94999999999999929, 1.115600667400684642E-11, -167.5000000000000284 ) ) ;
#122841=FACE_OUTER_BOUND ( 'NONE', #159805, .T. ) ;
#122886=CARTESIAN_POINT ( 'NONE',  ( -21.45000000000000284, 7.708578643773852157, -155.2500000000000284 ) ) ;
#122900=EDGE_LOOP ( 'NONE', ( #189118, #193198, #227379, #254982 ) ) ;
#122903=CARTESIAN_POINT ( 'NONE',  ( -23.15000000000000213, -8.999999999988844479, -157.6060308773475924 ) ) ;
#122931=DIRECTION ( 'NONE',  ( 0.000000000000000000, -0.8660254037844412611, -0.4999999999999956701 ) ) ;
#122938=VERTEX_POINT ( 'NONE', #46233 ) ;
#122952=ORIENTED_EDGE ( 'NONE', *, *, #110695, .T. ) ;
#122968=AXIS2_PLACEMENT_3D ( 'NONE', #27193, #229219, #230497 ) ;
#123018=ORIENTED_EDGE ( 'NONE', *, *, #33100, .T. ) ;
#123021=CARTESIAN_POINT ( 'NONE',  ( 20.87631937322888120, 10.47149503677486138, -141.5797458745818460 ) ) ;
#123046=DIRECTION ( 'NONE',  ( 0.000000000000000000, 0.000000000000000000, -1.000000000000000000 ) ) ;
#123059=VERTEX_POINT ( 'NONE', #113916 ) ;
#123066=( NAMED_UNIT ( * ) PLANE_ANGLE_UNIT ( ) SI_UNIT ( $, .RADIAN. ) );
#123088=VECTOR ( 'NONE', #53594, 1000.000000000000000 ) ;
#123092=CIRCLE ( 'NONE', #118997, 0.09999999999998898659 ) ;
#123124=ORIENTED_EDGE ( 'NONE', *, *, #169480, .T. ) ;
#123135=DIRECTION ( 'NONE',  ( 1.000000000000000000, 0.000000000000000000, 0.000000000000000000 ) ) ;
#123201=DIRECTION ( 'NONE',  ( 0.000000000000000000, 0.000000000000000000, -1.000000000000000000 ) ) ;
#123214=DIRECTION ( 'NONE',  ( 0.000000000000000000, -0.9887567792719341719, -0.1495327102803664099 ) ) ;
#123222=VECTOR ( 'NONE', #141085, 1000.000000000000000 ) ;
#123224=VERTEX_POINT ( 'NONE', #244127 ) ;
#123229=MECHANICAL_DESIGN_GEOMETRIC_PRESENTATION_REPRESENTATION('',(#89896),#14917);
#123264=EDGE_LOOP ( 'NONE', ( #49550, #74, #233072, #100879 ) ) ;
#123276=ORIENTED_EDGE ( 'NONE', *, *, #24931, .T. ) ;
#123283=CARTESIAN_POINT ( 'NONE',  ( -21.05000000000000071, -11.64999999998884306, -164.6000000000000227 ) ) ;
#123296=EDGE_CURVE ( 'NONE', #185310, #171186, #8109, .T. ) ;
#123318=CARTESIAN_POINT ( 'NONE',  ( -21.14999999999999858, -0.09999999998884338825, -127.4593430482987912 ) ) ;
#123337=CARTESIAN_POINT ( 'NONE',  ( 20.95566103547454517, 10.61824765095822087, -141.6318401929806043 ) ) ;
#123387=CARTESIAN_POINT ( 'NONE',  ( -21.05000000000000071, 1.115600667400684642E-11, -134.0000000000000000 ) ) ;
#123403=CARTESIAN_POINT ( 'NONE',  ( -18.50000000000000000, -9.421290279513540256, -174.3238821790264410 ) ) ;
#123419=EDGE_LOOP ( 'NONE', ( #20723, #158044, #65633, #31344 ) ) ;
#123442=CARTESIAN_POINT ( 'NONE',  ( -21.29999999999995808, 1.115600667400684642E-11, -134.0000000000000000 ) ) ;
#123482=DIRECTION ( 'NONE',  ( 1.000000000000000000, 0.000000000000000000, 0.000000000000000000 ) ) ;
#123501=ADVANCED_FACE ( 'NONE', ( #15838 ), #18372, .T. ) ;
#123511=DIRECTION ( 'NONE',  ( -1.000000000000000000, 0.000000000000000000, 0.000000000000000000 ) ) ;
#123512=CARTESIAN_POINT ( 'NONE',  ( 22.39999999999999858, 0.1000000000111554016, -126.2092204016266379 ) ) ;
#123515=VERTEX_POINT ( 'NONE', #138294 ) ;
#123522=ADVANCED_FACE ( 'NONE', ( #214012 ), #74543, .T. ) ;
#123542=EDGE_LOOP ( 'NONE', ( #70100, #239036, #246192, #117818 ) ) ;
#123543=CARTESIAN_POINT ( 'NONE',  ( 22.47809213839789066, 0.03753706763967752658, -122.3500266652122264 ) ) ;
#123554=DIRECTION ( 'NONE',  ( 0.000000000000000000, 0.000000000000000000, -1.000000000000000000 ) ) ;
#123555=LINE ( 'NONE', #242205, #117991 ) ;
#123557=SPHERICAL_SURFACE ( 'NONE', #102061, 0.1000000000000000056 ) ;
#123559=CARTESIAN_POINT ( 'NONE',  ( -1.739115166359751170E-14, 11.65000000001114699, -155.3500000000000227 ) ) ;
#123579=EDGE_CURVE ( 'NONE', #197139, #246280, #159195, .T. ) ;
#123580=ADVANCED_FACE ( 'NONE', ( #57477 ), #197487, .T. ) ;
#123628=CIRCLE ( 'NONE', #140158, 11.64999999999999325 ) ;
#123646=AXIS2_PLACEMENT_3D ( 'NONE', #111595, #191152, #188554 ) ;
#123681=DIRECTION ( 'NONE',  ( -1.000000000000000000, -2.952720810173289112E-16, 0.000000000000000000 ) ) ;
#123701=CYLINDRICAL_SURFACE ( 'NONE', #137282, 11.75000000000001066 ) ;
#123702=ORIENTED_EDGE ( 'NONE', *, *, #209373, .T. ) ;
#123715=DIRECTION ( 'NONE',  ( 0.000000000000000000, 0.000000000000000000, -1.000000000000000000 ) ) ;
#123717=CARTESIAN_POINT ( 'NONE',  ( -22.14074124539699540, 0.09905289585522827900, -126.6099221489562439 ) ) ;
#123740=DIRECTION ( 'NONE',  ( 0.000000000000000000, 0.2605042016806672911, -0.9654727137038716656 ) ) ;
#123741=DIRECTION ( 'NONE',  ( 1.000000000000000000, 0.000000000000000000, 0.000000000000000000 ) ) ;
#123747=TOROIDAL_SURFACE ( 'NONE', #127848, 0.4000000000000012990, 0.1000000000000000056 ) ;
#123781=CIRCLE ( 'NONE', #111315, 11.70000000000001528 ) ;
#123807=CIRCLE ( 'NONE', #32236, 0.09999999999998898659 ) ;
#123818=DIRECTION ( 'NONE',  ( 2.952720810173289112E-16, -1.000000000000000000, 0.000000000000000000 ) ) ;
#123831=CARTESIAN_POINT ( 'NONE',  ( -23.15000000000000213, 11.65000000001115588, -122.2500000000000284 ) ) ;
#123847=CIRCLE ( 'NONE', #70269, 0.09999999999999939493 ) ;
#123854=LINE ( 'NONE', #101675, #9206 ) ;
#123865=TOROIDAL_SURFACE ( 'NONE', #73806, 0.6000000000000013101, 0.1000000000000000056 ) ;
#123869=EDGE_CURVE ( 'NONE', #16854, #106553, #175887, .T. ) ;
#123888=CARTESIAN_POINT ( 'NONE',  ( 21.05000000000000071, -8.999999999988842703, -157.6060308773475640 ) ) ;
#123893=ORIENTED_EDGE ( 'NONE', *, *, #41408, .F. ) ;
#123920=CARTESIAN_POINT ( 'NONE',  ( -22.47071067811865319, 0.09909245471376171288, -126.2799252555019649 ) ) ;
#123931=ORIENTED_EDGE ( 'NONE', *, *, #81030, .F. ) ;
#123933=ADVANCED_FACE ( 'NONE', ( #35101 ), #157615, .F. ) ;
#123991=CARTESIAN_POINT ( 'NONE',  ( 21.05000000000000071, -11.64999999998883595, -164.6000000000000227 ) ) ;
#123998=ADVANCED_FACE ( 'NONE', ( #144392 ), #223946, .F. ) ;
#124020=CARTESIAN_POINT ( 'NONE',  ( 21.70464131381650219, 7.095358018979006864, -134.0000000000000000 ) ) ;
#124051=CIRCLE ( 'NONE', #190708, 0.1000000000000002554 ) ;
#124084=PLANE ( 'NONE',  #61836 ) ;
#124086=EDGE_CURVE ( 'NONE', #217669, #17731, #97706, .T. ) ;
#124113=DIRECTION ( 'NONE',  ( 0.000000000000000000, 0.000000000000000000, -1.000000000000000000 ) ) ;
#124130=ORIENTED_EDGE ( 'NONE', *, *, #51860, .T. ) ;
#124144=EDGE_CURVE ( 'NONE', #154872, #1294, #189973, .T. ) ;
#124152=PLANE ( 'NONE',  #26116 ) ;
#124156=CARTESIAN_POINT ( 'NONE',  ( 20.95512820512820440, 10.62384868372303615, -155.2500000000000284 ) ) ;
#124173=CARTESIAN_POINT ( 'NONE',  ( -21.14999999999999858, 1.115600667400684642E-11, -127.4593430482987912 ) ) ;
#124180=FACE_OUTER_BOUND ( 'NONE', #219116, .T. ) ;
#124199=DIRECTION ( 'NONE',  ( 0.000000000000000000, 0.000000000000000000, -1.000000000000000000 ) ) ;
#124203=AXIS2_PLACEMENT_3D ( 'NONE', #162058, #224568, #43380 ) ;
#124227=DIRECTION ( 'NONE',  ( 2.952720810173289112E-16, -1.000000000000000000, 0.000000000000000000 ) ) ;
#124239=CIRCLE ( 'NONE', #240933, 0.09999999999999939493 ) ;
#124243=EDGE_CURVE ( 'NONE', #91096, #58706, #38599, .T. ) ;
#124250=DIRECTION ( 'NONE',  ( -1.000000000000000000, -1.836970198721029934E-16, -3.186635328391151676E-31 ) ) ;
#124259=ORIENTED_EDGE ( 'NONE', *, *, #156547, .F. ) ;
#124306=CARTESIAN_POINT ( 'NONE',  ( -22.59999999999999787, 11.64957080755595520, -133.9000000000000057 ) ) ;
#124320=CARTESIAN_POINT ( 'NONE',  ( -22.50000000000000000, 0.1000000000111554016, -126.2092204016266379 ) ) ;
#124329=DIRECTION ( 'NONE',  ( -1.000000000000000000, 0.000000000000000000, 0.000000000000000000 ) ) ;
#124352=EDGE_LOOP ( 'NONE', ( #228919, #253224, #245833, #68374 ) ) ;
#124374=EDGE_CURVE ( 'NONE', #8351, #159790, #27025, .T. ) ;
#124387=DIRECTION ( 'NONE',  ( -1.000000000000000000, 0.000000000000000000, 0.000000000000000000 ) ) ;
#124390=AXIS2_PLACEMENT_3D ( 'NONE', #33297, #234015, #129783 ) ;
#124400=AXIS2_PLACEMENT_3D ( 'NONE', #251632, #232088, #113405 ) ;
#124412=AXIS2_PLACEMENT_3D ( 'NONE', #83548, #141003, #161861 ) ;
#124431=DIRECTION ( 'NONE',  ( -0.000000000000000000, 0.000000000000000000, 1.000000000000000000 ) ) ;
#124447=CARTESIAN_POINT ( 'NONE',  ( -18.59999999999999787, -1.164121893230052995, -175.3148480855716400 ) ) ;
#124454=FACE_OUTER_BOUND ( 'NONE', #32191, .T. ) ;
#124469=DIRECTION ( 'NONE',  ( 1.000000000000000000, -7.304098846218134667E-16, 4.607487905232622991E-31 ) ) ;
#124500=CARTESIAN_POINT ( 'NONE',  ( -23.25000000000000000, 11.65000000001115588, -122.2500000000000284 ) ) ;
#124507=ORIENTED_EDGE ( 'NONE', *, *, #140128, .F. ) ;
#124527=AXIS2_PLACEMENT_3D ( 'NONE', #129463, #87745, #12106 ) ;
#124543=CIRCLE ( 'NONE', #245160, 0.09999999999998898659 ) ;
#124575=EDGE_CURVE ( 'NONE', #65489, #223143, #252028, .T. ) ;
#124584=VECTOR ( 'NONE', #134866, 1000.000000000000114 ) ;
#124589=CARTESIAN_POINT ( 'NONE',  ( -18.50000000000000000, 7.120270961708746960, -171.1595630418393625 ) ) ;
#124590=VECTOR ( 'NONE', #19204, 1000.000000000000000 ) ;
#124602=ORIENTED_EDGE ( 'NONE', *, *, #241021, .T. ) ;
#124617=ORIENTED_EDGE ( 'NONE', *, *, #238975, .T. ) ;
#124618=CARTESIAN_POINT ( 'NONE',  ( 19.94784844284930969, 11.71308993304057999, -158.7021987172990976 ) ) ;
#124638=DIRECTION ( 'NONE',  ( 0.000000000000000000, 0.000000000000000000, -1.000000000000000000 ) ) ;
#124671=CARTESIAN_POINT ( 'NONE',  ( -20.85000000000000142, 11.75000000001115197, -160.7161343370219129 ) ) ;
#124675=CARTESIAN_POINT ( 'NONE',  ( -18.60000000000000142, -9.321008403350113269, -141.2359382490778899 ) ) ;
#124686=ORIENTED_EDGE ( 'NONE', *, *, #59276, .T. ) ;
#124693=CARTESIAN_POINT ( 'NONE',  ( 21.05000000000000071, -9.399999999988844834, -157.6060308773475640 ) ) ;
#124716=CARTESIAN_POINT ( 'NONE',  ( 23.25000000000000000, -11.48912529306489994, -164.4000000000000057 ) ) ;
#124773=AXIS2_PLACEMENT_3D ( 'NONE', #18888, #98383, #93291 ) ;
#124809=CARTESIAN_POINT ( 'NONE',  ( -20.94788355080264353, 10.30207779525982659, -172.9895520716782755 ) ) ;
#124822=ORIENTED_EDGE ( 'NONE', *, *, #228412, .F. ) ;
#124829=EDGE_CURVE ( 'NONE', #83182, #140569, #198044, .T. ) ;
#124867=ORIENTED_EDGE ( 'NONE', *, *, #177007, .T. ) ;
#124875=FACE_OUTER_BOUND ( 'NONE', #250899, .T. ) ;
#124896=LINE ( 'NONE', #126152, #106486 ) ;
#124910=AXIS2_PLACEMENT_3D ( 'NONE', #144327, #107795, #222585 ) ;
#124925=ORIENTED_EDGE ( 'NONE', *, *, #2809, .T. ) ;
#124979=ADVANCED_FACE ( 'NONE', ( #110779 ), #73373, .F. ) ;
#124991=CARTESIAN_POINT ( 'NONE',  ( -20.64999999999999858, 1.115600667400684642E-11, -167.5000000000000284 ) ) ;
#125043=CARTESIAN_POINT ( 'NONE',  ( 22.45380639572245940, 1.426796696685579650E-07, -122.2495671088909006 ) ) ;
#125050=CARTESIAN_POINT ( 'NONE',  ( 21.05000000000000071, -0.09999999998884338825, -127.4593430482987912 ) ) ;
#125106=VERTEX_POINT ( 'NONE', #172925 ) ;
#125112=CARTESIAN_POINT ( 'NONE',  ( 18.41789779300687258, -9.499999999988844479, -141.0320696663606839 ) ) ;
#125115=CARTESIAN_POINT ( 'NONE',  ( -21.33487959338958362, 6.725558151922345296, -134.0000000000000000 ) ) ;
#125134=VECTOR ( 'NONE', #247378, 1000.000000000000000 ) ;
#125137=ORIENTED_EDGE ( 'NONE', *, *, #193478, .T. ) ;
#125140=EDGE_CURVE ( 'NONE', #67744, #132345, #23296, .T. ) ;
#125150=DIRECTION ( 'NONE',  ( 1.000000000000000000, 2.952720810173289112E-16, -0.000000000000000000 ) ) ;
#125154=EDGE_CURVE ( 'NONE', #217170, #207209, #152053, .T. ) ;
#125164=CARTESIAN_POINT ( 'NONE',  ( 21.05000000000000071, -8.730841121484166578, -157.9019252810156786 ) ) ;
#125170=FACE_OUTER_BOUND ( 'NONE', #165969, .T. ) ;
#125172=DIRECTION ( 'NONE',  ( 0.000000000000000000, 0.000000000000000000, -1.000000000000000000 ) ) ;
#125176=ORIENTED_EDGE ( 'NONE', *, *, #57903, .F. ) ;
#125191=CIRCLE ( 'NONE', #208418, 11.70000000000001528 ) ;
#125228=CIRCLE ( 'NONE', #237828, 0.09999999999999939493 ) ;
#125250=EDGE_LOOP ( 'NONE', ( #112984, #74975, #41935, #69601, #2695, #232022, #30181, #214014, #82447, #257760, #123124, #69273 ) ) ;
#125255=ORIENTED_EDGE ( 'NONE', *, *, #51606, .F. ) ;
#125274=EDGE_CURVE ( 'NONE', #51801, #113685, #19528, .T. ) ;
#125284=EDGE_CURVE ( 'NONE', #189087, #117471, #39443, .T. ) ;
#125301=ORIENTED_EDGE ( 'NONE', *, *, #37997, .T. ) ;
#125315=DIRECTION ( 'NONE',  ( 0.000000000000000000, 0.000000000000000000, -1.000000000000000000 ) ) ;
#125320=CARTESIAN_POINT ( 'NONE',  ( 18.59999999999999432, -1.736257131586239844, -145.5686523290175387 ) ) ;
#125354=CARTESIAN_POINT ( 'NONE',  ( -21.05000000000000071, 1.115600667400684642E-11, -134.0000000000000000 ) ) ;
#125359=CARTESIAN_POINT ( 'NONE',  ( -22.47886152344871036, 0.03750093887284931121, -122.3500113569520806 ) ) ;
#125367=CARTESIAN_POINT ( 'NONE',  ( 21.05000000000000071, 10.42338541492404680, -141.4920519238701218 ) ) ;
#125385=CARTESIAN_POINT ( 'NONE',  ( 23.24999999999999289, 6.550000000011156231, -155.3500000000000227 ) ) ;
#125446=VERTEX_POINT ( 'NONE', #182790 ) ;
#125451=CARTESIAN_POINT ( 'NONE',  ( 18.59999999999999432, 1.162701749949165642, -142.1000000000000227 ) ) ;
#125471=ORIENTED_EDGE ( 'NONE', *, *, #2597, .T. ) ;
#125548=ADVANCED_FACE ( 'NONE', ( #54801 ), #134331, .T. ) ;
#125551=FACE_OUTER_BOUND ( 'NONE', #127677, .T. ) ;
#125559=LINE ( 'NONE', #186834, #186060 ) ;
#125574=CARTESIAN_POINT ( 'NONE',  ( 20.58091095332318332, 9.018470153363605135, -142.4186501821585864 ) ) ;
#125580=VECTOR ( 'NONE', #29605, 1000.000000000000000 ) ;
#125592=CARTESIAN_POINT ( 'NONE',  ( -20.85000000000000142, -1.835859311432481045, -179.0044391687985410 ) ) ;
#125600=PLANE ( 'NONE',  #224527 ) ;
#125614=DIRECTION ( 'NONE',  ( 0.000000000000000000, 0.000000000000000000, -1.000000000000000000 ) ) ;
#125623=VERTEX_POINT ( 'NONE', #239882 ) ;
#125658=CARTESIAN_POINT ( 'NONE',  ( 23.24999999999999645, 1.115600667400684642E-11, -167.5000000000000284 ) ) ;
#125676=CARTESIAN_POINT ( 'NONE',  ( -21.64999999999999858, 7.250000000011148416, -146.2500000000000284 ) ) ;
#125706=DIRECTION ( 'NONE',  ( 0.000000000000000000, 3.552713678800442159E-15, -1.000000000000000000 ) ) ;
#125725=VECTOR ( 'NONE', #135992, 1000.000000000000000 ) ;
#125726=CIRCLE ( 'NONE', #175630, 0.09999999999999817368 ) ;
#125743=LINE ( 'NONE', #183177, #234969 ) ;
#125746=CARTESIAN_POINT ( 'NONE',  ( 21.05000000000000071, 11.65000000001116298, -160.4851942293460638 ) ) ;
#125762=CIRCLE ( 'NONE', #121524, 4.149999999999987033 ) ;
#125774=AXIS2_PLACEMENT_3D ( 'NONE', #60507, #220873, #117920 ) ;
#125868=EDGE_CURVE ( 'NONE', #126399, #107215, #94349, .T. ) ;
#125882=CARTESIAN_POINT ( 'NONE',  ( 19.81427058490544013, 11.66856398039208109, -158.7500000000000284 ) ) ;
#125900=DIRECTION ( 'NONE',  ( 0.000000000000000000, 6.505213034913742890E-15, 1.000000000000000000 ) ) ;
#125909=ORIENTED_EDGE ( 'NONE', *, *, #243643, .T. ) ;
#125919=ORIENTED_EDGE ( 'NONE', *, *, #15321, .T. ) ;
#125925=AXIS2_PLACEMENT_3D ( 'NONE', #29370, #150566, #230092 ) ;
#125948=ORIENTED_EDGE ( 'NONE', *, *, #244919, .F. ) ;
#125953=CARTESIAN_POINT ( 'NONE',  ( -18.39999999999999503, -9.682403433465244902, -174.1568433774128266 ) ) ;
#125957=AXIS2_PLACEMENT_3D ( 'NONE', #113105, #11454, #153567 ) ;
#125985=CARTESIAN_POINT ( 'NONE',  ( -21.05000000000000071, -1.162701749926853712, -141.9000000000000341 ) ) ;
#126011=CYLINDRICAL_SURFACE ( 'NONE', #53584, 0.09999999999998898659 ) ;
#126068=AXIS2_PLACEMENT_3D ( 'NONE', #170288, #108969, #150681 ) ;
#126104=ORIENTED_EDGE ( 'NONE', *, *, #176592, .T. ) ;
#126112=ORIENTED_EDGE ( 'NONE', *, *, #83722, .F. ) ;
#126115=DIRECTION ( 'NONE',  ( 1.000000000000000000, -0.000000000000000000, -0.000000000000000000 ) ) ;
#126123=ADVANCED_FACE ( 'NONE', ( #226063 ), #61415, .T. ) ;
#126143=CIRCLE ( 'NONE', #105854, 0.09999999999999939493 ) ;
#126152=CARTESIAN_POINT ( 'NONE',  ( 20.04142135623730070, 11.75000000001115907, -122.2500000000000284 ) ) ;
#126168=EDGE_CURVE ( 'NONE', #68733, #229760, #140500, .T. ) ;
#126178=EDGE_CURVE ( 'NONE', #153112, #173033, #258030, .T. ) ;
#126187=EDGE_CURVE ( 'NONE', #42831, #189870, #123781, .T. ) ;
#126194=VERTEX_POINT ( 'NONE', #91724 ) ;
#126200=CARTESIAN_POINT ( 'NONE',  ( 18.49999999999999645, 1.115600667400684642E-11, -134.0000000000000000 ) ) ;
#126206=ADVANCED_FACE ( 'NONE', ( #171316 ), #2950, .F. ) ;
#126212=AXIS2_PLACEMENT_3D ( 'NONE', #142379, #164532, #45852 ) ;
#126222=ORIENTED_EDGE ( 'NONE', *, *, #132347, .T. ) ;
#126240=DIRECTION ( 'NONE',  ( 1.000000000000000000, 3.265361837132813093E-16, -0.000000000000000000 ) ) ;
#126260=CIRCLE ( 'NONE', #188617, 0.4000000000000114575 ) ;
#126297=FACE_OUTER_BOUND ( 'NONE', #30765, .T. ) ;
#126338=CIRCLE ( 'NONE', #247124, 0.09999999999999939493 ) ;
#126358=ORIENTED_EDGE ( 'NONE', *, *, #254163, .F. ) ;
#126363=DIRECTION ( 'NONE',  ( -1.000000000000000000, 0.000000000000000000, 0.000000000000000000 ) ) ;
#126399=VERTEX_POINT ( 'NONE', #244059 ) ;
#126465=DIRECTION ( 'NONE',  ( -1.000000000000000000, -1.836970198721029934E-16, 0.000000000000000000 ) ) ;
#126505=ORIENTED_EDGE ( 'NONE', *, *, #86892, .F. ) ;
#126556=AXIS2_PLACEMENT_3D ( 'NONE', #21262, #138571, #83729 ) ;
#126565=ADVANCED_FACE ( 'NONE', ( #53575 ), #212660, .T. ) ;
#126570=CARTESIAN_POINT ( 'NONE',  ( -18.59999999999999787, -1.261786168553869603, -142.0864989635454947 ) ) ;
#126576=ORIENTED_EDGE ( 'NONE', *, *, #249502, .F. ) ;
#126577=DIRECTION ( 'NONE',  ( 0.000000000000000000, 2.891205793294679805E-16, -1.000000000000000000 ) ) ;
#126582=CARTESIAN_POINT ( 'NONE',  ( -20.94999999999999929, -1.849153571964891274, -179.1059666197970728 ) ) ;
#126598=VECTOR ( 'NONE', #64220, 1000.000000000000000 ) ;
#126599=CYLINDRICAL_SURFACE ( 'NONE', #11290, 0.1000000000000004496 ) ;
#126602=VECTOR ( 'NONE', #135542, 1000.000000000000000 ) ;
#126604=CIRCLE ( 'NONE', #72640, 0.09999999999998898659 ) ;
#126605=CARTESIAN_POINT ( 'NONE',  ( -18.59999999999999787, 1.115600667400684642E-11, -167.5000000000000284 ) ) ;
#126613=LINE ( 'NONE', #189159, #111055 ) ;
#126619=LINE ( 'NONE', #165770, #117220 ) ;
#126635=CARTESIAN_POINT ( 'NONE',  ( -22.50000000000000000, 0.1000000000111554016, -122.3504291924552234 ) ) ;
#126644=CARTESIAN_POINT ( 'NONE',  ( 20.95512820512820085, 10.62384868372303615, -141.6649135690876449 ) ) ;
#126645=CARTESIAN_POINT ( 'NONE',  ( -21.55000000000000426, 7.708578643773852157, -155.1500000000000057 ) ) ;
#126654=EDGE_LOOP ( 'NONE', ( #11474, #119423, #199199, #160838 ) ) ;
#126660=ORIENTED_EDGE ( 'NONE', *, *, #188299, .F. ) ;
#126675=EDGE_LOOP ( 'NONE', ( #139876, #198897, #94702, #144301, #44806, #195466, #134876, #6858, #34014, #3314, #112814, #204420 ) ) ;
#126680=VECTOR ( 'NONE', #243287, 1000.000000000000000 ) ;
#126684=AXIS2_PLACEMENT_3D ( 'NONE', #90417, #72168, #95559 ) ;
#126687=FACE_OUTER_BOUND ( 'NONE', #251776, .T. ) ;
#126706=DIRECTION ( 'NONE',  ( 0.000000000000000000, 0.000000000000000000, -1.000000000000000000 ) ) ;
#126710=B_SPLINE_CURVE_WITH_KNOTS ( 'NONE', 3,
 ( #127562, #88403, #227944, #128855, #123717, #203242, #166719, #246228, #148416, #67583 ),
 .UNSPECIFIED., .F., .F.,
 ( 4, 3, 3, 4 ),
 ( 0.000000000000000000, 0.0002000000000002785953, 0.001000000000045107385, 0.001967863649472122601 ),
 .UNSPECIFIED. ) ;
#126714=VERTEX_POINT ( 'NONE', #177403 ) ;
#126729=EDGE_CURVE ( 'NONE', #92094, #160394, #220361, .T. ) ;
#126758=DIRECTION ( 'NONE',  ( -0.000000000000000000, 0.1298341882520022694, 0.9915357197604853789 ) ) ;
#126768=AXIS2_PLACEMENT_3D ( 'NONE', #49073, #227705, #205568 ) ;
#126772=EDGE_LOOP ( 'NONE', ( #37334, #128374, #13463 ) ) ;
#126776=EDGE_CURVE ( 'NONE', #96601, #151810, #40790, .T. ) ;
#126824=CARTESIAN_POINT ( 'NONE',  ( -20.64999999999999858, 1.115600667400684642E-11, -167.5000000000000284 ) ) ;
#126847=CARTESIAN_POINT ( 'NONE',  ( -20.64999999999999858, 7.150000000011155876, -155.1500000000000057 ) ) ;
#126878=CYLINDRICAL_SURFACE ( 'NONE', #171608, 0.09999999999999939493 ) ;
#126893=AXIS2_PLACEMENT_3D ( 'NONE', #48896, #33234, #90583 ) ;
#126902=VECTOR ( 'NONE', #115946, 1000.000000000000114 ) ;
#126905=CARTESIAN_POINT ( 'NONE',  ( 21.05000000000000071, -11.48912529306489994, -164.4000000000000057 ) ) ;
#126940=CIRCLE ( 'NONE', #197842, 0.09999999999999939493 ) ;
#126946=EDGE_LOOP ( 'NONE', ( #189557, #199619, #150435, #116342 ) ) ;
#127049=DIRECTION ( 'NONE',  ( 0.000000000000000000, 0.000000000000000000, -1.000000000000000000 ) ) ;
#127066=AXIS2_PLACEMENT_3D ( 'NONE', #31890, #192236, #9716 ) ;
#127105=LINE ( 'NONE', #241908, #154217 ) ;
#127114=ORIENTED_EDGE ( 'NONE', *, *, #79345, .T. ) ;
#127115=AXIS2_PLACEMENT_3D ( 'NONE', #50147, #55262, #119132 ) ;
#127160=ORIENTED_EDGE ( 'NONE', *, *, #131208, .F. ) ;
#127171=AXIS2_PLACEMENT_3D ( 'NONE', #35760, #116558, #95694 ) ;
#127187=FACE_OUTER_BOUND ( 'NONE', #49615, .T. ) ;
#127201=DIRECTION ( 'NONE',  ( 0.000000000000000000, 1.224646799142185182E-16, 1.000000000000000000 ) ) ;
#127212=DIRECTION ( 'NONE',  ( 0.000000000000000000, 0.4999999999999478195, -0.8660254037844686836 ) ) ;
#127213=DIRECTION ( 'NONE',  ( -1.000000000000000000, 0.000000000000000000, 0.000000000000000000 ) ) ;
#127253=CIRCLE ( 'NONE', #256351, 0.09999999999999817368 ) ;
#127290=AXIS2_PLACEMENT_3D ( 'NONE', #42642, #83018, #218693 ) ;
#127335=CARTESIAN_POINT ( 'NONE',  ( 18.33683296300457499, -9.511149971121650282, -174.4057074127099725 ) ) ;
#127350=DIRECTION ( 'NONE',  ( 1.000000000000000000, 0.000000000000000000, 0.000000000000000000 ) ) ;
#127352=DIRECTION ( 'NONE',  ( 1.734723475976817507E-14, 0.000000000000000000, -1.000000000000000000 ) ) ;
#127373=CARTESIAN_POINT ( 'NONE',  ( -20.87600722750343252, 10.33112638556969465, -173.0901228926974795 ) ) ;
#127388=DIRECTION ( 'NONE',  ( -0.000000000000000000, 1.000000000000000000, 1.734723475976807292E-15 ) ) ;
#127411=ORIENTED_EDGE ( 'NONE', *, *, #203542, .F. ) ;
#127417=DIRECTION ( 'NONE',  ( -1.000000000000000000, 0.000000000000000000, 0.000000000000000000 ) ) ;
#127429=DIRECTION ( 'NONE',  ( 1.000000000000000000, 0.000000000000000000, 0.000000000000000000 ) ) ;
#127460=DIRECTION ( 'NONE',  ( 0.000000000000000000, 0.01562500000001262185, 0.9998779222360095753 ) ) ;
#127467=ORIENTED_EDGE ( 'NONE', *, *, #86899, .F. ) ;
#127481=CIRCLE ( 'NONE', #202501, 0.8750000000000007772 ) ;
#127511=AXIS2_PLACEMENT_3D ( 'NONE', #36396, #78051, #153805 ) ;
#127532=CIRCLE ( 'NONE', #98260, 0.09999999999998898659 ) ;
#127562=CARTESIAN_POINT ( 'NONE',  ( -22.47071067811865319, 0.09909245471376171288, -126.2799252555019649 ) ) ;
#127584=CIRCLE ( 'NONE', #15156, 0.2000000000000057288 ) ;
#127586=CARTESIAN_POINT ( 'NONE',  ( 23.14999999999999858, 5.000000000011153745, -146.4052660189131245 ) ) ;
#127597=DIRECTION ( 'NONE',  ( 0.000000000000000000, 0.000000000000000000, 1.000000000000000000 ) ) ;
#127631=DIRECTION ( 'NONE',  ( -1.000000000000000000, -0.000000000000000000, -0.000000000000000000 ) ) ;
#127632=DIRECTION ( 'NONE',  ( -0.7070776581708965169, -0.7071359030027827286, -0.000000000000000000 ) ) ;
#127638=ORIENTED_EDGE ( 'NONE', *, *, #229332, .F. ) ;
#127657=B_SPLINE_CURVE_WITH_KNOTS ( 'NONE', 3,
 ( #220359, #102944, #144645, #83371, #245044, #125115, #45561 ),
 .UNSPECIFIED., .F., .F.,
 ( 4, 3, 4 ),
 ( 0.000000000000000000, 0.0009834301579439998740, 0.001767853679402675614 ),
 .UNSPECIFIED. ) ;
#127661=EDGE_CURVE ( 'NONE', #241817, #63155, #244100, .T. ) ;
#127677=EDGE_LOOP ( 'NONE', ( #5396, #225744, #22701, #197325, #54211, #236500, #1086, #158881, #254437, #230329, #98025, #161254, #179254, #193085, #50311, #35135 ) ) ;
#127738=AXIS2_PLACEMENT_3D ( 'NONE', #82756, #236720, #58075 ) ;
#127743=ORIENTED_EDGE ( 'NONE', *, *, #146712, .T. ) ;
#127816=DIRECTION ( 'NONE',  ( 0.000000000000000000, 0.000000000000000000, 1.000000000000000000 ) ) ;
#127833=ORIENTED_EDGE ( 'NONE', *, *, #165990, .T. ) ;
#127848=AXIS2_PLACEMENT_3D ( 'NONE', #214792, #176988, #76564 ) ;
#127855=CARTESIAN_POINT ( 'NONE',  ( 23.14999999999999147, 4.150000000011154988, -134.0000000000000000 ) ) ;
#127863=DIRECTION ( 'NONE',  ( 0.000000000000000000, 0.000000000000000000, -1.000000000000000000 ) ) ;
#127867=FACE_OUTER_BOUND ( 'NONE', #218456, .T. ) ;
#127928=EDGE_CURVE ( 'NONE', #54863, #18309, #167241, .T. ) ;
#127973=EDGE_CURVE ( 'NONE', #173033, #206061, #15484, .T. ) ;
#127985=FACE_OUTER_BOUND ( 'NONE', #25910, .T. ) ;
#127990=EDGE_CURVE ( 'NONE', #123224, #158124, #113280, .T. ) ;
#128012=VERTEX_POINT ( 'NONE', #115850 ) ;
#128034=CARTESIAN_POINT ( 'NONE',  ( -20.94999999999999929, -1.851028230129704522, -145.6539132694225032 ) ) ;
#128060=AXIS2_PLACEMENT_3D ( 'NONE', #20408, #76501, #135187 ) ;
#128128=VERTEX_POINT ( 'NONE', #137956 ) ;
#128129=CARTESIAN_POINT ( 'NONE',  ( 20.85000000000000142, -1.835859311432481045, -179.0044391687985410 ) ) ;
#128158=CARTESIAN_POINT ( 'NONE',  ( 20.41140022480508520, 10.41043084241320216, -141.6150013036338464 ) ) ;
#128184=CIRCLE ( 'NONE', #140640, 0.1000000000000002692 ) ;
#128229=AXIS2_PLACEMENT_3D ( 'NONE', #10710, #248023, #69414 ) ;
#128232=EDGE_CURVE ( 'NONE', #35759, #142216, #103233, .T. ) ;
#128233=DIRECTION ( 'NONE',  ( -0.000000000000000000, 1.000000000000000000, 2.891205793294679805E-16 ) ) ;
#128253=EDGE_LOOP ( 'NONE', ( #43734, #192440, #138050, #78040 ) ) ;
#128254=DIRECTION ( 'NONE',  ( -0.000000000000000000, -1.000000000000000000, -0.000000000000000000 ) ) ;
#128291=DIRECTION ( 'NONE',  ( 0.000000000000000000, 0.3738317757009345654, 0.9274965247785492695 ) ) ;
#128321=AXIS2_PLACEMENT_3D ( 'NONE', #49873, #129416, #231110 ) ;
#128374=ORIENTED_EDGE ( 'NONE', *, *, #130286, .T. ) ;
#128379=AXIS2_PLACEMENT_3D ( 'NONE', #74728, #252031, #175120 ) ;
#128380=ORIENTED_EDGE ( 'NONE', *, *, #156813, .F. ) ;
#128381=ORIENTED_EDGE ( 'NONE', *, *, #153750, .F. ) ;
#128405=AXIS2_PLACEMENT_3D ( 'NONE', #87347, #65227, #109482 ) ;
#128420=ADVANCED_FACE ( 'NONE', ( #57968 ), #86642, .T. ) ;
#128532=ORIENTED_EDGE ( 'NONE', *, *, #241486, .F. ) ;
#128546=AXIS2_PLACEMENT_3D ( 'NONE', #67175, #146678, #226204 ) ;
#128548=ORIENTED_EDGE ( 'NONE', *, *, #159471, .T. ) ;
#128566=AXIS2_PLACEMENT_3D ( 'NONE', #171410, #254708, #252175 ) ;
#128571=DIRECTION ( 'NONE',  ( 1.000000000000000000, 0.000000000000000000, 0.000000000000000000 ) ) ;
#128576=DIRECTION ( 'NONE',  ( -1.000000000000000000, -0.000000000000000000, -0.000000000000000000 ) ) ;
#128591=EDGE_CURVE ( 'NONE', #174999, #21693, #74246, .T. ) ;
#128597=FACE_OUTER_BOUND ( 'NONE', #129342, .T. ) ;
#128612=EDGE_CURVE ( 'NONE', #162622, #173033, #92955, .T. ) ;
#128628=CARTESIAN_POINT ( 'NONE',  ( 18.59999999999999076, 11.65000000001115943, -158.8500000000000227 ) ) ;
#128631=ADVANCED_FACE ( 'NONE', ( #91680 ), #16023, .T. ) ;
#128641=DIRECTION ( 'NONE',  ( 0.000000000000000000, 0.000000000000000000, -1.000000000000000000 ) ) ;
#128661=DIRECTION ( 'NONE',  ( 0.000000000000000000, 1.561251128379298294E-13, 1.000000000000000000 ) ) ;
#128688=LINE ( 'NONE', #208228, #125580 ) ;
#128702=TOROIDAL_SURFACE ( 'NONE', #178801, 0.4000000000000012990, 0.1000000000000000056 ) ;
#128726=ADVANCED_FACE ( 'NONE', ( #73585 ), #112685, .T. ) ;
#128727=DIRECTION ( 'NONE',  ( 1.000000000000000000, -0.000000000000000000, 0.000000000000000000 ) ) ;
#128764=EDGE_CURVE ( 'NONE', #47876, #149809, #178672, .T. ) ;
#128770=ORIENTED_EDGE ( 'NONE', *, *, #10910, .T. ) ;
#128783=CARTESIAN_POINT ( 'NONE',  ( -23.15000000000000213, -9.499999999988848032, -143.8939691226524644 ) ) ;
#128784=CARTESIAN_POINT ( 'NONE',  ( -18.39999999999999858, -9.599999999988849453, -174.1001893912220737 ) ) ;
#128789=DIRECTION ( 'NONE',  ( 1.000000000000000000, 0.000000000000000000, 0.000000000000000000 ) ) ;
#128806=ORIENTED_EDGE ( 'NONE', *, *, #5441, .F. ) ;
#128825=ORIENTED_EDGE ( 'NONE', *, *, #102325, .T. ) ;
#128855=CARTESIAN_POINT ( 'NONE',  ( -22.32929514600008503, 0.09907567812507747651, -126.4213524346235147 ) ) ;
#128872=EDGE_CURVE ( 'NONE', #176500, #153561, #136936, .T. ) ;
#128950=VERTEX_POINT ( 'NONE', #85071 ) ;
#128998=AXIS2_PLACEMENT_3D ( 'NONE', #113445, #215113, #117303 ) ;
#129033=DIRECTION ( 'NONE',  ( 0.000000000000000000, -0.000000000000000000, 1.000000000000000000 ) ) ;
#129070=DIRECTION ( 'NONE',  ( 0.000000000000000000, 0.000000000000000000, -1.000000000000000000 ) ) ;
#129111=DIRECTION ( 'NONE',  ( 1.713247197920696616E-14, 0.9876197685951252359, -0.1568667991644863424 ) ) ;
#129120=AXIS2_PLACEMENT_3D ( 'NONE', #7303, #206796, #86822 ) ;
#129135=EDGE_CURVE ( 'NONE', #208557, #37324, #153743, .T. ) ;
#129156=ADVANCED_FACE ( 'NONE', ( #139289 ), #197993, .F. ) ;
#129160=CARTESIAN_POINT ( 'NONE',  ( 20.94999999999999929, 5.000000000011153745, -155.5947339810869323 ) ) ;
#129176=CIRCLE ( 'NONE', #45773, 0.09999999999999860389 ) ;
#129193=AXIS2_PLACEMENT_3D ( 'NONE', #216387, #239825, #160303 ) ;
#129197=ORIENTED_EDGE ( 'NONE', *, *, #137926, .F. ) ;
#129218=CARTESIAN_POINT ( 'NONE',  ( 21.08804582317323906, 8.878166167103058726, -146.3499998294057605 ) ) ;
#129236=DIRECTION ( 'NONE',  ( 0.000000000000000000, -0.8700118002898359348, 0.4930308989875165082 ) ) ;
#129241=ORIENTED_EDGE ( 'NONE', *, *, #10910, .F. ) ;
#129243=EDGE_LOOP ( 'NONE', ( #213209, #155406, #198265, #103560 ) ) ;
#129261=DIRECTION ( 'NONE',  ( 0.000000000000000000, -1.000000000000000000, 0.000000000000000000 ) ) ;
#129276=ORIENTED_EDGE ( 'NONE', *, *, #49390, .F. ) ;
#129280=ORIENTED_EDGE ( 'NONE', *, *, #249679, .T. ) ;
#129305=ORIENTED_EDGE ( 'NONE', *, *, #151029, .F. ) ;
#129334=FACE_OUTER_BOUND ( 'NONE', #230697, .T. ) ;
#129342=EDGE_LOOP ( 'NONE', ( #131361, #29846, #185757, #38977 ) ) ;
#129345=EDGE_LOOP ( 'NONE', ( #92636, #106785, #138647 ) ) ;
#129391=DIRECTION ( 'NONE',  ( 0.000000000000000000, 0.000000000000000000, -1.000000000000000000 ) ) ;
#129416=DIRECTION ( 'NONE',  ( 1.000000000000000000, 0.000000000000000000, 0.000000000000000000 ) ) ;
#129435=ORIENTED_EDGE ( 'NONE', *, *, #148501, .F. ) ;
#129444=EDGE_CURVE ( 'NONE', #224878, #50997, #153349, .T. ) ;
#129452=DIRECTION ( 'NONE',  ( -0.000000000000000000, 0.000000000000000000, 1.000000000000000000 ) ) ;
#129460=EDGE_CURVE ( 'NONE', #205417, #155942, #108091, .T. ) ;
#129463=CARTESIAN_POINT ( 'NONE',  ( 23.24999999999999289, 11.65000000001116298, -134.1000000000000227 ) ) ;
#129490=ORIENTED_EDGE ( 'NONE', *, *, #9151, .T. ) ;
#129521=EDGE_CURVE ( 'NONE', #196244, #180058, #62282, .T. ) ;
#129556=VERTEX_POINT ( 'NONE', #212138 ) ;
#129557=VECTOR ( 'NONE', #76268, 1000.000000000000000 ) ;
#129572=DIRECTION ( 'NONE',  ( -1.000000000000000000, -0.000000000000000000, -0.000000000000000000 ) ) ;
#129588=EDGE_CURVE ( 'NONE', #360, #159084, #3448, .T. ) ;
#129601=CARTESIAN_POINT ( 'NONE',  ( 21.05000000000000071, -8.999999999988842703, -157.6060308773475640 ) ) ;
#129619=ORIENTED_EDGE ( 'NONE', *, *, #79738, .F. ) ;
#129635=DIRECTION ( 'NONE',  ( 1.000000000000000000, 2.952720810173289112E-16, -0.000000000000000000 ) ) ;
#129643=EDGE_CURVE ( 'NONE', #129684, #45297, #87214, .T. ) ;
#129680=ORIENTED_EDGE ( 'NONE', *, *, #203542, .T. ) ;
#129684=VERTEX_POINT ( 'NONE', #124589 ) ;
#129710=CARTESIAN_POINT ( 'NONE',  ( -23.15000000000000213, 1.115600667400684642E-11, -134.0000000000000000 ) ) ;
#129725=AXIS2_PLACEMENT_3D ( 'NONE', #134311, #15703, #193035 ) ;
#129732=EDGE_CURVE ( 'NONE', #47453, #160655, #49247, .T. ) ;
#129744=EDGE_CURVE ( 'NONE', #117646, #60099, #230095, .T. ) ;
#129760=LINE ( 'NONE', #107625, #168442 ) ;
#129764=ORIENTED_EDGE ( 'NONE', *, *, #140617, .T. ) ;
#129783=DIRECTION ( 'NONE',  ( 0.000000000000000000, 0.000000000000000000, -1.000000000000000000 ) ) ;
#129808=CARTESIAN_POINT ( 'NONE',  ( -18.50000000000000000, 10.29270135741298375, -172.9573618871519614 ) ) ;
#129856=AXIS2_PLACEMENT_3D ( 'NONE', #106723, #186293, #207138 ) ;
#129866=CARTESIAN_POINT ( 'NONE',  ( -23.25000000000000000, -8.596261682231832069, -158.0498724828497359 ) ) ;
#129878=EDGE_CURVE ( 'NONE', #151746, #185310, #36989, .T. ) ;
#129887=DIRECTION ( 'NONE',  ( 1.000000000000000000, 0.000000000000000000, 0.000000000000000000 ) ) ;
#129899=DIRECTION ( 'NONE',  ( 1.000000000000000000, -0.000000000000000000, -0.000000000000000000 ) ) ;
#129905=CYLINDRICAL_SURFACE ( 'NONE', #12654, 0.09999999999998898659 ) ;
#129916=DIRECTION ( 'NONE',  ( 1.000000000000000000, -0.000000000000000000, -0.000000000000000000 ) ) ;
#129919=CARTESIAN_POINT ( 'NONE',  ( -20.93302460841142931, 10.31565961587945246, -173.0364194119178478 ) ) ;
#129933=CARTESIAN_POINT ( 'NONE',  ( 21.05000000000000071, 1.115600667400684642E-11, -169.4000000000000625 ) ) ;
#129935=LINE ( 'NONE', #150802, #478 ) ;
#129958=CARTESIAN_POINT ( 'NONE',  ( 21.30000000000002558, 1.115600667400684642E-11, -134.0000000000000000 ) ) ;
#129965=VERTEX_POINT ( 'NONE', #76148 ) ;
#129988=ORIENTED_EDGE ( 'NONE', *, *, #81973, .F. ) ;
#129996=EDGE_LOOP ( 'NONE', ( #117489, #241442, #194344, #43946 ) ) ;
#130004=DIRECTION ( 'NONE',  ( 0.000000000000000000, 0.9876197685951252359, -0.1568667991644863424 ) ) ;
#130015=EDGE_LOOP ( 'NONE', ( #224119, #160797, #97359, #142668 ) ) ;
#130024=EDGE_CURVE ( 'NONE', #126194, #192257, #178458, .T. ) ;
#130031=ORIENTED_EDGE ( 'NONE', *, *, #178890, .T. ) ;
#130048=ORIENTED_EDGE ( 'NONE', *, *, #177007, .F. ) ;
#130062=EDGE_CURVE ( 'NONE', #188779, #129556, #211756, .T. ) ;
#130070=DIRECTION ( 'NONE',  ( 0.000000000000000000, -1.000000000000000000, 0.000000000000000000 ) ) ;
#130108=AXIS2_PLACEMENT_3D ( 'NONE', #255447, #54728, #113424 ) ;
#130144=DIRECTION ( 'NONE',  ( -3.265361837132813586E-16, 1.000000000000000000, 0.000000000000000000 ) ) ;
#130157=ORIENTED_EDGE ( 'NONE', *, *, #6773, .T. ) ;
#130173=CARTESIAN_POINT ( 'NONE',  ( 20.94999999999999929, -8.730841121484171907, -143.5980747189843783 ) ) ;
#130196=EDGE_LOOP ( 'NONE', ( #72635, #240537, #100774, #232284 ) ) ;
#130201=ORIENTED_EDGE ( 'NONE', *, *, #19366, .T. ) ;
#130210=CARTESIAN_POINT ( 'NONE',  ( 18.48536876927993688, -9.463527249856078072, -141.0486182650826379 ) ) ;
#130233=FACE_OUTER_BOUND ( 'NONE', #23273, .T. ) ;
#130239=VECTOR ( 'NONE', #99015, 1000.000000000000000 ) ;
#130254=DIRECTION ( 'NONE',  ( 1.000000000000000000, 0.000000000000000000, 0.000000000000000000 ) ) ;
#130261=CARTESIAN_POINT ( 'NONE',  ( -21.05000000000000071, 6.270085863700304962, -133.9651319969869405 ) ) ;
#130286=EDGE_CURVE ( 'NONE', #216709, #241817, #116269, .T. ) ;
#130289=VECTOR ( 'NONE', #69814, 1000.000000000000000 ) ;
#130296=CARTESIAN_POINT ( 'NONE',  ( 21.05000000000000071, -11.48912529306489994, -164.4000000000000057 ) ) ;
#130297=CARTESIAN_POINT ( 'NONE',  ( 18.60000000000001563, -9.364236010355611484, -141.1802544007246354 ) ) ;
#130305=ORIENTED_EDGE ( 'NONE', *, *, #89034, .F. ) ;
#130320=VERTEX_POINT ( 'NONE', #77137 ) ;
#130374=EDGE_CURVE ( 'NONE', #152529, #105943, #191110, .T. ) ;
#130385=DIRECTION ( 'NONE',  ( -1.000000000000000000, 0.000000000000000000, 0.000000000000000000 ) ) ;
#130399=CIRCLE ( 'NONE', #255436, 0.09999999999998898659 ) ;
#130405=FACE_OUTER_BOUND ( 'NONE', #86017, .T. ) ;
#130409=ADVANCED_FACE ( 'NONE', ( #140986 ), #200942, .T. ) ;
#130426=CARTESIAN_POINT ( 'NONE',  ( -20.64999999999999858, -8.663551401858001100, -157.9758988819327215 ) ) ;
#130440=EDGE_CURVE ( 'NONE', #227344, #237934, #121441, .T. ) ;
#130460=CARTESIAN_POINT ( 'NONE',  ( -20.64999999999999858, -8.999999999988844479, -157.6060308773475924 ) ) ;
#130480=ORIENTED_EDGE ( 'NONE', *, *, #106340, .T. ) ;
#130494=AXIS2_PLACEMENT_3D ( 'NONE', #194377, #36599, #34035 ) ;
#130499=VECTOR ( 'NONE', #244870, 1000.000000000000000 ) ;
#130503=CARTESIAN_POINT ( 'NONE',  ( -23.15000000000000213, 4.350000000011156054, -155.1500000000000057 ) ) ;
#130516=CARTESIAN_POINT ( 'NONE',  ( 21.05000000000000426, 10.56275983746217051, -141.4568139579186550 ) ) ;
#130537=CARTESIAN_POINT ( 'NONE',  ( 18.59999999999998366, 7.021664781911246322, -171.3335654018973173 ) ) ;
#130538=ORIENTED_EDGE ( 'NONE', *, *, #156273, .F. ) ;
#130550=CARTESIAN_POINT ( 'NONE',  ( 18.49999999999999289, 10.49142135624846617, -158.7500000000000284 ) ) ;
#130554=CARTESIAN_POINT ( 'NONE',  ( 23.15000000000000213, -9.499999999988848032, -143.8939691226524644 ) ) ;
#130586=ORIENTED_EDGE ( 'NONE', *, *, #112639, .T. ) ;
#130594=CIRCLE ( 'NONE', #230569, 4.099999999999992539 ) ;
#130607=CARTESIAN_POINT ( 'NONE',  ( 18.39999999999999858, -9.682403433465241349, -174.1568433774127982 ) ) ;
#130621=B_SPLINE_CURVE_WITH_KNOTS ( 'NONE', 3,
 ( #165211, #246040, #229047, #9989, #50371, #124809, #28305, #46528, #129919, #67394, #209468, #204322, #205606, #107801, #105187, #127373, #184767, #88210, #6117 ),
 .UNSPECIFIED., .F., .F.,
 ( 4, 3, 3, 3, 3, 3, 4 ),
 ( -2.000416914672224079E-06, 0.000000000000000000, 4.714008503745887858E-05, 9.979203887778508822E-05, 0.0001372215519229591648, 0.0001635031576220990037, 0.0001900083748504206697 ),
 .UNSPECIFIED. ) ;
#130655=ORIENTED_EDGE ( 'NONE', *, *, #18746, .T. ) ;
#130659=ORIENTED_EDGE ( 'NONE', *, *, #120242, .T. ) ;
#130663=ORIENTED_EDGE ( 'NONE', *, *, #48956, .T. ) ;
#130665=CARTESIAN_POINT ( 'NONE',  ( -23.25000000000000000, 2.000000000011154189, -147.2246219227621111 ) ) ;
#130683=CARTESIAN_POINT ( 'NONE',  ( 22.45305468355010348, -0.1008583690885486023, -122.2504328765103168 ) ) ;
#130686=CARTESIAN_POINT ( 'NONE',  ( 21.09610168723072832, 0.03358950690266722383, -127.6210442847752233 ) ) ;
#130692=DIRECTION ( 'NONE',  ( 1.000000000000000000, 0.000000000000000000, 0.000000000000000000 ) ) ;
#130710=ORIENTED_EDGE ( 'NONE', *, *, #152435, .F. ) ;
#130721=FACE_OUTER_BOUND ( 'NONE', #133306, .T. ) ;
#130726=DIRECTION ( 'NONE',  ( 0.000000000000000000, -0.01283462868042125823, -0.9999176327611367654 ) ) ;
#130746=PLANE ( 'NONE',  #222708 ) ;
#130773=LINE ( 'NONE', #193331, #206971 ) ;
#130785=DIRECTION ( 'NONE',  ( 0.000000000000000000, 0.000000000000000000, -1.000000000000000000 ) ) ;
#130797=CARTESIAN_POINT ( 'NONE',  ( -20.64999999999999858, 7.150000000011155876, -155.1500000000000057 ) ) ;
#130801=CARTESIAN_POINT ( 'NONE',  ( 21.00000000000000000, 9.750000000011153745, -155.1500000000000057 ) ) ;
#130818=DIRECTION ( 'NONE',  ( 0.000000000000000000, 0.000000000000000000, -1.000000000000000000 ) ) ;
#130820=DIRECTION ( 'NONE',  ( 1.000000000000000000, 7.304098846218135653E-16, 0.000000000000000000 ) ) ;
#130859=CARTESIAN_POINT ( 'NONE',  ( 23.14999999999999858, 5.500000000011153745, -155.0947339810869323 ) ) ;
#130866=EDGE_CURVE ( 'NONE', #55107, #111978, #87194, .T. ) ;
#130878=CIRCLE ( 'NONE', #172635, 0.09999999999998898659 ) ;
#130885=VECTOR ( 'NONE', #169024, 1000.000000000000000 ) ;
#130887=ORIENTED_EDGE ( 'NONE', *, *, #52279, .T. ) ;
#130895=EDGE_CURVE ( 'NONE', #5925, #27502, #101489, .T. ) ;
#130913=CARTESIAN_POINT ( 'NONE',  ( -2.995603634470829482E-16, 6.650000000011155876, -155.1500000000000057 ) ) ;
#130934=DIRECTION ( 'NONE',  ( -0.000000000000000000, -0.1298341882520022694, -0.9915357197604853789 ) ) ;
#130935=ORIENTED_EDGE ( 'NONE', *, *, #129521, .F. ) ;
#130947=ORIENTED_EDGE ( 'NONE', *, *, #91206, .F. ) ;
#130948=CIRCLE ( 'NONE', #35128, 0.09999999999998898659 ) ;
#130966=DIRECTION ( 'NONE',  ( 0.000000000000000000, 0.000000000000000000, -1.000000000000000000 ) ) ;
#130968=AXIS2_PLACEMENT_3D ( 'NONE', #163765, #102459, #127201 ) ;
#130990=ORIENTED_EDGE ( 'NONE', *, *, #135713, .F. ) ;
#131002=CARTESIAN_POINT ( 'NONE',  ( -21.29999999999995808, 1.115600667400684642E-11, -138.0500000000000114 ) ) ;
#131036=FACE_OUTER_BOUND ( 'NONE', #222070, .T. ) ;
#131043=DIRECTION ( 'NONE',  ( 1.000000000000000000, 7.304098846218134667E-16, -4.607487905232622991E-31 ) ) ;
#131063=VERTEX_POINT ( 'NONE', #194885 ) ;
#131069=FACE_OUTER_BOUND ( 'NONE', #25900, .T. ) ;
#131082=CARTESIAN_POINT ( 'NONE',  ( 21.04999999999908411, 8.776282895301829257, -146.1579090026525307 ) ) ;
#131099=ORIENTED_EDGE ( 'NONE', *, *, #194473, .F. ) ;
#131105=DIRECTION ( 'NONE',  ( 1.000000000000000000, -0.000000000000000000, -0.000000000000000000 ) ) ;
#131133=DIRECTION ( 'NONE',  ( -0.000000000000000000, -1.000000000000000000, 0.000000000000000000 ) ) ;
#131135=CIRCLE ( 'NONE', #147710, 0.09999999999999939493 ) ;
#131140=DIRECTION ( 'NONE',  ( 0.000000000000000000, 0.000000000000000000, -1.000000000000000000 ) ) ;
#131159=DIRECTION ( 'NONE',  ( 0.000000000000000000, 0.1350103645451876666, -0.9908441862701600211 ) ) ;
#131171=ORIENTED_EDGE ( 'NONE', *, *, #35396, .F. ) ;
#131176=CARTESIAN_POINT ( 'NONE',  ( 18.47135592147663274, -9.471088613254405431, -174.1835949398439993 ) ) ;
#131183=CARTESIAN_POINT ( 'NONE',  ( -21.05000000000000071, 11.75000000001115552, -160.4851942293460638 ) ) ;
#131187=FACE_OUTER_BOUND ( 'NONE', #38246, .T. ) ;
#131200=DIRECTION ( 'NONE',  ( 0.000000000000000000, 0.000000000000000000, 1.000000000000000000 ) ) ;
#131208=EDGE_CURVE ( 'NONE', #143461, #109066, #241524, .T. ) ;
#131219=ORIENTED_EDGE ( 'NONE', *, *, #98216, .T. ) ;
#131228=CARTESIAN_POINT ( 'NONE',  ( -21.65000000000000213, 7.708578643773852157, -155.1500000000000057 ) ) ;
#131255=ORIENTED_EDGE ( 'NONE', *, *, #218296, .F. ) ;
#131295=ORIENTED_EDGE ( 'NONE', *, *, #158306, .T. ) ;
#131298=LINE ( 'NONE', #137699, #219114 ) ;
#131320=VECTOR ( 'NONE', #61735, 1000.000000000000000 ) ;
#131322=ORIENTED_EDGE ( 'NONE', *, *, #107833, .T. ) ;
#131337=CARTESIAN_POINT ( 'NONE',  ( -20.64999999999999858, 4.350000000011156054, -155.1500000000000057 ) ) ;
#131344=ORIENTED_EDGE ( 'NONE', *, *, #197839, .F. ) ;
#131359=SPHERICAL_SURFACE ( 'NONE', #80430, 0.1000000000000000056 ) ;
#131361=ORIENTED_EDGE ( 'NONE', *, *, #167570, .F. ) ;
#131372=ORIENTED_EDGE ( 'NONE', *, *, #66446, .T. ) ;
#131373=ORIENTED_EDGE ( 'NONE', *, *, #12537, .F. ) ;
#131375=DIRECTION ( 'NONE',  ( 0.000000000000000000, -0.000000000000000000, 1.000000000000000000 ) ) ;
#131378=CARTESIAN_POINT ( 'NONE',  ( -21.11927991906891222, 0.009083679485028296058, -127.5515068815085158 ) ) ;
#131389=ORIENTED_EDGE ( 'NONE', *, *, #112576, .F. ) ;
#131401=CARTESIAN_POINT ( 'NONE',  ( -18.59999999999999787, -1.162701749926853712, -142.0000000000000284 ) ) ;
#131428=CARTESIAN_POINT ( 'NONE',  ( 21.14999999999999503, -0.1008583690875562017, -122.2504328765106294 ) ) ;
#131443=DIRECTION ( 'NONE',  ( -1.000000000000000000, 7.304098846218134667E-16, 4.217023435051625732E-16 ) ) ;
#131462=EDGE_CURVE ( 'NONE', #175543, #109393, #36811, .T. ) ;
#131487=FACE_OUTER_BOUND ( 'NONE', #210511, .T. ) ;
#131498=ORIENTED_EDGE ( 'NONE', *, *, #28924, .F. ) ;
#131529=CIRCLE ( 'NONE', #15022, 11.79999999999999893 ) ;
#131629=ORIENTED_EDGE ( 'NONE', *, *, #186099, .T. ) ;
#131638=AXIS2_PLACEMENT_3D ( 'NONE', #157316, #742, #141570 ) ;
#131661=LINE ( 'NONE', #226905, #149496 ) ;
#131674=ORIENTED_EDGE ( 'NONE', *, *, #129521, .T. ) ;
#131686=CIRCLE ( 'NONE', #115122, 0.5000000000000004441 ) ;
#131727=FACE_OUTER_BOUND ( 'NONE', #84451, .T. ) ;
#131732=CARTESIAN_POINT ( 'NONE',  ( -23.15000000000000213, 1.115650265596050101E-11, -129.9500000000000171 ) ) ;
#131782=FACE_OUTER_BOUND ( 'NONE', #188032, .T. ) ;
#131810=EDGE_LOOP ( 'NONE', ( #2882, #254026, #170592 ) ) ;
#131910=ORIENTED_EDGE ( 'NONE', *, *, #33601, .T. ) ;
#131929=EDGE_CURVE ( 'NONE', #187169, #152529, #245987, .T. ) ;
#131932=ORIENTED_EDGE ( 'NONE', *, *, #170528, .T. ) ;
#131936=CARTESIAN_POINT ( 'NONE',  ( 23.24999999999999289, 11.75000000001116263, -122.2500000000000284 ) ) ;
#131938=DIRECTION ( 'NONE',  ( 1.000000000000000000, 0.000000000000000000, -0.000000000000000000 ) ) ;
#131985=CIRCLE ( 'NONE', #15683, 0.09999999999999892308 ) ;
#131996=CARTESIAN_POINT ( 'NONE',  ( 23.14999999999999503, 6.650000000011155876, -146.1500000000000341 ) ) ;
#131997=DIRECTION ( 'NONE',  ( 0.000000000000000000, 0.000000000000000000, -1.000000000000000000 ) ) ;
#132021=CARTESIAN_POINT ( 'NONE',  ( 18.59999999999999076, -1.835859311432481045, -179.0044391687985410 ) ) ;
#132067=CIRCLE ( 'NONE', #73273, 0.1000000000000001860 ) ;
#132079=CARTESIAN_POINT ( 'NONE',  ( 21.05000000000000071, -0.09999999998884338825, -134.0000000000000000 ) ) ;
#132106=DIRECTION ( 'NONE',  ( 1.000000000000000000, -0.000000000000000000, -0.000000000000000000 ) ) ;
#132109=CARTESIAN_POINT ( 'NONE',  ( 20.85000000000000142, 11.65000000001115943, -167.5000000000000284 ) ) ;
#132110=ORIENTED_EDGE ( 'NONE', *, *, #6367, .F. ) ;
#132119=ADVANCED_FACE ( 'NONE', ( #6317 ), #196272, .T. ) ;
#132120=CARTESIAN_POINT ( 'NONE',  ( 18.59999999999999432, -1.162701749926853712, -142.1000000000000227 ) ) ;
#132123=PLANE ( 'NONE',  #134394 ) ;
#132140=EDGE_LOOP ( 'NONE', ( #30277, #105729, #24737, #111786 ) ) ;
#132156=EDGE_CURVE ( 'NONE', #83407, #160572, #83803, .T. ) ;
#132166=ORIENTED_EDGE ( 'NONE', *, *, #120242, .F. ) ;
#132174=CIRCLE ( 'NONE', #32239, 11.64999999999999325 ) ;
#132260=CARTESIAN_POINT ( 'NONE',  ( -20.94999999999999929, -11.48912529306489994, -164.4000000000000057 ) ) ;
#132268=VECTOR ( 'NONE', #128233, 1000.000000000000000 ) ;
#132328=LINE ( 'NONE', #227578, #130289 ) ;
#132341=( NAMED_UNIT ( * ) PLANE_ANGLE_UNIT ( ) SI_UNIT ( $, .RADIAN. ) );
#132345=VERTEX_POINT ( 'NONE', #204061 ) ;
#132347=EDGE_CURVE ( 'NONE', #37772, #143461, #4718, .T. ) ;
#132380=EDGE_CURVE ( 'NONE', #246321, #253143, #225475, .T. ) ;
#132409=DIRECTION ( 'NONE',  ( 0.000000000000000000, 0.000000000000000000, 1.000000000000000000 ) ) ;
#132412=CARTESIAN_POINT ( 'NONE',  ( 21.30000000000002558, 1.115600667400684642E-11, -129.9500000000000171 ) ) ;
#132425=CARTESIAN_POINT ( 'NONE',  ( -18.59999999999999787, 9.350000000011156942, -146.3500000000000227 ) ) ;
#132430=CARTESIAN_POINT ( 'NONE',  ( -18.50000000000000711, -9.419203418015495544, -141.2477858104287236 ) ) ;
#132447=DIRECTION ( 'NONE',  ( 0.000000000000000000, 0.000000000000000000, -1.000000000000000000 ) ) ;
#132450=EDGE_CURVE ( 'NONE', #89497, #62775, #212858, .T. ) ;
#132471=CARTESIAN_POINT ( 'NONE',  ( 18.46163235739458131, -9.480150806907193584, -174.1576105398774814 ) ) ;
#132477=EDGE_CURVE ( 'NONE', #126714, #220134, #31814, .T. ) ;
#132484=CARTESIAN_POINT ( 'NONE',  ( 21.05000000000000071, -8.999999999988842703, -157.6060308773475640 ) ) ;
#132488=DIRECTION ( 'NONE',  ( 1.000000000000000000, -0.000000000000000000, -0.000000000000000000 ) ) ;
#132491=LINE ( 'NONE', #150771, #165451 ) ;
#132500=EDGE_LOOP ( 'NONE', ( #208915, #119818, #43395, #241647 ) ) ;
#132580=FACE_OUTER_BOUND ( 'NONE', #146570, .T. ) ;
#132609=ORIENTED_EDGE ( 'NONE', *, *, #119450, .F. ) ;
#132624=ORIENTED_EDGE ( 'NONE', *, *, #174713, .F. ) ;
#132634=DIRECTION ( 'NONE',  ( -3.469446951953635015E-14, 1.000000000000000000, 0.000000000000000000 ) ) ;
#132666=CIRCLE ( 'NONE', #207687, 11.80000000000000426 ) ;
#132668=AXIS2_PLACEMENT_3D ( 'NONE', #232236, #212662, #56119 ) ;
#132731=DIRECTION ( 'NONE',  ( 0.000000000000000000, 0.8700118002898322711, -0.4930308989875231140 ) ) ;
#132740=DIRECTION ( 'NONE',  ( 0.000000000000000000, 0.000000000000000000, -1.000000000000000000 ) ) ;
#132754=CYLINDRICAL_SURFACE ( 'NONE', #121875, 11.75000000000001066 ) ;
#132770=ORIENTED_EDGE ( 'NONE', *, *, #45512, .F. ) ;
#132785=DIRECTION ( 'NONE',  ( 0.000000000000000000, 0.000000000000000000, -1.000000000000000000 ) ) ;
#132792=CARTESIAN_POINT ( 'NONE',  ( 20.04142135623730070, 11.75000000001115907, -158.6500000000000057 ) ) ;
#132794=CARTESIAN_POINT ( 'NONE',  ( -20.54999999999999716, 9.350000000011156942, -146.2500000000000284 ) ) ;
#132812=DIRECTION ( 'NONE',  ( 0.000000000000000000, 0.9999631594459053030, 0.008583690987162899758 ) ) ;
#132820=ORIENTED_EDGE ( 'NONE', *, *, #95897, .T. ) ;
#132824=EDGE_CURVE ( 'NONE', #13549, #120967, #172316, .T. ) ;
#132832=EDGE_CURVE ( 'NONE', #19242, #64247, #6646, .T. ) ;
#132862=CARTESIAN_POINT ( 'NONE',  ( -21.46681500593282621, 6.857511159395651035, -134.0000000000000000 ) ) ;
#132864=ORIENTED_EDGE ( 'NONE', *, *, #57747, .F. ) ;
#132926=CYLINDRICAL_SURFACE ( 'NONE', #245582, 0.09999999999999939493 ) ;
#132928=ORIENTED_EDGE ( 'NONE', *, *, #78318, .F. ) ;
#132929=DIRECTION ( 'NONE',  ( 0.000000000000000000, 0.000000000000000000, -1.000000000000000000 ) ) ;
#132937=ORIENTED_EDGE ( 'NONE', *, *, #234189, .T. ) ;
#132966=ORIENTED_EDGE ( 'NONE', *, *, #7114, .F. ) ;
#132971=DIRECTION ( 'NONE',  ( -1.000000000000000000, -0.000000000000000000, -0.000000000000000000 ) ) ;
#132997=DIRECTION ( 'NONE',  ( 0.000000000000000000, 0.000000000000000000, -1.000000000000000000 ) ) ;
#133001=ORIENTED_EDGE ( 'NONE', *, *, #82764, .F. ) ;
#133002=EDGE_CURVE ( 'NONE', #51801, #19242, #123854, .T. ) ;
#133010=ADVANCED_FACE ( 'NONE', ( #43033 ), #66439, .F. ) ;
#133068=ORIENTED_EDGE ( 'NONE', *, *, #249655, .F. ) ;
#133077=DIRECTION ( 'NONE',  ( 1.000000000000000000, -0.000000000000000000, -0.000000000000000000 ) ) ;
#133103=CARTESIAN_POINT ( 'NONE',  ( 21.04999999999999716, 8.894723818388550640, -142.4870843231475703 ) ) ;
#133105=CIRCLE ( 'NONE', #53976, 0.09999999999998807065 ) ;
#133110=CARTESIAN_POINT ( 'NONE',  ( 21.05000000000000071, 5.900000000011162093, -157.2809002353436654 ) ) ;
#133126=DIRECTION ( 'NONE',  ( 0.000000000000000000, -2.498001805406600196E-13, -1.000000000000000000 ) ) ;
#133179=ORIENTED_EDGE ( 'NONE', *, *, #238745, .T. ) ;
#133182=DIRECTION ( 'NONE',  ( 1.000000000000000000, 0.000000000000000000, -0.000000000000000000 ) ) ;
#133195=DIRECTION ( 'NONE',  ( -6.938893903907222856E-15, 1.000000000000000000, 0.000000000000000000 ) ) ;
#133229=CARTESIAN_POINT ( 'NONE',  ( -23.15000000000000213, 2.000000000011154189, -154.2753780772379173 ) ) ;
#133230=ORIENTED_EDGE ( 'NONE', *, *, #191068, .F. ) ;
#133237=VERTEX_POINT ( 'NONE', #11615 ) ;
#133279=AXIS2_PLACEMENT_3D ( 'NONE', #1191, #81996, #193325 ) ;
#133282=AXIS2_PLACEMENT_3D ( 'NONE', #73981, #133908, #236859 ) ;
#133283=AXIS2_PLACEMENT_3D ( 'NONE', #209463, #129916, #128661 ) ;
#133304=EDGE_CURVE ( 'NONE', #120342, #73323, #34861, .T. ) ;
#133306=EDGE_LOOP ( 'NONE', ( #221032, #131171, #196602, #241847 ) ) ;
#133315=DIRECTION ( 'NONE',  ( 0.000000000000000000, 0.1575844902526835067, 0.9875055080513738259 ) ) ;
#133319=DIRECTION ( 'NONE',  ( 0.000000000000000000, 0.000000000000000000, 1.000000000000000000 ) ) ;
#133322=LINE ( 'NONE', #15968, #166447 ) ;
#133325=AXIS2_PLACEMENT_3D ( 'NONE', #96429, #16928, #119894 ) ;
#133352=CARTESIAN_POINT ( 'NONE',  ( -20.85000000000000142, -11.74999999998884448, -164.6000000000000227 ) ) ;
#133357=CARTESIAN_POINT ( 'NONE',  ( 23.24999999999999289, 11.75000000001116263, -122.2500000000000284 ) ) ;
#133365=ORIENTED_EDGE ( 'NONE', *, *, #156919, .F. ) ;
#133372=ORIENTED_EDGE ( 'NONE', *, *, #220098, .F. ) ;
#133379=CARTESIAN_POINT ( 'NONE',  ( -18.46902351632712680, -9.509470118669714367, -140.9864539342573266 ) ) ;
#133383=CARTESIAN_POINT ( 'NONE',  ( 18.49999999999999289, 10.49142135624846439, -158.8500000000000227 ) ) ;
#133387=ORIENTED_EDGE ( 'NONE', *, *, #103192, .T. ) ;
#133393=CARTESIAN_POINT ( 'NONE',  ( -23.15000000000000213, -8.999999999988846255, -143.8939691226524644 ) ) ;
#133425=ORIENTED_EDGE ( 'NONE', *, *, #52716, .F. ) ;
#133444=ORIENTED_EDGE ( 'NONE', *, *, #67061, .F. ) ;
#133450=EDGE_CURVE ( 'NONE', #216916, #73323, #13660, .T. ) ;
#133467=CARTESIAN_POINT ( 'NONE',  ( 21.05000012384916275, 10.62872029888669978, -146.1779773300349632 ) ) ;
#133515=AXIS2_PLACEMENT_3D ( 'NONE', #221490, #102823, #203229 ) ;
#133524=ORIENTED_EDGE ( 'NONE', *, *, #210694, .F. ) ;
#133528=EDGE_CURVE ( 'NONE', #229458, #220002, #146912, .T. ) ;
#133543=ORIENTED_EDGE ( 'NONE', *, *, #32363, .F. ) ;
#133555=AXIS2_PLACEMENT_3D ( 'NONE', #73736, #75027, #72448 ) ;
#133595=CARTESIAN_POINT ( 'NONE',  ( -23.15000000000000213, 1.115600667400684642E-11, -165.5000000000000284 ) ) ;
#133624=CIRCLE ( 'NONE', #208488, 0.2000000000000057288 ) ;
#133639=CARTESIAN_POINT ( 'NONE',  ( 21.05000000000000071, 1.115600667400684642E-11, -134.0000000000000000 ) ) ;
#133675=AXIS2_PLACEMENT_3D ( 'NONE', #231363, #110108, #192239 ) ;
#133692=FACE_OUTER_BOUND ( 'NONE', #156668, .T. ) ;
#133709=CIRCLE ( 'NONE', #167077, 0.1999999999999987899 ) ;
#133733=AXIS2_PLACEMENT_3D ( 'NONE', #51247, #211656, #94248 ) ;
#133745=CARTESIAN_POINT ( 'NONE',  ( 18.50000000000000355, -9.421074344976293702, -174.3244720594309456 ) ) ;
#133758=CARTESIAN_POINT ( 'NONE',  ( -20.94999999999999929, 11.70000000001115126, -160.7450018504814011 ) ) ;
#133759=ADVANCED_FACE ( 'NONE', ( #116804 ), #33460, .F. ) ;
#133773=EDGE_LOOP ( 'NONE', ( #230817, #156815, #36098, #113353 ) ) ;
#133832=CARTESIAN_POINT ( 'NONE',  ( -20.99780126800952829, 11.60538868788763089, -160.5873525717050541 ) ) ;
#133833=EDGE_CURVE ( 'NONE', #13316, #32896, #47196, .T. ) ;
#133838=DIRECTION ( 'NONE',  ( 0.000000000000000000, -1.000000000000000000, 0.000000000000000000 ) ) ;
#133850=DIRECTION ( 'NONE',  ( 0.000000000000000000, 0.000000000000000000, -1.000000000000000000 ) ) ;
#133852=CARTESIAN_POINT ( 'NONE',  ( -22.47071067811865319, 0.09909245471376178227, -126.2799252555019649 ) ) ;
#133888=ORIENTED_EDGE ( 'NONE', *, *, #185484, .F. ) ;
#133900=CARTESIAN_POINT ( 'NONE',  ( 20.95265033839679347, 10.51225083247831371, -141.5657637560299804 ) ) ;
#133908=DIRECTION ( 'NONE',  ( 0.000000000000000000, -0.5000000000000004441, -0.8660254037844384856 ) ) ;
#133983=EDGE_LOOP ( 'NONE', ( #144757, #62393, #119091, #7868 ) ) ;
#133989=AXIS2_PLACEMENT_3D ( 'NONE', #16762, #194120, #235779 ) ;
#133997=EDGE_CURVE ( 'NONE', #229756, #134466, #163880, .T. ) ;
#134010=DIRECTION ( 'NONE',  ( 0.000000000000000000, 0.000000000000000000, -1.000000000000000000 ) ) ;
#134014=DIRECTION ( 'NONE',  ( -1.000000000000000000, -0.000000000000000000, -0.000000000000000000 ) ) ;
#134034=CARTESIAN_POINT ( 'NONE',  ( -23.15000000000000213, -11.48912529306489994, -164.4000000000000057 ) ) ;
#134040=AXIS2_PLACEMENT_3D ( 'NONE', #218999, #181186, #3814 ) ;
#134047=EDGE_CURVE ( 'NONE', #44736, #141516, #53644, .T. ) ;
#134052=CARTESIAN_POINT ( 'NONE',  ( -22.59999999999999787, 1.115600667400684642E-11, -134.0000000000000000 ) ) ;
#134054=VECTOR ( 'NONE', #131375, 1000.000000000000000 ) ;
#134071=ORIENTED_EDGE ( 'NONE', *, *, #62780, .F. ) ;
#134126=EDGE_CURVE ( 'NONE', #180230, #220173, #197180, .T. ) ;
#134148=AXIS2_PLACEMENT_3D ( 'NONE', #183668, #28478, #102808 ) ;
#134174=CIRCLE ( 'NONE', #55052, 0.4000000000000114575 ) ;
#134178=AXIS2_PLACEMENT_3D ( 'NONE', #63722, #140694, #157748 ) ;
#134225=EDGE_CURVE ( 'NONE', #62775, #99799, #241284, .T. ) ;
#134256=EDGE_CURVE ( 'NONE', #174999, #175804, #23542, .T. ) ;
#134278=DIRECTION ( 'NONE',  ( 0.000000000000000000, 0.000000000000000000, -1.000000000000000000 ) ) ;
#134292=CARTESIAN_POINT ( 'NONE',  ( -21.05000000000000071, 1.115600667400684642E-11, -167.5000000000000284 ) ) ;
#134301=DIRECTION ( 'NONE',  ( 0.000000000000000000, 0.9654727137038715545, -0.2605042016806676242 ) ) ;
#134311=CARTESIAN_POINT ( 'NONE',  ( -22.39999999999999858, 11.65000000001115588, -133.9000000000000057 ) ) ;
#134327=FACE_OUTER_BOUND ( 'NONE', #62792, .T. ) ;
#134331=CYLINDRICAL_SURFACE ( 'NONE', #252568, 11.75000000000001066 ) ;
#134366=DIRECTION ( 'NONE',  ( 0.000000000000000000, 1.000000000000000000, -6.308085367188393199E-16 ) ) ;
#134372=DIRECTION ( 'NONE',  ( 1.000000000000000000, -0.000000000000000000, -0.000000000000000000 ) ) ;
#134380=CARTESIAN_POINT ( 'NONE',  ( 20.94999999999999929, 1.115600667400684642E-11, -167.5000000000000284 ) ) ;
#134394=AXIS2_PLACEMENT_3D ( 'NONE', #73462, #211672, #29216 ) ;
#134395=VERTEX_POINT ( 'NONE', #109438 ) ;
#134406=DIRECTION ( 'NONE',  ( 0.000000000000000000, 0.000000000000000000, -1.000000000000000000 ) ) ;
#134414=ORIENTED_EDGE ( 'NONE', *, *, #41822, .T. ) ;
#134426=DIRECTION ( 'NONE',  ( 0.000000000000000000, 0.000000000000000000, 1.000000000000000000 ) ) ;
#134443=DIRECTION ( 'NONE',  ( 0.000000000000000000, 1.000000000000000000, 0.000000000000000000 ) ) ;
#134466=VERTEX_POINT ( 'NONE', #157611 ) ;
#134470=EDGE_CURVE ( 'NONE', #163431, #227883, #146701, .T. ) ;
#134494=CARTESIAN_POINT ( 'NONE',  ( 21.14999999999999858, 10.71339244341104013, -146.2500000000000284 ) ) ;
#134507=AXIS2_PLACEMENT_3D ( 'NONE', #78917, #123214, #243154 ) ;
#134559=ORIENTED_EDGE ( 'NONE', *, *, #33269, .T. ) ;
#134645=DIRECTION ( 'NONE',  ( 0.000000000000000000, 0.000000000000000000, 1.000000000000000000 ) ) ;
#134683=EDGE_LOOP ( 'NONE', ( #22989, #200841, #108242, #75803 ) ) ;
#134689=DIRECTION ( 'NONE',  ( 1.000000000000000000, -0.000000000000000000, -0.000000000000000000 ) ) ;
#134710=DIRECTION ( 'NONE',  ( 0.000000000000000000, 0.000000000000000000, -1.000000000000000000 ) ) ;
#134727=DIRECTION ( 'NONE',  ( 1.000000000000000000, 0.000000000000000000, 0.000000000000000000 ) ) ;
#134750=DIRECTION ( 'NONE',  ( 1.000000000000000000, -0.000000000000000000, -0.000000000000000000 ) ) ;
#134752=CIRCLE ( 'NONE', #151565, 0.09999999999998898659 ) ;
#134762=FACE_OUTER_BOUND ( 'NONE', #119853, .T. ) ;
#134766=ORIENTED_EDGE ( 'NONE', *, *, #80919, .F. ) ;
#134767=ORIENTED_EDGE ( 'NONE', *, *, #238745, .F. ) ;
#134808=VECTOR ( 'NONE', #133077, 1000.000000000000000 ) ;
#134812=ORIENTED_EDGE ( 'NONE', *, *, #37249, .F. ) ;
#134838=AXIS2_PLACEMENT_3D ( 'NONE', #243380, #7342, #144259 ) ;
#134840=ORIENTED_EDGE ( 'NONE', *, *, #89034, .T. ) ;
#134852=FACE_OUTER_BOUND ( 'NONE', #11460, .T. ) ;
#134866=DIRECTION ( 'NONE',  ( 2.557131231893036985E-16, -0.8660254037844383745, 0.5000000000000003331 ) ) ;
#134876=ORIENTED_EDGE ( 'NONE', *, *, #245230, .F. ) ;
#134880=EDGE_LOOP ( 'NONE', ( #153036, #131373, #173584, #97973 ) ) ;
#134887=CIRCLE ( 'NONE', #242686, 12.87499999999999822 ) ;
#134937=DIRECTION ( 'NONE',  ( 0.000000000000000000, 0.000000000000000000, -1.000000000000000000 ) ) ;
#134946=DIRECTION ( 'NONE',  ( -7.304098846218201720E-16, 1.000000000000000000, 0.000000000000000000 ) ) ;
#134970=AXIS2_PLACEMENT_3D ( 'NONE', #159132, #83383, #199539 ) ;
#134987=VECTOR ( 'NONE', #80878, 1000.000000000000000 ) ;
#134995=DIRECTION ( 'NONE',  ( 0.000000000000000000, -0.1350103645451904977, -0.9908441862701596881 ) ) ;
#135017=DIRECTION ( 'NONE',  ( -0.000000000000000000, -0.1350103645451928291, -0.9908441862701594660 ) ) ;
#135056=EDGE_LOOP ( 'NONE', ( #246357, #180075, #132966, #65369 ) ) ;
#135062=AXIS2_PLACEMENT_3D ( 'NONE', #176406, #214233, #115130 ) ;
#135078=ORIENTED_EDGE ( 'NONE', *, *, #61941, .F. ) ;
#135081=CIRCLE ( 'NONE', #243427, 0.4000000000000114575 ) ;
#135108=DIRECTION ( 'NONE',  ( 1.000000000000000000, 0.000000000000000000, 0.000000000000000000 ) ) ;
#135132=ORIENTED_EDGE ( 'NONE', *, *, #55736, .F. ) ;
#135151=ORIENTED_EDGE ( 'NONE', *, *, #163574, .T. ) ;
#135159=CIRCLE ( 'NONE', #193470, 0.1000000000000019207 ) ;
#135160=DIRECTION ( 'NONE',  ( 0.000000000000000000, 0.000000000000000000, 1.000000000000000000 ) ) ;
#135176=ORIENTED_EDGE ( 'NONE', *, *, #26467, .F. ) ;
#135187=DIRECTION ( 'NONE',  ( 0.000000000000000000, 1.000000000000000000, 0.000000000000000000 ) ) ;
#135191=LINE ( 'NONE', #170545, #176678 ) ;
#135196=ORIENTED_EDGE ( 'NONE', *, *, #107230, .T. ) ;
#135200=EDGE_CURVE ( 'NONE', #186782, #18582, #95683, .T. ) ;
#135231=CARTESIAN_POINT ( 'NONE',  ( -21.05000000000000071, 6.540656951712399803, -134.0000000000000284 ) ) ;
#135241=ORIENTED_EDGE ( 'NONE', *, *, #167198, .F. ) ;
#135264=DIRECTION ( 'NONE',  ( 0.000000000000000000, 0.000000000000000000, -1.000000000000000000 ) ) ;
#135270=FACE_OUTER_BOUND ( 'NONE', #40257, .T. ) ;
#135289=DIRECTION ( 'NONE',  ( 0.000000000000000000, 1.000000000000000000, 0.000000000000000000 ) ) ;
#135320=VERTEX_POINT ( 'NONE', #2995 ) ;
#135433=DIRECTION ( 'NONE',  ( -0.000000000000000000, 0.8660254037844502539, 0.4999999999999799050 ) ) ;
#135434=ORIENTED_EDGE ( 'NONE', *, *, #32247, .T. ) ;
#135442=ORIENTED_EDGE ( 'NONE', *, *, #105078, .F. ) ;
#135497=CIRCLE ( 'NONE', #118961, 0.1000000000000001860 ) ;
#135520=ORIENTED_EDGE ( 'NONE', *, *, #76943, .F. ) ;
#135539=EDGE_LOOP ( 'NONE', ( #57128, #54908, #36621, #124822 ) ) ;
#135542=DIRECTION ( 'NONE',  ( -0.000000000000000000, 0.000000000000000000, -1.000000000000000000 ) ) ;
#135561=DIRECTION ( 'NONE',  ( 1.000000000000000000, 0.000000000000000000, 0.000000000000000000 ) ) ;
#135572=CIRCLE ( 'NONE', #239644, 0.09999999999998898659 ) ;
#135580=DIRECTION ( 'NONE',  ( 0.000000000000000000, 0.000000000000000000, -1.000000000000000000 ) ) ;
#135627=CIRCLE ( 'NONE', #152236, 0.09999999999998898659 ) ;
#135695=DIRECTION ( 'NONE',  ( 1.000000000000000000, -0.000000000000000000, -0.000000000000000000 ) ) ;
#135713=EDGE_CURVE ( 'NONE', #129684, #121951, #184860, .T. ) ;
#135724=CIRCLE ( 'NONE', #56581, 7.900000000000000355 ) ;
#135730=CARTESIAN_POINT ( 'NONE',  ( -23.15000000000000213, 2.000000000011154189, -154.2753780772379173 ) ) ;
#135740=VECTOR ( 'NONE', #90055, 1000.000000000000000 ) ;
#135752=DIRECTION ( 'NONE',  ( -0.000000000000000000, -0.4791956752371546724, -0.8777080977375153470 ) ) ;
#135814=CARTESIAN_POINT ( 'NONE',  ( -21.37071067811865532, 8.070710678129811910, -155.1500000000000057 ) ) ;
#135820=CARTESIAN_POINT ( 'NONE',  ( -20.85000000000000142, 1.115600667400684642E-11, -167.5000000000000284 ) ) ;
#135871=VERTEX_POINT ( 'NONE', #77594 ) ;
#135914=DIRECTION ( 'NONE',  ( 2.557131231893037478E-16, -0.8660254037844385966, 0.5000000000000003331 ) ) ;
#135916=ADVANCED_FACE ( 'NONE', ( #98423 ), #140146, .T. ) ;
#135921=DIRECTION ( 'NONE',  ( 0.000000000000000000, 1.000000000000000000, 0.000000000000000000 ) ) ;
#135924=DIRECTION ( 'NONE',  ( 1.000000000000000000, 0.000000000000000000, 0.000000000000000000 ) ) ;
#135935=EDGE_LOOP ( 'NONE', ( #153427, #43176, #83364, #201383 ) ) ;
#135956=AXIS2_PLACEMENT_3D ( 'NONE', #78380, #79655, #200907 ) ;
#135991=AXIS2_PLACEMENT_3D ( 'NONE', #184929, #104085, #46686 ) ;
#135992=DIRECTION ( 'NONE',  ( 1.000000000000000000, 0.000000000000000000, 0.000000000000000000 ) ) ;
#135999=CIRCLE ( 'NONE', #227591, 0.09999999999998898659 ) ;
#136004=ORIENTED_EDGE ( 'NONE', *, *, #10132, .T. ) ;
#136018=DIRECTION ( 'NONE',  ( 1.000000000000000000, 0.000000000000000000, 0.000000000000000000 ) ) ;
#136039=FACE_OUTER_BOUND ( 'NONE', #9066, .T. ) ;
#136046=ORIENTED_EDGE ( 'NONE', *, *, #137017, .T. ) ;
#136084=DIRECTION ( 'NONE',  ( 0.000000000000000000, 0.000000000000000000, -1.000000000000000000 ) ) ;
#136129=CARTESIAN_POINT ( 'NONE',  ( -20.94999999999999929, 11.75000000001115197, -140.8416006898971489 ) ) ;
#136152=VECTOR ( 'NONE', #64055, 1000.000000000000000 ) ;
#136158=ORIENTED_EDGE ( 'NONE', *, *, #52420, .F. ) ;
#136206=CIRCLE ( 'NONE', #115389, 0.09999999999998898659 ) ;
#136208=DIRECTION ( 'NONE',  ( 0.000000000000000000, 0.000000000000000000, 1.000000000000000000 ) ) ;
#136214=DIRECTION ( 'NONE',  ( 0.000000000000000000, -1.000000000000000000, -0.000000000000000000 ) ) ;
#136217=DIRECTION ( 'NONE',  ( 0.000000000000000000, 0.000000000000000000, 1.000000000000000000 ) ) ;
#136220=VECTOR ( 'NONE', #221198, 1000.000000000000000 ) ;
#136227=EDGE_LOOP ( 'NONE', ( #68790, #52015, #7046, #60310 ) ) ;
#136234=CARTESIAN_POINT ( 'NONE',  ( -20.85000000000000142, -0.3238857010591806307, -167.4575895893140114 ) ) ;
#136270=AXIS2_PLACEMENT_3D ( 'NONE', #131996, #96683, #176287 ) ;
#136319=CYLINDRICAL_SURFACE ( 'NONE', #213449, 0.09999999999999939493 ) ;
#136324=VERTEX_POINT ( 'NONE', #166818 ) ;
#136351=ORIENTED_EDGE ( 'NONE', *, *, #188224, .F. ) ;
#136361=DIRECTION ( 'NONE',  ( 1.000000000000000000, 1.836970198721029934E-16, 0.000000000000000000 ) ) ;
#136443=DIRECTION ( 'NONE',  ( 1.000000000000000000, -0.000000000000000000, 0.000000000000000000 ) ) ;
#136452=EDGE_CURVE ( 'NONE', #218711, #142216, #156054, .T. ) ;
#136456=CIRCLE ( 'NONE', #169855, 11.80000000000000426 ) ;
#136468=ORIENTED_EDGE ( 'NONE', *, *, #130374, .F. ) ;
#136494=DIRECTION ( 'NONE',  ( 1.296989514748957922E-15, -0.9887567792719341719, 0.1495327102803664099 ) ) ;
#136500=ORIENTED_EDGE ( 'NONE', *, *, #87901, .F. ) ;
#136508=CARTESIAN_POINT ( 'NONE',  ( -21.04999999999999716, 6.440770893673127162, -134.0175971870084481 ) ) ;
#136510=EDGE_CURVE ( 'NONE', #222594, #90426, #118644, .T. ) ;
#136548=ORIENTED_EDGE ( 'NONE', *, *, #25806, .F. ) ;
#136564=CARTESIAN_POINT ( 'NONE',  ( -23.15000000000000213, 11.75000000001115552, -146.1500000000000341 ) ) ;
#136574=DIRECTION ( 'NONE',  ( 0.000000000000000000, -0.4999999999999413247, 0.8660254037844724584 ) ) ;
#136576=VECTOR ( 'NONE', #96925, 1000.000000000000000 ) ;
#136582=DIRECTION ( 'NONE',  ( 0.000000000000000000, 0.000000000000000000, 1.000000000000000000 ) ) ;
#136585=DIRECTION ( 'NONE',  ( -1.000000000000000000, -0.000000000000000000, -0.000000000000000000 ) ) ;
#136607=ORIENTED_EDGE ( 'NONE', *, *, #13120, .T. ) ;
#136611=LINE ( 'NONE', #153692, #105031 ) ;
#136617=AXIS2_PLACEMENT_3D ( 'NONE', #109194, #250006, #227875 ) ;
#136634=ORIENTED_EDGE ( 'NONE', *, *, #49097, .F. ) ;
#136636=CARTESIAN_POINT ( 'NONE',  ( -20.99142135623731065, 11.60000000001115161, -160.5717967697245285 ) ) ;
#136657=AXIS2_PLACEMENT_3D ( 'NONE', #241475, #2837, #221877 ) ;
#136668=DIRECTION ( 'NONE',  ( 0.000000000000000000, 1.000000000000000000, 0.000000000000000000 ) ) ;
#136674=AXIS2_PLACEMENT_3D ( 'NONE', #71147, #185935, #150666 ) ;
#136705=DIRECTION ( 'NONE',  ( 0.000000000000000000, 0.000000000000000000, -1.000000000000000000 ) ) ;
#136735=CARTESIAN_POINT ( 'NONE',  ( 18.59999999999999432, -1.637172712959223952, -145.5821533654720383 ) ) ;
#136758=VERTEX_POINT ( 'NONE', #57748 ) ;
#136768=ORIENTED_EDGE ( 'NONE', *, *, #46126, .F. ) ;
#136778=CARTESIAN_POINT ( 'NONE',  ( -20.94999999999999929, -11.64999999998884483, -137.0000000000000000 ) ) ;
#136783=DIRECTION ( 'NONE',  ( 0.000000000000000000, 6.308085367183347448E-16, 1.000000000000000000 ) ) ;
#136788=CARTESIAN_POINT ( 'NONE',  ( 21.00000000000000000, 9.750000000011153745, -155.1500000000000057 ) ) ;
#136796=DIRECTION ( 'NONE',  ( 0.000000000000000000, 0.000000000000000000, 1.000000000000000000 ) ) ;
#136809=EDGE_CURVE ( 'NONE', #22303, #236473, #251141, .T. ) ;
#136813=ORIENTED_EDGE ( 'NONE', *, *, #5020, .T. ) ;
#136841=ORIENTED_EDGE ( 'NONE', *, *, #18429, .F. ) ;
#136850=CARTESIAN_POINT ( 'NONE',  ( 21.05000000000000071, 5.850000000011156942, -157.3675027757221017 ) ) ;
#136921=DIRECTION ( 'NONE',  ( 0.000000000000000000, 0.000000000000000000, -1.000000000000000000 ) ) ;
#136936=CIRCLE ( 'NONE', #91142, 0.1000000000000043493 ) ;
#136937=TOROIDAL_SURFACE ( 'NONE', #178673, 0.2000000000000000111, 0.1000000000000000056 ) ;
#136946=ORIENTED_EDGE ( 'NONE', *, *, #8288, .F. ) ;
#136947=DIRECTION ( 'NONE',  ( -1.000000000000000000, 0.000000000000000000, 0.000000000000000000 ) ) ;
#136954=DIRECTION ( 'NONE',  ( -1.000000000000000000, 0.000000000000000000, 0.000000000000000000 ) ) ;
#136963=DIRECTION ( 'NONE',  ( 1.000000000000000000, 2.952720810173289112E-16, -0.000000000000000000 ) ) ;
#136992=EDGE_CURVE ( 'NONE', #105589, #151810, #142163, .T. ) ;
#136995=AXIS2_PLACEMENT_3D ( 'NONE', #222895, #44285, #203349 ) ;
#136998=EDGE_LOOP ( 'NONE', ( #112684, #25483, #178616, #38355 ) ) ;
#137017=EDGE_CURVE ( 'NONE', #217227, #72782, #197890, .T. ) ;
#137031=CIRCLE ( 'NONE', #28746, 0.1000000000000033223 ) ;
#137032=ORIENTED_EDGE ( 'NONE', *, *, #206833, .F. ) ;
#137043=EDGE_CURVE ( 'NONE', #79296, #222594, #151419, .T. ) ;
#137044=CIRCLE ( 'NONE', #216137, 11.75000000000001066 ) ;
#137099=EDGE_CURVE ( 'NONE', #49547, #117646, #109710, .T. ) ;
#137112=ORIENTED_EDGE ( 'NONE', *, *, #83486, .F. ) ;
#137197=EDGE_LOOP ( 'NONE', ( #193153, #33995, #182223 ) ) ;
#137235=DIRECTION ( 'NONE',  ( 1.000000000000000000, 0.000000000000000000, 0.000000000000000000 ) ) ;
#137278=AXIS2_PLACEMENT_3D ( 'NONE', #60594, #18907, #198832 ) ;
#137282=AXIS2_PLACEMENT_3D ( 'NONE', #225333, #224059, #46705 ) ;
#137288=CARTESIAN_POINT ( 'NONE',  ( 18.59999999999999787, -9.523946312306552642, -174.3820279953382624 ) ) ;
#137333=CARTESIAN_POINT ( 'NONE',  ( 21.05000000000000071, 6.344359042054848352, -133.9851443651061231 ) ) ;
#137342=ORIENTED_EDGE ( 'NONE', *, *, #108338, .T. ) ;
#137348=CIRCLE ( 'NONE', #4260, 12.87499999999999822 ) ;
#137351=CIRCLE ( 'NONE', #124910, 11.64999999999999325 ) ;
#137359=ORIENTED_EDGE ( 'NONE', *, *, #175404, .F. ) ;
#137379=ORIENTED_EDGE ( 'NONE', *, *, #158573, .T. ) ;
#137395=EDGE_LOOP ( 'NONE', ( #35747, #130935, #130538, #228961 ) ) ;
#137427=FACE_OUTER_BOUND ( 'NONE', #206591, .T. ) ;
#137438=DIRECTION ( 'NONE',  ( 0.000000000000000000, 0.000000000000000000, -1.000000000000000000 ) ) ;
#137456=VECTOR ( 'NONE', #164166, 1000.000000000000000 ) ;
#137459=EDGE_CURVE ( 'NONE', #29064, #231902, #45598, .T. ) ;
#137461=EDGE_CURVE ( 'NONE', #3992, #152770, #200981, .T. ) ;
#137468=ORIENTED_EDGE ( 'NONE', *, *, #178797, .F. ) ;
#137470=CARTESIAN_POINT ( 'NONE',  ( -22.50000000000000000, 1.115600667400684642E-11, -122.3504291924552234 ) ) ;
#137471=CYLINDRICAL_SURFACE ( 'NONE', #155227, 11.80000000000000426 ) ;
#137505=DIRECTION ( 'NONE',  ( -1.000000000000000000, 0.000000000000000000, 0.000000000000000000 ) ) ;
#137510=EDGE_LOOP ( 'NONE', ( #86785, #98064, #104763, #45096 ) ) ;
#137512=CARTESIAN_POINT ( 'NONE',  ( 21.05000000000000071, 8.776282895303632259, -142.4880007215843705 ) ) ;
#137540=AXIS2_PLACEMENT_3D ( 'NONE', #136850, #15661, #178585 ) ;
#137561=FACE_BOUND ( 'NONE', #83724, .T. ) ;
#137587=CIRCLE ( 'NONE', #121083, 0.09999999999999864553 ) ;
#137609=VERTEX_POINT ( 'NONE', #76694 ) ;
#137625=VECTOR ( 'NONE', #183061, 999.9999999999998863 ) ;
#137663=CARTESIAN_POINT ( 'NONE',  ( -20.95000000000000639, 11.75000000001115019, -160.7161343370219129 ) ) ;
#137664=AXIS2_PLACEMENT_3D ( 'NONE', #220990, #26681, #166208 ) ;
#137680=ORIENTED_EDGE ( 'NONE', *, *, #225763, .F. ) ;
#137699=CARTESIAN_POINT ( 'NONE',  ( 20.94999999999999574, -1.249999999988843369, -142.0000000000000284 ) ) ;
#137714=VERTEX_POINT ( 'NONE', #28323 ) ;
#137783=FACE_OUTER_BOUND ( 'NONE', #135056, .T. ) ;
#137817=DIRECTION ( 'NONE',  ( 1.000000000000000000, 0.000000000000000000, 0.000000000000000000 ) ) ;
#137841=ORIENTED_EDGE ( 'NONE', *, *, #176201, .F. ) ;
#137847=DIRECTION ( 'NONE',  ( 0.000000000000000000, -1.000000000000000000, 0.000000000000000000 ) ) ;
#137857=TOROIDAL_SURFACE ( 'NONE', #250302, 0.2000000000000000111, 0.1000000000000000056 ) ;
#137863=FACE_OUTER_BOUND ( 'NONE', #246794, .T. ) ;
#137885=CIRCLE ( 'NONE', #162883, 0.09999999999999939493 ) ;
#137919=DIRECTION ( 'NONE',  ( 0.000000000000000000, 0.000000000000000000, -1.000000000000000000 ) ) ;
#137926=EDGE_CURVE ( 'NONE', #241225, #129556, #51284, .T. ) ;
#137939=CARTESIAN_POINT ( 'NONE',  ( 20.95346350065193519, 8.887177249185651107, -142.5117319470354005 ) ) ;
#137956=CARTESIAN_POINT ( 'NONE',  ( 21.05000000000000071, -11.74999999998883560, -164.4000000000000057 ) ) ;
#137981=CARTESIAN_POINT ( 'NONE',  ( -20.64999999999999858, 1.115600667400684642E-11, -167.5000000000000284 ) ) ;
#137986=DIRECTION ( 'NONE',  ( 0.000000000000000000, 0.000000000000000000, -1.000000000000000000 ) ) ;
#137992=CIRCLE ( 'NONE', #225476, 11.75000000000001066 ) ;
#138029=TOROIDAL_SURFACE ( 'NONE', #21534, 0.2000000000000000111, 0.1000000000000000056 ) ;
#138050=ORIENTED_EDGE ( 'NONE', *, *, #126729, .F. ) ;
#138069=ORIENTED_EDGE ( 'NONE', *, *, #209218, .T. ) ;
#138083=DIRECTION ( 'NONE',  ( 0.000000000000000000, 0.000000000000000000, -1.000000000000000000 ) ) ;
#138103=ORIENTED_EDGE ( 'NONE', *, *, #18445, .F. ) ;
#138115=DIRECTION ( 'NONE',  ( 0.000000000000000000, -6.938893903907222067E-15, -1.000000000000000000 ) ) ;
#138126=CARTESIAN_POINT ( 'NONE',  ( -22.57320508075686405, 11.75000000001115552, -134.0000000000000568 ) ) ;
#138170=FACE_OUTER_BOUND ( 'NONE', #3178, .T. ) ;
#138186=DIRECTION ( 'NONE',  ( -1.000000000000000000, 0.000000000000000000, 0.000000000000000000 ) ) ;
#138207=EDGE_LOOP ( 'NONE', ( #92550, #89343, #67582, #204971 ) ) ;
#138208=CYLINDRICAL_SURFACE ( 'NONE', #16533, 0.09999999999999939493 ) ;
#138211=VECTOR ( 'NONE', #229245, 1000.000000000000000 ) ;
#138251=CARTESIAN_POINT ( 'NONE',  ( 20.85882249326303040, 10.33248238083634796, -173.0948465439131496 ) ) ;
#138286=CIRCLE ( 'NONE', #130108, 0.09999999999999864553 ) ;
#138294=CARTESIAN_POINT ( 'NONE',  ( 20.94999999999999929, 5.850000000011160495, -157.3675027757221017 ) ) ;
#138301=AXIS2_PLACEMENT_3D ( 'NONE', #254263, #193039, #156508 ) ;
#138307=CYLINDRICAL_SURFACE ( 'NONE', #162366, 12.87499999999999822 ) ;
#138315=CIRCLE ( 'NONE', #96804, 12.97499999999998721 ) ;
#138316=ORIENTED_EDGE ( 'NONE', *, *, #221842, .F. ) ;
#138358=ORIENTED_EDGE ( 'NONE', *, *, #52296, .F. ) ;
#138419=CARTESIAN_POINT ( 'NONE',  ( -21.64999999999999858, 7.350000000011155166, -155.1500000000000057 ) ) ;
#138433=ADVANCED_FACE ( 'NONE', ( #59057 ), #121658, .F. ) ;
#138440=FACE_OUTER_BOUND ( 'NONE', #115829, .T. ) ;
#138446=CARTESIAN_POINT ( 'NONE',  ( 21.05000000000000071, 11.75000000001116263, -160.4851942293460638 ) ) ;
#138466=AXIS2_PLACEMENT_3D ( 'NONE', #28894, #150098, #247887 ) ;
#138469=ORIENTED_EDGE ( 'NONE', *, *, #134047, .T. ) ;
#138477=CARTESIAN_POINT ( 'NONE',  ( -22.39999999999999858, 7.790779598384560245, -133.9000000000000057 ) ) ;
#138515=ADVANCED_FACE ( 'NONE', ( #104601 ), #34776, .F. ) ;
#138571=DIRECTION ( 'NONE',  ( 1.000000000000000000, 0.000000000000000000, 0.000000000000000000 ) ) ;
#138586=EDGE_CURVE ( 'NONE', #206051, #147657, #76742, .T. ) ;
#138599=DIRECTION ( 'NONE',  ( 1.000000000000000000, -0.000000000000000000, -0.000000000000000000 ) ) ;
#138612=ORIENTED_EDGE ( 'NONE', *, *, #43939, .F. ) ;
#138626=EDGE_LOOP ( 'NONE', ( #180775, #181015, #70516, #18623 ) ) ;
#138633=CARTESIAN_POINT ( 'NONE',  ( 20.94999999999999929, 6.650000000011155876, -146.1500000000000341 ) ) ;
#138634=ORIENTED_EDGE ( 'NONE', *, *, #117263, .F. ) ;
#138647=ORIENTED_EDGE ( 'NONE', *, *, #152465, .T. ) ;
#138664=DIRECTION ( 'NONE',  ( -1.000000000000000000, 0.000000000000000000, 0.000000000000000000 ) ) ;
#138727=ORIENTED_EDGE ( 'NONE', *, *, #202565, .F. ) ;
#138731=DIRECTION ( 'NONE',  ( 0.000000000000000000, 1.000000000000000000, 0.000000000000000000 ) ) ;
#138739=DIRECTION ( 'NONE',  ( 0.000000000000000000, 0.000000000000000000, -1.000000000000000000 ) ) ;
#138771=VECTOR ( 'NONE', #204677, 1000.000000000000000 ) ;
#138782=CARTESIAN_POINT ( 'NONE',  ( 21.14999999999999503, 1.115600667400684642E-11, -127.7500000000000284 ) ) ;
#138790=VECTOR ( 'NONE', #80547, 1000.000000000000114 ) ;
#138813=EDGE_CURVE ( 'NONE', #198298, #220754, #141845, .T. ) ;
#138820=DIRECTION ( 'NONE',  ( 0.000000000000000000, 0.000000000000000000, 1.000000000000000000 ) ) ;
#138846=EDGE_CURVE ( 'NONE', #154130, #199909, #226499, .T. ) ;
#138849=ORIENTED_EDGE ( 'NONE', *, *, #236277, .T. ) ;
#138851=CIRCLE ( 'NONE', #72273, 0.09999999999999484301 ) ;
#138861=DIRECTION ( 'NONE',  ( -0.000000000000000000, 0.000000000000000000, -1.000000000000000000 ) ) ;
#138896=VERTEX_POINT ( 'NONE', #163996 ) ;
#138952=AXIS2_PLACEMENT_3D ( 'NONE', #164027, #101426, #6216 ) ;
#138955=ORIENTED_EDGE ( 'NONE', *, *, #242384, .F. ) ;
#138990=ORIENTED_EDGE ( 'NONE', *, *, #55536, .T. ) ;
#139021=EDGE_LOOP ( 'NONE', ( #230989, #246361, #38376, #128380 ) ) ;
#139040=AXIS2_PLACEMENT_3D ( 'NONE', #121054, #101401, #179725 ) ;
#139054=CARTESIAN_POINT ( 'NONE',  ( -18.46093223321780030, -9.480682968263337784, -141.0845505139267004 ) ) ;
#139056=ORIENTED_EDGE ( 'NONE', *, *, #176783, .T. ) ;
#139059=CIRCLE ( 'NONE', #14225, 4.149999999999987033 ) ;
#139072=CARTESIAN_POINT ( 'NONE',  ( 20.94999999999999574, -11.48912529306490349, -137.1000000000000227 ) ) ;
#139075=DIRECTION ( 'NONE',  ( 0.000000000000000000, 0.7397360091702755991, -0.6728971962616832059 ) ) ;
#139100=CARTESIAN_POINT ( 'NONE',  ( 22.00411653962158809, 7.253442868381323017, -133.9009618942314432 ) ) ;
#139122=VECTOR ( 'NONE', #99264, 1000.000000000000114 ) ;
#139138=DIRECTION ( 'NONE',  ( 0.000000000000000000, 0.000000000000000000, -1.000000000000000000 ) ) ;
#139142=LINE ( 'NONE', #218690, #103843 ) ;
#139164=ADVANCED_FACE ( 'NONE', ( #59399 ), #226638, .T. ) ;
#139167=DIRECTION ( 'NONE',  ( -1.000000000000000000, -0.000000000000000000, 0.000000000000000000 ) ) ;
#139185=DIRECTION ( 'NONE',  ( 0.000000000000000000, 0.4999999999999348299, -0.8660254037844762331 ) ) ;
#139239=AXIS2_PLACEMENT_3D ( 'NONE', #89580, #184832, #209543 ) ;
#139263=CARTESIAN_POINT ( 'NONE',  ( 22.39999999999999503, 11.75000000001115552, -133.9000000000000057 ) ) ;
#139276=CARTESIAN_POINT ( 'NONE',  ( 20.85000000000000142, -11.74999999998883560, -164.6000000000000227 ) ) ;
#139278=( BOUNDED_CURVE ( )  B_SPLINE_CURVE ( 3, ( #179517, #154825, #119540, #59511 ),
 .UNSPECIFIED., .F., .T. ) 
 B_SPLINE_CURVE_WITH_KNOTS ( ( 4, 4 ),
 ( 3.192897208853993529, 4.712388980384689674 ),
 .UNSPECIFIED. ) 
 CURVE ( )  GEOMETRIC_REPRESENTATION_ITEM ( )  RATIONAL_B_SPLINE_CURVE ( ( 1.000000000000000000, 0.8166740347213228279, 0.8166740347213228279, 1.000000000000000000 ) ) 
 REPRESENTATION_ITEM ( '' )  );
#139289=FACE_OUTER_BOUND ( 'NONE', #250674, .T. ) ;
#139329=AXIS2_PLACEMENT_3D ( 'NONE', #108384, #49685, #210061 ) ;
#139450=DIRECTION ( 'NONE',  ( 2.952720810173289112E-16, -1.000000000000000000, -0.000000000000000000 ) ) ;
#139476=EDGE_CURVE ( 'NONE', #28264, #99799, #252189, .T. ) ;
#139520=DIRECTION ( 'NONE',  ( 0.000000000000000000, 0.000000000000000000, 1.000000000000000000 ) ) ;
#139581=EDGE_CURVE ( 'NONE', #131063, #169539, #130399, .T. ) ;
#139588=ORIENTED_EDGE ( 'NONE', *, *, #253676, .T. ) ;
#139630=ORIENTED_EDGE ( 'NONE', *, *, #110613, .F. ) ;
#139634=ORIENTED_EDGE ( 'NONE', *, *, #101478, .T. ) ;
#139646=VERTEX_POINT ( 'NONE', #77398 ) ;
#139653=CARTESIAN_POINT ( 'NONE',  ( 21.14999999999999858, 11.65000000001116298, -146.1500000000000341 ) ) ;
#139686=VERTEX_POINT ( 'NONE', #215631 ) ;
#139740=CARTESIAN_POINT ( 'NONE',  ( 23.25000000000000000, -11.64999999998883595, -122.2500000000000284 ) ) ;
#139753=VECTOR ( 'NONE', #78521, 1000.000000000000000 ) ;
#139769=CARTESIAN_POINT ( 'NONE',  ( -21.05000000000000071, -1.851028230129704522, -145.6539132694225032 ) ) ;
#139786=COLOUR_RGB ( '', 0.09019608, 0.27058824, 0.51372549) ;
#139789=CARTESIAN_POINT ( 'NONE',  ( 23.14999999999999147, 1.115600667400684642E-11, -134.0000000000000000 ) ) ;
#139865=DIRECTION ( 'NONE',  ( 1.000000000000000000, 0.000000000000000000, 0.000000000000000000 ) ) ;
#139876=ORIENTED_EDGE ( 'NONE', *, *, #101079, .T. ) ;
#139887=ORIENTED_EDGE ( 'NONE', *, *, #78337, .F. ) ;
#139891=TOROIDAL_SURFACE ( 'NONE', #219020, 4.149999999999999467, 0.1000000000000000056 ) ;
#139918=ADVANCED_FACE ( 'NONE', ( #124180 ), #162030, .T. ) ;
#139939=DIRECTION ( 'NONE',  ( 1.000000000000000000, 0.000000000000000000, 0.000000000000000000 ) ) ;
#139955=ADVANCED_FACE ( 'NONE', ( #53616 ), #10640, .F. ) ;
#139967=AXIS2_PLACEMENT_3D ( 'NONE', #169704, #190532, #95251 ) ;
#139986=ADVANCED_FACE ( 'NONE', ( #150165 ), #108454, .F. ) ;
#139989=CARTESIAN_POINT ( 'NONE',  ( -21.00250684356850073, 11.75000000001115197, -141.0148057687580092 ) ) ;
#139991=AXIS2_PLACEMENT_3D ( 'NONE', #23005, #82911, #127213 ) ;
#140001=ORIENTED_EDGE ( 'NONE', *, *, #23417, .F. ) ;
#140037=CARTESIAN_POINT ( 'NONE',  ( 23.24999999999999645, 1.115600667400684642E-11, -134.0000000000000000 ) ) ;
#140041=ORIENTED_EDGE ( 'NONE', *, *, #211974, .F. ) ;
#140048=CARTESIAN_POINT ( 'NONE',  ( -20.85000000000000142, -11.74999999998884448, -167.5000000000000000 ) ) ;
#140054=CARTESIAN_POINT ( 'NONE',  ( -23.25000000000000000, -8.596261682231835621, -143.4501275171502925 ) ) ;
#140059=DIRECTION ( 'NONE',  ( 0.000000000000000000, 0.000000000000000000, -1.000000000000000000 ) ) ;
#140084=DIRECTION ( 'NONE',  ( 0.000000000000000000, -7.993605777301079759E-15, 1.000000000000000000 ) ) ;
#140119=CARTESIAN_POINT ( 'NONE',  ( -20.94999999999999929, 7.021664781911246322, -171.3335654018973173 ) ) ;
#140125=DIRECTION ( 'NONE',  ( 1.000000000000000000, 1.875376730785737719E-16, 0.000000000000000000 ) ) ;
#140128=EDGE_CURVE ( 'NONE', #70299, #173723, #36651, .T. ) ;
#140134=CARTESIAN_POINT ( 'NONE',  ( 20.94999999999999929, 1.835341550235569663, -145.5551512925629822 ) ) ;
#140146=CYLINDRICAL_SURFACE ( 'NONE', #35088, 0.09999999999999939493 ) ;
#140158=AXIS2_PLACEMENT_3D ( 'NONE', #104859, #184436, #137919 ) ;
#140176=VERTEX_POINT ( 'NONE', #217794 ) ;
#140203=CARTESIAN_POINT ( 'NONE',  ( 21.05000000000000071, 1.115653327213047955E-11, -138.3000000000000398 ) ) ;
#140206=AXIS2_PLACEMENT_3D ( 'NONE', #229833, #129452, #169911 ) ;
#140209=DIRECTION ( 'NONE',  ( 1.000000000000000000, -0.000000000000000000, -0.000000000000000000 ) ) ;
#140216=EDGE_CURVE ( 'NONE', #175804, #47883, #226613, .T. ) ;
#140279=VERTEX_POINT ( 'NONE', #140861 ) ;
#140311=CARTESIAN_POINT ( 'NONE',  ( 18.59999999999999076, 1.835341550235567887, -145.5551512925629822 ) ) ;
#140320=CARTESIAN_POINT ( 'NONE',  ( 21.97500000000000497, 9.750000000011153745, -146.2500000000000568 ) ) ;
#140365=CARTESIAN_POINT ( 'NONE',  ( -21.65000000000000213, 7.750000000011155521, -146.3500000000000227 ) ) ;
#140367=EDGE_LOOP ( 'NONE', ( #35423, #131910, #20172, #204952 ) ) ;
#140379=CARTESIAN_POINT ( 'NONE',  ( -20.54999999999999716, -8.663551401858004652, -143.5241011180673070 ) ) ;
#140391=ORIENTED_EDGE ( 'NONE', *, *, #256074, .T. ) ;
#140406=DIRECTION ( 'NONE',  ( 0.000000000000000000, 2.891205793294679805E-16, -1.000000000000000000 ) ) ;
#140411=FACE_OUTER_BOUND ( 'NONE', #243875, .T. ) ;
#140417=VERTEX_POINT ( 'NONE', #89852 ) ;
#140430=ADVANCED_FACE ( 'NONE', ( #187703 ), #168165, .T. ) ;
#140434=ORIENTED_EDGE ( 'NONE', *, *, #211974, .T. ) ;
#140455=DIRECTION ( 'NONE',  ( -0.000000000000000000, -0.000000000000000000, 1.000000000000000000 ) ) ;
#140475=DIRECTION ( 'NONE',  ( 0.000000000000000000, 0.000000000000000000, -1.000000000000000000 ) ) ;
#140496=AXIS2_PLACEMENT_3D ( 'NONE', #24343, #77861, #58291 ) ;
#140500=CIRCLE ( 'NONE', #173900, 0.09999999999999749367 ) ;
#140532=ORIENTED_EDGE ( 'NONE', *, *, #40936, .F. ) ;
#140569=VERTEX_POINT ( 'NONE', #159798 ) ;
#140584=EDGE_LOOP ( 'NONE', ( #169890, #257862, #15851, #222762 ) ) ;
#140588=AXIS2_PLACEMENT_3D ( 'NONE', #133639, #213170, #29450 ) ;
#140617=EDGE_CURVE ( 'NONE', #249928, #222594, #89432, .T. ) ;
#140640=AXIS2_PLACEMENT_3D ( 'NONE', #217377, #40075, #195296 ) ;
#140650=CARTESIAN_POINT ( 'NONE',  ( 21.05000000000000071, 1.115600667400684642E-11, -146.9749999999999943 ) ) ;
#140653=CARTESIAN_POINT ( 'NONE',  ( -21.05000000000000071, 1.115600667400684642E-11, -155.7000000000000455 ) ) ;
#140661=EDGE_CURVE ( 'NONE', #244782, #155996, #13558, .T. ) ;
#140662=CARTESIAN_POINT ( 'NONE',  ( 23.14999999999999147, 1.115600667400684642E-11, -134.0000000000000000 ) ) ;
#140690=DIRECTION ( 'NONE',  ( 0.000000000000000000, 0.000000000000000000, -1.000000000000000000 ) ) ;
#140694=DIRECTION ( 'NONE',  ( -1.000000000000000000, -2.952720810173289112E-16, 0.000000000000000000 ) ) ;
#140768=DIRECTION ( 'NONE',  ( -0.000000000000000000, 0.1298341882520022694, 0.9915357197604853789 ) ) ;
#140805=ADVANCED_FACE ( 'NONE', ( #160793 ), #218408, .F. ) ;
#140821=ORIENTED_EDGE ( 'NONE', *, *, #52932, .F. ) ;
#140831=FACE_OUTER_BOUND ( 'NONE', #130015, .T. ) ;
#140838=VERTEX_POINT ( 'NONE', #385 ) ;
#140861=CARTESIAN_POINT ( 'NONE',  ( 18.59999999999997655, 1.115600667400684642E-11, -175.4000000000000341 ) ) ;
#140944=VERTEX_POINT ( 'NONE', #17401 ) ;
#140965=ORIENTED_EDGE ( 'NONE', *, *, #97142, .F. ) ;
#140985=CYLINDRICAL_SURFACE ( 'NONE', #2340, 0.09999999999999892308 ) ;
#140986=FACE_OUTER_BOUND ( 'NONE', #153532, .T. ) ;
#140993=ADVANCED_FACE ( 'NONE', ( #143753 ), #227147, .T. ) ;
#141003=DIRECTION ( 'NONE',  ( 0.000000000000000000, 0.9887567792719341719, -0.1495327102803664099 ) ) ;
#141036=CARTESIAN_POINT ( 'NONE',  ( 21.05000000000000071, 1.115600667400684642E-11, -134.1000000000000227 ) ) ;
#141072=CARTESIAN_POINT ( 'NONE',  ( -22.46246831459151494, 0.02191216695058596786, -122.3501354387900619 ) ) ;
#141078=CARTESIAN_POINT ( 'NONE',  ( 21.05000000000000071, 10.62950747927168216, -141.6279793999966898 ) ) ;
#141085=DIRECTION ( 'NONE',  ( -1.000000000000000000, 0.000000000000000000, 0.000000000000000000 ) ) ;
#141125=ADVANCED_FACE ( 'NONE', ( #129334 ), #253122, .F. ) ;
#141128=CARTESIAN_POINT ( 'NONE',  ( 20.94999999999999929, 11.75000000001115552, -160.7161343370219413 ) ) ;
#141160=CARTESIAN_POINT ( 'NONE',  ( -20.54999999999999716, 2.000000000011154189, -154.6753780772379514 ) ) ;
#141161=CARTESIAN_POINT ( 'NONE',  ( -21.98333005346336932, 1.115600667400684642E-11, -126.6259246709433626 ) ) ;
#141172=DIRECTION ( 'NONE',  ( -1.000000000000000000, -0.000000000000000000, -0.000000000000000000 ) ) ;
#141173=DIRECTION ( 'NONE',  ( -1.000000000000000000, 0.000000000000000000, -0.000000000000000000 ) ) ;
#141201=AXIS2_PLACEMENT_3D ( 'NONE', #55734, #14101, #136574 ) ;
#141213=ORIENTED_EDGE ( 'NONE', *, *, #238851, .T. ) ;
#141251=EDGE_CURVE ( 'NONE', #175518, #217669, #238712, .T. ) ;
#141257=EDGE_CURVE ( 'NONE', #221635, #58706, #10706, .T. ) ;
#141259=ORIENTED_EDGE ( 'NONE', *, *, #2188, .F. ) ;
#141295=VERTEX_POINT ( 'NONE', #182607 ) ;
#141327=ORIENTED_EDGE ( 'NONE', *, *, #36981, .F. ) ;
#141331=FACE_OUTER_BOUND ( 'NONE', #226733, .T. ) ;
#141400=ORIENTED_EDGE ( 'NONE', *, *, #87414, .F. ) ;
#141449=CIRCLE ( 'NONE', #212393, 12.87499999999999822 ) ;
#141454=AXIS2_PLACEMENT_3D ( 'NONE', #202992, #239565, #85574 ) ;
#141463=DIRECTION ( 'NONE',  ( 0.000000000000000000, 0.9908441862701782288, -0.1350103645450542456 ) ) ;
#141468=FACE_BOUND ( 'NONE', #197243, .T. ) ;
#141490=VERTEX_POINT ( 'NONE', #208593 ) ;
#141516=VERTEX_POINT ( 'NONE', #11674 ) ;
#141570=DIRECTION ( 'NONE',  ( 0.000000000000000000, 0.000000000000000000, -1.000000000000000000 ) ) ;
#141604=CARTESIAN_POINT ( 'NONE',  ( 20.95420533658165141, 10.54586447477073285, -141.5675060206932585 ) ) ;
#141616=DIRECTION ( 'NONE',  ( 0.000000000000000000, -0.8700118002898321601, 0.4930308989875230030 ) ) ;
#141621=DIRECTION ( 'NONE',  ( 0.000000000000000000, 2.664535259100315349E-15, -1.000000000000000000 ) ) ;
#141644=CIRCLE ( 'NONE', #75052, 0.1999999999999987899 ) ;
#141653=PLANE ( 'NONE',  #224254 ) ;
#141711=ORIENTED_EDGE ( 'NONE', *, *, #232215, .F. ) ;
#141724=DIRECTION ( 'NONE',  ( 9.044546369203339308E-15, -0.7397360091702694929, -0.6728971962616898672 ) ) ;
#141728=DIRECTION ( 'NONE',  ( 1.000000000000000000, 0.000000000000000000, 0.000000000000000000 ) ) ;
#141729=CARTESIAN_POINT ( 'NONE',  ( 20.94999999999999929, 1.115600667400684642E-11, -175.3000000000000398 ) ) ;
#141734=AXIS2_PLACEMENT_3D ( 'NONE', #109693, #230965, #250491 ) ;
#141737=CARTESIAN_POINT ( 'NONE',  ( 20.94999999999999574, 1.115600667400684642E-11, -134.0000000000000000 ) ) ;
#141773=FACE_OUTER_BOUND ( 'NONE', #23935, .T. ) ;
#141776=AXIS2_PLACEMENT_3D ( 'NONE', #67073, #240570, #141463 ) ;
#141804=DIRECTION ( 'NONE',  ( 1.836970198721029934E-16, -1.000000000000000000, -0.000000000000000000 ) ) ;
#141813=CARTESIAN_POINT ( 'NONE',  ( 23.24999999999999289, 6.450000000011156587, -155.1500000000000057 ) ) ;
#141845=LINE ( 'NONE', #200543, #255641 ) ;
#141899=CARTESIAN_POINT ( 'NONE',  ( -18.43707690579161351, -9.682403433465241349, -174.1568433774128266 ) ) ;
#141906=EDGE_LOOP ( 'NONE', ( #122118, #133372, #115652, #76526 ) ) ;
#141924=EDGE_LOOP ( 'NONE', ( #182540, #16053, #234974, #140391 ) ) ;
#141971=VECTOR ( 'NONE', #6792, 1000.000000000000000 ) ;
#141987=CARTESIAN_POINT ( 'NONE',  ( -22.50000000000000000, 11.64987090377452361, -133.9174801091271263 ) ) ;
#142119=CARTESIAN_POINT ( 'NONE',  ( 20.92356734117541706, 10.31973158071402175, -173.0505334713354841 ) ) ;
#142163=B_SPLINE_CURVE_WITH_KNOTS ( 'NONE', 3,
 ( #124173, #184117, #141161, #203698 ),
 .UNSPECIFIED., .F., .F.,
 ( 4, 4 ),
 ( 0.000000000000000000, 0.001767853679387123601 ),
 .UNSPECIFIED. ) ;
#142216=VERTEX_POINT ( 'NONE', #134494 ) ;
#142256=DIRECTION ( 'NONE',  ( 0.000000000000000000, 0.000000000000000000, 1.000000000000000000 ) ) ;
#142257=VECTOR ( 'NONE', #71135, 1000.000000000000000 ) ;
#142270=DIRECTION ( 'NONE',  ( 2.952720810173288619E-16, -1.000000000000000000, 0.000000000000000000 ) ) ;
#142324=CIRCLE ( 'NONE', #208969, 6.329289321881370611 ) ;
#142346=CARTESIAN_POINT ( 'NONE',  ( -18.58671080940901277, -9.406932858815459042, -141.1241544649047910 ) ) ;
#142379=CARTESIAN_POINT ( 'NONE',  ( -23.15000000000000213, 11.65000000001115588, -122.2500000000000284 ) ) ;
#142381=ORIENTED_EDGE ( 'NONE', *, *, #123869, .F. ) ;
#142388=ADVANCED_FACE ( 'NONE', ( #195802 ), #238756, .T. ) ;
#142404=EDGE_CURVE ( 'NONE', #13799, #208746, #40591, .T. ) ;
#142465=CIRCLE ( 'NONE', #54967, 0.9750000000000036415 ) ;
#142484=VERTEX_POINT ( 'NONE', #243877 ) ;
#142494=DIRECTION ( 'NONE',  ( 0.000000000000000000, 0.6728971962617388280, -0.7397360091702248619 ) ) ;
#142506=TOROIDAL_SURFACE ( 'NONE', #30125, 1.900000000000002576, 0.1000000000000000056 ) ;
#142535=CIRCLE ( 'NONE', #30156, 0.5000000000000004441 ) ;
#142538=DIRECTION ( 'NONE',  ( 1.000000000000000000, 0.000000000000000000, 0.000000000000000000 ) ) ;
#142539=CARTESIAN_POINT ( 'NONE',  ( -20.00857864376270001, 9.150000000011157653, -146.3500000000000227 ) ) ;
#142555=ORIENTED_EDGE ( 'NONE', *, *, #165006, .F. ) ;
#142558=CARTESIAN_POINT ( 'NONE',  ( 20.54374330479337374, 10.50501031423420351, -141.7256836348881279 ) ) ;
#142566=CARTESIAN_POINT ( 'NONE',  ( 23.14999999999999503, 11.65000000001116298, -160.4851942293460922 ) ) ;
#142596=EDGE_CURVE ( 'NONE', #138896, #44452, #151219, .T. ) ;
#142638=AXIS2_PLACEMENT_3D ( 'NONE', #68821, #8836, #209603 ) ;
#142661=CYLINDRICAL_SURFACE ( 'NONE', #108645, 0.09999999999999939493 ) ;
#142664=CARTESIAN_POINT ( 'NONE',  ( 20.94999999999999574, 10.62357026049396680, -141.4919452032305855 ) ) ;
#142668=ORIENTED_EDGE ( 'NONE', *, *, #205273, .T. ) ;
#142677=AXIS2_PLACEMENT_3D ( 'NONE', #201651, #118276, #23046 ) ;
#142699=CARTESIAN_POINT ( 'NONE',  ( -23.15000000000000213, 4.250000000011156409, -155.1500000000000057 ) ) ;
#142751=FACE_OUTER_BOUND ( 'NONE', #133983, .T. ) ;
#142795=EDGE_LOOP ( 'NONE', ( #200875, #138469, #191340, #142854, #10505, #225985, #201484 ) ) ;
#142846=ORIENTED_EDGE ( 'NONE', *, *, #30230, .T. ) ;
#142854=ORIENTED_EDGE ( 'NONE', *, *, #166826, .T. ) ;
#142884=CIRCLE ( 'NONE', #97074, 0.09999999999999892308 ) ;
#142891=EDGE_LOOP ( 'NONE', ( #46288, #150453, #8880, #45426 ) ) ;
#142894=ADVANCED_FACE ( 'NONE', ( #217570 ), #220168, .T. ) ;
#142904=VERTEX_POINT ( 'NONE', #46635 ) ;
#142950=EDGE_CURVE ( 'NONE', #44801, #229458, #244001, .T. ) ;
#143006=FACE_BOUND ( 'NONE', #107692, .T. ) ;
#143034=CARTESIAN_POINT ( 'NONE',  ( 21.05000000000000071, 4.813084112160684214, -155.5584822434762202 ) ) ;
#143068=ORIENTED_EDGE ( 'NONE', *, *, #2542, .T. ) ;
#143085=CARTESIAN_POINT ( 'NONE',  ( 22.49436431346199683, 0.06690352973341695542, -122.3500490523465629 ) ) ;
#143100=AXIS2_PLACEMENT_3D ( 'NONE', #221391, #166610, #244816 ) ;
#143184=DIRECTION ( 'NONE',  ( 0.000000000000000000, 0.000000000000000000, 1.000000000000000000 ) ) ;
#143185=CARTESIAN_POINT ( 'NONE',  ( 21.05000000000000071, 1.349084418638171412, -141.9864989635455004 ) ) ;
#143220=AXIS2_PLACEMENT_3D ( 'NONE', #100990, #102288, #18928 ) ;
#143249=CIRCLE ( 'NONE', #80696, 0.1000000000000106914 ) ;
#143261=ORIENTED_EDGE ( 'NONE', *, *, #233532, .F. ) ;
#143262=EDGE_CURVE ( 'NONE', #237217, #59718, #11643, .T. ) ;
#143287=CYLINDRICAL_SURFACE ( 'NONE', #71113, 0.09999999999999939493 ) ;
#143307=ORIENTED_EDGE ( 'NONE', *, *, #125868, .F. ) ;
#143320=DIRECTION ( 'NONE',  ( -1.000000000000000000, -0.000000000000000000, -0.000000000000000000 ) ) ;
#143334=CARTESIAN_POINT ( 'NONE',  ( -21.05000000000000071, -1.835341550213255957, -145.6551512925629766 ) ) ;
#143365=DIRECTION ( 'NONE',  ( 0.000000000000000000, -0.1568667991644693838, -0.9876197685951279004 ) ) ;
#143367=CYLINDRICAL_SURFACE ( 'NONE', #25137, 2.000000000000001776 ) ;
#143370=CARTESIAN_POINT ( 'NONE',  ( 21.00000000000000000, 9.750000000011153745, -155.1500000000000057 ) ) ;
#143377=LINE ( 'NONE', #2572, #76955 ) ;
#143423=VERTEX_POINT ( 'NONE', #166332 ) ;
#143461=VERTEX_POINT ( 'NONE', #150592 ) ;
#143464=ADVANCED_FACE ( 'NONE', ( #146702 ), #206706, .T. ) ;
#143481=CIRCLE ( 'NONE', #47779, 0.09999999999998898659 ) ;
#143533=CARTESIAN_POINT ( 'NONE',  ( -20.94999999999999929, 1.115649653272650466E-11, -171.5000000000000284 ) ) ;
#143555=AXIS2_PLACEMENT_3D ( 'NONE', #16695, #32429, #194054 ) ;
#143578=VECTOR ( 'NONE', #56215, 1000.000000000000114 ) ;
#143622=DIRECTION ( 'NONE',  ( -0.000000000000000000, 0.000000000000000000, 1.000000000000000000 ) ) ;
#143627=DIRECTION ( 'NONE',  ( 0.000000000000000000, 0.000000000000000000, -1.000000000000000000 ) ) ;
#143628=DIRECTION ( 'NONE',  ( 0.000000000000000000, -1.000000000000000000, 0.000000000000000000 ) ) ;
#143631=CARTESIAN_POINT ( 'NONE',  ( 21.05000000000000071, 10.60832956796513216, -141.5916850132954039 ) ) ;
#143656=ORIENTED_EDGE ( 'NONE', *, *, #247152, .F. ) ;
#143729=CARTESIAN_POINT ( 'NONE',  ( 21.14999999999999858, 10.71339244341104013, -146.2500000000000568 ) ) ;
#143730=ORIENTED_EDGE ( 'NONE', *, *, #225924, .F. ) ;
#143753=FACE_OUTER_BOUND ( 'NONE', #162051, .T. ) ;
#143808=CARTESIAN_POINT ( 'NONE',  ( 23.15000000000000213, -11.64999999998883595, -164.4000000000000057 ) ) ;
#143835=CIRCLE ( 'NONE', #31465, 0.09999999999999939493 ) ;
#143836=LINE ( 'NONE', #44760, #182234 ) ;
#143839=LINE ( 'NONE', #99562, #99253 ) ;
#143853=DIRECTION ( 'NONE',  ( 0.000000000000000000, 0.000000000000000000, -1.000000000000000000 ) ) ;
#143865=ORIENTED_EDGE ( 'NONE', *, *, #140661, .F. ) ;
#143871=LINE ( 'NONE', #145150, #99595 ) ;
#143877=DIRECTION ( 'NONE',  ( 0.000000000000000000, 0.000000000000000000, -1.000000000000000000 ) ) ;
#143904=CARTESIAN_POINT ( 'NONE',  ( -18.50000000000000000, 11.65000000001115588, -167.5000000000000284 ) ) ;
#143918=ORIENTED_EDGE ( 'NONE', *, *, #762, .F. ) ;
#143988=ORIENTED_EDGE ( 'NONE', *, *, #69646, .T. ) ;
#144021=DIRECTION ( 'NONE',  ( 0.000000000000000000, 0.000000000000000000, 1.000000000000000000 ) ) ;
#144023=LINE ( 'NONE', #245710, #166772 ) ;
#144027=CARTESIAN_POINT ( 'NONE',  ( -20.54999999999999716, 1.940186915899004161, -154.6708807889467039 ) ) ;
#144037=AXIS2_PLACEMENT_3D ( 'NONE', #85093, #42167, #241637 ) ;
#144143=LINE ( 'NONE', #47610, #179757 ) ;
#144158=DIRECTION ( 'NONE',  ( -0.000000000000000000, 1.000000000000000000, 0.000000000000000000 ) ) ;
#144194=EDGE_LOOP ( 'NONE', ( #21694, #48821, #45706 ) ) ;
#144202=DIRECTION ( 'NONE',  ( 0.7071067811865475727, -0.7071067811865475727, 0.000000000000000000 ) ) ;
#144225=FACE_OUTER_BOUND ( 'NONE', #238683, .T. ) ;
#144233=DIRECTION ( 'NONE',  ( 0.000000000000000000, 0.000000000000000000, -1.000000000000000000 ) ) ;
#144247=CARTESIAN_POINT ( 'NONE',  ( 21.30000000000002558, 1.115600667400684642E-11, -134.0000000000000000 ) ) ;
#144255=CARTESIAN_POINT ( 'NONE',  ( -20.54999999999999716, -8.999999999988844479, -158.0060308773475981 ) ) ;
#144259=DIRECTION ( 'NONE',  ( 0.000000000000000000, 0.000000000000000000, 1.000000000000000000 ) ) ;
#144261=DIRECTION ( 'NONE',  ( 0.000000000000000000, 0.000000000000000000, -1.000000000000000000 ) ) ;
#144262=CARTESIAN_POINT ( 'NONE',  ( 20.94999999999999574, 1.261786168576181755, -142.0864989635454947 ) ) ;
#144265=ORIENTED_EDGE ( 'NONE', *, *, #89732, .T. ) ;
#144268=EDGE_LOOP ( 'NONE', ( #13189, #9331, #213734 ) ) ;
#144285=ORIENTED_EDGE ( 'NONE', *, *, #188299, .T. ) ;
#144300=EDGE_CURVE ( 'NONE', #94122, #101205, #176878, .T. ) ;
#144301=ORIENTED_EDGE ( 'NONE', *, *, #81030, .T. ) ;
#144304=EDGE_LOOP ( 'NONE', ( #212606, #254401, #105610, #158562 ) ) ;
#144305=CARTESIAN_POINT ( 'NONE',  ( 18.59999999999999076, 6.550000000011156231, -155.1500000000000057 ) ) ;
#144327=CARTESIAN_POINT ( 'NONE',  ( -18.50000000000000000, 1.115600667400684642E-11, -167.5000000000000284 ) ) ;
#144342=CIRCLE ( 'NONE', #248434, 4.049999999999998046 ) ;
#144392=FACE_OUTER_BOUND ( 'NONE', #175379, .T. ) ;
#144406=AXIS2_PLACEMENT_3D ( 'NONE', #104674, #35175, #68156 ) ;
#144429=AXIS2_PLACEMENT_3D ( 'NONE', #53015, #92149, #171724 ) ;
#144441=CIRCLE ( 'NONE', #90284, 0.09999999999998715472 ) ;
#144444=VERTEX_POINT ( 'NONE', #131002 ) ;
#144453=AXIS2_PLACEMENT_3D ( 'NONE', #121786, #146444, #125614 ) ;
#144477=EDGE_CURVE ( 'NONE', #7471, #233607, #73993, .T. ) ;
#144518=FACE_OUTER_BOUND ( 'NONE', #26660, .T. ) ;
#144540=CARTESIAN_POINT ( 'NONE',  ( 20.84999999999999432, -1.164121893230052995, -175.4148480855716059 ) ) ;
#144556=VECTOR ( 'NONE', #185291, 1000.000000000000114 ) ;
#144563=CARTESIAN_POINT ( 'NONE',  ( -20.07928932188135107, 9.220710678129810489, -155.1500000000000057 ) ) ;
#144587=AXIS2_PLACEMENT_3D ( 'NONE', #79999, #157024, #236525 ) ;
#144622=DIRECTION ( 'NONE',  ( 0.000000000000000000, 0.000000000000000000, -1.000000000000000000 ) ) ;
#144628=AXIS2_PLACEMENT_3D ( 'NONE', #11856, #27583, #56067 ) ;
#144645=CARTESIAN_POINT ( 'NONE',  ( -21.93642651522410247, 7.327166239336959208, -134.0000000000000000 ) ) ;
#144646=ADVANCED_FACE ( 'NONE', ( #86403 ), #66876, .T. ) ;
#144653=SPHERICAL_SURFACE ( 'NONE', #240154, 0.1000000000000000056 ) ;
#144656=ORIENTED_EDGE ( 'NONE', *, *, #36589, .T. ) ;
#144661=CARTESIAN_POINT ( 'NONE',  ( 21.09107601085585415, 0.03930716472822039925, -127.6361220246393913 ) ) ;
#144662=DIRECTION ( 'NONE',  ( 0.000000000000000000, 0.000000000000000000, -1.000000000000000000 ) ) ;
#144664=LINE ( 'NONE', #246352, #189988 ) ;
#144666=CIRCLE ( 'NONE', #124412, 0.09999999999999158173 ) ;
#144673=DIRECTION ( 'NONE',  ( -0.000000000000000000, -0.000000000000000000, 1.000000000000000000 ) ) ;
#144687=DIRECTION ( 'NONE',  ( -1.000000000000000000, 0.000000000000000000, 0.000000000000000000 ) ) ;
#144757=ORIENTED_EDGE ( 'NONE', *, *, #54945, .F. ) ;
#144793=EDGE_CURVE ( 'NONE', #111920, #251883, #86580, .T. ) ;
#144796=FACE_OUTER_BOUND ( 'NONE', #136227, .T. ) ;
#144809=AXIS2_PLACEMENT_3D ( 'NONE', #214852, #36246, #152351 ) ;
#144821=EDGE_CURVE ( 'NONE', #257964, #175390, #119968, .T. ) ;
#144822=DIRECTION ( 'NONE',  ( 0.000000000000000000, -0.000000000000000000, -1.000000000000000000 ) ) ;
#144842=EDGE_LOOP ( 'NONE', ( #131498, #228137, #195681, #1423 ) ) ;
#144866=EDGE_CURVE ( 'NONE', #153155, #218074, #72025, .T. ) ;
#144900=DIRECTION ( 'NONE',  ( 0.000000000000000000, 0.000000000000000000, -1.000000000000000000 ) ) ;
#144917=CARTESIAN_POINT ( 'NONE',  ( -20.85000000000000142, -1.164121893230052995, -175.2148480855716173 ) ) ;
#144946=CARTESIAN_POINT ( 'NONE',  ( 20.99780126800918723, 11.60538868788781031, -160.5873525717055372 ) ) ;
#144963=ADVANCED_FACE ( 'NONE', ( #198377 ), #165750, .T. ) ;
#145031=EDGE_CURVE ( 'NONE', #205417, #107215, #204782, .T. ) ;
#145034=CIRCLE ( 'NONE', #65941, 0.09999999999999982514 ) ;
#145038=DIRECTION ( 'NONE',  ( 0.000000000000000000, 0.4999999999999478195, -0.8660254037844686836 ) ) ;
#145041=ORIENTED_EDGE ( 'NONE', *, *, #182328, .F. ) ;
#145050=ADVANCED_FACE ( 'NONE', ( #245223 ), #44458, .F. ) ;
#145062=DIRECTION ( 'NONE',  ( -0.000000000000000000, 1.000000000000000000, -0.000000000000000000 ) ) ;
#145073=AXIS2_PLACEMENT_3D ( 'NONE', #156555, #178686, #199518 ) ;
#145076=DIRECTION ( 'NONE',  ( 0.000000000000000000, 0.000000000000000000, -1.000000000000000000 ) ) ;
#145087=DIRECTION ( 'NONE',  ( 0.000000000000000000, 1.000000000000000000, 2.891205793294679805E-16 ) ) ;
#145102=CARTESIAN_POINT ( 'NONE',  ( 22.60000000000000142, 0.1008583691098682150, -122.2504328765106294 ) ) ;
#145107=DIRECTION ( 'NONE',  ( -0.000000000000000000, 1.000000000000000000, -0.000000000000000000 ) ) ;
#145122=CARTESIAN_POINT ( 'NONE',  ( 20.97217846901851956, 8.875441724720829484, -142.5012276839372305 ) ) ;
#145150=CARTESIAN_POINT ( 'NONE',  ( -20.64999999999999858, 4.250000000011156409, -146.2500000000000284 ) ) ;
#145159=LINE ( 'NONE', #164748, #168196 ) ;
#145167=AXIS2_PLACEMENT_3D ( 'NONE', #216442, #153964, #36571 ) ;
#145177=CARTESIAN_POINT ( 'NONE',  ( -22.50000000000000000, 1.115600667400684642E-11, -127.7500000000000284 ) ) ;
#145243=DIRECTION ( 'NONE',  ( -7.304098846218134667E-16, 1.000000000000000000, -0.000000000000000000 ) ) ;
#145265=EDGE_CURVE ( 'NONE', #91601, #96601, #211891, .T. ) ;
#145272=CARTESIAN_POINT ( 'NONE',  ( 20.99999999999997868, 1.115600667400684642E-11, -134.0000000000000000 ) ) ;
#145290=ORIENTED_EDGE ( 'NONE', *, *, #214153, .F. ) ;
#145297=AXIS2_PLACEMENT_3D ( 'NONE', #214409, #80008, #16248 ) ;
#145445=FACE_OUTER_BOUND ( 'NONE', #206083, .T. ) ;
#145470=EDGE_CURVE ( 'NONE', #160216, #135320, #3777, .T. ) ;
#145478=EDGE_CURVE ( 'NONE', #206061, #157661, #233987, .T. ) ;
#145483=AXIS2_PLACEMENT_3D ( 'NONE', #240583, #243148, #25407 ) ;
#145519=DIRECTION ( 'NONE',  ( -1.000000000000000000, 0.000000000000000000, 0.000000000000000000 ) ) ;
#145529=ORIENTED_EDGE ( 'NONE', *, *, #112389, .F. ) ;
#145539=AXIS2_PLACEMENT_3D ( 'NONE', #22066, #79434, #83272 ) ;
#145548=DIRECTION ( 'NONE',  ( 0.000000000000000000, 0.9908441862701782288, 0.1350103645450542456 ) ) ;
#145555=CIRCLE ( 'NONE', #66464, 0.1000000000000001860 ) ;
#145557=CARTESIAN_POINT ( 'NONE',  ( 22.47071067811864964, 0.09909245471376176839, -126.2799252555019649 ) ) ;
#145564=CARTESIAN_POINT ( 'NONE',  ( 20.85000000000000142, -1.736705739456431807, -179.0174225876237415 ) ) ;
#145571=PLANE ( 'NONE',  #114166 ) ;
#145580=CIRCLE ( 'NONE', #228989, 0.09999999999999939493 ) ;
#145590=DIRECTION ( 'NONE',  ( -0.000000000000000000, -0.000000000000000000, -1.000000000000000000 ) ) ;
#145607=DIRECTION ( 'NONE',  ( -1.000000000000000000, -0.000000000000000000, 0.000000000000000000 ) ) ;
#145618=EDGE_LOOP ( 'NONE', ( #65766, #79072, #116984, #133001 ) ) ;
#145630=DIRECTION ( 'NONE',  ( -1.000000000000000000, 0.000000000000000000, 0.000000000000000000 ) ) ;
#145669=VECTOR ( 'NONE', #70496, 999.9999999999998863 ) ;
#145672=DIRECTION ( 'NONE',  ( 1.000000000000000000, 7.304098846218134667E-16, 0.000000000000000000 ) ) ;
#145676=EDGE_CURVE ( 'NONE', #170589, #129684, #195338, .T. ) ;
#145682=CARTESIAN_POINT ( 'NONE',  ( 20.94999999999999929, 1.115600667400684642E-11, -167.5000000000000284 ) ) ;
#145734=CARTESIAN_POINT ( 'NONE',  ( -23.15000000000000213, 11.65000000001115588, -155.3500000000000227 ) ) ;
#145736=ORIENTED_EDGE ( 'NONE', *, *, #203050, .T. ) ;
#145764=DIRECTION ( 'NONE',  ( 0.000000000000000000, 0.1568667991644863147, 0.9876197685951252359 ) ) ;
#145778=CARTESIAN_POINT ( 'NONE',  ( -20.94999999999999929, 0.2561057921033771945, -133.9651035583277121 ) ) ;
#145784=AXIS2_PLACEMENT_3D ( 'NONE', #252066, #235085, #74761 ) ;
#145798=FACE_OUTER_BOUND ( 'NONE', #112006, .T. ) ;
#145800=FACE_OUTER_BOUND ( 'NONE', #4724, .T. ) ;
#145807=CARTESIAN_POINT ( 'NONE',  ( 21.05000000000000071, 5.850000000011105428, -144.1324972242779836 ) ) ;
#145819=ORIENTED_EDGE ( 'NONE', *, *, #111258, .T. ) ;
#145820=ORIENTED_EDGE ( 'NONE', *, *, #141251, .F. ) ;
#145824=DIRECTION ( 'NONE',  ( 0.000000000000000000, 0.000000000000000000, 1.000000000000000000 ) ) ;
#145865=ADVANCED_FACE ( 'NONE', ( #43510 ), #125600, .F. ) ;
#145875=EDGE_CURVE ( 'NONE', #4110, #131063, #143871, .T. ) ;
#145876=EDGE_LOOP ( 'NONE', ( #13713, #200218, #26307, #121273 ) ) ;
#145890=CARTESIAN_POINT ( 'NONE',  ( 21.05000000000000071, 1.115600667400684642E-11, -167.5000000000000284 ) ) ;
#145906=ADVANCED_FACE ( 'NONE', ( #188156 ), #5628, .F. ) ;
#145939=CYLINDRICAL_SURFACE ( 'NONE', #69291, 0.09999999999999939493 ) ;
#145946=CARTESIAN_POINT ( 'NONE',  ( 21.04999999999999716, 1.115141236730093910E-11, -127.4593430482987912 ) ) ;
#145961=CARTESIAN_POINT ( 'NONE',  ( -20.64999999999999858, 7.150000000011155876, -146.3500000000000227 ) ) ;
#145973=AXIS2_PLACEMENT_3D ( 'NONE', #128129, #148991, #46007 ) ;
#146020=DIRECTION ( 'NONE',  ( -1.836970198721029934E-16, 1.000000000000000000, 0.000000000000000000 ) ) ;
#146053=CIRCLE ( 'NONE', #250124, 11.90000000000000746 ) ;
#146062=CARTESIAN_POINT ( 'NONE',  ( -20.54999999999999716, 1.115600667400684642E-11, -134.0000000000000000 ) ) ;
#146074=VERTEX_POINT ( 'NONE', #60187 ) ;
#146083=CARTESIAN_POINT ( 'NONE',  ( -23.15000000000000213, 1.115600667400684642E-11, -134.0000000000000000 ) ) ;
#146124=LINE ( 'NONE', #148713, #175747 ) ;
#146145=DIRECTION ( 'NONE',  ( 0.000000000000000000, -0.4930308989874729320, -0.8700118002898605818 ) ) ;
#146149=CARTESIAN_POINT ( 'NONE',  ( 23.24999999999999645, 1.115600667400684642E-11, -134.0000000000000000 ) ) ;
#146164=DIRECTION ( 'NONE',  ( 0.000000000000000000, 0.000000000000000000, -1.000000000000000000 ) ) ;
#146167=CARTESIAN_POINT ( 'NONE',  ( -20.54999999999999716, -9.499999999988846255, -157.6060308773475924 ) ) ;
#146175=DIRECTION ( 'NONE',  ( 0.000000000000000000, 0.000000000000000000, -1.000000000000000000 ) ) ;
#146193=LINE ( 'NONE', #108371, #236221 ) ;
#146206=AXIS2_PLACEMENT_3D ( 'NONE', #56676, #77532, #136217 ) ;
#146213=CARTESIAN_POINT ( 'NONE',  ( 20.85000000000000142, 7.120270961708750512, -171.1595630418393625 ) ) ;
#146234=CARTESIAN_POINT ( 'NONE',  ( 20.99749315643149217, 11.75000000001115907, -160.4851942312420761 ) ) ;
#146248=EDGE_LOOP ( 'NONE', ( #7007, #55998, #55511, #249461 ) ) ;
#146258=CARTESIAN_POINT ( 'NONE',  ( 18.49999999999999645, 10.28015861706802347, -158.7245720712022319 ) ) ;
#146276=AXIS2_PLACEMENT_3D ( 'NONE', #177974, #235351, #174154 ) ;
#146278=DIRECTION ( 'NONE',  ( -0.000000000000000000, -1.000000000000000000, 0.000000000000000000 ) ) ;
#146305=DIRECTION ( 'NONE',  ( 1.000000000000000000, -0.000000000000000000, -0.000000000000000000 ) ) ;
#146306=ORIENTED_EDGE ( 'NONE', *, *, #180584, .F. ) ;
#146307=CYLINDRICAL_SURFACE ( 'NONE', #214307, 0.09999999999999939493 ) ;
#146335=VERTEX_POINT ( 'NONE', #54748 ) ;
#146339=CIRCLE ( 'NONE', #167236, 0.1000000000000096922 ) ;
#146364=DIRECTION ( 'NONE',  ( 0.000000000000000000, -0.000000000000000000, -1.000000000000000000 ) ) ;
#146399=CARTESIAN_POINT ( 'NONE',  ( 20.13684514580102913, 9.495855392761558988, -142.1430316856892091 ) ) ;
#146400=EDGE_CURVE ( 'NONE', #47876, #146335, #41580, .T. ) ;
#146437=DIRECTION ( 'NONE',  ( 1.000000000000000000, 0.000000000000000000, -0.000000000000000000 ) ) ;
#146440=ORIENTED_EDGE ( 'NONE', *, *, #19507, .T. ) ;
#146444=DIRECTION ( 'NONE',  ( -1.000000000000000000, -0.000000000000000000, 0.000000000000000000 ) ) ;
#146469=FACE_OUTER_BOUND ( 'NONE', #96640, .T. ) ;
#146476=ADVANCED_FACE ( 'NONE', ( #131727 ), #112186, .F. ) ;
#146482=ORIENTED_EDGE ( 'NONE', *, *, #101979, .F. ) ;
#146556=CIRCLE ( 'NONE', #204827, 0.09999999999999939493 ) ;
#146570=EDGE_LOOP ( 'NONE', ( #226962, #72064, #237373, #112986 ) ) ;
#146579=DIRECTION ( 'NONE',  ( -1.000000000000000000, 0.000000000000000000, 0.000000000000000000 ) ) ;
#146596=AXIS2_PLACEMENT_3D ( 'NONE', #130665, #91551, #109813 ) ;
#146678=DIRECTION ( 'NONE',  ( 0.000000000000000000, -1.000000000000000000, 0.000000000000000000 ) ) ;
#146690=EDGE_LOOP ( 'NONE', ( #165440, #136813, #68396, #171860 ) ) ;
#146701=CIRCLE ( 'NONE', #200903, 2.000000000000001776 ) ;
#146702=FACE_OUTER_BOUND ( 'NONE', #236748, .T. ) ;
#146705=DIRECTION ( 'NONE',  ( 0.000000000000000000, 0.000000000000000000, -1.000000000000000000 ) ) ;
#146712=EDGE_CURVE ( 'NONE', #253858, #129965, #6323, .T. ) ;
#146765=CARTESIAN_POINT ( 'NONE',  ( -18.49999999999997158, -9.321008403350129257, -141.2359382490778614 ) ) ;
#146784=ORIENTED_EDGE ( 'NONE', *, *, #20589, .T. ) ;
#146790=CARTESIAN_POINT ( 'NONE',  ( -18.59999999999999787, -9.480686695267820596, -174.4411151687578467 ) ) ;
#146811=DIRECTION ( 'NONE',  ( 0.000000000000000000, -0.8777080977375715243, 0.4791956752370512551 ) ) ;
#146821=DIRECTION ( 'NONE',  ( -1.000000000000000000, 0.000000000000000000, 0.000000000000000000 ) ) ;
#146837=CYLINDRICAL_SURFACE ( 'NONE', #238158, 0.09999999999999939493 ) ;
#146867=CARTESIAN_POINT ( 'NONE',  ( -20.54999999999999716, 4.350000000011156054, -146.3500000000000227 ) ) ;
#146887=CARTESIAN_POINT ( 'NONE',  ( -23.15000000000000213, 1.115651490242849210E-11, -129.8500000000000227 ) ) ;
#146912=CIRCLE ( 'NONE', #250967, 0.09999999999999344136 ) ;
#146931=EDGE_CURVE ( 'NONE', #179208, #109066, #67133, .T. ) ;
#146949=EDGE_LOOP ( 'NONE', ( #170361, #59759, #254664, #109788, #235444, #95837, #96100, #161782, #169888, #9492, #55607, #219479, #33329, #121339, #47682, #214644, #195885, #158230 ) ) ;
#146951=EDGE_CURVE ( 'NONE', #211620, #243100, #127105, .T. ) ;
#146973=VERTEX_POINT ( 'NONE', #87952 ) ;
#147017=ADVANCED_FACE ( 'NONE', ( #171415 ), #116930, .F. ) ;
#147019=EDGE_LOOP ( 'NONE', ( #66797, #18972, #185194, #230767 ) ) ;
#147030=DIRECTION ( 'NONE',  ( 0.000000000000000000, -0.000000000000000000, -1.000000000000000000 ) ) ;
#147076=EDGE_CURVE ( 'NONE', #176425, #133237, #237730, .T. ) ;
#147107=DIRECTION ( 'NONE',  ( 0.000000000000000000, 0.000000000000000000, 1.000000000000000000 ) ) ;
#147108=DIRECTION ( 'NONE',  ( 0.000000000000000000, 0.000000000000000000, -1.000000000000000000 ) ) ;
#147156=VECTOR ( 'NONE', #209947, 1000.000000000000000 ) ;
#147207=ORIENTED_EDGE ( 'NONE', *, *, #175125, .F. ) ;
#147212=TOROIDAL_SURFACE ( 'NONE', #234704, 3.899999999999999467, 0.1000000000000000056 ) ;
#147243=DIRECTION ( 'NONE',  ( 1.000000000000000000, -0.000000000000000000, -0.000000000000000000 ) ) ;
#147279=AXIS2_PLACEMENT_3D ( 'NONE', #165744, #27537, #150032 ) ;
#147284=EDGE_CURVE ( 'NONE', #196636, #105532, #159530, .T. ) ;
#147350=CIRCLE ( 'NONE', #9788, 0.09999999999999892308 ) ;
#147379=CIRCLE ( 'NONE', #201353, 3.899999999999999467 ) ;
#147382=EDGE_LOOP ( 'NONE', ( #117932, #193687, #137032, #43864, #54586 ) ) ;
#147393=CARTESIAN_POINT ( 'NONE',  ( -21.05000000000000071, 1.115653327213047955E-11, -129.7000000000000455 ) ) ;
#147462=CIRCLE ( 'NONE', #30970, 0.5999999999999894307 ) ;
#147495=CARTESIAN_POINT ( 'NONE',  ( 21.12400222705959507, 8.778511907088271116, -146.2500000000000568 ) ) ;
#147504=SPHERICAL_SURFACE ( 'NONE', #139329, 0.1000000000000000056 ) ;
#147558=CARTESIAN_POINT ( 'NONE',  ( 20.94999999999999929, -11.64999999998883595, -164.5000000000000000 ) ) ;
#147570=DIRECTION ( 'NONE',  ( 1.000000000000000000, 0.000000000000000000, 0.000000000000000000 ) ) ;
#147576=EDGE_CURVE ( 'NONE', #211620, #149376, #256261, .T. ) ;
#147610=DIRECTION ( 'NONE',  ( 1.000000000000000000, -0.000000000000000000, -0.000000000000000000 ) ) ;
#147634=ORIENTED_EDGE ( 'NONE', *, *, #102294, .T. ) ;
#147640=AXIS2_PLACEMENT_3D ( 'NONE', #231749, #36118, #174378 ) ;
#147649=ORIENTED_EDGE ( 'NONE', *, *, #230377, .T. ) ;
#147650=CARTESIAN_POINT ( 'NONE',  ( 20.94999999999999929, -11.29603075032412640, -164.4521008403361577 ) ) ;
#147657=VERTEX_POINT ( 'NONE', #238343 ) ;
#147688=ORIENTED_EDGE ( 'NONE', *, *, #230377, .F. ) ;
#147690=CARTESIAN_POINT ( 'NONE',  ( 22.39999999999999503, -0.1008583690875579364, -122.2504328765106294 ) ) ;
#147692=EDGE_LOOP ( 'NONE', ( #10768, #28693, #14561, #121470 ) ) ;
#147709=ORIENTED_EDGE ( 'NONE', *, *, #159403, .T. ) ;
#147710=AXIS2_PLACEMENT_3D ( 'NONE', #208047, #108917, #188457 ) ;
#147715=CARTESIAN_POINT ( 'NONE',  ( 20.51284917709620359, 10.31088662285602275, -141.6724731855920254 ) ) ;
#147724=EDGE_CURVE ( 'NONE', #218711, #27654, #188935, .T. ) ;
#147727=LINE ( 'NONE', #83844, #113213 ) ;
#147741=ORIENTED_EDGE ( 'NONE', *, *, #32363, .T. ) ;
#147784=CARTESIAN_POINT ( 'NONE',  ( 18.49999999999999645, 1.866714910068465239, -145.7526752462820241 ) ) ;
#147801=CARTESIAN_POINT ( 'NONE',  ( -22.45437739390953169, 1.115486826172573664E-11, -122.3504291884013071 ) ) ;
#147826=EDGE_CURVE ( 'NONE', #224742, #174422, #127532, .T. ) ;
#147894=CIRCLE ( 'NONE', #256143, 0.09999999999998898659 ) ;
#147901=EDGE_CURVE ( 'NONE', #27502, #169538, #49126, .T. ) ;
#147923=CARTESIAN_POINT ( 'NONE',  ( 21.14999999999999858, 6.650000000011155876, -146.2500000000000284 ) ) ;
#147929=DIRECTION ( 'NONE',  ( 0.000000000000000000, -0.1350103645451876666, 0.9908441862701600211 ) ) ;
#147930=VERTEX_POINT ( 'NONE', #229066 ) ;
#147943=DIRECTION ( 'NONE',  ( 1.836970198721029934E-16, -1.000000000000000000, -0.000000000000000000 ) ) ;
#147957=DIRECTION ( 'NONE',  ( 0.000000000000000000, 0.000000000000000000, 1.000000000000000000 ) ) ;
#147960=DIRECTION ( 'NONE',  ( -0.000000000000000000, 1.000000000000000000, 0.000000000000000000 ) ) ;
#148000=CARTESIAN_POINT ( 'NONE',  ( -22.57320508075687115, 11.75000000001115552, -134.0000000000000000 ) ) ;
#148015=CIRCLE ( 'NONE', #35632, 12.87500000000000000 ) ;
#148017=AXIS2_PLACEMENT_3D ( 'NONE', #184220, #206370, #145087 ) ;
#148040=ORIENTED_EDGE ( 'NONE', *, *, #137099, .T. ) ;
#148098=DIRECTION ( 'NONE',  ( -1.000000000000000000, -0.000000000000000000, -0.000000000000000000 ) ) ;
#148102=CARTESIAN_POINT ( 'NONE',  ( -18.59999999999999787, 10.33248238083634440, -173.0948465439131496 ) ) ;
#148103=CIRCLE ( 'NONE', #193894, 0.09999999999998898659 ) ;
#148179=AXIS2_PLACEMENT_3D ( 'NONE', #169437, #109405, #248945 ) ;
#148192=EDGE_CURVE ( 'NONE', #18309, #4224, #173559, .T. ) ;
#148226=ORIENTED_EDGE ( 'NONE', *, *, #183954, .T. ) ;
#148247=DIRECTION ( 'NONE',  ( 1.000000000000000000, 0.000000000000000000, 0.000000000000000000 ) ) ;
#148252=ORIENTED_EDGE ( 'NONE', *, *, #115673, .T. ) ;
#148268=ORIENTED_EDGE ( 'NONE', *, *, #125284, .T. ) ;
#148284=CARTESIAN_POINT ( 'NONE',  ( 23.24999999999999289, 11.75000000001116263, -146.1500000000000341 ) ) ;
#148355=CARTESIAN_POINT ( 'NONE',  ( -20.85000000000000142, -1.835859311432479268, -179.0044391687985410 ) ) ;
#148386=CARTESIAN_POINT ( 'NONE',  ( -21.08884785362073089, 0.04978309507788075683, -127.6428066325744055 ) ) ;
#148396=VERTEX_POINT ( 'NONE', #154388 ) ;
#148400=ORIENTED_EDGE ( 'NONE', *, *, #235663, .T. ) ;
#148410=VERTEX_POINT ( 'NONE', #64235 ) ;
#148416=CARTESIAN_POINT ( 'NONE',  ( -21.30740335185486245, 0.09893452578700702438, -127.4433420779720336 ) ) ;
#148458=CARTESIAN_POINT ( 'NONE',  ( 22.50046968638161005, 0.04516984715173957138, -122.2499548455251812 ) ) ;
#148481=CARTESIAN_POINT ( 'NONE',  ( 20.94999999999999929, 1.115600667400684642E-11, -167.5000000000000284 ) ) ;
#148501=EDGE_CURVE ( 'NONE', #190865, #203670, #2979, .T. ) ;
#148505=AXIS2_PLACEMENT_3D ( 'NONE', #256747, #58580, #138115 ) ;
#148508=AXIS2_PLACEMENT_3D ( 'NONE', #194081, #192785, #55790 ) ;
#148533=EDGE_CURVE ( 'NONE', #182048, #42426, #7078, .T. ) ;
#148539=DIRECTION ( 'NONE',  ( 1.000000000000000000, -0.000000000000000000, -0.000000000000000000 ) ) ;
#148600=CIRCLE ( 'NONE', #248530, 7.900000000000000355 ) ;
#148609=ORIENTED_EDGE ( 'NONE', *, *, #17851, .T. ) ;
#148624=CIRCLE ( 'NONE', #81935, 0.2000000000000057288 ) ;
#148630=EDGE_CURVE ( 'NONE', #36655, #237217, #63598, .T. ) ;
#148643=CARTESIAN_POINT ( 'NONE',  ( 18.39999999999999858, -9.599999999988845900, -174.1001893912220737 ) ) ;
#148646=EDGE_CURVE ( 'NONE', #187889, #118509, #161355, .T. ) ;
#148667=DIRECTION ( 'NONE',  ( -1.000000000000000000, 0.000000000000000000, 0.000000000000000000 ) ) ;
#148678=AXIS2_PLACEMENT_3D ( 'NONE', #103316, #182893, #231010 ) ;
#148684=CYLINDRICAL_SURFACE ( 'NONE', #175882, 0.09999999999999939493 ) ;
#148690=VERTEX_POINT ( 'NONE', #23225 ) ;
#148713=CARTESIAN_POINT ( 'NONE',  ( 23.15000000000000213, -11.74999999998883737, -146.2500000000000284 ) ) ;
#148721=FACE_OUTER_BOUND ( 'NONE', #876, .T. ) ;
#148723=ORIENTED_EDGE ( 'NONE', *, *, #132380, .T. ) ;
#148774=CARTESIAN_POINT ( 'NONE',  ( -18.59999999999999787, 9.250000000011157297, -146.3500000000000227 ) ) ;
#148811=ORIENTED_EDGE ( 'NONE', *, *, #167200, .T. ) ;
#148815=EDGE_CURVE ( 'NONE', #248851, #201727, #61260, .T. ) ;
#148840=DIRECTION ( 'NONE',  ( 0.000000000000000000, 1.000000000000000000, 0.000000000000000000 ) ) ;
#148855=CARTESIAN_POINT ( 'NONE',  ( 21.56666275994540172, 1.115600667400684642E-11, -127.0426315931066910 ) ) ;
#148872=DIRECTION ( 'NONE',  ( 0.000000000000000000, 0.9875055080513743810, -0.1575844902526802316 ) ) ;
#148905=CARTESIAN_POINT ( 'NONE',  ( -20.94999999999999929, -11.29603075032412640, -164.4521008403361577 ) ) ;
#148927=VERTEX_POINT ( 'NONE', #34780 ) ;
#148933=EDGE_CURVE ( 'NONE', #250075, #198238, #228036, .T. ) ;
#148935=CARTESIAN_POINT ( 'NONE',  ( 21.14999999999999858, 6.650000000011155876, -146.3500000000000227 ) ) ;
#148961=CYLINDRICAL_SURFACE ( 'NONE', #199178, 0.09999999999998898659 ) ;
#148970=EDGE_LOOP ( 'NONE', ( #49286, #85521, #87872, #106409 ) ) ;
#148991=DIRECTION ( 'NONE',  ( 0.000000000000000000, 1.000000000000000000, 0.000000000000000000 ) ) ;
#148998=DIRECTION ( 'NONE',  ( 0.000000000000000000, 1.000000000000000000, 0.000000000000000000 ) ) ;
#149003=AXIS2_PLACEMENT_3D ( 'NONE', #176641, #117915, #197457 ) ;
#149030=DIRECTION ( 'NONE',  ( -1.000000000000000000, -0.000000000000000000, 0.000000000000000000 ) ) ;
#149046=CARTESIAN_POINT ( 'NONE',  ( -18.50000000000000000, 9.350000000011156942, -155.3500000000000227 ) ) ;
#149056=EDGE_CURVE ( 'NONE', #142484, #175914, #132174, .T. ) ;
#149072=FACE_OUTER_BOUND ( 'NONE', #33614, .T. ) ;
#149122=DIRECTION ( 'NONE',  ( 7.304098846218134667E-16, -1.000000000000000000, 0.000000000000000000 ) ) ;
#149129=SPHERICAL_SURFACE ( 'NONE', #180092, 0.1000000000000000056 ) ;
#149151=TOROIDAL_SURFACE ( 'NONE', #211695, 12.77500000000000036, 0.1000000000000000056 ) ;
#149176=VECTOR ( 'NONE', #27598, 1000.000000000000000 ) ;
#149188=ORIENTED_EDGE ( 'NONE', *, *, #140216, .T. ) ;
#149217=EDGE_CURVE ( 'NONE', #157514, #11174, #98817, .T. ) ;
#149220=ADVANCED_FACE ( 'NONE', ( #227496 ), #228807, .F. ) ;
#149235=DIRECTION ( 'NONE',  ( 0.000000000000000000, 0.000000000000000000, -1.000000000000000000 ) ) ;
#149250=ORIENTED_EDGE ( 'NONE', *, *, #193963, .F. ) ;
#149282=EDGE_CURVE ( 'NONE', #146074, #197727, #248891, .T. ) ;
#149328=VERTEX_POINT ( 'NONE', #235217 ) ;
#149343=AXIS2_PLACEMENT_3D ( 'NONE', #162217, #65649, #5651 ) ;
#149347=DIRECTION ( 'NONE',  ( 0.000000000000000000, 0.000000000000000000, -1.000000000000000000 ) ) ;
#149354=CARTESIAN_POINT ( 'NONE',  ( 23.24999999999999289, 11.75000000001116263, -134.1000000000000227 ) ) ;
#149371=CIRCLE ( 'NONE', #16104, 4.049999999999998934 ) ;
#149376=VERTEX_POINT ( 'NONE', #116554 ) ;
#149399=EDGE_CURVE ( 'NONE', #217170, #63340, #211468, .T. ) ;
#149405=CARTESIAN_POINT ( 'NONE',  ( -18.52643265882458579, 10.31973158071402530, -173.0505334713354841 ) ) ;
#149407=CARTESIAN_POINT ( 'NONE',  ( -21.05000000000000071, -1.162701749926853712, -142.1000000000000227 ) ) ;
#149414=FACE_OUTER_BOUND ( 'NONE', #122900, .T. ) ;
#149424=DIRECTION ( 'NONE',  ( 0.000000000000000000, 1.000000000000000000, 0.000000000000000000 ) ) ;
#149428=EDGE_LOOP ( 'NONE', ( #1758, #231759, #127638, #45886 ) ) ;
#149484=CYLINDRICAL_SURFACE ( 'NONE', #72329, 0.09999999999998898659 ) ;
#149496=VECTOR ( 'NONE', #112122, 1000.000000000000000 ) ;
#149502=FACE_OUTER_BOUND ( 'NONE', #255510, .T. ) ;
#149510=CARTESIAN_POINT ( 'NONE',  ( -21.05000000000000071, -1.162701749926853712, -142.0000000000000284 ) ) ;
#149557=CARTESIAN_POINT ( 'NONE',  ( 20.94999999999999574, -1.162701749926853712, -142.0000000000000284 ) ) ;
#149560=EDGE_CURVE ( 'NONE', #109286, #239010, #253341, .T. ) ;
#149580=CYLINDRICAL_SURFACE ( 'NONE', #31520, 0.09999999999999939493 ) ;
#149617=CARTESIAN_POINT ( 'NONE',  ( -21.05000000000000071, -11.48912529306490349, -137.1000000000000227 ) ) ;
#149620=AXIS2_PLACEMENT_3D ( 'NONE', #221797, #219247, #121475 ) ;
#149669=VERTEX_POINT ( 'NONE', #229767 ) ;
#149678=CARTESIAN_POINT ( 'NONE',  ( 21.05000000000000071, 1.115625160336667635E-11, -165.5000000000000284 ) ) ;
#149707=DIRECTION ( 'NONE',  ( 0.000000000000000000, 0.000000000000000000, -1.000000000000000000 ) ) ;
#149710=CIRCLE ( 'NONE', #120665, 0.09999999999999939493 ) ;
#149723=CARTESIAN_POINT ( 'NONE',  ( 18.59999999999999076, 6.550000000011156231, -155.2500000000000284 ) ) ;
#149807=AXIS2_PLACEMENT_3D ( 'NONE', #21720, #77816, #180795 ) ;
#149808=CARTESIAN_POINT ( 'NONE',  ( 21.12757541349815682, 6.473380571262609351, -133.9948387841902786 ) ) ;
#149809=VERTEX_POINT ( 'NONE', #214059 ) ;
#149814=CARTESIAN_POINT ( 'NONE',  ( 18.59999999999999787, -9.321008403350148797, -141.2359382490778614 ) ) ;
#149832=CARTESIAN_POINT ( 'NONE',  ( -21.05000000000000071, -11.39257802169451672, -137.0739495798319467 ) ) ;
#149854=AXIS2_PLACEMENT_3D ( 'NONE', #11900, #151406, #76974 ) ;
#149858=CARTESIAN_POINT ( 'NONE',  ( -21.05000000000000071, 6.257814610487270279, -133.9022097086912311 ) ) ;
#149872=AXIS2_PLACEMENT_3D ( 'NONE', #94175, #35538, #14683 ) ;
#149875=CARTESIAN_POINT ( 'NONE',  ( -23.25000000000000000, 1.115650265596050101E-11, -129.9500000000000171 ) ) ;
#149928=VERTEX_POINT ( 'NONE', #221730 ) ;
#149930=FACE_OUTER_BOUND ( 'NONE', #116417, .T. ) ;
#149957=DIRECTION ( 'NONE',  ( 0.000000000000000000, 0.000000000000000000, -1.000000000000000000 ) ) ;
#149977=ORIENTED_EDGE ( 'NONE', *, *, #247540, .F. ) ;
#149979=ADVANCED_FACE ( 'NONE', ( #86064 ), #108240, .T. ) ;
#149994=AXIS2_PLACEMENT_3D ( 'NONE', #204663, #109415, #84689 ) ;
#150005=CARTESIAN_POINT ( 'NONE',  ( -23.15000000000000213, 1.115600667400684642E-11, -167.5000000000000284 ) ) ;
#150032=DIRECTION ( 'NONE',  ( 1.000000000000000000, 0.000000000000000000, 0.000000000000000000 ) ) ;
#150033=CARTESIAN_POINT ( 'NONE',  ( 18.50000000000000000, -10.35479209691423996, -161.2565409830737906 ) ) ;
#150085=CIRCLE ( 'NONE', #250017, 11.64999999999999325 ) ;
#150098=DIRECTION ( 'NONE',  ( 0.000000000000000000, 1.000000000000000000, 0.000000000000000000 ) ) ;
#150133=ORIENTED_EDGE ( 'NONE', *, *, #218514, .F. ) ;
#150155=CARTESIAN_POINT ( 'NONE',  ( 18.47654891039379521, -9.465274948371149577, -141.1259759051946219 ) ) ;
#150165=FACE_OUTER_BOUND ( 'NONE', #192447, .T. ) ;
#150213=ORIENTED_EDGE ( 'NONE', *, *, #256705, .F. ) ;
#150231=CIRCLE ( 'NONE', #246084, 11.64999999999999325 ) ;
#150236=DIRECTION ( 'NONE',  ( 1.000000000000000000, -0.000000000000000000, -0.000000000000000000 ) ) ;
#150238=DIRECTION ( 'NONE',  ( 7.304098846218134667E-16, -1.000000000000000000, 0.000000000000000000 ) ) ;
#150242=ORIENTED_EDGE ( 'NONE', *, *, #164123, .T. ) ;
#150258=CARTESIAN_POINT ( 'NONE',  ( 20.94999999999999574, 6.400000000011158541, -143.9304246300615944 ) ) ;
#150259=DIRECTION ( 'NONE',  ( 0.000000000000000000, 0.4999999999999956701, -0.8660254037844411501 ) ) ;
#150271=CYLINDRICAL_SURFACE ( 'NONE', #254477, 0.09999999999998898659 ) ;
#150273=CARTESIAN_POINT ( 'NONE',  ( 21.10257677756356642, 0.02495074957914743610, -127.6016182574673508 ) ) ;
#150297=CARTESIAN_POINT ( 'NONE',  ( 21.05000000000000071, -8.999999999988842703, -158.0060308773475697 ) ) ;
#150407=CARTESIAN_POINT ( 'NONE',  ( 22.39999999999999503, 11.65000000001116298, -133.9000000000000057 ) ) ;
#150418=VECTOR ( 'NONE', #231519, 1000.000000000000000 ) ;
#150435=ORIENTED_EDGE ( 'NONE', *, *, #211034, .F. ) ;
#150440=EDGE_LOOP ( 'NONE', ( #48269, #84033, #141259, #141400, #42273 ) ) ;
#150453=ORIENTED_EDGE ( 'NONE', *, *, #101079, .F. ) ;
#150486=CARTESIAN_POINT ( 'NONE',  ( 23.14999999999998437, 11.75000000001115552, -134.0000000000000000 ) ) ;
#150495=AXIS2_PLACEMENT_3D ( 'NONE', #244474, #65838, #28035 ) ;
#150505=CARTESIAN_POINT ( 'NONE',  ( -21.14999999999999858, 6.540656951712397138, -134.1000000000000227 ) ) ;
#150508=CARTESIAN_POINT ( 'NONE',  ( 20.85000000000000142, -1.749999999988843813, -179.1189500386222733 ) ) ;
#150551=CARTESIAN_POINT ( 'NONE',  ( -23.25000000000000000, -1.835859311432481045, -179.1044391687985353 ) ) ;
#150554=AXIS2_PLACEMENT_3D ( 'NONE', #142566, #64336, #143853 ) ;
#150566=DIRECTION ( 'NONE',  ( 0.000000000000000000, 0.000000000000000000, -1.000000000000000000 ) ) ;
#150582=AXIS2_PLACEMENT_3D ( 'NONE', #170344, #111608, #86876 ) ;
#150592=CARTESIAN_POINT ( 'NONE',  ( -22.39999999999999858, 11.75000000001115552, -134.1000000000000227 ) ) ;
#150597=VERTEX_POINT ( 'NONE', #163425 ) ;
#150629=EDGE_CURVE ( 'NONE', #111004, #153822, #143836, .T. ) ;
#150645=DIRECTION ( 'NONE',  ( 0.000000000000000000, 1.000000000000000000, 0.000000000000000000 ) ) ;
#150652=ORIENTED_EDGE ( 'NONE', *, *, #163781, .F. ) ;
#150666=DIRECTION ( 'NONE',  ( 0.000000000000000000, 0.000000000000000000, -1.000000000000000000 ) ) ;
#150681=DIRECTION ( 'NONE',  ( 0.000000000000000000, 0.1495327102803792052, -0.9887567792719320625 ) ) ;
#150706=DIRECTION ( 'NONE',  ( 0.000000000000000000, 0.000000000000000000, -1.000000000000000000 ) ) ;
#150740=CIRCLE ( 'NONE', #9095, 0.09999999999998898659 ) ;
#150743=LINE ( 'NONE', #230266, #96186 ) ;
#150751=CARTESIAN_POINT ( 'NONE',  ( 18.49362639424878907, -9.442604367877251548, -174.2644409335108264 ) ) ;
#150756=CIRCLE ( 'NONE', #38344, 0.09999999999999939493 ) ;
#150771=CARTESIAN_POINT ( 'NONE',  ( -23.15000000000000213, -11.74999999998884448, -122.2500000000000284 ) ) ;
#150786=SPHERICAL_SURFACE ( 'NONE', #248674, 0.1000000000000000056 ) ;
#150798=DIRECTION ( 'NONE',  ( 0.000000000000000000, 0.000000000000000000, -1.000000000000000000 ) ) ;
#150802=CARTESIAN_POINT ( 'NONE',  ( 18.49999999999998934, 6.550000000011156231, -144.0170271704400307 ) ) ;
#150813=CARTESIAN_POINT ( 'NONE',  ( -23.15000000000000213, 1.115600667400684642E-11, -134.0000000000000000 ) ) ;
#150815=DIRECTION ( 'NONE',  ( 0.000000000000000000, 1.000000000000000000, -6.308085367188393199E-16 ) ) ;
#150836=DIRECTION ( 'NONE',  ( 0.000000000000000000, 0.6728971962617388280, 0.7397360091702248619 ) ) ;
#150848=DIRECTION ( 'NONE',  ( 0.000000000000000000, 0.9999631594459056361, -0.008583690987128059571 ) ) ;
#150850=AXIS2_PLACEMENT_3D ( 'NONE', #139789, #219333, #40746 ) ;
#150856=EDGE_CURVE ( 'NONE', #1294, #162055, #115579, .T. ) ;
#150857=DIRECTION ( 'NONE',  ( 0.000000000000000000, 0.000000000000000000, -1.000000000000000000 ) ) ;
#150861=DIRECTION ( 'NONE',  ( 0.000000000000000000, 1.000000000000000000, 0.000000000000000000 ) ) ;
#150878=CARTESIAN_POINT ( 'NONE',  ( 20.85000000000000142, -1.835859311432481045, -179.0044391687985410 ) ) ;
#150882=DIRECTION ( 'NONE',  ( -1.000000000000000000, -0.000000000000000000, -0.000000000000000000 ) ) ;
#150919=ORIENTED_EDGE ( 'NONE', *, *, #241311, .F. ) ;
#150920=VECTOR ( 'NONE', #158970, 1000.000000000000000 ) ;
#150949=ORIENTED_EDGE ( 'NONE', *, *, #228203, .T. ) ;
#150953=CARTESIAN_POINT ( 'NONE',  ( -21.09316766718153247, 0.03926340232583294676, -127.6298466875253013 ) ) ;
#151029=EDGE_CURVE ( 'NONE', #111004, #24563, #161772, .T. ) ;
#151062=DIRECTION ( 'NONE',  ( 0.000000000000000000, 0.000000000000000000, -1.000000000000000000 ) ) ;
#151087=TOROIDAL_SURFACE ( 'NONE', #105239, 0.6000000000000015321, 0.1000000000000000056 ) ;
#151097=ORIENTED_EDGE ( 'NONE', *, *, #155351, .F. ) ;
#151114=ORIENTED_EDGE ( 'NONE', *, *, #127661, .T. ) ;
#151120=AXIS2_PLACEMENT_3D ( 'NONE', #177500, #135752, #77071 ) ;
#151132=CARTESIAN_POINT ( 'NONE',  ( 20.94999999999999929, 6.650000000011155876, -144.0170271704400307 ) ) ;
#151135=CARTESIAN_POINT ( 'NONE',  ( -21.05000000000000071, 6.540656951712397138, -134.1000000000000227 ) ) ;
#151136=DIRECTION ( 'NONE',  ( -1.000000000000000000, 0.000000000000000000, -0.000000000000000000 ) ) ;
#151152=CARTESIAN_POINT ( 'NONE',  ( -21.05000000000000071, 1.115600667400684642E-11, -167.5000000000000284 ) ) ;
#151188=ORIENTED_EDGE ( 'NONE', *, *, #50290, .F. ) ;
#151219=LINE ( 'NONE', #95076, #173625 ) ;
#151232=DIRECTION ( 'NONE',  ( 0.000000000000000000, -0.4999999999999348299, 0.8660254037844762331 ) ) ;
#151255=CARTESIAN_POINT ( 'NONE',  ( 20.94999999999999929, 1.115625160336667635E-11, -165.5000000000000284 ) ) ;
#151287=DIRECTION ( 'NONE',  ( 1.000000000000000000, 0.000000000000000000, 0.000000000000000000 ) ) ;
#151332=AXIS2_PLACEMENT_3D ( 'NONE', #217132, #114207, #56765 ) ;
#151378=CARTESIAN_POINT ( 'NONE',  ( 21.05000000000000071, -11.64999999998883595, -164.5000000000000000 ) ) ;
#151381=CARTESIAN_POINT ( 'NONE',  ( -21.14999999999999858, 11.75000000001115552, -140.7838656629781724 ) ) ;
#151404=CIRCLE ( 'NONE', #38971, 12.87499999999999822 ) ;
#151406=DIRECTION ( 'NONE',  ( -1.000000000000000000, 0.000000000000000000, 0.000000000000000000 ) ) ;
#151412=DIRECTION ( 'NONE',  ( 1.000000000000000000, 0.000000000000000000, 0.000000000000000000 ) ) ;
#151419=B_SPLINE_CURVE_WITH_KNOTS ( 'NONE', 3,
 ( #62895, #103286, #182873, #159446, #238981, #90140 ),
 .UNSPECIFIED., .F., .F.,
 ( 4, 2, 4 ),
 ( 0.000000000000000000, 0.0001895189928937342824, 0.0003790379857874685648 ),
 .UNSPECIFIED. ) ;
#151425=CARTESIAN_POINT ( 'NONE',  ( 21.98333005346336222, 1.115600667400684642E-11, -126.6259246709433626 ) ) ;
#151426=CIRCLE ( 'NONE', #51410, 7.899999999999990585 ) ;
#151446=TOROIDAL_SURFACE ( 'NONE', #93154, 0.2000000000000000111, 0.1000000000000000056 ) ;
#151452=DIRECTION ( 'NONE',  ( 0.000000000000000000, 0.000000000000000000, -1.000000000000000000 ) ) ;
#151456=EDGE_LOOP ( 'NONE', ( #25105, #25999, #222404, #81169 ) ) ;
#151478=PRODUCT ( 'Injection Molded Chain Links 5', 'Injection Molded Chain Links 5', '', ( #112221 ) ) ;
#151494=AXIS2_PLACEMENT_3D ( 'NONE', #16827, #257928, #197999 ) ;
#151520=AXIS2_PLACEMENT_3D ( 'NONE', #47530, #166252, #245762 ) ;
#151538=EDGE_CURVE ( 'NONE', #43801, #118232, #29839, .T. ) ;
#151547=ORIENTED_EDGE ( 'NONE', *, *, #133304, .F. ) ;
#151559=ORIENTED_EDGE ( 'NONE', *, *, #63669, .F. ) ;
#151563=ADVANCED_FACE ( 'NONE', ( #27280 ), #246294, .F. ) ;
#151565=AXIS2_PLACEMENT_3D ( 'NONE', #89790, #126363, #211043 ) ;
#151578=CARTESIAN_POINT ( 'NONE',  ( -21.07928932188134041, 6.328516656404449492, -133.9011048543456184 ) ) ;
#151590=ORIENTED_EDGE ( 'NONE', *, *, #41055, .F. ) ;
#151601=CARTESIAN_POINT ( 'NONE',  ( 18.51024323315077069, 10.31104185824064068, -173.0204516983106089 ) ) ;
#151602=DIRECTION ( 'NONE',  ( -1.000000000000000000, -0.000000000000000000, -0.000000000000000000 ) ) ;
#151610=ORIENTED_EDGE ( 'NONE', *, *, #160958, .F. ) ;
#151622=CARTESIAN_POINT ( 'NONE',  ( 18.59999999999997655, 11.75000000001115552, -167.5000000000000284 ) ) ;
#151635=EDGE_CURVE ( 'NONE', #91128, #56702, #181835, .T. ) ;
#151650=DIRECTION ( 'NONE',  ( -1.000000000000000000, -0.000000000000000000, -0.000000000000000000 ) ) ;
#151669=CIRCLE ( 'NONE', #39238, 0.09999999999999907574 ) ;
#151706=FACE_OUTER_BOUND ( 'NONE', #208177, .T. ) ;
#151746=VERTEX_POINT ( 'NONE', #224792 ) ;
#151756=ORIENTED_EDGE ( 'NONE', *, *, #190258, .T. ) ;
#151810=VERTEX_POINT ( 'NONE', #185690 ) ;
#151818=CARTESIAN_POINT ( 'NONE',  ( 21.05933563467872105, 10.72452471209247626, -146.1936477489559536 ) ) ;
#151827=CARTESIAN_POINT ( 'NONE',  ( 18.49999999999999289, 11.65000000001115943, -122.2500000000000284 ) ) ;
#151859=CYLINDRICAL_SURFACE ( 'NONE', #22960, 0.1000000000000098310 ) ;
#151886=LINE ( 'NONE', #191007, #160050 ) ;
#151923=EDGE_CURVE ( 'NONE', #83610, #91096, #58981, .T. ) ;
#151941=AXIS2_PLACEMENT_3D ( 'NONE', #20719, #220189, #136783 ) ;
#151954=FACE_OUTER_BOUND ( 'NONE', #231752, .T. ) ;
#151975=CARTESIAN_POINT ( 'NONE',  ( -18.50000000000000000, -1.866714910046153308, -145.7526752462820241 ) ) ;
#151976=TOROIDAL_SURFACE ( 'NONE', #60354, 0.4000000000000003553, 0.1000000000000000056 ) ;
#151980=ORIENTED_EDGE ( 'NONE', *, *, #179030, .T. ) ;
#151981=VECTOR ( 'NONE', #29018, 1000.000000000000000 ) ;
#151992=DIRECTION ( 'NONE',  ( 0.000000000000000000, 0.000000000000000000, 1.000000000000000000 ) ) ;
#151998=LINE ( 'NONE', #249786, #150418 ) ;
#152012=CIRCLE ( 'NONE', #93527, 0.09999999999998898659 ) ;
#152017=CYLINDRICAL_SURFACE ( 'NONE', #10005, 0.09999999999998898659 ) ;
#152043=CIRCLE ( 'NONE', #239516, 0.09999999999999939493 ) ;
#152053=LINE ( 'NONE', #52919, #169052 ) ;
#152061=CARTESIAN_POINT ( 'NONE',  ( 18.58719872626880232, -9.566644397587491966, -174.3224781963970429 ) ) ;
#152062=CIRCLE ( 'NONE', #18761, 0.09999999999999967248 ) ;
#152088=FACE_OUTER_BOUND ( 'NONE', #57813, .T. ) ;
#152090=AXIS2_PLACEMENT_3D ( 'NONE', #57767, #198569, #96869 ) ;
#152092=ADVANCED_FACE ( 'NONE', ( #23774 ), #253857, .T. ) ;
#152122=CYLINDRICAL_SURFACE ( 'NONE', #220022, 0.09999999999998898659 ) ;
#152125=AXIS2_PLACEMENT_3D ( 'NONE', #216242, #37643, #238382 ) ;
#152150=ORIENTED_EDGE ( 'NONE', *, *, #89091, .F. ) ;
#152162=AXIS2_PLACEMENT_3D ( 'NONE', #188324, #129635, #50090 ) ;
#152206=CIRCLE ( 'NONE', #122968, 2.000000000000001776 ) ;
#152229=FACE_OUTER_BOUND ( 'NONE', #155202, .T. ) ;
#152236=AXIS2_PLACEMENT_3D ( 'NONE', #14329, #93829, #153864 ) ;
#152238=DIRECTION ( 'NONE',  ( -1.000000000000000000, 0.000000000000000000, 0.000000000000000000 ) ) ;
#152312=DIRECTION ( 'NONE',  ( -2.940209281316621509E-16, 1.000000000000000000, 0.000000000000000000 ) ) ;
#152324=ORIENTED_EDGE ( 'NONE', *, *, #178797, .T. ) ;
#152335=VECTOR ( 'NONE', #186714, 1000.000000000000000 ) ;
#152341=ORIENTED_EDGE ( 'NONE', *, *, #189999, .T. ) ;
#152351=DIRECTION ( 'NONE',  ( 0.000000000000000000, 0.000000000000000000, 1.000000000000000000 ) ) ;
#152365=DIRECTION ( 'NONE',  ( -1.000000000000000000, -0.000000000000000000, -0.000000000000000000 ) ) ;
#152399=FACE_OUTER_BOUND ( 'NONE', #187096, .T. ) ;
#152400=EDGE_LOOP ( 'NONE', ( #200122, #49179, #192473, #77153 ) ) ;
#152406=ADVANCED_FACE ( 'NONE', ( #187955 ), #9307, .T. ) ;
#152435=EDGE_CURVE ( 'NONE', #18582, #136324, #95810, .T. ) ;
#152465=EDGE_CURVE ( 'NONE', #135871, #114955, #129176, .T. ) ;
#152468=CARTESIAN_POINT ( 'NONE',  ( 18.60000000000000142, -9.321008403350125704, -141.2359382490778899 ) ) ;
#152482=EDGE_CURVE ( 'NONE', #207656, #49547, #162494, .T. ) ;
#152515=EDGE_CURVE ( 'NONE', #225500, #4224, #127657, .T. ) ;
#152523=CIRCLE ( 'NONE', #131638, 0.5000000000000004441 ) ;
#152526=ORIENTED_EDGE ( 'NONE', *, *, #30056, .F. ) ;
#152529=VERTEX_POINT ( 'NONE', #66410 ) ;
#152535=EDGE_CURVE ( 'NONE', #184016, #23909, #120809, .T. ) ;
#152569=VECTOR ( 'NONE', #111813, 1000.000000000000000 ) ;
#152573=ADVANCED_FACE ( 'NONE', ( #224186 ), #183329, .F. ) ;
#152665=CARTESIAN_POINT ( 'NONE',  ( 23.14999999999999503, 11.65000000001116298, -155.3500000000000227 ) ) ;
#152669=ORIENTED_EDGE ( 'NONE', *, *, #7426, .T. ) ;
#152675=DIRECTION ( 'NONE',  ( 1.000000000000000000, -0.000000000000000000, -0.000000000000000000 ) ) ;
#152682=CARTESIAN_POINT ( 'NONE',  ( 22.48970261584622321, 11.65000000001115588, -133.9446305117826341 ) ) ;
#152720=AXIS2_PLACEMENT_3D ( 'NONE', #98396, #174177, #58009 ) ;
#152729=CIRCLE ( 'NONE', #223406, 0.1000000000000001860 ) ;
#152749=DIRECTION ( 'NONE',  ( 0.000000000000000000, 0.000000000000000000, -1.000000000000000000 ) ) ;
#152766=DIRECTION ( 'NONE',  ( 1.000000000000000000, 0.000000000000000000, 0.000000000000000000 ) ) ;
#152770=VERTEX_POINT ( 'NONE', #58361 ) ;
#152817=ORIENTED_EDGE ( 'NONE', *, *, #178890, .F. ) ;
#152827=FACE_OUTER_BOUND ( 'NONE', #123542, .T. ) ;
#152828=B_SPLINE_CURVE_WITH_KNOTS ( 'NONE', 3,
 ( #75109, #192460, #248575, #114200, #90770, #13822, #9967 ),
 .UNSPECIFIED., .F., .F.,
 ( 4, 3, 4 ),
 ( 0.000000000000000000, 1.860045280646151707E-05, 5.251155757305330614E-05 ),
 .UNSPECIFIED. ) ;
#152845=CIRCLE ( 'NONE', #173708, 0.5000000000000013323 ) ;
#152861=EDGE_CURVE ( 'NONE', #107215, #196105, #120993, .T. ) ;
#152898=AXIS2_PLACEMENT_3D ( 'NONE', #201650, #41327, #161260 ) ;
#152908=CARTESIAN_POINT ( 'NONE',  ( -22.39999999999999858, 11.75000000001115552, -134.0000000000000284 ) ) ;
#152950=FACE_OUTER_BOUND ( 'NONE', #171725, .T. ) ;
#152997=ORIENTED_EDGE ( 'NONE', *, *, #191309, .F. ) ;
#153001=DIRECTION ( 'NONE',  ( 1.000000000000000000, 0.000000000000000000, 0.000000000000000000 ) ) ;
#153034=ADVANCED_FACE ( 'NONE', ( #187342 ), #129905, .T. ) ;
#153036=ORIENTED_EDGE ( 'NONE', *, *, #53738, .F. ) ;
#153044=CARTESIAN_POINT ( 'NONE',  ( 23.14999999999999858, 1.115600667400684642E-11, -134.0000000000000000 ) ) ;
#153060=DIRECTION ( 'NONE',  ( 1.000000000000000000, -0.000000000000000000, -0.000000000000000000 ) ) ;
#153075=CARTESIAN_POINT ( 'NONE',  ( 21.05000000000000071, 10.72371710471867701, -146.1500000000000341 ) ) ;
#153090=CARTESIAN_POINT ( 'NONE',  ( -20.54999999999999716, 4.350000000011156054, -155.1500000000000057 ) ) ;
#153097=DIRECTION ( 'NONE',  ( -1.000000000000000000, 0.000000000000000000, 0.000000000000000000 ) ) ;
#153111=CARTESIAN_POINT ( 'NONE',  ( 21.11833042828123652, 6.445644693866283248, -133.9928994909406299 ) ) ;
#153112=VERTEX_POINT ( 'NONE', #13826 ) ;
#153155=VERTEX_POINT ( 'NONE', #15117 ) ;
#153182=VECTOR ( 'NONE', #183757, 1000.000000000000000 ) ;
#153183=DIRECTION ( 'NONE',  ( 1.000000000000000000, -0.000000000000000000, -0.000000000000000000 ) ) ;
#153237=VECTOR ( 'NONE', #102765, 1000.000000000000000 ) ;
#153241=AXIS2_PLACEMENT_3D ( 'NONE', #224615, #103371, #108530 ) ;
#153289=CARTESIAN_POINT ( 'NONE',  ( -22.39999999999999858, -0.1008583690875579364, -122.2504328765106294 ) ) ;
#153296=DIRECTION ( 'NONE',  ( -1.000000000000000000, -2.952720810173289112E-16, 0.000000000000000000 ) ) ;
#153301=CIRCLE ( 'NONE', #40862, 0.09999999999998898659 ) ;
#153349=CIRCLE ( 'NONE', #240796, 0.5000000000000004441 ) ;
#153363=ORIENTED_EDGE ( 'NONE', *, *, #121271, .F. ) ;
#153365=CARTESIAN_POINT ( 'NONE',  ( 18.37172112093885801, -9.570961652231641636, -174.3167344534841448 ) ) ;
#153386=CARTESIAN_POINT ( 'NONE',  ( 20.94999999999999929, 14.05000000001115623, -161.9863049292391111 ) ) ;
#153392=AXIS2_PLACEMENT_3D ( 'NONE', #249331, #150236, #229750 ) ;
#153393=CARTESIAN_POINT ( 'NONE',  ( 23.25000000000000000, -8.999999999988844479, -143.8939691226524644 ) ) ;
#153409=CARTESIAN_POINT ( 'NONE',  ( -22.50000000000000000, 1.115600667400684642E-11, -127.7500000000000284 ) ) ;
#153427=ORIENTED_EDGE ( 'NONE', *, *, #126729, .T. ) ;
#153443=AXIS2_PLACEMENT_3D ( 'NONE', #64597, #223664, #162446 ) ;
#153446=CARTESIAN_POINT ( 'NONE',  ( 23.24999999999999289, 4.150000000011154988, -134.0000000000000000 ) ) ;
#153487=CARTESIAN_POINT ( 'NONE',  ( -20.54999999999999716, -8.999999999988846255, -143.8939691226524644 ) ) ;
#153513=CARTESIAN_POINT ( 'NONE',  ( 0.000000000000000000, 0.000000000000000000, 0.000000000000000000 ) ) ;
#153532=EDGE_LOOP ( 'NONE', ( #40772, #136548, #210761, #152817 ) ) ;
#153561=VERTEX_POINT ( 'NONE', #17072 ) ;
#153567=DIRECTION ( 'NONE',  ( -1.000000000000000000, 0.000000000000000000, 0.000000000000000000 ) ) ;
#153582=DIRECTION ( 'NONE',  ( -4.408576920032448588E-17, 0.1350103645451876666, 0.9908441862701600211 ) ) ;
#153645=CARTESIAN_POINT ( 'NONE',  ( 23.14999999999999503, 11.65000000001116298, -146.1500000000000341 ) ) ;
#153671=DIRECTION ( 'NONE',  ( 1.000000000000000000, 0.000000000000000000, -0.000000000000000000 ) ) ;
#153679=CARTESIAN_POINT ( 'NONE',  ( 18.49999999999999289, 7.021664781911246322, -171.3335654018973173 ) ) ;
#153692=CARTESIAN_POINT ( 'NONE',  ( 21.05000000000000071, -1.249999999988843369, -141.9000000000000341 ) ) ;
#153743=CIRCLE ( 'NONE', #95425, 12.77500000000000924 ) ;
#153749=CARTESIAN_POINT ( 'NONE',  ( 20.95000000000000284, 11.60000000001116227, -160.5717967697245285 ) ) ;
#153750=EDGE_CURVE ( 'NONE', #58852, #119168, #65154, .T. ) ;
#153777=DIRECTION ( 'NONE',  ( 0.000000000000000000, -1.000000000000000000, 6.308085367188393199E-16 ) ) ;
#153805=DIRECTION ( 'NONE',  ( 0.000000000000000000, 2.851451713636794872E-13, 1.000000000000000000 ) ) ;
#153822=VERTEX_POINT ( 'NONE', #114566 ) ;
#153844=CIRCLE ( 'NONE', #28946, 2.000000000000002665 ) ;
#153857=ORIENTED_EDGE ( 'NONE', *, *, #160485, .T. ) ;
#153864=DIRECTION ( 'NONE',  ( 0.000000000000000000, 1.224646799142185182E-16, 1.000000000000000000 ) ) ;
#153880=SPHERICAL_SURFACE ( 'NONE', #254291, 0.1000000000000000056 ) ;
#153897=CARTESIAN_POINT ( 'NONE',  ( 21.00000000000000000, 9.750000000011153745, -155.1500000000000057 ) ) ;
#153919=CIRCLE ( 'NONE', #41447, 0.09999999999998898659 ) ;
#153940=FACE_OUTER_BOUND ( 'NONE', #3218, .T. ) ;
#153943=ORIENTED_EDGE ( 'NONE', *, *, #98770, .F. ) ;
#153955=EDGE_CURVE ( 'NONE', #208289, #240530, #60993, .T. ) ;
#153958=VECTOR ( 'NONE', #151602, 1000.000000000000000 ) ;
#153964=DIRECTION ( 'NONE',  ( 1.000000000000000000, -0.000000000000000000, 0.000000000000000000 ) ) ;
#153995=FACE_OUTER_BOUND ( 'NONE', #173874, .T. ) ;
#154014=CARTESIAN_POINT ( 'NONE',  ( -23.25000000000000000, -0.09999999998884338825, -122.3504291924552234 ) ) ;
#154022=DIRECTION ( 'NONE',  ( 1.000000000000000000, 0.000000000000000000, 0.000000000000000000 ) ) ;
#154026=SURFACE_STYLE_FILL_AREA ( #236072 ) ;
#154037=ORIENTED_EDGE ( 'NONE', *, *, #94659, .T. ) ;
#154039=ORIENTED_EDGE ( 'NONE', *, *, #52959, .T. ) ;
#154043=CYLINDRICAL_SURFACE ( 'NONE', #18462, 0.09999999999999939493 ) ;
#154049=CARTESIAN_POINT ( 'NONE',  ( -21.05000000000000071, 11.65000000001115588, -160.4851942293460638 ) ) ;
#154064=ORIENTED_EDGE ( 'NONE', *, *, #136452, .T. ) ;
#154105=VERTEX_POINT ( 'NONE', #204350 ) ;
#154130=VERTEX_POINT ( 'NONE', #141813 ) ;
#154148=VERTEX_POINT ( 'NONE', #205630 ) ;
#154174=ORIENTED_EDGE ( 'NONE', *, *, #163258, .T. ) ;
#154183=VERTEX_POINT ( 'NONE', #105212 ) ;
#154193=DIRECTION ( 'NONE',  ( -0.000000000000000000, -0.000000000000000000, 1.000000000000000000 ) ) ;
#154208=TOROIDAL_SURFACE ( 'NONE', #58448, 12.77499999999999858, 0.1000000000000000056 ) ;
#154217=VECTOR ( 'NONE', #147960, 1000.000000000000000 ) ;
#154240=EDGE_LOOP ( 'NONE', ( #58500, #187522, #2447, #101430 ) ) ;
#154245=DIRECTION ( 'NONE',  ( 0.000000000000000000, 0.000000000000000000, 1.000000000000000000 ) ) ;
#154251=VERTEX_POINT ( 'NONE', #10015 ) ;
#154265=FACE_OUTER_BOUND ( 'NONE', #225968, .T. ) ;
#154335=ORIENTED_EDGE ( 'NONE', *, *, #119416, .F. ) ;
#154361=DIRECTION ( 'NONE',  ( 0.7071067811865474617, 0.7071067811865474617, 0.000000000000000000 ) ) ;
#154372=ORIENTED_EDGE ( 'NONE', *, *, #169271, .T. ) ;
#154388=CARTESIAN_POINT ( 'NONE',  ( 18.49999999999999645, -1.362429037182155023, -175.3888812479212334 ) ) ;
#154402=FACE_OUTER_BOUND ( 'NONE', #178104, .T. ) ;
#154414=DIRECTION ( 'NONE',  ( -1.000000000000000000, -3.265361837132813093E-16, 0.000000000000000000 ) ) ;
#154439=FACE_OUTER_BOUND ( 'NONE', #183963, .T. ) ;
#154442=CIRCLE ( 'NONE', #41991, 0.09999999999999939493 ) ;
#154474=EDGE_CURVE ( 'NONE', #101205, #53590, #192621, .T. ) ;
#154497=DIRECTION ( 'NONE',  ( -3.469446951953995998E-14, 0.000000000000000000, 1.000000000000000000 ) ) ;
#154505=DIRECTION ( 'NONE',  ( 1.000000000000000000, 2.952720810173289112E-16, -0.000000000000000000 ) ) ;
#154517=FILL_AREA_STYLE ('',( #253569 ) ) ;
#154526=FACE_OUTER_BOUND ( 'NONE', #156958, .T. ) ;
#154528=CARTESIAN_POINT ( 'NONE',  ( 23.24999999999999645, 3.900000000011155432, -167.5000000000000284 ) ) ;
#154540=CARTESIAN_POINT ( 'NONE',  ( 21.13920837816993270, 8.783247050131068434, -146.2500000000000284 ) ) ;
#154559=DIRECTION ( 'NONE',  ( 0.000000000000000000, 1.000000000000000000, 2.891205793294679805E-16 ) ) ;
#154566=EDGE_CURVE ( 'NONE', #125623, #44063, #113321, .T. ) ;
#154579=LINE ( 'NONE', #257432, #4778 ) ;
#154586=EDGE_CURVE ( 'NONE', #54863, #109286, #864, .T. ) ;
#154590=CYLINDRICAL_SURFACE ( 'NONE', #37485, 0.1000000000000028644 ) ;
#154592=CARTESIAN_POINT ( 'NONE',  ( -21.07928932188134041, 6.328516656404449492, -133.9011048543456184 ) ) ;
#154627=CARTESIAN_POINT ( 'NONE',  ( 21.09813707148777340, 6.385062105747659977, -133.9686485004704934 ) ) ;
#154634=CARTESIAN_POINT ( 'NONE',  ( 18.44206774312976194, -9.491027357528897923, -174.1262275046982779 ) ) ;
#154638=CARTESIAN_POINT ( 'NONE',  ( -23.25000000000000000, 4.250000000011156409, -155.1500000000000057 ) ) ;
#154664=CARTESIAN_POINT ( 'NONE',  ( 18.59999999999999787, -11.74999999998883737, -158.8500000000000227 ) ) ;
#154712=DIRECTION ( 'NONE',  ( -0.000000000000000000, -0.000000000000000000, -1.000000000000000000 ) ) ;
#154727=AXIS2_PLACEMENT_3D ( 'NONE', #217214, #97243, #20343 ) ;
#154753=CIRCLE ( 'NONE', #79702, 0.09999999999998898659 ) ;
#154770=DIRECTION ( 'NONE',  ( -1.000000000000000000, 0.000000000000000000, 0.000000000000000000 ) ) ;
#154779=CARTESIAN_POINT ( 'NONE',  ( 21.05000000000000071, 8.826429739528350638, -142.4140547129437095 ) ) ;
#154790=DIRECTION ( 'NONE',  ( 0.000000000000000000, 0.000000000000000000, 1.000000000000000000 ) ) ;
#154817=AXIS2_PLACEMENT_3D ( 'NONE', #109000, #43908, #247230 ) ;
#154825=CARTESIAN_POINT ( 'NONE',  ( 20.46382478191414833, 8.901379558713770734, -142.5457280948831169 ) ) ;
#154840=CARTESIAN_POINT ( 'NONE',  ( -21.09107601085575467, 6.363877975371003970, -133.9606928352826003 ) ) ;
#154853=CARTESIAN_POINT ( 'NONE',  ( -20.94999999999999929, -11.48912529306489994, -164.5000000000000000 ) ) ;
#154863=VECTOR ( 'NONE', #203044, 1000.000000000000000 ) ;
#154872=VERTEX_POINT ( 'NONE', #61822 ) ;
#154880=ORIENTED_EDGE ( 'NONE', *, *, #98015, .T. ) ;
#154881=CARTESIAN_POINT ( 'NONE',  ( 20.94999999999999929, 1.115600667400684642E-11, -134.0000000000000000 ) ) ;
#154889=AXIS2_PLACEMENT_3D ( 'NONE', #25653, #184712, #119629 ) ;
#154890=EDGE_CURVE ( 'NONE', #104833, #95993, #484, .T. ) ;
#154899=EDGE_LOOP ( 'NONE', ( #219756, #55430, #58465, #110782 ) ) ;
#154901=DIRECTION ( 'NONE',  ( 0.000000000000000000, 1.000000000000000000, 0.000000000000000000 ) ) ;
#154921=CARTESIAN_POINT ( 'NONE',  ( 18.57071067811864040, 10.17928932189250091, -155.2500000000000284 ) ) ;
#154941=EDGE_LOOP ( 'NONE', ( #253367, #211650, #167957, #86330 ) ) ;
#154984=CARTESIAN_POINT ( 'NONE',  ( 20.95392731769792150, 8.883061479199918509, -142.5222279795713121 ) ) ;
#155014=DIRECTION ( 'NONE',  ( -1.000000000000000000, 0.000000000000000000, 0.000000000000000000 ) ) ;
#155045=EDGE_CURVE ( 'NONE', #203005, #75879, #4585, .T. ) ;
#155087=VERTEX_POINT ( 'NONE', #133352 ) ;
#155124=EDGE_CURVE ( 'NONE', #63728, #13549, #18536, .T. ) ;
#155170=CARTESIAN_POINT ( 'NONE',  ( -20.64999999999999858, 7.150000000011155876, -155.1500000000000057 ) ) ;
#155202=EDGE_LOOP ( 'NONE', ( #150919, #92824, #91237, #84555 ) ) ;
#155206=DIRECTION ( 'NONE',  ( 0.000000000000000000, 0.000000000000000000, -1.000000000000000000 ) ) ;
#155227=AXIS2_PLACEMENT_3D ( 'NONE', #177919, #16288, #257370 ) ;
#155281=ORIENTED_EDGE ( 'NONE', *, *, #12066, .T. ) ;
#155292=SURFACE_SIDE_STYLE ('',( #154026 ) ) ;
#155324=ORIENTED_EDGE ( 'NONE', *, *, #229300, .T. ) ;
#155337=DIRECTION ( 'NONE',  ( 0.000000000000000000, 0.000000000000000000, 1.000000000000000000 ) ) ;
#155351=EDGE_CURVE ( 'NONE', #223143, #80694, #126619, .T. ) ;
#155372=EDGE_LOOP ( 'NONE', ( #186144, #130048, #87295, #205316 ) ) ;
#155406=ORIENTED_EDGE ( 'NONE', *, *, #254388, .T. ) ;
#155409=ORIENTED_EDGE ( 'NONE', *, *, #221045, .F. ) ;
#155417=DIRECTION ( 'NONE',  ( 1.000000000000000000, -3.965082230804126670E-15, 0.000000000000000000 ) ) ;
#155422=VERTEX_POINT ( 'NONE', #35262 ) ;
#155424=EDGE_CURVE ( 'NONE', #212362, #42512, #95199, .T. ) ;
#155447=CARTESIAN_POINT ( 'NONE',  ( -20.94999999999999929, 5.900000000011102586, -144.2190997646564483 ) ) ;
#155449=EDGE_CURVE ( 'NONE', #248851, #120967, #254722, .T. ) ;
#155493=ADVANCED_FACE ( 'NONE', ( #153940 ), #254249, .T. ) ;
#155508=CIRCLE ( 'NONE', #188782, 0.1000000000000089567 ) ;
#155536=DIRECTION ( 'NONE',  ( 2.715809747126116508E-16, -1.000000000000000000, 4.345295595401786413E-15 ) ) ;
#155573=ORIENTED_EDGE ( 'NONE', *, *, #47501, .T. ) ;
#155582=CARTESIAN_POINT ( 'NONE',  ( -18.42637059832563651, -9.496945461878544492, -174.1090773097998579 ) ) ;
#155634=CARTESIAN_POINT ( 'NONE',  ( 21.06089410995830491, 10.72529553213474429, -146.2023807310431778 ) ) ;
#155689=LINE ( 'NONE', #196075, #136576 ) ;
#155721=ADVANCED_FACE ( 'NONE', ( #67619 ), #169766, .T. ) ;
#155830=CIRCLE ( 'NONE', #43383, 0.09999999999999939493 ) ;
#155834=DIRECTION ( 'NONE',  ( -1.000000000000000000, 0.000000000000000000, 0.000000000000000000 ) ) ;
#155845=DIRECTION ( 'NONE',  ( 0.000000000000000000, 0.000000000000000000, -1.000000000000000000 ) ) ;
#155851=FACE_OUTER_BOUND ( 'NONE', #1557, .T. ) ;
#155869=EDGE_CURVE ( 'NONE', #206400, #73136, #234270, .T. ) ;
#155871=VECTOR ( 'NONE', #32982, 1000.000000000000000 ) ;
#155875=ADVANCED_FACE ( 'NONE', ( #233147 ), #132754, .T. ) ;
#155889=AXIS2_PLACEMENT_3D ( 'NONE', #129958, #127417, #28354 ) ;
#155905=EDGE_LOOP ( 'NONE', ( #125909, #143656, #118791, #129305 ) ) ;
#155928=VECTOR ( 'NONE', #193581, 1000.000000000000000 ) ;
#155930=SPHERICAL_SURFACE ( 'NONE', #151332, 0.1000000000000000056 ) ;
#155942=VERTEX_POINT ( 'NONE', #119607 ) ;
#155946=DIRECTION ( 'NONE',  ( 0.000000000000000000, 1.776356839400306474E-15, 1.000000000000000000 ) ) ;
#155975=FACE_OUTER_BOUND ( 'NONE', #102547, .T. ) ;
#155996=VERTEX_POINT ( 'NONE', #76601 ) ;
#156002=DIRECTION ( 'NONE',  ( 1.000000000000000000, 0.000000000000000000, 0.000000000000000000 ) ) ;
#156028=FACE_OUTER_BOUND ( 'NONE', #245162, .T. ) ;
#156054=CIRCLE ( 'NONE', #214302, 0.09999999999999949207 ) ;
#156059=DIRECTION ( 'NONE',  ( 0.000000000000000000, 0.000000000000000000, 1.000000000000000000 ) ) ;
#156063=VERTEX_POINT ( 'NONE', #106411 ) ;
#156067=DIRECTION ( 'NONE',  ( 0.000000000000000000, -0.8660254037844411501, -0.4999999999999956701 ) ) ;
#156097=CARTESIAN_POINT ( 'NONE',  ( -23.15000000000000213, 11.65000000001115588, -146.1500000000000341 ) ) ;
#156098=VERTEX_POINT ( 'NONE', #144255 ) ;
#156108=AXIS2_PLACEMENT_3D ( 'NONE', #84012, #3225, #180604 ) ;
#156129=CARTESIAN_POINT ( 'NONE',  ( -21.05000000000000071, 6.299230910103442049, -133.9015624999997556 ) ) ;
#156148=DIRECTION ( 'NONE',  ( 1.000000000000000000, 3.265361837132813093E-16, -0.000000000000000000 ) ) ;
#156163=VERTEX_POINT ( 'NONE', #162584 ) ;
#156204=CARTESIAN_POINT ( 'NONE',  ( -18.50000000000000000, 11.65000000001115232, -134.1000000000000227 ) ) ;
#156219=LINE ( 'NONE', #235715, #76384 ) ;
#156222=DIRECTION ( 'NONE',  ( -0.000000000000000000, -1.000000000000000000, 0.000000000000000000 ) ) ;
#156253=EDGE_CURVE ( 'NONE', #56702, #991, #46834, .T. ) ;
#156267=ADVANCED_FACE ( 'NONE', ( #216768 ), #98076, .T. ) ;
#156273=EDGE_CURVE ( 'NONE', #180198, #196244, #89433, .T. ) ;
#156275=CARTESIAN_POINT ( 'NONE',  ( 20.95512820512820440, 8.876151316299271343, -142.5586289951409640 ) ) ;
#156284=DIRECTION ( 'NONE',  ( -1.000000000000000000, -1.040834085586090568E-13, 0.000000000000000000 ) ) ;
#156289=DIRECTION ( 'NONE',  ( -2.602085213965226419E-14, -0.000000000000000000, -1.000000000000000000 ) ) ;
#156323=CARTESIAN_POINT ( 'NONE',  ( 23.25000000000000000, -11.74999999998883560, -146.1500000000000341 ) ) ;
#156374=TOROIDAL_SURFACE ( 'NONE', #247919, 0.2000000000000000111, 0.1000000000000000056 ) ;
#156382=DIRECTION ( 'NONE',  ( 0.000000000000000000, -0.000000000000000000, 1.000000000000000000 ) ) ;
#156420=CARTESIAN_POINT ( 'NONE',  ( -21.05000000000000071, 5.900000000011102586, -144.2190997646564483 ) ) ;
#156471=ORIENTED_EDGE ( 'NONE', *, *, #175404, .T. ) ;
#156495=EDGE_CURVE ( 'NONE', #251548, #16273, #243305, .T. ) ;
#156508=DIRECTION ( 'NONE',  ( 1.000000000000000000, 0.000000000000000000, 0.000000000000000000 ) ) ;
#156541=ORIENTED_EDGE ( 'NONE', *, *, #76642, .T. ) ;
#156547=EDGE_CURVE ( 'NONE', #159476, #8211, #147462, .T. ) ;
#156555=CARTESIAN_POINT ( 'NONE',  ( -20.54999999999999716, -8.999999999988846255, -143.8939691226524644 ) ) ;
#156556=DIRECTION ( 'NONE',  ( 1.000000000000000000, 0.000000000000000000, 0.000000000000000000 ) ) ;
#156572=EDGE_CURVE ( 'NONE', #46944, #241842, #230875, .T. ) ;
#156586=EDGE_LOOP ( 'NONE', ( #97596, #96085 ) ) ;
#156596=CARTESIAN_POINT ( 'NONE',  ( 20.89192007715128341, 10.32898536001801304, -173.0826683222764757 ) ) ;
#156626=DIRECTION ( 'NONE',  ( 0.000000000000000000, 1.000000000000000000, 0.000000000000000000 ) ) ;
#156661=ORIENTED_EDGE ( 'NONE', *, *, #124243, .F. ) ;
#156668=EDGE_LOOP ( 'NONE', ( #18111, #39661, #112379, #230016 ) ) ;
#156681=ORIENTED_EDGE ( 'NONE', *, *, #151923, .F. ) ;
#156684=EDGE_LOOP ( 'NONE', ( #207744, #18105, #91514, #166707, #195012 ) ) ;
#156695=CARTESIAN_POINT ( 'NONE',  ( 21.00000000000000000, 9.750000000011153745, -146.3500000000000227 ) ) ;
#156796=ADVANCED_FACE ( 'NONE', ( #23438 ), #121266, .T. ) ;
#156807=CIRCLE ( 'NONE', #123646, 0.09999999999999939493 ) ;
#156812=ORIENTED_EDGE ( 'NONE', *, *, #249128, .T. ) ;
#156813=EDGE_CURVE ( 'NONE', #170648, #52565, #18270, .T. ) ;
#156815=ORIENTED_EDGE ( 'NONE', *, *, #86285, .F. ) ;
#156835=CARTESIAN_POINT ( 'NONE',  ( 18.59999999999999076, 10.20857864377385127, -155.3500000000000227 ) ) ;
#156857=VECTOR ( 'NONE', #173779, 1000.000000000000000 ) ;
#156859=CARTESIAN_POINT ( 'NONE',  ( -18.41418431465367789, -9.499999999989068300, -174.1001893912213916 ) ) ;
#156863=DIRECTION ( 'NONE',  ( -1.000000000000000000, -2.952720810173289112E-16, 0.000000000000000000 ) ) ;
#156882=ORIENTED_EDGE ( 'NONE', *, *, #210005, .F. ) ;
#156919=EDGE_CURVE ( 'NONE', #32896, #111115, #192759, .T. ) ;
#156945=CARTESIAN_POINT ( 'NONE',  ( 21.05000000000000071, 6.257814610487288043, -133.9022097086912311 ) ) ;
#156958=EDGE_LOOP ( 'NONE', ( #113209, #76469, #7158, #130659, #232490, #66792, #17168, #121927, #130480, #107035 ) ) ;
#156966=DIRECTION ( 'NONE',  ( 0.000000000000000000, -0.4999999999999478195, 0.8660254037844686836 ) ) ;
#157024=DIRECTION ( 'NONE',  ( 0.000000000000000000, -0.1298341882520022694, -0.9915357197604852679 ) ) ;
#157025=ORIENTED_EDGE ( 'NONE', *, *, #209243, .F. ) ;
#157069=CARTESIAN_POINT ( 'NONE',  ( -21.07928932188134041, 6.328516656404449492, -133.9011048543456184 ) ) ;
#157097=EDGE_CURVE ( 'NONE', #85287, #178254, #48051, .T. ) ;
#157106=VECTOR ( 'NONE', #106400, 1000.000000000000000 ) ;
#157171=ORIENTED_EDGE ( 'NONE', *, *, #51860, .F. ) ;
#157183=CYLINDRICAL_SURFACE ( 'NONE', #85527, 0.1000000000000101225 ) ;
#157213=FACE_OUTER_BOUND ( 'NONE', #212295, .T. ) ;
#157220=ORIENTED_EDGE ( 'NONE', *, *, #76943, .T. ) ;
#157232=PLANE ( 'NONE',  #127738 ) ;
#157263=EDGE_CURVE ( 'NONE', #50799, #149928, #68644, .T. ) ;
#157316=CARTESIAN_POINT ( 'NONE',  ( -23.15000000000000213, 2.000000000011154189, -154.2753780772379173 ) ) ;
#157332=TOROIDAL_SURFACE ( 'NONE', #228040, 0.2000000000000000111, 0.1000000000000000056 ) ;
#157355=CLOSED_SHELL ( 'NONE', ( #207491, #45052, #10233, #75638, #34670, #166599, #1189, #3132, #172394, #99534, #244584, #242625, #152573, #15740, #123580, #140805, #25335, #97396, #216637, #674, #106418, #206079, #177904, #49698, #108923, #39395, #238787, #53039, #217810, #226049, #13767, #183399, #204033, #104597, #77374, #31632, #25016, #95189, #105166, #181839, #218326, #95296, #84096, #16251, #156267, #54354, #210635, #201631, #223677, #17949, #238663, #206065, #71192, #163573, #185680, #11662, #156796, #155493, #50476, #66551, #253564, #55804, #21675, #93555, #74474, #183567, #104965, #151563, #129156, #57196, #31023, #210999, #18447, #155875, #225211, #146476, #69753, #46597, #68162, #214543, #109167, #215495, #29353, #125548, #46141, #145865, #11579, #42832, #34906, #174653, #29242, #107393, #210707, #187084, #53879, #145050, #175202, #196638, #145906, #163340, #44847, #133759, #49024, #197302, #256943, #18729, #109928, #138433, #41151, #199514, #113633, #100542, #23051, #101003, #235146, #33035, #20626, #206757, #81023, #249365, #246780, #221304, #1736, #47867, #96468, #46409, #219180, #173778, #149979, #221822, #79773, #139955, #18717, #159505, #230724, #140430, #191914, #194010, #244015, #41446, #50894, #51627, #13023, #83348, #12051, #33301, #207064, #89512, #107001, #8507, #103940, #246990, #196535, #139164, #77602, #56062, #217671, #39252, #121120, #186589, #205676, #141125, #202219, #133010, #120835, #180398, #244890, #248003, #139986, #177382, #79277, #64733, #115055, #152406, #189293, #53516, #231539, #255223, #59498, #78659, #183284, #215372, #216248, #253166, #224496, #13324, #17860, #60356, #26450, #233457, #126565, #207777, #253453, #238401, #245869, #235420, #257643, #21629, #253727, #182999, #170093, #144963, #50711, #112009, #240251, #164272, #168091, #239710, #202422, #119596, #123501, #84349, #122349, #101304, #38593, #121507, #3035, #184221, #44041, #147017, #172802, #163824, #59490, #182834, #211715, #244401, #32230, #62708, #128631, #99125, #111544, #175185, #100449, #70612, #252142, #172500, #21766, #107096, #8501, #84904, #153034, #22616, #26988, #13739, #23063, #120375, #247307, #1652, #241891, #240196, #114382, #254773, #65768, #142388, #217128, #190729, #109472, #128420, #104465, #142894, #138515, #36841, #199813, #139918, #32706, #113943, #163895, #238011, #14133, #209052, #170554, #104439, #233653, #190888, #122245, #205998, #162731, #33494, #235334, #44658, #221190, #233696, #37951, #237978, #61644, #249520, #229686, #200740, #104758, #209688, #27617, #185374, #221978, #49643, #140993, #363, #254036, #102433, #198435, #13776, #50786, #82857, #55462, #80155, #173674, #219575, #193860, #105831, #60348, #119738, #70069, #52404, #187161, #2951, #119895, #225167, #92978, #231131, #163550, #105602, #89479, #55194, #215249, #78708, #158723, #233326, #194467, #240623, #205755, #43447, #66752, #61806, #165857, #255673, #185416, #225899, #215084, #24593, #128726, #132119, #212016, #149220, #199781, #119220, #247578, #177424, #248999, #123522, #236647, #61427, #95114, #144646, #205444, #215710, #191684, #218223, #246652, #108261, #7811, #33710, #51035, #249750, #172617, #491, #35777, #198663, #248031, #11121, #162112, #4257, #183388, #163988, #218133, #219157, #123998, #160878, #73553, #189385, #173399, #4509, #72396, #92402, #256662, #78630, #187329, #192709, #118262, #9219, #250731, #97133, #115025, #236691, #84632, #107644, #114204, #115322, #248683, #38937, #126206, #122637, #124979, #93289, #67347, #196086, #244536, #54691, #245075, #230267, #118240, #7458, #33676, #25845, #240791, #225554, #45482, #232203, #152092, #245206, #45209, #176146, #165789, #60230, #237498, #27970, #58599, #143464, #3480, #223243, #71867, #109490, #196398, #214531, #183899, #126123, #210384, #207640, #41828, #93571, #11010, #9612, #219871, #208913, #115227, #182462, #123933, #256959, #69495, #40494, #37554, #257109, #226156, #14950, #76101, #9546, #109457, #102014, #246116, #40853, #60300, #73145, #93692, #98852, #219184, #115339, #14475, #26371, #243734, #130409, #212692, #40508, #155721, #32637, #10898, #195515, #36428, #83765, #135916, #77427 ) ) ;
#157356=DIRECTION ( 'NONE',  ( 0.000000000000000000, 0.000000000000000000, 1.000000000000000000 ) ) ;
#157364=ORIENTED_EDGE ( 'NONE', *, *, #133002, .T. ) ;
#157403=CARTESIAN_POINT ( 'NONE',  ( -20.64999999999999858, 2.000000000011154189, -154.2753780772379173 ) ) ;
#157406=DIRECTION ( 'NONE',  ( 0.000000000000000000, 1.000000000000000000, 0.000000000000000000 ) ) ;
#157407=CARTESIAN_POINT ( 'NONE',  ( 22.50000000000000000, 0.1000000000111554016, -122.2500000000000284 ) ) ;
#157408=EDGE_CURVE ( 'NONE', #154183, #157514, #239594, .T. ) ;
#157436=CARTESIAN_POINT ( 'NONE',  ( 22.49999999999999645, 11.64987090377452184, -133.9174801091270695 ) ) ;
#157449=EDGE_CURVE ( 'NONE', #37340, #257831, #6133, .T. ) ;
#157459=DIRECTION ( 'NONE',  ( 1.000000000000000000, -0.000000000000000000, -0.000000000000000000 ) ) ;
#157462=DIRECTION ( 'NONE',  ( 0.000000000000000000, 4.510281037540195239E-13, 1.000000000000000000 ) ) ;
#157514=VERTEX_POINT ( 'NONE', #198847 ) ;
#157540=DIRECTION ( 'NONE',  ( 0.000000000000000000, 1.000000000000000000, 0.000000000000000000 ) ) ;
#157551=ORIENTED_EDGE ( 'NONE', *, *, #184123, .T. ) ;
#157569=CARTESIAN_POINT ( 'NONE',  ( 20.95083306685154056, 8.916842641901356004, -142.4773248532583807 ) ) ;
#157611=CARTESIAN_POINT ( 'NONE',  ( 23.14999999999998437, 1.115600667400684642E-11, -138.0500000000000114 ) ) ;
#157615=CYLINDRICAL_SURFACE ( 'NONE', #185032, 0.09999999999998898659 ) ;
#157648=CIRCLE ( 'NONE', #70152, 3.999999999999999112 ) ;
#157661=VERTEX_POINT ( 'NONE', #63180 ) ;
#157668=AXIS2_PLACEMENT_3D ( 'NONE', #182076, #25573, #105049 ) ;
#157689=EDGE_CURVE ( 'NONE', #56718, #59718, #86581, .T. ) ;
#157713=FACE_OUTER_BOUND ( 'NONE', #220743, .T. ) ;
#157735=EDGE_LOOP ( 'NONE', ( #218911, #233296, #227246, #183472 ) ) ;
#157741=EDGE_CURVE ( 'NONE', #143461, #219189, #44925, .T. ) ;
#157748=DIRECTION ( 'NONE',  ( 2.952720810173288619E-16, -1.000000000000000000, 0.000000000000000000 ) ) ;
#157790=ORIENTED_EDGE ( 'NONE', *, *, #155869, .T. ) ;
#157842=ORIENTED_EDGE ( 'NONE', *, *, #90946, .T. ) ;
#157867=CARTESIAN_POINT ( 'NONE',  ( -20.54999999999999716, -8.663551401858001100, -157.9758988819327215 ) ) ;
#157882=CIRCLE ( 'NONE', #178523, 11.75000000000001066 ) ;
#157889=CARTESIAN_POINT ( 'NONE',  ( 20.94999027547553894, 10.29326151435327219, -172.9592822510415147 ) ) ;
#157909=ORIENTED_EDGE ( 'NONE', *, *, #218752, .F. ) ;
#157937=CIRCLE ( 'NONE', #112119, 0.1000000000000000472 ) ;
#157938=EDGE_CURVE ( 'NONE', #55661, #230402, #86135, .T. ) ;
#157939=VECTOR ( 'NONE', #15408, 1000.000000000000000 ) ;
#157940=DIRECTION ( 'NONE',  ( 0.000000000000000000, 1.000000000000000000, 0.000000000000000000 ) ) ;
#157963=VERTEX_POINT ( 'NONE', #167028 ) ;
#157993=EDGE_LOOP ( 'NONE', ( #7609, #184600, #117824, #241300 ) ) ;
#157999=AXIS2_PLACEMENT_3D ( 'NONE', #42623, #197840, #99998 ) ;
#158044=ORIENTED_EDGE ( 'NONE', *, *, #234358, .F. ) ;
#158050=ORIENTED_EDGE ( 'NONE', *, *, #3507, .F. ) ;
#158058=PLANE ( 'NONE',  #177809 ) ;
#158073=AXIS2_PLACEMENT_3D ( 'NONE', #48427, #5428, #206230 ) ;
#158080=CIRCLE ( 'NONE', #128998, 0.09999999999999939493 ) ;
#158089=AXIS2_PLACEMENT_3D ( 'NONE', #122375, #201906, #182354 ) ;
#158101=DIRECTION ( 'NONE',  ( 1.000000000000000000, 0.000000000000000000, 0.000000000000000000 ) ) ;
#158104=CIRCLE ( 'NONE', #187292, 0.09999999999998898659 ) ;
#158124=VERTEX_POINT ( 'NONE', #173471 ) ;
#158131=CARTESIAN_POINT ( 'NONE',  ( -18.50000000000000000, 1.115600667400684642E-11, -167.5000000000000284 ) ) ;
#158181=ORIENTED_EDGE ( 'NONE', *, *, #122451, .T. ) ;
#158190=VERTEX_POINT ( 'NONE', #61376 ) ;
#158221=DIRECTION ( 'NONE',  ( 1.000000000000000000, -0.000000000000000000, -0.000000000000000000 ) ) ;
#158223=ORIENTED_EDGE ( 'NONE', *, *, #86709, .F. ) ;
#158228=VERTEX_POINT ( 'NONE', #199630 ) ;
#158230=ORIENTED_EDGE ( 'NONE', *, *, #127928, .F. ) ;
#158236=EDGE_LOOP ( 'NONE', ( #17318, #28702, #96050, #152526 ) ) ;
#158242=CARTESIAN_POINT ( 'NONE',  ( 21.04999999999999361, 6.299230910098046365, -133.9015625000000114 ) ) ;
#158261=AXIS2_PLACEMENT_3D ( 'NONE', #167620, #247119, #230136 ) ;
#158302=DIRECTION ( 'NONE',  ( 0.000000000000000000, -1.000000000000000000, 0.000000000000000000 ) ) ;
#158306=EDGE_CURVE ( 'NONE', #162622, #157661, #23578, .T. ) ;
#158308=CARTESIAN_POINT ( 'NONE',  ( -20.85000000000000142, -1.164121893230052995, -175.4148480855716059 ) ) ;
#158356=LINE ( 'NONE', #39684, #172654 ) ;
#158427=DIRECTION ( 'NONE',  ( -0.000000000000000000, -0.000000000000000000, 1.000000000000000000 ) ) ;
#158435=AXIS2_PLACEMENT_3D ( 'NONE', #76878, #174754, #134278 ) ;
#158450=ORIENTED_EDGE ( 'NONE', *, *, #79657, .T. ) ;
#158456=CARTESIAN_POINT ( 'NONE',  ( 23.14999999999999858, 4.813084112160680661, -145.9415177565238366 ) ) ;
#158471=ORIENTED_EDGE ( 'NONE', *, *, #249286, .F. ) ;
#158486=TOROIDAL_SURFACE ( 'NONE', #25206, 0.2000000000000000111, 0.1000000000000000056 ) ;
#158558=LINE ( 'NONE', #60695, #90145 ) ;
#158562=ORIENTED_EDGE ( 'NONE', *, *, #180288, .F. ) ;
#158573=EDGE_CURVE ( 'NONE', #136758, #132345, #169242, .T. ) ;
#158583=ORIENTED_EDGE ( 'NONE', *, *, #95209, .T. ) ;
#158592=AXIS2_PLACEMENT_3D ( 'NONE', #108357, #91365, #50909 ) ;
#158595=EDGE_LOOP ( 'NONE', ( #205728, #134414, #217545, #141327 ) ) ;
#158625=VERTEX_POINT ( 'NONE', #257926 ) ;
#158641=AXIS2_PLACEMENT_3D ( 'NONE', #226504, #47877, #28371 ) ;
#158689=ORIENTED_EDGE ( 'NONE', *, *, #256294, .T. ) ;
#158694=ORIENTED_EDGE ( 'NONE', *, *, #90828, .F. ) ;
#158707=DIRECTION ( 'NONE',  ( 0.000000000000000000, 0.000000000000000000, -1.000000000000000000 ) ) ;
#158716=CIRCLE ( 'NONE', #238347, 0.09999999999998898659 ) ;
#158723=ADVANCED_FACE ( 'NONE', ( #2355 ), #164024, .T. ) ;
#158725=ORIENTED_EDGE ( 'NONE', *, *, #40448, .T. ) ;
#158764=CARTESIAN_POINT ( 'NONE',  ( -20.64999999999999858, -8.999999999988844479, -157.6060308773475924 ) ) ;
#158765=AXIS2_PLACEMENT_3D ( 'NONE', #108890, #111467, #9795 ) ;
#158812=ORIENTED_EDGE ( 'NONE', *, *, #152861, .F. ) ;
#158816=CARTESIAN_POINT ( 'NONE',  ( 21.13507111622890022, 10.71768338700954537, -146.2491685863608097 ) ) ;
#158823=CARTESIAN_POINT ( 'NONE',  ( -18.59999999999999787, -1.164121893230052995, -175.4148480855716059 ) ) ;
#158828=ORIENTED_EDGE ( 'NONE', *, *, #20852, .F. ) ;
#158832=CARTESIAN_POINT ( 'NONE',  ( 20.95224633520496127, 8.900522166568386240, -142.4932764479212892 ) ) ;
#158845=CARTESIAN_POINT ( 'NONE',  ( -21.05000000000000071, -11.48912529306489994, -164.4000000000000057 ) ) ;
#158881=ORIENTED_EDGE ( 'NONE', *, *, #201004, .T. ) ;
#158889=ORIENTED_EDGE ( 'NONE', *, *, #45901, .F. ) ;
#158903=ORIENTED_EDGE ( 'NONE', *, *, #44759, .T. ) ;
#158935=ORIENTED_EDGE ( 'NONE', *, *, #21274, .F. ) ;
#158942=TOROIDAL_SURFACE ( 'NONE', #63036, 11.70000000000000107, 0.1000000000000000056 ) ;
#158950=CARTESIAN_POINT ( 'NONE',  ( -21.14999999999999858, -11.74999999998884448, -134.0000000000000000 ) ) ;
#158959=AXIS2_PLACEMENT_3D ( 'NONE', #101661, #37899, #120013 ) ;
#158970=DIRECTION ( 'NONE',  ( 1.000000000000000000, -0.000000000000000000, -0.000000000000000000 ) ) ;
#158986=AXIS2_PLACEMENT_3D ( 'NONE', #84276, #43924, #83016 ) ;
#159005=CARTESIAN_POINT ( 'NONE',  ( -23.25000000000000000, -11.64999999998884483, -122.2500000000000284 ) ) ;
#159009=AXIS2_PLACEMENT_3D ( 'NONE', #214114, #95443, #89323 ) ;
#159019=DIRECTION ( 'NONE',  ( 1.000000000000000000, 0.000000000000000000, 0.000000000000000000 ) ) ;
#159022=CYLINDRICAL_SURFACE ( 'NONE', #137540, 0.1000000000000098310 ) ;
#159043=CIRCLE ( 'NONE', #196412, 0.09999999999998898659 ) ;
#159066=EDGE_LOOP ( 'NONE', ( #51062, #42124, #237703, #68518 ) ) ;
#159069=DIRECTION ( 'NONE',  ( -0.7071067811865388020, 0.7071067811865561215, 0.000000000000000000 ) ) ;
#159084=VERTEX_POINT ( 'NONE', #179438 ) ;
#159118=AXIS2_PLACEMENT_3D ( 'NONE', #210047, #52220, #13124 ) ;
#159131=CARTESIAN_POINT ( 'NONE',  ( -21.05000000000000071, -11.64999999998884306, -164.5000000000000000 ) ) ;
#159132=CARTESIAN_POINT ( 'NONE',  ( -20.94999999999999929, 1.115600667400684642E-11, -167.5000000000000284 ) ) ;
#159150=CARTESIAN_POINT ( 'NONE',  ( 20.94999999999999929, 10.29288807859936838, -172.9580020160121876 ) ) ;
#159195=LINE ( 'NONE', #199604, #114101 ) ;
#159233=VERTEX_POINT ( 'NONE', #17469 ) ;
#159241=ORIENTED_EDGE ( 'NONE', *, *, #248653, .T. ) ;
#159292=AXIS2_PLACEMENT_3D ( 'NONE', #64709, #47698, #8592 ) ;
#159296=CIRCLE ( 'NONE', #225874, 11.64999999999999325 ) ;
#159310=CARTESIAN_POINT ( 'NONE',  ( 18.59999999999999787, -1.362429037182151470, -175.3888812479212334 ) ) ;
#159314=DIRECTION ( 'NONE',  ( 1.000000000000000000, 0.000000000000000000, 0.000000000000000000 ) ) ;
#159320=CIRCLE ( 'NONE', #42584, 7.899999999999990585 ) ;
#159346=VERTEX_POINT ( 'NONE', #21354 ) ;
#159361=AXIS2_PLACEMENT_3D ( 'NONE', #158131, #235063, #282 ) ;
#159375=ORIENTED_EDGE ( 'NONE', *, *, #206587, .T. ) ;
#159384=VERTEX_POINT ( 'NONE', #61736 ) ;
#159395=CARTESIAN_POINT ( 'NONE',  ( 21.05000000000000071, 0.09779029131994770863, -127.7421853895238968 ) ) ;
#159403=EDGE_CURVE ( 'NONE', #106574, #142904, #40431, .T. ) ;
#159409=CARTESIAN_POINT ( 'NONE',  ( -18.46907102845852577, -9.473727364752955182, -174.1760347387365471 ) ) ;
#159446=CARTESIAN_POINT ( 'NONE',  ( 21.04999999999999716, 6.304455821958825368, -134.0210354765401348 ) ) ;
#159451=EDGE_CURVE ( 'NONE', #229756, #46556, #194538, .T. ) ;
#159471=EDGE_CURVE ( 'NONE', #156063, #53590, #136206, .T. ) ;
#159476=VERTEX_POINT ( 'NONE', #27781 ) ;
#159500=ORIENTED_EDGE ( 'NONE', *, *, #248670, .T. ) ;
#159501=DIRECTION ( 'NONE',  ( 0.000000000000000000, 0.000000000000000000, -1.000000000000000000 ) ) ;
#159505=ADVANCED_FACE ( 'NONE', ( #225910 ), #8198, .T. ) ;
#159510=ORIENTED_EDGE ( 'NONE', *, *, #178662, .T. ) ;
#159530=LINE ( 'NONE', #196080, #204394 ) ;
#159533=ORIENTED_EDGE ( 'NONE', *, *, #229133, .F. ) ;
#159543=ORIENTED_EDGE ( 'NONE', *, *, #222749, .T. ) ;
#159545=PLANE ( 'NONE',  #118814 ) ;
#159586=CARTESIAN_POINT ( 'NONE',  ( -21.00219873199047171, 11.60538868788763089, -140.9126474282950312 ) ) ;
#159600=DIRECTION ( 'NONE',  ( 0.000000000000000000, 0.000000000000000000, -1.000000000000000000 ) ) ;
#159609=EDGE_CURVE ( 'NONE', #104833, #229356, #177780, .T. ) ;
#159630=DIRECTION ( 'NONE',  ( 0.000000000000000000, 1.000000000000000000, -6.308085367188393199E-16 ) ) ;
#159642=DIRECTION ( 'NONE',  ( 0.000000000000000000, 0.1350103645451876666, -0.9908441862701600211 ) ) ;
#159661=CIRCLE ( 'NONE', #51294, 0.5000000000000004441 ) ;
#159663=AXIS2_PLACEMENT_3D ( 'NONE', #61963, #103621, #118072 ) ;
#159686=DIRECTION ( 'NONE',  ( 1.000000000000000000, 0.000000000000000000, 0.000000000000000000 ) ) ;
#159688=CARTESIAN_POINT ( 'NONE',  ( -22.50000000000000000, 1.115600667400684642E-11, -122.3504291924552234 ) ) ;
#159704=CARTESIAN_POINT ( 'NONE',  ( -23.25000000000000000, 1.115651490242849210E-11, -129.8500000000000227 ) ) ;
#159736=DIRECTION ( 'NONE',  ( 3.469446951953498700E-14, -0.7899159663865300551, -0.6132151058540831201 ) ) ;
#159780=DIRECTION ( 'NONE',  ( 3.469446951953635015E-14, -0.000000000000000000, 1.000000000000000000 ) ) ;
#159790=VERTEX_POINT ( 'NONE', #230456 ) ;
#159798=CARTESIAN_POINT ( 'NONE',  ( 18.49999999999999289, 10.29270135741298731, -172.9573618871519614 ) ) ;
#159805=EDGE_LOOP ( 'NONE', ( #193817, #172336, #91532, #156681 ) ) ;
#159834=DIRECTION ( 'NONE',  ( 0.000000000000000000, 0.000000000000000000, 1.000000000000000000 ) ) ;
#159855=EDGE_LOOP ( 'NONE', ( #119388, #203107, #174982, #204791 ) ) ;
#159869=CIRCLE ( 'NONE', #189076, 0.09999999999998898659 ) ;
#159898=ORIENTED_EDGE ( 'NONE', *, *, #145875, .F. ) ;
#159919=DIRECTION ( 'NONE',  ( -0.000000000000000000, -0.000000000000000000, 1.000000000000000000 ) ) ;
#159936=EDGE_CURVE ( 'NONE', #173723, #134395, #244566, .T. ) ;
#159937=CARTESIAN_POINT ( 'NONE',  ( -21.05000000000000071, -0.08579911626261706170, -127.5860211185120221 ) ) ;
#159966=VERTEX_POINT ( 'NONE', #34851 ) ;
#159967=CARTESIAN_POINT ( 'NONE',  ( -18.41799967126738480, -9.499999999988851584, -141.0320698132550774 ) ) ;
#159982=AXIS2_PLACEMENT_3D ( 'NONE', #126905, #42234, #102163 ) ;
#159986=DIRECTION ( 'NONE',  ( -1.000000000000000000, 0.000000000000000000, 0.000000000000000000 ) ) ;
#160012=EDGE_CURVE ( 'NONE', #237128, #186823, #200314, .T. ) ;
#160037=EDGE_LOOP ( 'NONE', ( #66946, #194872, #234938, #187741 ) ) ;
#160050=VECTOR ( 'NONE', #210548, 1000.000000000000000 ) ;
#160074=DIRECTION ( 'NONE',  ( 0.000000000000000000, 0.9998779222360102414, 0.01562499999996356907 ) ) ;
#160091=CARTESIAN_POINT ( 'NONE',  ( -20.94999999999999574, 11.62071067812980907, -160.6315833476590456 ) ) ;
#160107=ORIENTED_EDGE ( 'NONE', *, *, #62413, .F. ) ;
#160118=CIRCLE ( 'NONE', #72628, 11.69999999999998863 ) ;
#160127=DIRECTION ( 'NONE',  ( 0.000000000000000000, 0.000000000000000000, -1.000000000000000000 ) ) ;
#160144=EDGE_LOOP ( 'NONE', ( #162295, #27456, #158903, #143261 ) ) ;
#160207=CYLINDRICAL_SURFACE ( 'NONE', #216059, 0.09999999999998898659 ) ;
#160213=DIRECTION ( 'NONE',  ( 0.000000000000000000, 1.000000000000000000, 0.000000000000000000 ) ) ;
#160216=VERTEX_POINT ( 'NONE', #28119 ) ;
#160218=CARTESIAN_POINT ( 'NONE',  ( -21.14999999999999858, 11.75000000001115552, -140.7838656629781724 ) ) ;
#160269=EDGE_LOOP ( 'NONE', ( #7843, #192675, #216174, #174412, #171913, #111105 ) ) ;
#160275=CARTESIAN_POINT ( 'NONE',  ( -20.64999999999999858, 7.150000000011155876, -155.2500000000000284 ) ) ;
#160303=DIRECTION ( 'NONE',  ( 1.000000000000000000, 0.000000000000000000, 0.000000000000000000 ) ) ;
#160307=CARTESIAN_POINT ( 'NONE',  ( -22.59999999999999787, 11.74956712350054566, -133.8991416309013118 ) ) ;
#160322=EDGE_LOOP ( 'NONE', ( #61186, #299, #256291, #137359 ) ) ;
#160335=ORIENTED_EDGE ( 'NONE', *, *, #163708, .F. ) ;
#160361=CARTESIAN_POINT ( 'NONE',  ( -21.05000000000000071, -0.09999999998884338825, -127.4593430482987912 ) ) ;
#160364=LINE ( 'NONE', #82038, #201335 ) ;
#160381=ORIENTED_EDGE ( 'NONE', *, *, #205610, .F. ) ;
#160382=CARTESIAN_POINT ( 'NONE',  ( -23.15000000000000213, 11.65000000001115588, -160.4851942293460638 ) ) ;
#160394=VERTEX_POINT ( 'NONE', #4356 ) ;
#160398=CYLINDRICAL_SURFACE ( 'NONE', #145073, 0.5000000000000004441 ) ;
#160417=CARTESIAN_POINT ( 'NONE',  ( -21.05000000000000071, -11.74999999998884448, -164.4000000000000057 ) ) ;
#160435=CIRCLE ( 'NONE', #23056, 0.09999999999999817368 ) ;
#160439=CARTESIAN_POINT ( 'NONE',  ( 20.90851465518106167, 10.32532329027886320, -173.0699343018359855 ) ) ;
#160452=DIRECTION ( 'NONE',  ( -0.000000000000000000, 0.000000000000000000, 1.000000000000000000 ) ) ;
#160467=DIRECTION ( 'NONE',  ( 1.000000000000000000, -0.000000000000000000, -0.000000000000000000 ) ) ;
#160485=EDGE_CURVE ( 'NONE', #146074, #87859, #249417, .T. ) ;
#160489=AXIS2_PLACEMENT_3D ( 'NONE', #133357, #90359, #253282 ) ;
#160508=CARTESIAN_POINT ( 'NONE',  ( -23.15000000000000213, 1.115600667400684642E-11, -167.5000000000000284 ) ) ;
#160538=DIRECTION ( 'NONE',  ( 1.000000000000000000, 0.000000000000000000, 0.000000000000000000 ) ) ;
#160547=DIRECTION ( 'NONE',  ( -1.000000000000000000, 0.000000000000000000, 0.000000000000000000 ) ) ;
#160569=CARTESIAN_POINT ( 'NONE',  ( 18.59999999999999432, 1.162701749949165642, -142.1000000000000227 ) ) ;
#160572=VERTEX_POINT ( 'NONE', #151622 ) ;
#160595=CARTESIAN_POINT ( 'NONE',  ( -23.25000000000000000, 7.021664781911246322, -171.3335654018973173 ) ) ;
#160626=CARTESIAN_POINT ( 'NONE',  ( -21.64999999999999858, 7.350000000011155166, -146.3500000000000227 ) ) ;
#160655=VERTEX_POINT ( 'NONE', #195876 ) ;
#160661=CARTESIAN_POINT ( 'NONE',  ( -22.43310005002225438, 0.005636942152031573783, -122.3503378728656230 ) ) ;
#160666=CARTESIAN_POINT ( 'NONE',  ( 20.95429693346634181, 10.54330487990709209, -141.5608825383131659 ) ) ;
#160669=AXIS2_PLACEMENT_3D ( 'NONE', #13803, #248554, #93330 ) ;
#160682=CYLINDRICAL_SURFACE ( 'NONE', #165922, 0.09999999999998898659 ) ;
#160716=CARTESIAN_POINT ( 'NONE',  ( 20.96077737575349786, 11.62390063401585394, -160.6407919571063303 ) ) ;
#160787=LINE ( 'NONE', #62937, #216695 ) ;
#160793=FACE_OUTER_BOUND ( 'NONE', #39482, .T. ) ;
#160797=ORIENTED_EDGE ( 'NONE', *, *, #97142, .T. ) ;
#160838=ORIENTED_EDGE ( 'NONE', *, *, #139476, .T. ) ;
#160853=CARTESIAN_POINT ( 'NONE',  ( 21.05000000000000426, 0.06570161033324331545, -127.7416839426680184 ) ) ;
#160878=ADVANCED_FACE ( 'NONE', ( #229555 ), #161945, .T. ) ;
#160891=CARTESIAN_POINT ( 'NONE',  ( -23.15000000000000213, 1.115600667400684642E-11, -155.7000000000000455 ) ) ;
#160910=CARTESIAN_POINT ( 'NONE',  ( 20.94999999999999574, 1.849084418638171856, -145.6560105214471434 ) ) ;
#160923=DIRECTION ( 'NONE',  ( 1.000000000000000000, 0.000000000000000000, 0.000000000000000000 ) ) ;
#160926=DIRECTION ( 'NONE',  ( -0.000000000000000000, 0.000000000000000000, 1.000000000000000000 ) ) ;
#160943=FACE_OUTER_BOUND ( 'NONE', #47728, .T. ) ;
#160945=EDGE_CURVE ( 'NONE', #242008, #111920, #82767, .T. ) ;
#160948=PLANE ( 'NONE',  #24470 ) ;
#160953=ORIENTED_EDGE ( 'NONE', *, *, #237370, .T. ) ;
#160958=EDGE_CURVE ( 'NONE', #118232, #92094, #157882, .T. ) ;
#160974=CARTESIAN_POINT ( 'NONE',  ( 21.14999999999999858, 6.550000000011156231, -146.3500000000000227 ) ) ;
#161010=ORIENTED_EDGE ( 'NONE', *, *, #82271, .F. ) ;
#161059=EDGE_CURVE ( 'NONE', #238843, #83407, #174751, .T. ) ;
#161123=ORIENTED_EDGE ( 'NONE', *, *, #126168, .T. ) ;
#161138=ORIENTED_EDGE ( 'NONE', *, *, #104156, .F. ) ;
#161168=CIRCLE ( 'NONE', #115372, 0.09999999999998898659 ) ;
#161202=VERTEX_POINT ( 'NONE', #238523 ) ;
#161216=AXIS2_PLACEMENT_3D ( 'NONE', #185334, #65381, #144900 ) ;
#161237=AXIS2_PLACEMENT_3D ( 'NONE', #83430, #200849, #104289 ) ;
#161239=DIRECTION ( 'NONE',  ( -6.938893903907222856E-15, 1.000000000000000000, 2.891205793294679805E-16 ) ) ;
#161254=ORIENTED_EDGE ( 'NONE', *, *, #67960, .T. ) ;
#161260=DIRECTION ( 'NONE',  ( 1.000000000000000000, 0.000000000000000000, 0.000000000000000000 ) ) ;
#161265=EDGE_CURVE ( 'NONE', #202658, #248652, #37224, .T. ) ;
#161278=DIRECTION ( 'NONE',  ( 0.000000000000000000, 1.000000000000000000, 0.000000000000000000 ) ) ;
#161297=ORIENTED_EDGE ( 'NONE', *, *, #209001, .F. ) ;
#161301=CARTESIAN_POINT ( 'NONE',  ( 21.53699400384038753, 1.197367947672160239E-11, -127.2122882067533709 ) ) ;
#161308=AXIS2_PLACEMENT_3D ( 'NONE', #206847, #162597, #141728 ) ;
#161322=CARTESIAN_POINT ( 'NONE',  ( 21.05000000000000071, -8.999999999988842703, -158.1060308773475640 ) ) ;
#161326=CYLINDRICAL_SURFACE ( 'NONE', #256394, 0.09999999999999939493 ) ;
#161333=CARTESIAN_POINT ( 'NONE',  ( 22.60000000000000142, 0.1008583691098682150, -122.2504328765106294 ) ) ;
#161354=DIRECTION ( 'NONE',  ( 1.000000000000000000, -0.000000000000000000, -0.000000000000000000 ) ) ;
#161355=( BOUNDED_CURVE ( )  B_SPLINE_CURVE ( 3, ( #42758, #243521, #66172, #184825 ),
 .UNSPECIFIED., .F., .F. ) 
 B_SPLINE_CURVE_WITH_KNOTS ( ( 4, 4 ),
 ( 4.712388980384689674, 6.231880751915385375 ),
 .UNSPECIFIED. ) 
 CURVE ( )  GEOMETRIC_REPRESENTATION_ITEM ( )  RATIONAL_B_SPLINE_CURVE ( ( 1.000000000000000000, 0.8166740347213230500, 0.8166740347213230500, 1.000000000000000000 ) ) 
 REPRESENTATION_ITEM ( '' )  );
#161369=EDGE_LOOP ( 'NONE', ( #172335, #97621, #133179, #137342 ) ) ;
#161382=AXIS2_PLACEMENT_3D ( 'NONE', #87236, #186370, #224188 ) ;
#161414=DIRECTION ( 'NONE',  ( -1.000000000000000000, -0.000000000000000000, -0.000000000000000000 ) ) ;
#161430=ORIENTED_EDGE ( 'NONE', *, *, #191068, .T. ) ;
#161517=CIRCLE ( 'NONE', #178279, 0.09999999999999939493 ) ;
#161587=CARTESIAN_POINT ( 'NONE',  ( -22.50000000000000000, 11.64957080755595520, -133.9000000000000057 ) ) ;
#161658=FACE_OUTER_BOUND ( 'NONE', #23305, .T. ) ;
#161662=DIRECTION ( 'NONE',  ( 1.000000000000000000, 0.000000000000000000, -0.000000000000000000 ) ) ;
#161677=DIRECTION ( 'NONE',  ( 1.000000000000000000, -0.000000000000000000, -0.000000000000000000 ) ) ;
#161681=CARTESIAN_POINT ( 'NONE',  ( -20.94999999999999929, 1.115600667400684642E-11, -163.4000000000000341 ) ) ;
#161697=PLANE ( 'NONE',  #243254 ) ;
#161712=DIRECTION ( 'NONE',  ( 0.000000000000000000, 1.000000000000000000, 0.000000000000000000 ) ) ;
#161746=CARTESIAN_POINT ( 'NONE',  ( 21.05000000000000071, -9.499999999988844479, -157.6060308773475640 ) ) ;
#161772=CIRCLE ( 'NONE', #90809, 11.80000000000000426 ) ;
#161773=ORIENTED_EDGE ( 'NONE', *, *, #103494, .F. ) ;
#161782=ORIENTED_EDGE ( 'NONE', *, *, #43398, .T. ) ;
#161795=DIRECTION ( 'NONE',  ( -1.000000000000000000, 0.000000000000000000, 0.000000000000000000 ) ) ;
#161800=ORIENTED_EDGE ( 'NONE', *, *, #228588, .F. ) ;
#161824=CYLINDRICAL_SURFACE ( 'NONE', #252971, 0.1000000000000089567 ) ;
#161830=DIRECTION ( 'NONE',  ( 1.000000000000000000, 0.000000000000000000, 0.000000000000000000 ) ) ;
#161861=DIRECTION ( 'NONE',  ( 0.000000000000000000, 0.1495327102803792052, 0.9887567792719320625 ) ) ;
#161871=DIRECTION ( 'NONE',  ( 1.000000000000000000, -0.000000000000000000, -0.000000000000000000 ) ) ;
#161917=EDGE_LOOP ( 'NONE', ( #79132, #37947, #139630, #89754 ) ) ;
#161925=DIRECTION ( 'NONE',  ( -1.000000000000000000, 0.000000000000000000, 0.000000000000000000 ) ) ;
#161945=TOROIDAL_SURFACE ( 'NONE', #191169, 11.65000000000000036, 0.1000000000000000056 ) ;
#161956=CARTESIAN_POINT ( 'NONE',  ( 21.30000000000002558, 1.115600667400684642E-11, -134.0000000000000000 ) ) ;
#161970=VERTEX_POINT ( 'NONE', #194034 ) ;
#161989=CARTESIAN_POINT ( 'NONE',  ( 21.02374657821588855, 11.60000000083178406, -160.5717967701983184 ) ) ;
#162004=DIRECTION ( 'NONE',  ( 0.7071067811865474617, 0.7071067811865474617, -0.000000000000000000 ) ) ;
#162030=SPHERICAL_SURFACE ( 'NONE', #122404, 0.1000000000000000056 ) ;
#162039=CARTESIAN_POINT ( 'NONE',  ( 20.94999999999999574, -1.162701749926853712, -142.1000000000000227 ) ) ;
#162044=DIRECTION ( 'NONE',  ( 1.000000000000000000, -0.000000000000000000, -0.000000000000000000 ) ) ;
#162051=EDGE_LOOP ( 'NONE', ( #28392, #186454, #76087, #62811 ) ) ;
#162055=VERTEX_POINT ( 'NONE', #201705 ) ;
#162058=CARTESIAN_POINT ( 'NONE',  ( -20.64999999999999858, 2.000000000011154189, -154.6753780772379514 ) ) ;
#162102=CARTESIAN_POINT ( 'NONE',  ( -21.05000000000000071, -1.162701749926853712, -142.0000000000000284 ) ) ;
#162112=ADVANCED_FACE ( 'NONE', ( #185998 ), #126011, .F. ) ;
#162123=CARTESIAN_POINT ( 'NONE',  ( 21.87500000000000355, 9.750000000011153745, -155.1500000000000057 ) ) ;
#162136=CARTESIAN_POINT ( 'NONE',  ( -18.59999999999999787, 11.65000000001115232, -155.3500000000000227 ) ) ;
#162159=CARTESIAN_POINT ( 'NONE',  ( 20.21494484322224849, 9.303170737879936425, -142.3402651917702997 ) ) ;
#162160=DIRECTION ( 'NONE',  ( 1.000000000000000000, 0.000000000000000000, 0.000000000000000000 ) ) ;
#162207=VECTOR ( 'NONE', #68609, 1000.000000000000000 ) ;
#162217=CARTESIAN_POINT ( 'NONE',  ( -20.54999999999999716, 7.250000000011155521, -146.2500000000000284 ) ) ;
#162220=CYLINDRICAL_SURFACE ( 'NONE', #206731, 0.09999999999999939493 ) ;
#162239=CYLINDRICAL_SURFACE ( 'NONE', #28602, 0.09999999999999939493 ) ;
#162263=CYLINDRICAL_SURFACE ( 'NONE', #192369, 0.09999999999999939493 ) ;
#162295=ORIENTED_EDGE ( 'NONE', *, *, #179030, .F. ) ;
#162341=EDGE_CURVE ( 'NONE', #175390, #71001, #104518, .T. ) ;
#162342=DIRECTION ( 'NONE',  ( -0.000000000000000000, -0.1350103645451876666, -0.9908441862701600211 ) ) ;
#162366=AXIS2_PLACEMENT_3D ( 'NONE', #43090, #39263, #78347 ) ;
#162367=ORIENTED_EDGE ( 'NONE', *, *, #110445, .T. ) ;
#162372=EDGE_LOOP ( 'NONE', ( #138612, #60364, #138634, #77764 ) ) ;
#162428=CIRCLE ( 'NONE', #70862, 0.09999999999998898659 ) ;
#162434=VECTOR ( 'NONE', #131443, 1000.000000000000000 ) ;
#162446=DIRECTION ( 'NONE',  ( 0.000000000000000000, 0.000000000000000000, -1.000000000000000000 ) ) ;
#162454=DIRECTION ( 'NONE',  ( -0.000000000000000000, -0.000000000000000000, 1.000000000000000000 ) ) ;
#162474=CARTESIAN_POINT ( 'NONE',  ( 20.95576188350343116, 10.60898054497455512, -141.6112337227543208 ) ) ;
#162480=ORIENTED_EDGE ( 'NONE', *, *, #238701, .F. ) ;
#162481=CARTESIAN_POINT ( 'NONE',  ( 18.50000972452444969, 10.29326151435342851, -172.9592822510414578 ) ) ;
#162494=CIRCLE ( 'NONE', #191549, 0.09999999999999939493 ) ;
#162548=CARTESIAN_POINT ( 'NONE',  ( -18.31331870001081086, -9.536294719169568168, -174.3685786909853732 ) ) ;
#162577=DIRECTION ( 'NONE',  ( 0.000000000000000000, 1.000000000000000000, -0.000000000000000000 ) ) ;
#162584=CARTESIAN_POINT ( 'NONE',  ( -22.48660254037843487, 11.65000000001115588, -133.9500000000000455 ) ) ;
#162597=DIRECTION ( 'NONE',  ( 0.000000000000000000, -0.000000000000000000, 1.000000000000000000 ) ) ;
#162622=VERTEX_POINT ( 'NONE', #133110 ) ;
#162649=AXIS2_PLACEMENT_3D ( 'NONE', #125746, #185739, #205277 ) ;
#162670=TOROIDAL_SURFACE ( 'NONE', #66805, 11.65000000000000036, 0.1000000000000000056 ) ;
#162674=CIRCLE ( 'NONE', #241771, 0.09999999999999939493 ) ;
#162678=CARTESIAN_POINT ( 'NONE',  ( 22.46250603428203618, 0.02114417614996233138, -122.3501369026599264 ) ) ;
#162684=ORIENTED_EDGE ( 'NONE', *, *, #108338, .F. ) ;
#162731=ADVANCED_FACE ( 'NONE', ( #198204 ), #138208, .T. ) ;
#162739=CARTESIAN_POINT ( 'NONE',  ( -18.59999999999999787, 11.65000000001115232, -141.0148057706540214 ) ) ;
#162785=LINE ( 'NONE', #205734, #153237 ) ;
#162821=ORIENTED_EDGE ( 'NONE', *, *, #133528, .F. ) ;
#162842=CARTESIAN_POINT ( 'NONE',  ( 20.94999999999999929, 11.65000000001115943, -160.6583993101029648 ) ) ;
#162850=CARTESIAN_POINT ( 'NONE',  ( 21.05000000000000071, 1.115600667400684642E-11, -134.0000000000000000 ) ) ;
#162873=AXIS2_PLACEMENT_3D ( 'NONE', #43640, #20229, #159736 ) ;
#162877=AXIS2_PLACEMENT_3D ( 'NONE', #190887, #153060, #236397 ) ;
#162883=AXIS2_PLACEMENT_3D ( 'NONE', #226117, #127049, #25400 ) ;
#162888=DIRECTION ( 'NONE',  ( 1.000000000000000000, -0.000000000000000000, -0.000000000000000000 ) ) ;
#162891=FACE_OUTER_BOUND ( 'NONE', #93603, .T. ) ;
#162893=VECTOR ( 'NONE', #134937, 1000.000000000000000 ) ;
#162903=CARTESIAN_POINT ( 'NONE',  ( 22.49999999999999645, 0.04562336060759585726, -122.3494956614463405 ) ) ;
#162909=CYLINDRICAL_SURFACE ( 'NONE', #117929, 4.049999999999998046 ) ;
#162931=EDGE_LOOP ( 'NONE', ( #131674, #204197, #230741, #218156 ) ) ;
#162977=CARTESIAN_POINT ( 'NONE',  ( 21.05000000000000071, -0.09999993529482809063, -127.5219217789050674 ) ) ;
#163035=VECTOR ( 'NONE', #180189, 1000.000000000000000 ) ;
#163068=ORIENTED_EDGE ( 'NONE', *, *, #121231, .F. ) ;
#163107=EDGE_CURVE ( 'NONE', #126399, #115616, #12450, .T. ) ;
#163128=LINE ( 'NONE', #237520, #139122 ) ;
#163142=ORIENTED_EDGE ( 'NONE', *, *, #249655, .T. ) ;
#163149=CARTESIAN_POINT ( 'NONE',  ( 21.14999999999999858, 6.540656951712400691, -134.0000000000000000 ) ) ;
#163154=CARTESIAN_POINT ( 'NONE',  ( 21.05000000000000071, 1.115600667400684642E-11, -134.0000000000000000 ) ) ;
#163186=ORIENTED_EDGE ( 'NONE', *, *, #151635, .F. ) ;
#163189=VERTEX_POINT ( 'NONE', #143034 ) ;
#163207=DIRECTION ( 'NONE',  ( 1.000000000000000000, 0.000000000000000000, 0.000000000000000000 ) ) ;
#163218=CARTESIAN_POINT ( 'NONE',  ( 18.59999999999999432, -9.480686695267811714, -174.4411151687578752 ) ) ;
#163258=EDGE_CURVE ( 'NONE', #56718, #230402, #47784, .T. ) ;
#163261=CARTESIAN_POINT ( 'NONE',  ( 20.99551997958415583, 11.75000000001125144, -160.6516591376888528 ) ) ;
#163276=FACE_BOUND ( 'NONE', #214540, .T. ) ;
#163315=LINE ( 'NONE', #204975, #193576 ) ;
#163340=ADVANCED_FACE ( 'NONE', ( #149502 ), #9964, .F. ) ;
#163344=ORIENTED_EDGE ( 'NONE', *, *, #156813, .T. ) ;
#163364=ORIENTED_EDGE ( 'NONE', *, *, #219592, .T. ) ;
#163408=FACE_OUTER_BOUND ( 'NONE', #141924, .T. ) ;
#163425=CARTESIAN_POINT ( 'NONE',  ( 21.05000000000000071, -1.360870587180885716, -142.0729979270909951 ) ) ;
#163431=VERTEX_POINT ( 'NONE', #94625 ) ;
#163448=EDGE_LOOP ( 'NONE', ( #173755, #192415, #80261, #32240 ) ) ;
#163467=EDGE_CURVE ( 'NONE', #220244, #87859, #191824, .T. ) ;
#163479=LINE ( 'NONE', #64382, #173487 ) ;
#163480=AXIS2_PLACEMENT_3D ( 'NONE', #32317, #227922, #107976 ) ;
#163499=CARTESIAN_POINT ( 'NONE',  ( -20.64999999999999858, 1.115600667400684642E-11, -134.0000000000000000 ) ) ;
#163503=FACE_OUTER_BOUND ( 'NONE', #160269, .T. ) ;
#163528=DIRECTION ( 'NONE',  ( 0.000000000000000000, -0.9654727137038715545, 0.2605042016806676242 ) ) ;
#163550=ADVANCED_FACE ( 'NONE', ( #118048 ), #197577, .T. ) ;
#163561=ORIENTED_EDGE ( 'NONE', *, *, #6731, .F. ) ;
#163573=ADVANCED_FACE ( 'NONE', ( #24116 ), #61937, .T. ) ;
#163574=EDGE_CURVE ( 'NONE', #150597, #203670, #8512, .T. ) ;
#163603=ORIENTED_EDGE ( 'NONE', *, *, #255063, .T. ) ;
#163628=AXIS2_PLACEMENT_3D ( 'NONE', #58018, #37216, #236667 ) ;
#163635=EDGE_LOOP ( 'NONE', ( #116527, #37512, #155281, #254832 ) ) ;
#163640=EDGE_CURVE ( 'NONE', #4681, #173033, #233404, .T. ) ;
#163647=EDGE_CURVE ( 'NONE', #106553, #37051, #144023, .T. ) ;
#163677=DIRECTION ( 'NONE',  ( 1.000000000000000000, 0.000000000000000000, 0.000000000000000000 ) ) ;
#163708=EDGE_CURVE ( 'NONE', #248652, #120342, #93537, .T. ) ;
#163719=CIRCLE ( 'NONE', #22086, 0.2000000000000057288 ) ;
#163746=EDGE_LOOP ( 'NONE', ( #96329, #107250, #109135, #54921 ) ) ;
#163757=CARTESIAN_POINT ( 'NONE',  ( 18.49999999999998934, 10.29288807859941457, -172.9580020160121592 ) ) ;
#163765=CARTESIAN_POINT ( 'NONE',  ( -23.15000000000000213, 1.115648428625851357E-11, -163.6000000000000512 ) ) ;
#163769=ORIENTED_EDGE ( 'NONE', *, *, #121231, .T. ) ;
#163776=CARTESIAN_POINT ( 'NONE',  ( 21.05000000000000071, -11.64999999998883595, -134.0000000000000000 ) ) ;
#163781=EDGE_CURVE ( 'NONE', #155087, #59363, #254204, .T. ) ;
#163785=EDGE_CURVE ( 'NONE', #221551, #141516, #229288, .T. ) ;
#163821=CARTESIAN_POINT ( 'NONE',  ( -18.47130263965437180, -9.471155585952832467, -174.1834047654767801 ) ) ;
#163823=EDGE_LOOP ( 'NONE', ( #182726, #164286, #119570, #225115 ) ) ;
#163824=ADVANCED_FACE ( 'NONE', ( #35682 ), #173927, .T. ) ;
#163878=AXIS2_PLACEMENT_3D ( 'NONE', #25009, #246589, #168400 ) ;
#163880=CIRCLE ( 'NONE', #9743, 4.049999999999998934 ) ;
#163895=ADVANCED_FACE ( 'NONE', ( #233854 ), #175091, .F. ) ;
#163899=ORIENTED_EDGE ( 'NONE', *, *, #144300, .T. ) ;
#163926=AXIS2_PLACEMENT_3D ( 'NONE', #78428, #32937, #73334 ) ;
#163930=ORIENTED_EDGE ( 'NONE', *, *, #126187, .T. ) ;
#163935=EDGE_CURVE ( 'NONE', #102830, #64347, #125228, .T. ) ;
#163956=DIRECTION ( 'NONE',  ( -0.4999999999999799050, 0.000000000000000000, -0.8660254037844502539 ) ) ;
#163959=SPHERICAL_SURFACE ( 'NONE', #121357, 0.1000000000000000056 ) ;
#163987=ORIENTED_EDGE ( 'NONE', *, *, #138846, .F. ) ;
#163988=ADVANCED_FACE ( 'NONE', ( #120361 ), #137857, .F. ) ;
#163996=CARTESIAN_POINT ( 'NONE',  ( 21.05000000000000071, -8.663551401858002876, -143.5241011180673070 ) ) ;
#164016=ORIENTED_EDGE ( 'NONE', *, *, #47769, .F. ) ;
#164020=VERTEX_POINT ( 'NONE', #246679 ) ;
#164024=CYLINDRICAL_SURFACE ( 'NONE', #98239, 0.09999999999998898659 ) ;
#164027=CARTESIAN_POINT ( 'NONE',  ( -18.59999999999999787, -9.499999999988842703, -146.1500000000000341 ) ) ;
#164031=AXIS2_PLACEMENT_3D ( 'NONE', #131228, #15146, #109089 ) ;
#164046=DIRECTION ( 'NONE',  ( 0.000000000000000000, 1.776356839400308446E-15, -1.000000000000000000 ) ) ;
#164061=CARTESIAN_POINT ( 'NONE',  ( 23.14999999999999858, 1.115600667400684642E-11, -167.5000000000000284 ) ) ;
#164084=FACE_OUTER_BOUND ( 'NONE', #249262, .T. ) ;
#164121=VECTOR ( 'NONE', #37522, 1000.000000000000227 ) ;
#164123=EDGE_CURVE ( 'NONE', #242008, #158190, #74187, .T. ) ;
#164166=DIRECTION ( 'NONE',  ( -0.000000000000000000, -0.000000000000000000, -1.000000000000000000 ) ) ;
#164176=CARTESIAN_POINT ( 'NONE',  ( 20.94999999999999929, 1.115600667400684642E-11, -167.5000000000000284 ) ) ;
#164209=AXIS2_PLACEMENT_3D ( 'NONE', #190419, #229533, #27517 ) ;
#164226=CIRCLE ( 'NONE', #210017, 0.1000000000000028644 ) ;
#164236=CARTESIAN_POINT ( 'NONE',  ( 18.43579564894478295, -9.519327535281362884, -140.9729766438603633 ) ) ;
#164245=DIRECTION ( 'NONE',  ( 1.000000000000000000, 0.000000000000000000, 0.000000000000000000 ) ) ;
#164272=ADVANCED_FACE ( 'NONE', ( #226463 ), #163959, .T. ) ;
#164284=CARTESIAN_POINT ( 'NONE',  ( -22.39999999999999503, 7.790779598384560245, -134.0000000000000000 ) ) ;
#164286=ORIENTED_EDGE ( 'NONE', *, *, #229883, .T. ) ;
#164337=EDGE_LOOP ( 'NONE', ( #91884, #20943, #49239, #4563 ) ) ;
#164349=( BOUNDED_SURFACE ( )  B_SPLINE_SURFACE ( 3, 2, ( 
 ( #255106, #32292, #191370 ),
 ( #12729, #251296, #212203 ),
 ( #173110, #73995, #58222 ),
 ( #179497, #200325, #159937 ),
 ( #240742, #201600, #180769 ),
 ( #76513, #60797, #41282 ) ),
 .UNSPECIFIED., .F., .F., .F. ) 
 B_SPLINE_SURFACE_WITH_KNOTS ( ( 4, 2, 4 ),
 ( 3, 3 ),
 ( 0.0001792624049599564567, 0.0003686986002124703144, 0.0005581347954649841991 ),
 ( 0.000000000000000000, 1.000000000000000000 ),
 .UNSPECIFIED. ) 
 GEOMETRIC_REPRESENTATION_ITEM ( )  RATIONAL_B_SPLINE_SURFACE ( (
 ( 1.000000000000000000, 0.9238795325112719725, 1.000000000000000000),
 ( 1.000000000000000000, 0.9229318695243835524, 1.000000000000000000),
 ( 1.000000000000000000, 0.8926288119223798612, 1.000000000000000000),
 ( 1.000000000000000000, 0.8123777807278315111, 1.000000000000000000),
 ( 1.000000000000000000, 0.7629087100926418286, 1.000000000000000000),
 ( 1.000000000000000000, 0.7071067811865597852, 1.000000000000000000) ) ) 
 REPRESENTATION_ITEM ( '' )  SURFACE ( )  );
#164355=ORIENTED_EDGE ( 'NONE', *, *, #209843, .T. ) ;
#164402=DIRECTION ( 'NONE',  ( 0.000000000000000000, -0.9893560106964500722, 0.1455152366551550613 ) ) ;
#164414=CARTESIAN_POINT ( 'NONE',  ( -23.15000000000000213, 2.600000000011156054, -122.2500000000000284 ) ) ;
#164436=EDGE_CURVE ( 'NONE', #216709, #239387, #129935, .T. ) ;
#164446=DIRECTION ( 'NONE',  ( 0.000000000000000000, 0.000000000000000000, 1.000000000000000000 ) ) ;
#164497=EDGE_CURVE ( 'NONE', #179358, #116282, #128688, .T. ) ;
#164502=EDGE_CURVE ( 'NONE', #140279, #27375, #200207, .T. ) ;
#164504=CARTESIAN_POINT ( 'NONE',  ( 21.09787244211752011, 8.775370707348422172, -146.2392533843176352 ) ) ;
#164516=DIRECTION ( 'NONE',  ( -1.000000000000000000, 0.000000000000000000, 0.000000000000000000 ) ) ;
#164532=DIRECTION ( 'NONE',  ( 0.000000000000000000, 0.000000000000000000, -1.000000000000000000 ) ) ;
#164543=CARTESIAN_POINT ( 'NONE',  ( 20.94999999999999929, 11.65000000001115943, -160.7161343370219129 ) ) ;
#164544=FACE_OUTER_BOUND ( 'NONE', #4932, .T. ) ;
#164649=CIRCLE ( 'NONE', #252115, 0.09999999999999939493 ) ;
#164659=CARTESIAN_POINT ( 'NONE',  ( 20.94999999999999929, 5.500000000011153745, -146.4052660189131245 ) ) ;
#164669=ORIENTED_EDGE ( 'NONE', *, *, #81416, .T. ) ;
#164694=EDGE_CURVE ( 'NONE', #104833, #83651, #9695, .T. ) ;
#164698=EDGE_CURVE ( 'NONE', #42134, #41545, #21549, .T. ) ;
#164703=ORIENTED_EDGE ( 'NONE', *, *, #214250, .T. ) ;
#164710=FACE_OUTER_BOUND ( 'NONE', #118523, .T. ) ;
#164745=AXIS2_PLACEMENT_3D ( 'NONE', #217991, #39416, #226676 ) ;
#164748=CARTESIAN_POINT ( 'NONE',  ( -21.05000000000000071, 1.261786168576181755, -142.0864989635454947 ) ) ;
#164771=AXIS2_PLACEMENT_3D ( 'NONE', #219366, #82402, #64161 ) ;
#164800=CARTESIAN_POINT ( 'NONE',  ( -23.15000000000000213, 11.60000000001115517, -160.5717967697245285 ) ) ;
#164821=( BOUNDED_SURFACE ( )  B_SPLINE_SURFACE ( 3, 2, ( 
 ( #122563, #145946, #23482 ),
 ( #241226, #24762, #162977 ),
 ( #165538, #224200, #205927 ),
 ( #144661, #203373, #204631 ),
 ( #7742, #66425, #87247 ),
 ( #187675, #166843, #246346 ) ),
 .UNSPECIFIED., .F., .F., .T. ) 
 B_SPLINE_SURFACE_WITH_KNOTS ( ( 4, 2, 4 ),
 ( 3, 3 ),
 ( 0.0001300404313046571046, 0.0003183318589266508720, 0.0005066232865486446123 ),
 ( 0.000000000000000000, 1.000000000000000000 ),
 .UNSPECIFIED. ) 
 GEOMETRIC_REPRESENTATION_ITEM ( )  RATIONAL_B_SPLINE_SURFACE ( (
 ( 1.000000000000000000, 0.7071067811865597852, 1.000000000000000000),
 ( 1.000000000000000000, 0.7625113560538043789, 1.000000000000000000),
 ( 1.000000000000000000, 0.8126073484691690441, 1.000000000000000000),
 ( 1.000000000000000000, 0.8923049332729230398, 1.000000000000000000),
 ( 1.000000000000000000, 0.9231914937772274232, 1.000000000000000000),
 ( 1.000000000000000000, 0.9238795325112714174, 1.000000000000000000) ) ) 
 REPRESENTATION_ITEM ( '' )  SURFACE ( )  );
#164841=EDGE_CURVE ( 'NONE', #12431, #222371, #125762, .T. ) ;
#164842=VECTOR ( 'NONE', #15920, 1000.000000000000000 ) ;
#164845=AXIS2_PLACEMENT_3D ( 'NONE', #24019, #174464, #135264 ) ;
#164864=ORIENTED_EDGE ( 'NONE', *, *, #188753, .T. ) ;
#164866=ORIENTED_EDGE ( 'NONE', *, *, #89303, .F. ) ;
#164892=DIRECTION ( 'NONE',  ( -1.000000000000000000, -0.000000000000000000, 0.000000000000000000 ) ) ;
#164903=ORIENTED_EDGE ( 'NONE', *, *, #176330, .F. ) ;
#164926=ORIENTED_EDGE ( 'NONE', *, *, #199696, .T. ) ;
#164954=ORIENTED_EDGE ( 'NONE', *, *, #221902, .F. ) ;
#164978=EDGE_CURVE ( 'NONE', #12568, #40580, #109002, .T. ) ;
#164985=DIRECTION ( 'NONE',  ( 1.000000000000000000, -0.000000000000000000, -0.000000000000000000 ) ) ;
#165006=EDGE_CURVE ( 'NONE', #165926, #113603, #200599, .T. ) ;
#165012=CARTESIAN_POINT ( 'NONE',  ( 18.59999999999999787, -1.835341550213255957, -145.5551512925629822 ) ) ;
#165023=CARTESIAN_POINT ( 'NONE',  ( 19.75857864376269291, 11.65000000001116476, -158.7500000000000284 ) ) ;
#165024=DIRECTION ( 'NONE',  ( 0.000000000000000000, 0.000000000000000000, 1.000000000000000000 ) ) ;
#165025=EDGE_LOOP ( 'NONE', ( #218151, #81922, #255616, #101503 ) ) ;
#165028=DIRECTION ( 'NONE',  ( 1.000000000000000000, 0.000000000000000000, 0.000000000000000000 ) ) ;
#165071=DIRECTION ( 'NONE',  ( 0.7071067811865474617, 0.7071067811865474617, 0.000000000000000000 ) ) ;
#165091=DIRECTION ( 'NONE',  ( 0.000000000000000000, 0.000000000000000000, -1.000000000000000000 ) ) ;
#165095=DIRECTION ( 'NONE',  ( -2.952720810173288619E-16, 1.000000000000000000, 0.000000000000000000 ) ) ;
#165109=ORIENTED_EDGE ( 'NONE', *, *, #156547, .T. ) ;
#165113=ORIENTED_EDGE ( 'NONE', *, *, #148533, .T. ) ;
#165160=FACE_OUTER_BOUND ( 'NONE', #157735, .T. ) ;
#165175=CIRCLE ( 'NONE', #115283, 0.09999999999998898659 ) ;
#165178=CARTESIAN_POINT ( 'NONE',  ( 18.36493879433247756, -9.500000806178645618, -174.4221486603523488 ) ) ;
#165187=FACE_OUTER_BOUND ( 'NONE', #158236, .T. ) ;
#165211=CARTESIAN_POINT ( 'NONE',  ( -20.94999999999999929, 10.29270135741298731, -172.9573618871519614 ) ) ;
#165251=ORIENTED_EDGE ( 'NONE', *, *, #164694, .F. ) ;
#165276=ORIENTED_EDGE ( 'NONE', *, *, #75259, .F. ) ;
#165312=CIRCLE ( 'NONE', #82075, 0.09999999999999484301 ) ;
#165314=FACE_OUTER_BOUND ( 'NONE', #215597, .T. ) ;
#165316=VERTEX_POINT ( 'NONE', #52374 ) ;
#165337=LINE ( 'NONE', #143185, #169840 ) ;
#165364=FACE_OUTER_BOUND ( 'NONE', #89697, .T. ) ;
#165384=CARTESIAN_POINT ( 'NONE',  ( -21.05000000000000071, 1.115600667400684642E-11, -167.5000000000000284 ) ) ;
#165391=VERTEX_POINT ( 'NONE', #101753 ) ;
#165440=ORIENTED_EDGE ( 'NONE', *, *, #228087, .F. ) ;
#165451=VECTOR ( 'NONE', #214582, 1000.000000000000000 ) ;
#165466=CARTESIAN_POINT ( 'NONE',  ( -23.25000000000000000, -11.74999999998884448, -164.4000000000000057 ) ) ;
#165470=ORIENTED_EDGE ( 'NONE', *, *, #214819, .T. ) ;
#165520=CARTESIAN_POINT ( 'NONE',  ( 18.58703555224998638, -9.406336740777428318, -141.1249446412470547 ) ) ;
#165531=ORIENTED_EDGE ( 'NONE', *, *, #187097, .T. ) ;
#165538=CARTESIAN_POINT ( 'NONE',  ( 21.11825140030063253, 0.007203620644165132682, -127.5545924345806412 ) ) ;
#165546=ORIENTED_EDGE ( 'NONE', *, *, #41055, .T. ) ;
#165577=EDGE_LOOP ( 'NONE', ( #210616, #182706, #118869, #253162, #126660 ) ) ;
#165585=FACE_OUTER_BOUND ( 'NONE', #146248, .T. ) ;
#165607=FACE_OUTER_BOUND ( 'NONE', #104934, .T. ) ;
#165612=CARTESIAN_POINT ( 'NONE',  ( -20.94999999999999929, -11.64999999998884483, -136.9000000000000341 ) ) ;
#165628=ORIENTED_EDGE ( 'NONE', *, *, #73020, .T. ) ;
#165642=ORIENTED_EDGE ( 'NONE', *, *, #195277, .T. ) ;
#165668=CIRCLE ( 'NONE', #53216, 0.09999999999998898659 ) ;
#165670=DIRECTION ( 'NONE',  ( 1.000000000000000000, 0.000000000000000000, 0.000000000000000000 ) ) ;
#165698=CARTESIAN_POINT ( 'NONE',  ( 23.14999999999998437, -4.049999999988842525, -134.0000000000000000 ) ) ;
#165700=CARTESIAN_POINT ( 'NONE',  ( -21.05000000000000071, -1.249999999988843369, -142.0000000000000284 ) ) ;
#165727=ORIENTED_EDGE ( 'NONE', *, *, #84352, .T. ) ;
#165744=CARTESIAN_POINT ( 'NONE',  ( -23.15000000000000213, 11.65000000001115588, -155.3500000000000227 ) ) ;
#165750=TOROIDAL_SURFACE ( 'NONE', #219878, 11.65000000000000036, 0.1000000000000000056 ) ;
#165770=CARTESIAN_POINT ( 'NONE',  ( -20.54999999999999716, -8.999999999988846255, -143.3939691226524644 ) ) ;
#165785=CIRCLE ( 'NONE', #86619, 0.09999999999998898659 ) ;
#165786=CARTESIAN_POINT ( 'NONE',  ( -22.49756042579671700, 0.07804633702833754794, -122.3501350388976903 ) ) ;
#165789=ADVANCED_FACE ( 'NONE', ( #226200 ), #151087, .T. ) ;
#165792=DIRECTION ( 'NONE',  ( 1.000000000000000000, -7.304098846218134667E-16, -0.000000000000000000 ) ) ;
#165794=CARTESIAN_POINT ( 'NONE',  ( 21.05000000000000071, 10.47338541492405284, -141.5786544642485580 ) ) ;
#165795=CARTESIAN_POINT ( 'NONE',  ( 20.97462148592277842, 8.874737576461731337, -146.2546443317310434 ) ) ;
#165809=DIRECTION ( 'NONE',  ( 0.000000000000000000, -1.000000000000000000, 0.000000000000000000 ) ) ;
#165814=DIRECTION ( 'NONE',  ( 1.000000000000000000, 0.000000000000000000, 0.000000000000000000 ) ) ;
#165854=CARTESIAN_POINT ( 'NONE',  ( 18.52928932188133970, 10.27928932189250055, -158.6500000000000057 ) ) ;
#165857=ADVANCED_FACE ( 'NONE', ( #9754 ), #246928, .T. ) ;
#165862=DIRECTION ( 'NONE',  ( 1.000000000000000000, 0.000000000000000000, 0.000000000000000000 ) ) ;
#165922=AXIS2_PLACEMENT_3D ( 'NONE', #99366, #281, #235062 ) ;
#165926=VERTEX_POINT ( 'NONE', #236503 ) ;
#165946=DIRECTION ( 'NONE',  ( 0.000000000000000000, 0.000000000000000000, -1.000000000000000000 ) ) ;
#165969=EDGE_LOOP ( 'NONE', ( #51635, #220816, #102388, #136841, #105505 ) ) ;
#165981=FACE_OUTER_BOUND ( 'NONE', #34378, .T. ) ;
#165990=EDGE_CURVE ( 'NONE', #37772, #156163, #9606, .T. ) ;
#166000=DIRECTION ( 'NONE',  ( -0.000000000000000000, 0.8660254037844411501, 0.4999999999999956701 ) ) ;
#166045=CARTESIAN_POINT ( 'NONE',  ( 18.49999999999999289, 10.25000000001115552, -155.3500000000000227 ) ) ;
#166086=ORIENTED_EDGE ( 'NONE', *, *, #80450, .F. ) ;
#166208=DIRECTION ( 'NONE',  ( 0.000000000000000000, 0.000000000000000000, -1.000000000000000000 ) ) ;
#166252=DIRECTION ( 'NONE',  ( 0.000000000000000000, -0.000000000000000000, -1.000000000000000000 ) ) ;
#166332=CARTESIAN_POINT ( 'NONE',  ( 21.05000000000000071, 6.650000000011155876, -146.1500000000000341 ) ) ;
#166351=DIRECTION ( 'NONE',  ( 2.952720810173289112E-16, -1.000000000000000000, 0.000000000000000000 ) ) ;
#166366=ORIENTED_EDGE ( 'NONE', *, *, #77030, .T. ) ;
#166381=CIRCLE ( 'NONE', #149620, 0.09999999999999939493 ) ;
#166389=DIRECTION ( 'NONE',  ( -2.840903330521631775E-16, 0.8700118002898321601, -0.4930308989875230030 ) ) ;
#166412=CARTESIAN_POINT ( 'NONE',  ( -18.37151313414829801, -9.571014125766513558, -174.3166629092390281 ) ) ;
#166433=LINE ( 'NONE', #132412, #54799 ) ;
#166447=VECTOR ( 'NONE', #215, 1000.000000000000000 ) ;
#166453=CARTESIAN_POINT ( 'NONE',  ( 21.07016717457009491, 1.115540062193308597E-11, -127.6790591618991186 ) ) ;
#166473=CARTESIAN_POINT ( 'NONE',  ( -21.05000000000000071, 0.2561057921033771945, -133.9651035583277121 ) ) ;
#166507=DIRECTION ( 'NONE',  ( -0.000000000000000000, 1.000000000000000000, -1.224646799147352961E-16 ) ) ;
#166530=FACE_OUTER_BOUND ( 'NONE', #193686, .T. ) ;
#166568=CYLINDRICAL_SURFACE ( 'NONE', #9603, 0.09999999999999939493 ) ;
#166599=ADVANCED_FACE ( 'NONE', ( #28769 ), #59251, .T. ) ;
#166609=TOROIDAL_SURFACE ( 'NONE', #149854, 11.70000000000000107, 0.1000000000000000056 ) ;
#166610=DIRECTION ( 'NONE',  ( -1.000000000000000000, -0.000000000000000000, -0.000000000000000000 ) ) ;
#166643=CARTESIAN_POINT ( 'NONE',  ( -18.59999999999999787, -9.480686695267820596, -174.4411151687578752 ) ) ;
#166696=DIRECTION ( 'NONE',  ( -0.000000000000000000, -1.897661533703519897E-16, 1.000000000000000000 ) ) ;
#166707=ORIENTED_EDGE ( 'NONE', *, *, #106982, .F. ) ;
#166712=CIRCLE ( 'NONE', #25221, 0.09999999999998898659 ) ;
#166719=CARTESIAN_POINT ( 'NONE',  ( -21.76363531954647357, 0.09900187431060442078, -126.9870634521282966 ) ) ;
#166720=DIRECTION ( 'NONE',  ( -1.000000000000000000, -0.000000000000000000, 0.000000000000000000 ) ) ;
#166772=VECTOR ( 'NONE', #146579, 1000.000000000000000 ) ;
#166818=CARTESIAN_POINT ( 'NONE',  ( -18.59999999999999787, 1.261786168576181755, -142.0864989635454947 ) ) ;
#166826=EDGE_CURVE ( 'NONE', #61931, #82879, #173419, .T. ) ;
#166832=CARTESIAN_POINT ( 'NONE',  ( -18.50000000000000000, -1.637172712959223952, -145.5821533654720383 ) ) ;
#166843=CARTESIAN_POINT ( 'NONE',  ( 21.04999999999999716, 0.09843750001147472117, -127.7007690899077090 ) ) ;
#166872=CARTESIAN_POINT ( 'NONE',  ( -23.25000000000000000, -1.149570369564537842, -175.3159124845019790 ) ) ;
#166879=ORIENTED_EDGE ( 'NONE', *, *, #155351, .T. ) ;
#166885=AXIS2_PLACEMENT_3D ( 'NONE', #103396, #65575, #64298 ) ;
#166886=DIRECTION ( 'NONE',  ( 0.000000000000000000, 1.000000000000000000, -6.308085367188393199E-16 ) ) ;
#166892=CARTESIAN_POINT ( 'NONE',  ( -18.50000000000000000, 1.115600667400684642E-11, -167.5000000000000284 ) ) ;
#166907=EDGE_LOOP ( 'NONE', ( #210466, #235866, #208375, #250304 ) ) ;
#167001=CARTESIAN_POINT ( 'NONE',  ( -20.94999999999999929, 11.65000000001115588, -141.0148057706540214 ) ) ;
#167011=DIRECTION ( 'NONE',  ( 3.616040088954497272E-32, -1.224646799147352961E-16, 1.000000000000000000 ) ) ;
#167019=CARTESIAN_POINT ( 'NONE',  ( -20.85000000000000142, -1.149570369564537842, -175.3159124845019790 ) ) ;
#167028=CARTESIAN_POINT ( 'NONE',  ( 18.59999999999999432, -1.162701749926853712, -142.0000000000000284 ) ) ;
#167077=AXIS2_PLACEMENT_3D ( 'NONE', #14560, #88916, #247998 ) ;
#167093=CARTESIAN_POINT ( 'NONE',  ( 21.15000000000000213, 8.786607556611267356, -146.2500000000000568 ) ) ;
#167094=AXIS2_PLACEMENT_3D ( 'NONE', #93653, #175780, #54523 ) ;
#167132=EDGE_CURVE ( 'NONE', #71001, #18309, #135191, .T. ) ;
#167155=CARTESIAN_POINT ( 'NONE',  ( 18.49999999999999289, 10.37342005529114886, -158.7657881246250895 ) ) ;
#167156=ORIENTED_EDGE ( 'NONE', *, *, #32886, .T. ) ;
#167168=CARTESIAN_POINT ( 'NONE',  ( 18.49999999999999289, 10.20857864377385127, -122.2500000000000284 ) ) ;
#167198=EDGE_CURVE ( 'NONE', #151746, #116136, #160118, .T. ) ;
#167200=EDGE_CURVE ( 'NONE', #136324, #180198, #193916, .T. ) ;
#167236=AXIS2_PLACEMENT_3D ( 'NONE', #118920, #198434, #99312 ) ;
#167241=B_SPLINE_CURVE_WITH_KNOTS ( 'NONE', 3,
 ( #149858, #213664, #130261, #71607, #229389, #35068, #209820, #151135 ),
 .UNSPECIFIED., .F., .F.,
 ( 4, 2, 2, 4 ),
 ( 0.000000000000000000, 9.550056980125525518E-05, 0.0001910011396025105104, 0.0003820022792049782489 ),
 .UNSPECIFIED. ) ;
#167263=ORIENTED_EDGE ( 'NONE', *, *, #242159, .F. ) ;
#167266=DIRECTION ( 'NONE',  ( 1.000000000000000000, 0.000000000000000000, 0.000000000000000000 ) ) ;
#167280=FACE_OUTER_BOUND ( 'NONE', #194829, .T. ) ;
#167301=CARTESIAN_POINT ( 'NONE',  ( 20.30531438145591139, 10.09690106110208596, -141.7960178072733584 ) ) ;
#167328=DIRECTION ( 'NONE',  ( 5.421010862427554711E-16, -1.000000000000000000, -3.252606517456533024E-15 ) ) ;
#167361=EDGE_CURVE ( 'NONE', #134395, #240778, #199039, .T. ) ;
#167367=DIRECTION ( 'NONE',  ( 1.000000000000000000, -0.000000000000000000, -0.000000000000000000 ) ) ;
#167405=FACE_OUTER_BOUND ( 'NONE', #146949, .T. ) ;
#167460=AXIS2_PLACEMENT_3D ( 'NONE', #250763, #90401, #130818 ) ;
#167464=CARTESIAN_POINT ( 'NONE',  ( -18.50000000000000000, 11.75000000001115197, -134.1000000000000227 ) ) ;
#167480=AXIS2_PLACEMENT_3D ( 'NONE', #148643, #228174, #129070 ) ;
#167483=CARTESIAN_POINT ( 'NONE',  ( -20.00857864376270001, 9.350000000011156942, -146.3500000000000227 ) ) ;
#167488=AXIS2_PLACEMENT_3D ( 'NONE', #23364, #20781, #220262 ) ;
#167499=DIRECTION ( 'NONE',  ( 0.000000000000000000, 0.000000000000000000, -1.000000000000000000 ) ) ;
#167570=EDGE_CURVE ( 'NONE', #163189, #68733, #132328, .T. ) ;
#167583=CARTESIAN_POINT ( 'NONE',  ( -22.59080734064477625, 11.75000000001115907, -133.9692502919030233 ) ) ;
#167587=CARTESIAN_POINT ( 'NONE',  ( -23.25000000000000000, 1.115600667400684642E-11, -134.0000000000000000 ) ) ;
#167600=ORIENTED_EDGE ( 'NONE', *, *, #241486, .T. ) ;
#167603=DIRECTION ( 'NONE',  ( 0.000000000000000000, 1.000000000000000000, 0.000000000000000000 ) ) ;
#167606=ORIENTED_EDGE ( 'NONE', *, *, #9940, .T. ) ;
#167608=CARTESIAN_POINT ( 'NONE',  ( 20.04142135623730070, 11.65000000001115943, -158.6500000000000057 ) ) ;
#167620=CARTESIAN_POINT ( 'NONE',  ( 21.14999999999999858, 8.786607556611267356, -146.3500000000000227 ) ) ;
#167629=CARTESIAN_POINT ( 'NONE',  ( 21.14999999999999858, 11.65000000001115943, -134.1000000000000227 ) ) ;
#167697=CARTESIAN_POINT ( 'NONE',  ( 22.01447462590973814, 0.09903700007069084210, -126.7361997987701017 ) ) ;
#167768=CARTESIAN_POINT ( 'NONE',  ( 18.49999999999999289, 11.75000000001115552, -158.8500000000000227 ) ) ;
#167787=CARTESIAN_POINT ( 'NONE',  ( 20.94999999999999929, 6.450000000011156587, -144.0170271704400307 ) ) ;
#167792=CARTESIAN_POINT ( 'NONE',  ( 20.94999999999999929, -11.48912529306489994, -164.4000000000000057 ) ) ;
#167797=DIRECTION ( 'NONE',  ( -0.000000000000000000, 1.000000000000000000, 0.000000000000000000 ) ) ;
#167812=AXIS2_PLACEMENT_3D ( 'NONE', #75021, #154559, #136208 ) ;
#167848=AXIS2_PLACEMENT_3D ( 'NONE', #116849, #3296, #198942 ) ;
#167865=LINE ( 'NONE', #24497, #197880 ) ;
#167924=ORIENTED_EDGE ( 'NONE', *, *, #56339, .F. ) ;
#167928=ORIENTED_EDGE ( 'NONE', *, *, #55553, .T. ) ;
#167957=ORIENTED_EDGE ( 'NONE', *, *, #156572, .F. ) ;
#167958=DIRECTION ( 'NONE',  ( 1.000000000000000000, 3.265361837132813093E-16, -0.000000000000000000 ) ) ;
#167967=EDGE_CURVE ( 'NONE', #82879, #63155, #221469, .T. ) ;
#168005=EDGE_CURVE ( 'NONE', #160572, #45962, #215100, .T. ) ;
#168007=DIRECTION ( 'NONE',  ( 0.000000000000000000, 0.000000000000000000, -1.000000000000000000 ) ) ;
#168033=CARTESIAN_POINT ( 'NONE',  ( -23.25000000000000000, -11.64999999998884483, -164.4000000000000057 ) ) ;
#168036=DIRECTION ( 'NONE',  ( 1.000000000000000000, 2.952720810173289112E-16, -0.000000000000000000 ) ) ;
#168045=AXIS2_PLACEMENT_3D ( 'NONE', #28923, #49718, #169711 ) ;
#168049=CARTESIAN_POINT ( 'NONE',  ( 20.94999999999999929, 5.000000000011153745, -146.4052660189131245 ) ) ;
#168085=DIRECTION ( 'NONE',  ( 1.000000000000000000, -0.000000000000000000, -0.000000000000000000 ) ) ;
#168091=ADVANCED_FACE ( 'NONE', ( #256739 ), #13401, .T. ) ;
#168165=PLANE ( 'NONE',  #64315 ) ;
#168195=DIRECTION ( 'NONE',  ( 0.000000000000000000, -1.000000000000000000, -0.000000000000000000 ) ) ;
#168196=VECTOR ( 'NONE', #203859, 1000.000000000000000 ) ;
#168241=AXIS2_PLACEMENT_3D ( 'NONE', #102245, #219654, #594 ) ;
#168258=ORIENTED_EDGE ( 'NONE', *, *, #1790, .F. ) ;
#168260=AXIS2_PLACEMENT_3D ( 'NONE', #183723, #119922, #179879 ) ;
#168271=VECTOR ( 'NONE', #30632, 1000.000000000000000 ) ;
#168295=AXIS2_PLACEMENT_3D ( 'NONE', #185746, #86613, #7095 ) ;
#168310=DIRECTION ( 'NONE',  ( 2.952720810173289112E-16, -1.000000000000000000, -0.000000000000000000 ) ) ;
#168317=DIRECTION ( 'NONE',  ( 0.000000000000000000, 0.000000000000000000, -1.000000000000000000 ) ) ;
#168366=ORIENTED_EDGE ( 'NONE', *, *, #12349, .F. ) ;
#168378=EDGE_CURVE ( 'NONE', #140417, #63155, #92488, .T. ) ;
#168400=DIRECTION ( 'NONE',  ( 0.000000000000000000, 0.000000000000000000, 1.000000000000000000 ) ) ;
#168426=CARTESIAN_POINT ( 'NONE',  ( 21.05000000000000426, 10.72371710471866812, -141.5944173916130921 ) ) ;
#168442=VECTOR ( 'NONE', #89335, 1000.000000000000000 ) ;
#168459=VECTOR ( 'NONE', #136214, 1000.000000000000000 ) ;
#168460=CARTESIAN_POINT ( 'NONE',  ( 18.49999999999999289, 10.49142135624846439, -158.8500000000000227 ) ) ;
#168482=ORIENTED_EDGE ( 'NONE', *, *, #14862, .T. ) ;
#168534=AXIS2_PLACEMENT_3D ( 'NONE', #89841, #130254, #11620 ) ;
#168554=CARTESIAN_POINT ( 'NONE',  ( -23.15000000000000213, 1.925233644870972816, -146.7302435331261563 ) ) ;
#168559=FACE_OUTER_BOUND ( 'NONE', #188573, .T. ) ;
#168581=ORIENTED_EDGE ( 'NONE', *, *, #176096, .T. ) ;
#168594=CIRCLE ( 'NONE', #51996, 0.09999999999999939493 ) ;
#168606=DIRECTION ( 'NONE',  ( 0.000000000000000000, -0.8777080977375715243, 0.4791956752370512551 ) ) ;
#168613=DIRECTION ( 'NONE',  ( 0.000000000000000000, -1.000000000000000000, 0.000000000000000000 ) ) ;
#168621=CARTESIAN_POINT ( 'NONE',  ( -20.94999999999999929, 1.115600667400684642E-11, -163.5000000000000284 ) ) ;
#168658=EDGE_CURVE ( 'NONE', #150597, #204820, #13585, .T. ) ;
#168671=DIRECTION ( 'NONE',  ( -0.000000000000000000, 1.000000000000000000, 1.734723475976807292E-15 ) ) ;
#168677=CARTESIAN_POINT ( 'NONE',  ( 20.94999999999999574, 1.162701749949165642, -142.1000000000000227 ) ) ;
#168707=ORIENTED_EDGE ( 'NONE', *, *, #210005, .T. ) ;
#168713=FACE_OUTER_BOUND ( 'NONE', #149428, .T. ) ;
#168714=CARTESIAN_POINT ( 'NONE',  ( 20.84999999999998721, 11.75000000001115552, -167.5000000000000284 ) ) ;
#168764=AXIS2_PLACEMENT_3D ( 'NONE', #148935, #27727, #210190 ) ;
#168801=DIRECTION ( 'NONE',  ( 1.000000000000000000, 0.000000000000000000, 0.000000000000000000 ) ) ;
#168805=DIRECTION ( 'NONE',  ( 0.000000000000000000, 0.000000000000000000, -1.000000000000000000 ) ) ;
#168853=EDGE_CURVE ( 'NONE', #1294, #27375, #55412, .T. ) ;
#168860=AXIS2_PLACEMENT_3D ( 'NONE', #18220, #177330, #45484 ) ;
#168862=DIRECTION ( 'NONE',  ( -5.603264701231743991E-32, 1.897661533703519897E-16, -1.000000000000000000 ) ) ;
#168863=DIRECTION ( 'NONE',  ( 1.000000000000000000, 0.000000000000000000, 0.000000000000000000 ) ) ;
#168866=CARTESIAN_POINT ( 'NONE',  ( 18.59999999999999076, 11.65000000001115943, -158.8500000000000227 ) ) ;
#168883=CYLINDRICAL_SURFACE ( 'NONE', #125925, 0.09999999999999939493 ) ;
#168930=ORIENTED_EDGE ( 'NONE', *, *, #203291, .F. ) ;
#168953=AXIS2_PLACEMENT_3D ( 'NONE', #182932, #145062, #165946 ) ;
#168986=DIRECTION ( 'NONE',  ( 1.000000000000000000, 0.000000000000000000, 0.000000000000000000 ) ) ;
#168992=EDGE_CURVE ( 'NONE', #71001, #179208, #205270, .T. ) ;
#168994=CARTESIAN_POINT ( 'NONE',  ( 21.22070241538126467, 0.09891903054618129965, -127.5300537271303938 ) ) ;
#169023=VERTEX_POINT ( 'NONE', #70392 ) ;
#169024=DIRECTION ( 'NONE',  ( -1.000000000000000000, 0.000000000000000000, 0.000000000000000000 ) ) ;
#169029=FACE_OUTER_BOUND ( 'NONE', #160144, .T. ) ;
#169052=VECTOR ( 'NONE', #193730, 1000.000000000000000 ) ;
#169065=CARTESIAN_POINT ( 'NONE',  ( -18.59999999999999787, 11.65000000001115232, -146.2500000000000284 ) ) ;
#169068=ORIENTED_EDGE ( 'NONE', *, *, #238614, .F. ) ;
#169078=DIRECTION ( 'NONE',  ( 0.000000000000000000, -2.428612866367527723E-14, -1.000000000000000000 ) ) ;
#169083=TOROIDAL_SURFACE ( 'NONE', #256466, 0.2000000000000000111, 0.1000000000000000056 ) ;
#169129=TOROIDAL_SURFACE ( 'NONE', #227357, 11.70000000000000462, 0.1000000000000000056 ) ;
#169242=CIRCLE ( 'NONE', #127511, 0.2000000000000057288 ) ;
#169257=EDGE_CURVE ( 'NONE', #174422, #73834, #201376, .T. ) ;
#169271=EDGE_CURVE ( 'NONE', #223519, #7738, #30716, .T. ) ;
#169285=CARTESIAN_POINT ( 'NONE',  ( 18.49999999999999645, 1.728086936805617757, -120.8844350051678020 ) ) ;
#169304=CARTESIAN_POINT ( 'NONE',  ( -21.05000000000000071, -0.09999999998884338825, -122.3504291924552234 ) ) ;
#169307=DIRECTION ( 'NONE',  ( 0.000000000000000000, -1.000000000000000000, 0.000000000000000000 ) ) ;
#169391=CARTESIAN_POINT ( 'NONE',  ( 21.08884785362045378, 6.357193367436396514, -133.9502169049331712 ) ) ;
#169399=CARTESIAN_POINT ( 'NONE',  ( 22.59999999999999787, 11.64957080755595520, -133.9000000000000057 ) ) ;
#169437=CARTESIAN_POINT ( 'NONE',  ( -21.05000000000000071, -1.162701749926853712, -142.1000000000000227 ) ) ;
#169456=AXIS2_PLACEMENT_3D ( 'NONE', #150505, #65816, #149235 ) ;
#169480=EDGE_CURVE ( 'NONE', #169539, #53590, #30951, .T. ) ;
#169538=VERTEX_POINT ( 'NONE', #20363 ) ;
#169539=VERTEX_POINT ( 'NONE', #56860 ) ;
#169560=DIRECTION ( 'NONE',  ( 1.000000000000000000, 0.000000000000000000, -0.000000000000000000 ) ) ;
#169572=DIRECTION ( 'NONE',  ( 0.000000000000000000, 0.000000000000000000, -1.000000000000000000 ) ) ;
#169602=ORIENTED_EDGE ( 'NONE', *, *, #234304, .F. ) ;
#169626=FACE_OUTER_BOUND ( 'NONE', #115825, .T. ) ;
#169632=AXIS2_PLACEMENT_3D ( 'NONE', #116982, #101217, #97377 ) ;
#169649=DIRECTION ( 'NONE',  ( -1.000000000000000000, 0.000000000000000000, 0.000000000000000000 ) ) ;
#169650=DIRECTION ( 'NONE',  ( 0.000000000000000000, -1.000000000000000000, 0.000000000000000000 ) ) ;
#169671=CARTESIAN_POINT ( 'NONE',  ( 21.04999999999999716, 8.871279686006799281, -146.1500000000000341 ) ) ;
#169704=CARTESIAN_POINT ( 'NONE',  ( -18.59999999999999787, 1.115600667400684642E-11, -167.5000000000000284 ) ) ;
#169711=DIRECTION ( 'NONE',  ( 0.000000000000000000, 0.000000000000000000, -1.000000000000000000 ) ) ;
#169716=SPHERICAL_SURFACE ( 'NONE', #84936, 0.1000000000000000056 ) ;
#169733=AXIS2_PLACEMENT_3D ( 'NONE', #90997, #233107, #89701 ) ;
#169761=CARTESIAN_POINT ( 'NONE',  ( 21.14999999999999858, 11.65000000001115943, -134.1000000000000227 ) ) ;
#169766=( BOUNDED_SURFACE ( )  B_SPLINE_SURFACE ( 3, 2, ( 
 ( #208443, #5051, #222833 ),
 ( #162903, #148458, #104164 ),
 ( #188853, #125043, #242399 ),
 ( #66348, #187596, #44224 ) ),
 .UNSPECIFIED., .F., .F., .F. ) 
 B_SPLINE_SURFACE_WITH_KNOTS ( ( 4, 4 ),
 ( 3, 3 ),
 ( -1.761828530288944705E-19, 0.0003124336600439507920 ),
 ( 0.000000000000000000, 1.000000000000000000 ),
 .UNSPECIFIED. ) 
 GEOMETRIC_REPRESENTATION_ITEM ( )  RATIONAL_B_SPLINE_SURFACE ( (
 ( 1.000000000000000000, 0.7071067811865475727, 1.000000000000000000),
 ( 1.000000000000000000, 0.7089187706049394633, 1.000000000000000000),
 ( 1.000000000000000000, 0.7039288185052764435, 1.000000000000000000),
 ( 1.000000000000000000, 0.7040654476015688612, 1.000000000000000000) ) ) 
 REPRESENTATION_ITEM ( '' )  SURFACE ( )  );
#169787=ORIENTED_EDGE ( 'NONE', *, *, #34341, .T. ) ;
#169828=DIRECTION ( 'NONE',  ( -1.000000000000000000, -0.000000000000000000, 0.000000000000000000 ) ) ;
#169840=VECTOR ( 'NONE', #104044, 1000.000000000000000 ) ;
#169853=PLANE ( 'NONE',  #248292 ) ;
#169855=AXIS2_PLACEMENT_3D ( 'NONE', #165384, #7586, #244907 ) ;
#169888=ORIENTED_EDGE ( 'NONE', *, *, #93068, .T. ) ;
#169890=ORIENTED_EDGE ( 'NONE', *, *, #75467, .F. ) ;
#169891=ORIENTED_EDGE ( 'NONE', *, *, #89732, .F. ) ;
#169898=ORIENTED_EDGE ( 'NONE', *, *, #222517, .F. ) ;
#169911=DIRECTION ( 'NONE',  ( 1.000000000000000000, 0.000000000000000000, 0.000000000000000000 ) ) ;
#169926=DIRECTION ( 'NONE',  ( -0.000000000000000000, -0.1350103645451904977, 0.9908441862701596881 ) ) ;
#169997=FACE_BOUND ( 'NONE', #100769, .T. ) ;
#170003=FACE_OUTER_BOUND ( 'NONE', #99303, .T. ) ;
#170009=CARTESIAN_POINT ( 'NONE',  ( 22.47071067811865319, 0.09909245471376171288, -126.2799252555019649 ) ) ;
#170034=ORIENTED_EDGE ( 'NONE', *, *, #241667, .T. ) ;
#170044=CIRCLE ( 'NONE', #224143, 0.09999999999998898659 ) ;
#170071=DIRECTION ( 'NONE',  ( 0.7071067811865475727, -0.7071067811865475727, 0.000000000000000000 ) ) ;
#170072=CARTESIAN_POINT ( 'NONE',  ( 20.94999999999999574, 10.47338541492405994, -141.5786544642485580 ) ) ;
#170093=ADVANCED_FACE ( 'NONE', ( #219505 ), #202526, .T. ) ;
#170099=AXIS2_PLACEMENT_3D ( 'NONE', #241651, #158302, #83817 ) ;
#170125=CIRCLE ( 'NONE', #57632, 0.09999999999999939493 ) ;
#170133=EDGE_CURVE ( 'NONE', #50042, #4950, #135081, .T. ) ;
#170144=CIRCLE ( 'NONE', #236717, 0.09999999999999939493 ) ;
#170154=ORIENTED_EDGE ( 'NONE', *, *, #176955, .T. ) ;
#170190=CIRCLE ( 'NONE', #215902, 0.1000000000000002692 ) ;
#170192=AXIS2_PLACEMENT_3D ( 'NONE', #57546, #178834, #160547 ) ;
#170246=VERTEX_POINT ( 'NONE', #91569 ) ;
#170268=DIRECTION ( 'NONE',  ( 0.000000000000000000, 0.000000000000000000, 1.000000000000000000 ) ) ;
#170281=EDGE_CURVE ( 'NONE', #153822, #200447, #6888, .T. ) ;
#170288=CARTESIAN_POINT ( 'NONE',  ( -23.15000000000000213, 1.910280373842936141, -146.6313678551989597 ) ) ;
#170321=CARTESIAN_POINT ( 'NONE',  ( -21.22070241538126112, 6.469946272880768845, -133.9010809694649993 ) ) ;
#170344=CARTESIAN_POINT ( 'NONE',  ( 18.59999999999999432, -1.162701749926853712, -142.1000000000000227 ) ) ;
#170361=ORIENTED_EDGE ( 'NONE', *, *, #154586, .T. ) ;
#170379=LINE ( 'NONE', #133758, #198859 ) ;
#170380=UNCERTAINTY_MEASURE_WITH_UNIT (LENGTH_MEASURE( 1.000000000000000082E-05 ), #57419, 'distance_accuracy_value', 'NONE');
#170382=DIRECTION ( 'NONE',  ( 0.000000000000000000, 0.000000000000000000, 1.000000000000000000 ) ) ;
#170385=DIRECTION ( 'NONE',  ( -1.000000000000000000, -0.000000000000000000, -0.000000000000000000 ) ) ;
#170437=ORIENTED_EDGE ( 'NONE', *, *, #37365, .F. ) ;
#170468=FACE_OUTER_BOUND ( 'NONE', #18613, .T. ) ;
#170472=ORIENTED_EDGE ( 'NONE', *, *, #9210, .F. ) ;
#170487=AXIS2_PLACEMENT_3D ( 'NONE', #47035, #206136, #50881 ) ;
#170494=DIRECTION ( 'NONE',  ( 0.000000000000000000, 0.000000000000000000, -1.000000000000000000 ) ) ;
#170524=DIRECTION ( 'NONE',  ( 1.000000000000000000, 0.000000000000000000, -0.000000000000000000 ) ) ;
#170528=EDGE_CURVE ( 'NONE', #257284, #101749, #247769, .T. ) ;
#170537=ORIENTED_EDGE ( 'NONE', *, *, #241311, .T. ) ;
#170545=CARTESIAN_POINT ( 'NONE',  ( -21.05000000000000071, 6.300000000011169554, -134.1000000000000227 ) ) ;
#170554=ADVANCED_FACE ( 'NONE', ( #186525 ), #197821, .T. ) ;
#170571=CARTESIAN_POINT ( 'NONE',  ( -21.08376601933334271, 0.06377601094103312052, -127.6580527287243001 ) ) ;
#170574=VECTOR ( 'NONE', #38048, 1000.000000000000000 ) ;
#170581=VERTEX_POINT ( 'NONE', #206082 ) ;
#170589=VERTEX_POINT ( 'NONE', #33581 ) ;
#170592=ORIENTED_EDGE ( 'NONE', *, *, #253676, .F. ) ;
#170610=ORIENTED_EDGE ( 'NONE', *, *, #55270, .T. ) ;
#170643=CARTESIAN_POINT ( 'NONE',  ( -18.59999999999999787, -1.162701749926853712, -142.1000000000000227 ) ) ;
#170648=VERTEX_POINT ( 'NONE', #15272 ) ;
#170659=CARTESIAN_POINT ( 'NONE',  ( 20.85000000000000142, 1.115600667400684642E-11, -167.5000000000000284 ) ) ;
#170707=DIRECTION ( 'NONE',  ( 0.000000000000000000, 2.168404344971247498E-15, 1.000000000000000000 ) ) ;
#170765=ORIENTED_EDGE ( 'NONE', *, *, #203291, .T. ) ;
#170777=EDGE_CURVE ( 'NONE', #130320, #84861, #64547, .T. ) ;
#170811=CARTESIAN_POINT ( 'NONE',  ( 21.13461538461538325, 8.885417037985616773, -146.3500000000000227 ) ) ;
#170841=ORIENTED_EDGE ( 'NONE', *, *, #191309, .T. ) ;
#170849=CIRCLE ( 'NONE', #29182, 11.80000000000000426 ) ;
#170870=AXIS2_PLACEMENT_3D ( 'NONE', #91973, #52838, #171551 ) ;
#170878=ORIENTED_EDGE ( 'NONE', *, *, #145478, .F. ) ;
#170961=CYLINDRICAL_SURFACE ( 'NONE', #107572, 0.09999999999998898659 ) ;
#170967=DIRECTION ( 'NONE',  ( 0.000000000000000000, 0.000000000000000000, 1.000000000000000000 ) ) ;
#171022=CARTESIAN_POINT ( 'NONE',  ( 23.14999999999999858, 1.115600667400684642E-11, -167.5000000000000284 ) ) ;
#171027=EDGE_CURVE ( 'NONE', #43473, #175390, #71083, .T. ) ;
#171037=VERTEX_POINT ( 'NONE', #133595 ) ;
#171070=CARTESIAN_POINT ( 'NONE',  ( 23.14999999999998437, 1.115600667400684642E-11, -134.0000000000000000 ) ) ;
#171086=ORIENTED_EDGE ( 'NONE', *, *, #81038, .T. ) ;
#171090=FACE_OUTER_BOUND ( 'NONE', #233893, .T. ) ;
#171118=LINE ( 'NONE', #51080, #235685 ) ;
#171158=DIRECTION ( 'NONE',  ( 0.000000000000000000, -0.000000000000000000, 1.000000000000000000 ) ) ;
#171167=AXIS2_PLACEMENT_3D ( 'NONE', #79412, #238504, #220245 ) ;
#171180=VERTEX_POINT ( 'NONE', #124320 ) ;
#171186=VERTEX_POINT ( 'NONE', #160891 ) ;
#171189=CARTESIAN_POINT ( 'NONE',  ( 23.24999999999999289, 11.65000000001116298, -122.2500000000000284 ) ) ;
#171203=FACE_OUTER_BOUND ( 'NONE', #111734, .T. ) ;
#171209=CARTESIAN_POINT ( 'NONE',  ( -20.54999999999999716, 2.500000000011154633, -154.2753780772379173 ) ) ;
#171231=CARTESIAN_POINT ( 'NONE',  ( -18.59999999999999787, -1.637172712959223952, -145.5821533654720383 ) ) ;
#171239=EDGE_CURVE ( 'NONE', #244782, #104618, #223129, .T. ) ;
#171246=ORIENTED_EDGE ( 'NONE', *, *, #82634, .F. ) ;
#171258=DIRECTION ( 'NONE',  ( -1.000000000000000000, -2.952720810173289112E-16, 0.000000000000000000 ) ) ;
#171293=DIRECTION ( 'NONE',  ( 0.000000000000000000, 0.000000000000000000, -1.000000000000000000 ) ) ;
#171298=CIRCLE ( 'NONE', #58782, 0.09999999999998898659 ) ;
#171316=FACE_OUTER_BOUND ( 'NONE', #132140, .T. ) ;
#171326=ORIENTED_EDGE ( 'NONE', *, *, #234304, .T. ) ;
#171371=AXIS2_PLACEMENT_3D ( 'NONE', #22557, #96902, #159501 ) ;
#171373=DIRECTION ( 'NONE',  ( 0.000000000000000000, 0.01562500000001262185, 0.9998779222360095753 ) ) ;
#171396=ORIENTED_EDGE ( 'NONE', *, *, #61683, .T. ) ;
#171400=VERTEX_POINT ( 'NONE', #232429 ) ;
#171405=DIRECTION ( 'NONE',  ( 0.000000000000000000, 0.000000000000000000, 1.000000000000000000 ) ) ;
#171410=CARTESIAN_POINT ( 'NONE',  ( -20.64999999999999858, 1.115600667400684642E-11, -146.9749999999999943 ) ) ;
#171413=AXIS2_PLACEMENT_3D ( 'NONE', #189130, #87446, #10506 ) ;
#171415=FACE_OUTER_BOUND ( 'NONE', #232263, .T. ) ;
#171430=CARTESIAN_POINT ( 'NONE',  ( -18.59999999999999787, -1.835859311432481045, -179.0044391687985410 ) ) ;
#171462=CIRCLE ( 'NONE', #150582, 0.09999999999999939493 ) ;
#171516=DIRECTION ( 'NONE',  ( 1.000000000000000000, -0.000000000000000000, -0.000000000000000000 ) ) ;
#171530=CARTESIAN_POINT ( 'NONE',  ( 21.05281448260627641, 8.776010158548784190, -146.1735579118114288 ) ) ;
#171551=DIRECTION ( 'NONE',  ( 0.000000000000000000, 0.000000000000000000, -1.000000000000000000 ) ) ;
#171559=CARTESIAN_POINT ( 'NONE',  ( 18.59999999999999787, -9.399999999988843058, -174.3820418481727188 ) ) ;
#171572=CARTESIAN_POINT ( 'NONE',  ( -20.64999999999999858, 7.150000000011155876, -146.2500000000000284 ) ) ;
#171574=LINE ( 'NONE', #104168, #238027 ) ;
#171587=VECTOR ( 'NONE', #227950, 1000.000000000000114 ) ;
#171590=VECTOR ( 'NONE', #225512, 1000.000000000000000 ) ;
#171608=AXIS2_PLACEMENT_3D ( 'NONE', #210278, #31661, #111168 ) ;
#171612=LINE ( 'NONE', #166473, #228959 ) ;
#171628=CARTESIAN_POINT ( 'NONE',  ( 18.44444291854881612, -9.490101180932075664, -174.1289039648910375 ) ) ;
#171630=CARTESIAN_POINT ( 'NONE',  ( 18.44208962362688098, -9.552340496897864242, -174.3421730554626379 ) ) ;
#171640=CARTESIAN_POINT ( 'NONE',  ( 18.52351027002947603, -9.642162904684033364, -174.2150469505097874 ) ) ;
#171649=CARTESIAN_POINT ( 'NONE',  ( 21.05000000000000071, 6.257814610487280937, -133.9022097086912311 ) ) ;
#171675=ORIENTED_EDGE ( 'NONE', *, *, #45085, .F. ) ;
#171721=ORIENTED_EDGE ( 'NONE', *, *, #46960, .T. ) ;
#171724=DIRECTION ( 'NONE',  ( 0.000000000000000000, 1.734723475976997999E-14, -1.000000000000000000 ) ) ;
#171725=EDGE_LOOP ( 'NONE', ( #195651, #195229, #49401, #145736, #131322, #26441, #205846, #218402, #131932, #23708 ) ) ;
#171763=EDGE_CURVE ( 'NONE', #217031, #80663, #246522, .T. ) ;
#171820=AXIS2_PLACEMENT_3D ( 'NONE', #28104, #189721, #12389 ) ;
#171833=CARTESIAN_POINT ( 'NONE',  ( -20.94999999999999929, -11.64999999998884483, -164.5000000000000000 ) ) ;
#171860=ORIENTED_EDGE ( 'NONE', *, *, #147284, .T. ) ;
#171870=LINE ( 'NONE', #200057, #41705 ) ;
#171873=DIRECTION ( 'NONE',  ( 0.000000000000000000, 0.000000000000000000, -1.000000000000000000 ) ) ;
#171878=EDGE_LOOP ( 'NONE', ( #231089, #239643, #52123, #232414 ) ) ;
#171892=AXIS2_PLACEMENT_3D ( 'NONE', #215778, #37182, #116694 ) ;
#171913=ORIENTED_EDGE ( 'NONE', *, *, #109488, .F. ) ;
#171976=DIRECTION ( 'NONE',  ( 1.000000000000000000, 0.000000000000000000, 0.000000000000000000 ) ) ;
#171977=ORIENTED_EDGE ( 'NONE', *, *, #111082, .F. ) ;
#171993=EDGE_CURVE ( 'NONE', #76541, #138896, #185901, .T. ) ;
#172087=EDGE_CURVE ( 'NONE', #242008, #112934, #48535, .T. ) ;
#172113=VECTOR ( 'NONE', #245433, 1000.000000000000000 ) ;
#172122=DIRECTION ( 'NONE',  ( 0.000000000000000000, 1.000000000000000000, 0.000000000000000000 ) ) ;
#172138=DIRECTION ( 'NONE',  ( 1.000000000000000000, 0.000000000000000000, 0.000000000000000000 ) ) ;
#172150=DIRECTION ( 'NONE',  ( -1.000000000000000000, -0.000000000000000000, 0.000000000000000000 ) ) ;
#172155=DIRECTION ( 'NONE',  ( 1.000000000000000000, -0.000000000000000000, -0.000000000000000000 ) ) ;
#172164=LINE ( 'NONE', #54732, #126602 ) ;
#172170=EDGE_CURVE ( 'NONE', #42512, #186782, #19517, .T. ) ;
#172172=AXIS2_PLACEMENT_3D ( 'NONE', #130296, #89882, #70367 ) ;
#172201=EDGE_CURVE ( 'NONE', #208557, #33915, #135999, .T. ) ;
#172221=CARTESIAN_POINT ( 'NONE',  ( 23.15000000000000213, -11.48912529306489816, -164.4000000000000057 ) ) ;
#172243=EDGE_CURVE ( 'NONE', #240530, #147657, #102670, .T. ) ;
#172254=CARTESIAN_POINT ( 'NONE',  ( -20.94999999999999929, 1.115650877919449413E-11, -171.6000000000000227 ) ) ;
#172257=EDGE_LOOP ( 'NONE', ( #108912, #215931, #51180, #42193 ) ) ;
#172300=ORIENTED_EDGE ( 'NONE', *, *, #78639, .T. ) ;
#172316=LINE ( 'NONE', #212687, #67279 ) ;
#172335=ORIENTED_EDGE ( 'NONE', *, *, #220919, .F. ) ;
#172336=ORIENTED_EDGE ( 'NONE', *, *, #178662, .F. ) ;
#172350=ORIENTED_EDGE ( 'NONE', *, *, #214625, .T. ) ;
#172359=SPHERICAL_SURFACE ( 'NONE', #30966, 0.1000000000000000056 ) ;
#172390=CIRCLE ( 'NONE', #151520, 0.09999999999999939493 ) ;
#172394=ADVANCED_FACE ( 'NONE', ( #173158 ), #123747, .F. ) ;
#172414=VERTEX_POINT ( 'NONE', #233105 ) ;
#172428=ORIENTED_EDGE ( 'NONE', *, *, #233841, .T. ) ;
#172429=VERTEX_POINT ( 'NONE', #111855 ) ;
#172440=CARTESIAN_POINT ( 'NONE',  ( -21.14999999999999858, 11.65000000001115588, -140.7838656629781724 ) ) ;
#172452=ORIENTED_EDGE ( 'NONE', *, *, #147724, .T. ) ;
#172471=EDGE_CURVE ( 'NONE', #38015, #169538, #102281, .T. ) ;
#172486=ORIENTED_EDGE ( 'NONE', *, *, #246273, .T. ) ;
#172496=FACE_OUTER_BOUND ( 'NONE', #71422, .T. ) ;
#172500=ADVANCED_FACE ( 'NONE', ( #60844 ), #223668, .T. ) ;
#172549=CARTESIAN_POINT ( 'NONE',  ( 23.14999999999999858, 1.115600667400684642E-11, -171.5000000000000284 ) ) ;
#172581=DIRECTION ( 'NONE',  ( 0.000000000000000000, -0.000000000000000000, 1.000000000000000000 ) ) ;
#172582=ORIENTED_EDGE ( 'NONE', *, *, #127990, .T. ) ;
#172592=CARTESIAN_POINT ( 'NONE',  ( -23.15000000000000213, -11.64999999998884483, -164.4000000000000057 ) ) ;
#172594=CARTESIAN_POINT ( 'NONE',  ( -20.94999999999999929, -1.162701749926853712, -142.1000000000000227 ) ) ;
#172598=EDGE_LOOP ( 'NONE', ( #238925, #234227, #250246, #124259 ) ) ;
#172610=CARTESIAN_POINT ( 'NONE',  ( -21.05000000000000071, 14.05000000001115623, -139.5136950707610026 ) ) ;
#172617=ADVANCED_FACE ( 'NONE', ( #231189 ), #252325, .F. ) ;
#172628=DIRECTION ( 'NONE',  ( -1.000000000000000000, -0.000000000000000000, -0.000000000000000000 ) ) ;
#172635=AXIS2_PLACEMENT_3D ( 'NONE', #221943, #43347, #6776 ) ;
#172654=VECTOR ( 'NONE', #198723, 1000.000000000000000 ) ;
#172660=AXIS2_PLACEMENT_3D ( 'NONE', #232888, #114194, #29559 ) ;
#172689=AXIS2_PLACEMENT_3D ( 'NONE', #18347, #256907, #23522 ) ;
#172697=VECTOR ( 'NONE', #134750, 1000.000000000000000 ) ;
#172728=ORIENTED_EDGE ( 'NONE', *, *, #154474, .F. ) ;
#172756=ORIENTED_EDGE ( 'NONE', *, *, #79345, .F. ) ;
#172779=DIRECTION ( 'NONE',  ( -1.836970198721029934E-16, 1.000000000000000000, 0.000000000000000000 ) ) ;
#172781=DIRECTION ( 'NONE',  ( -1.000000000000000000, -0.000000000000000000, -0.000000000000000000 ) ) ;
#172802=ADVANCED_FACE ( 'NONE', ( #36469 ), #229513, .T. ) ;
#172808=ORIENTED_EDGE ( 'NONE', *, *, #196909, .F. ) ;
#172846=CARTESIAN_POINT ( 'NONE',  ( -18.58222699835055280, 10.33200063080771969, -173.0931674956643178 ) ) ;
#172879=DIRECTION ( 'NONE',  ( 0.000000000000000000, 0.000000000000000000, 1.000000000000000000 ) ) ;
#172918=DIRECTION ( 'NONE',  ( 1.000000000000000000, 0.000000000000000000, 0.000000000000000000 ) ) ;
#172925=CARTESIAN_POINT ( 'NONE',  ( 20.94999999999999929, 1.115624548013267999E-11, -165.6000000000000227 ) ) ;
#172998=EDGE_CURVE ( 'NONE', #231078, #84586, #110889, .T. ) ;
#173013=CARTESIAN_POINT ( 'NONE',  ( -20.94999999999999929, 11.63687328911532859, -160.6782407866750475 ) ) ;
#173033=VERTEX_POINT ( 'NONE', #255432 ) ;
#173071=AXIS2_PLACEMENT_3D ( 'NONE', #201988, #186285, #122460 ) ;
#173074=EDGE_CURVE ( 'NONE', #222383, #7645, #177560, .T. ) ;
#173106=DIRECTION ( 'NONE',  ( -0.000000000000000000, -1.000000000000000000, 6.308085367188393199E-16 ) ) ;
#173110=CARTESIAN_POINT ( 'NONE',  ( -21.09096482362077651, 0.03944827878506227542, -127.6364556345950518 ) ) ;
#173113=CARTESIAN_POINT ( 'NONE',  ( 20.94999999999999929, 10.38178547073510316, -173.0078453638842007 ) ) ;
#173123=AXIS2_PLACEMENT_3D ( 'NONE', #125592, #180437, #184279 ) ;
#173145=FACE_OUTER_BOUND ( 'NONE', #100481, .T. ) ;
#173151=CARTESIAN_POINT ( 'NONE',  ( 18.49999999999999289, 6.650000000011155876, -155.1500000000000057 ) ) ;
#173154=CARTESIAN_POINT ( 'NONE',  ( -20.54999999999999716, 2.400000000011155432, -154.2753780772379173 ) ) ;
#173158=FACE_OUTER_BOUND ( 'NONE', #173706, .T. ) ;
#173351=ORIENTED_EDGE ( 'NONE', *, *, #132450, .T. ) ;
#173370=ORIENTED_EDGE ( 'NONE', *, *, #133833, .F. ) ;
#173386=EDGE_CURVE ( 'NONE', #256406, #247600, #76523, .T. ) ;
#173398=ORIENTED_EDGE ( 'NONE', *, *, #153955, .F. ) ;
#173399=ADVANCED_FACE ( 'NONE', ( #218589 ), #176949, .T. ) ;
#173419=LINE ( 'NONE', #194240, #238358 ) ;
#173469=ORIENTED_EDGE ( 'NONE', *, *, #66649, .T. ) ;
#173471=CARTESIAN_POINT ( 'NONE',  ( -23.15000000000000213, -9.499999999988846255, -157.6060308773475924 ) ) ;
#173487=VECTOR ( 'NONE', #159630, 1000.000000000000000 ) ;
#173537=DIRECTION ( 'NONE',  ( 0.000000000000000000, 0.000000000000000000, 1.000000000000000000 ) ) ;
#173559=CIRCLE ( 'NONE', #169456, 0.09999999999998898659 ) ;
#173584=ORIENTED_EDGE ( 'NONE', *, *, #64486, .T. ) ;
#173604=DIRECTION ( 'NONE',  ( -2.952720810173289112E-16, 1.000000000000000000, -0.000000000000000000 ) ) ;
#173612=AXIS2_PLACEMENT_3D ( 'NONE', #20325, #708, #75172 ) ;
#173618=ORIENTED_EDGE ( 'NONE', *, *, #17769, .T. ) ;
#173625=VECTOR ( 'NONE', #35150, 1000.000000000000000 ) ;
#173627=EDGE_LOOP ( 'NONE', ( #72614, #70332, #204168, #196961 ) ) ;
#173636=EDGE_CURVE ( 'NONE', #79296, #135320, #22383, .T. ) ;
#173637=CARTESIAN_POINT ( 'NONE',  ( 20.94999999999999929, 10.72371710471868056, -146.1500000000000341 ) ) ;
#173638=CARTESIAN_POINT ( 'NONE',  ( 18.49999999999999289, 10.20857864377385127, -155.3500000000000227 ) ) ;
#173661=VECTOR ( 'NONE', #102312, 1000.000000000000000 ) ;
#173664=EDGE_LOOP ( 'NONE', ( #167156, #25508, #66295, #35198, #174439 ) ) ;
#173674=ADVANCED_FACE ( 'NONE', ( #76208 ), #126599, .T. ) ;
#173678=CARTESIAN_POINT ( 'NONE',  ( 18.49999999999999645, -1.299733671219632791, -124.0281295228694347 ) ) ;
#173706=EDGE_LOOP ( 'NONE', ( #147688, #234627, #163561, #155324 ) ) ;
#173708=AXIS2_PLACEMENT_3D ( 'NONE', #127586, #168036, #205836 ) ;
#173717=AXIS2_PLACEMENT_3D ( 'NONE', #181392, #1426, #60114 ) ;
#173718=AXIS2_PLACEMENT_3D ( 'NONE', #136788, #234615, #76819 ) ;
#173723=VERTEX_POINT ( 'NONE', #125320 ) ;
#173741=EDGE_CURVE ( 'NONE', #87859, #242592, #26229, .T. ) ;
#173755=ORIENTED_EDGE ( 'NONE', *, *, #221902, .T. ) ;
#173778=ADVANCED_FACE ( 'NONE', ( #169626 ), #50884, .F. ) ;
#173779=DIRECTION ( 'NONE',  ( -0.000000000000000000, -1.000000000000000000, 6.308085367188393199E-16 ) ) ;
#173799=EDGE_CURVE ( 'NONE', #36655, #169538, #32360, .T. ) ;
#173801=AXIS2_PLACEMENT_3D ( 'NONE', #101852, #100559, #86136 ) ;
#173818=CARTESIAN_POINT ( 'NONE',  ( 20.04142135623730070, 11.65000000001115943, -155.3500000000000227 ) ) ;
#173825=VERTEX_POINT ( 'NONE', #131732 ) ;
#173844=ORIENTED_EDGE ( 'NONE', *, *, #44470, .T. ) ;
#173874=EDGE_LOOP ( 'NONE', ( #66816, #43387, #56850, #154037 ) ) ;
#173900=AXIS2_PLACEMENT_3D ( 'NONE', #223508, #224794, #128291 ) ;
#173927=SPHERICAL_SURFACE ( 'NONE', #224961, 0.1000000000000000056 ) ;
#174005=DIRECTION ( 'NONE',  ( -0.000000000000000000, 1.000000000000000000, -0.000000000000000000 ) ) ;
#174007=ORIENTED_EDGE ( 'NONE', *, *, #149282, .F. ) ;
#174014=CIRCLE ( 'NONE', #40731, 11.75000000000000000 ) ;
#174072=CIRCLE ( 'NONE', #94908, 0.2000000000000057288 ) ;
#174076=TOROIDAL_SURFACE ( 'NONE', #61610, 0.4000000000000005773, 0.1000000000000000056 ) ;
#174088=VERTEX_POINT ( 'NONE', #184980 ) ;
#174097=CARTESIAN_POINT ( 'NONE',  ( -18.59999999999999787, -1.835341550213255957, -145.5551512925629822 ) ) ;
#174133=CARTESIAN_POINT ( 'NONE',  ( 18.59999999999999787, -1.249999999988843369, -175.3004807544151049 ) ) ;
#174135=CYLINDRICAL_SURFACE ( 'NONE', #167812, 0.09999999999998898659 ) ;
#174154=DIRECTION ( 'NONE',  ( -3.265361837132813093E-16, 1.000000000000000000, 0.000000000000000000 ) ) ;
#174165=CARTESIAN_POINT ( 'NONE',  ( -20.85000000000000142, 11.75000000001115197, -160.7161343370219129 ) ) ;
#174174=AXIS2_PLACEMENT_3D ( 'NONE', #17040, #136963, #216501 ) ;
#174177=DIRECTION ( 'NONE',  ( 0.000000000000000000, 1.000000000000000000, -3.469446951953635015E-14 ) ) ;
#174190=CARTESIAN_POINT ( 'NONE',  ( 21.05000000000000071, 1.115600667400684642E-11, -134.0000000000000000 ) ) ;
#174203=CARTESIAN_POINT ( 'NONE',  ( 21.14250536705908345, 6.518172176891880554, -134.0000000000000000 ) ) ;
#174214=ORIENTED_EDGE ( 'NONE', *, *, #142404, .F. ) ;
#174279=DIRECTION ( 'NONE',  ( 0.000000000000000000, -1.000000000000000000, -0.000000000000000000 ) ) ;
#174304=ORIENTED_EDGE ( 'NONE', *, *, #93877, .F. ) ;
#174320=CARTESIAN_POINT ( 'NONE',  ( -21.53699400384953577, 1.355070199499284871E-11, -127.2122882067625653 ) ) ;
#174378=DIRECTION ( 'NONE',  ( 0.000000000000000000, 0.000000000000000000, 1.000000000000000000 ) ) ;
#174412=ORIENTED_EDGE ( 'NONE', *, *, #76075, .F. ) ;
#174422=VERTEX_POINT ( 'NONE', #62159 ) ;
#174423=DIRECTION ( 'NONE',  ( -0.000000000000000000, -1.000000000000000000, -0.000000000000000000 ) ) ;
#174428=DIRECTION ( 'NONE',  ( -3.265361837132813093E-16, 1.000000000000000000, 0.000000000000000000 ) ) ;
#174439=ORIENTED_EDGE ( 'NONE', *, *, #210476, .F. ) ;
#174464=DIRECTION ( 'NONE',  ( 1.000000000000000000, 0.000000000000000000, 0.000000000000000000 ) ) ;
#174503=ORIENTED_EDGE ( 'NONE', *, *, #176096, .F. ) ;
#174539=DIRECTION ( 'NONE',  ( 0.000000000000000000, -1.000000000000000000, 0.000000000000000000 ) ) ;
#174564=EDGE_CURVE ( 'NONE', #85588, #80694, #95036, .T. ) ;
#174575=AXIS2_PLACEMENT_3D ( 'NONE', #177569, #38044, #22335 ) ;
#174632=DIRECTION ( 'NONE',  ( 1.000000000000000000, 0.000000000000000000, 0.000000000000000000 ) ) ;
#174653=ADVANCED_FACE ( 'NONE', ( #149414 ), #30752, .F. ) ;
#174669=VERTEX_POINT ( 'NONE', #213198 ) ;
#174676=EDGE_LOOP ( 'NONE', ( #28172, #52418, #108208, #131099 ) ) ;
#174684=DIRECTION ( 'NONE',  ( 1.000000000000000000, 3.265361837132813093E-16, -0.000000000000000000 ) ) ;
#174693=CARTESIAN_POINT ( 'NONE',  ( -18.59999999999999787, 11.75000000001115552, -167.5000000000000284 ) ) ;
#174713=EDGE_CURVE ( 'NONE', #222383, #178251, #192371, .T. ) ;
#174725=DIRECTION ( 'NONE',  ( 1.000000000000000000, 0.000000000000000000, 0.000000000000000000 ) ) ;
#174751=LINE ( 'NONE', #230850, #245134 ) ;
#174754=DIRECTION ( 'NONE',  ( 1.000000000000000000, 0.000000000000000000, -0.000000000000000000 ) ) ;
#174788=FACE_OUTER_BOUND ( 'NONE', #171878, .T. ) ;
#174850=LINE ( 'NONE', #93965, #240874 ) ;
#174855=DIRECTION ( 'NONE',  ( 0.000000000000000000, 0.000000000000000000, -1.000000000000000000 ) ) ;
#174864=ORIENTED_EDGE ( 'NONE', *, *, #156253, .F. ) ;
#174928=AXIS2_PLACEMENT_3D ( 'NONE', #216841, #141173, #255922 ) ;
#174952=ORIENTED_EDGE ( 'NONE', *, *, #186895, .T. ) ;
#174968=CARTESIAN_POINT ( 'NONE',  ( 20.85000000000000142, -1.835859311432481045, -179.0044391687985410 ) ) ;
#174969=VERTEX_POINT ( 'NONE', #85215 ) ;
#174982=ORIENTED_EDGE ( 'NONE', *, *, #173636, .F. ) ;
#174999=VERTEX_POINT ( 'NONE', #164800 ) ;
#175056=CARTESIAN_POINT ( 'NONE',  ( -18.50000000000000000, 9.250000000011157297, -146.3500000000000227 ) ) ;
#175091=( BOUNDED_SURFACE ( )  B_SPLINE_SURFACE ( 3, 2, ( 
 ( #236413, #16112, #153075 ),
 ( #95614, #133467, #175212 ),
 ( #254656, #216842, #155634 ),
 ( #197286, #212997, #96865 ),
 ( #18654, #240283, #182887 ),
 ( #44644, #220708, #143729 ) ),
 .UNSPECIFIED., .F., .F., .F. ) 
 B_SPLINE_SURFACE_WITH_KNOTS ( ( 4, 2, 4 ),
 ( 3, 3 ),
 ( 0.0001342700090130150253, 0.0002909192928057470397, 0.0004475685765984790000 ),
 ( 0.000000000000000000, 1.000000000000000000 ),
 .UNSPECIFIED. ) 
 GEOMETRIC_REPRESENTATION_ITEM ( )  RATIONAL_B_SPLINE_SURFACE ( (
 ( 1.000000000000000000, 0.7250110520819876836, 1.000000000000000000),
 ( 1.000000000000000000, 0.7257599279136505155, 1.000000000000000000),
 ( 1.000000000000000000, 0.7137594617280778042, 1.000000000000000000),
 ( 1.000000000000000000, 0.6959270178813201646, 1.000000000000000000),
 ( 1.000000000000000000, 0.6919879549336411806, 1.000000000000000000),
 ( 1.000000000000000000, 0.7071067811865475727, 1.000000000000000000) ) ) 
 REPRESENTATION_ITEM ( '' )  SURFACE ( )  );
#175120=DIRECTION ( 'NONE',  ( 0.000000000000000000, 1.734723475976998188E-13, 1.000000000000000000 ) ) ;
#175125=EDGE_CURVE ( 'NONE', #64347, #209723, #68266, .T. ) ;
#175136=CARTESIAN_POINT ( 'NONE',  ( -20.94999999999999929, 1.115600667400684642E-11, -167.5000000000000284 ) ) ;
#175143=VERTEX_POINT ( 'NONE', #21155 ) ;
#175185=ADVANCED_FACE ( 'NONE', ( #154265 ), #181884, .F. ) ;
#175202=ADVANCED_FACE ( 'NONE', ( #101913 ), #240185, .F. ) ;
#175212=CARTESIAN_POINT ( 'NONE',  ( 21.05000000000000071, 10.72371711693665652, -146.1762396011381497 ) ) ;
#175224=ORIENTED_EDGE ( 'NONE', *, *, #90006, .T. ) ;
#175310=EDGE_CURVE ( 'NONE', #129965, #241817, #232622, .T. ) ;
#175333=CARTESIAN_POINT ( 'NONE',  ( -23.25000000000000000, 4.350000000011156054, -146.1500000000000341 ) ) ;
#175355=( LENGTH_UNIT ( ) NAMED_UNIT ( * ) SI_UNIT ( .MILLI., .METRE. ) );
#175379=EDGE_LOOP ( 'NONE', ( #135151, #161800, #43161, #205727 ) ) ;
#175380=CYLINDRICAL_SURFACE ( 'NONE', #52111, 0.5000000000000004441 ) ;
#175387=CARTESIAN_POINT ( 'NONE',  ( 20.85000000000000142, 1.115600667400684642E-11, -167.5000000000000284 ) ) ;
#175390=VERTEX_POINT ( 'NONE', #120912 ) ;
#175404=EDGE_CURVE ( 'NONE', #156098, #33432, #20597, .T. ) ;
#175410=CARTESIAN_POINT ( 'NONE',  ( -22.59999999999999787, 0.1008583691098682150, -122.2504328765106294 ) ) ;
#175417=DIRECTION ( 'NONE',  ( -1.000000000000000000, -0.000000000000000000, -0.000000000000000000 ) ) ;
#175433=CARTESIAN_POINT ( 'NONE',  ( -18.50000000000000000, 11.75000000001115552, -146.1500000000000341 ) ) ;
#175436=AXIS2_PLACEMENT_3D ( 'NONE', #113634, #90195, #91510 ) ;
#175449=FACE_OUTER_BOUND ( 'NONE', #57592, .T. ) ;
#175452=DIRECTION ( 'NONE',  ( 1.000000000000000000, 0.000000000000000000, 0.000000000000000000 ) ) ;
#175458=DIRECTION ( 'NONE',  ( 0.000000000000000000, -0.9908441862701782288, 0.1350103645450542456 ) ) ;
#175489=DIRECTION ( 'NONE',  ( 0.000000000000000000, 0.000000000000000000, -1.000000000000000000 ) ) ;
#175510=CIRCLE ( 'NONE', #150554, 0.09999999999998898659 ) ;
#175513=ORIENTED_EDGE ( 'NONE', *, *, #237466, .T. ) ;
#175518=VERTEX_POINT ( 'NONE', #184694 ) ;
#175524=ORIENTED_EDGE ( 'NONE', *, *, #144821, .F. ) ;
#175529=AXIS2_PLACEMENT_3D ( 'NONE', #114563, #156289, #208855 ) ;
#175534=DIRECTION ( 'NONE',  ( -1.000000000000000000, 0.000000000000000000, 0.000000000000000000 ) ) ;
#175543=VERTEX_POINT ( 'NONE', #144262 ) ;
#175555=FACE_OUTER_BOUND ( 'NONE', #191413, .T. ) ;
#175575=CARTESIAN_POINT ( 'NONE',  ( 22.50000000000000000, 1.115600667400684642E-11, -134.0000000000000000 ) ) ;
#175592=AXIS2_PLACEMENT_3D ( 'NONE', #233486, #76947, #238594 ) ;
#175594=ORIENTED_EDGE ( 'NONE', *, *, #75089, .F. ) ;
#175610=ORIENTED_EDGE ( 'NONE', *, *, #194827, .F. ) ;
#175630=AXIS2_PLACEMENT_3D ( 'NONE', #229849, #169926, #48633 ) ;
#175680=AXIS2_PLACEMENT_3D ( 'NONE', #13566, #250866, #89229 ) ;
#175704=AXIS2_PLACEMENT_3D ( 'NONE', #122240, #25703, #201760 ) ;
#175739=CYLINDRICAL_SURFACE ( 'NONE', #237017, 0.09999999999999939493 ) ;
#175747=VECTOR ( 'NONE', #168310, 1000.000000000000000 ) ;
#175761=DIRECTION ( 'NONE',  ( -1.000000000000000000, 0.000000000000000000, 0.000000000000000000 ) ) ;
#175780=DIRECTION ( 'NONE',  ( 1.000000000000000000, 0.000000000000000000, 0.000000000000000000 ) ) ;
#175804=VERTEX_POINT ( 'NONE', #180555 ) ;
#175837=AXIS2_PLACEMENT_3D ( 'NONE', #86244, #182836, #245361 ) ;
#175882=AXIS2_PLACEMENT_3D ( 'NONE', #247765, #5271, #30034 ) ;
#175887=B_SPLINE_CURVE_WITH_KNOTS ( 'NONE', 3,
 ( #152468, #130297, #28691, #231998, #91183, #250254, #208583, #29954 ),
 .UNSPECIFIED., .F., .F.,
 ( 4, 2, 2, 4 ),
 ( 0.000000000000000000, 0.0002114466876441993754, 0.0003171700314663004590, 0.0004228933752884015697 ),
 .UNSPECIFIED. ) ;
#175892=CARTESIAN_POINT ( 'NONE',  ( 23.24999999999999645, 1.115600667400684642E-11, -134.0000000000000000 ) ) ;
#175914=VERTEX_POINT ( 'NONE', #46164 ) ;
#175918=CARTESIAN_POINT ( 'NONE',  ( -23.15000000000000213, -11.64999999998884483, -134.0000000000000000 ) ) ;
#175940=LINE ( 'NONE', #36430, #126902 ) ;
#175962=CARTESIAN_POINT ( 'NONE',  ( -23.15000000000000213, 11.65000000001115588, -155.3500000000000227 ) ) ;
#175963=CARTESIAN_POINT ( 'NONE',  ( -20.64999999999999858, 4.350000000011156054, -155.1500000000000057 ) ) ;
#176006=CARTESIAN_POINT ( 'NONE',  ( 18.59999999999999076, -1.835859311432481045, -179.1044391687985353 ) ) ;
#176076=AXIS2_PLACEMENT_3D ( 'NONE', #24494, #23215, #242221 ) ;
#176096=EDGE_CURVE ( 'NONE', #154148, #60110, #153919, .T. ) ;
#176126=AXIS2_PLACEMENT_3D ( 'NONE', #223178, #26284, #245331 ) ;
#176145=LINE ( 'NONE', #77012, #101622 ) ;
#176146=ADVANCED_FACE ( 'NONE', ( #236363 ), #120931, .T. ) ;
#176201=EDGE_CURVE ( 'NONE', #46813, #172429, #85, .T. ) ;
#176277=CARTESIAN_POINT ( 'NONE',  ( 21.30000000000002558, 1.115650265596050101E-11, -129.9500000000000171 ) ) ;
#176285=EDGE_LOOP ( 'NONE', ( #222845, #41548, #120574 ) ) ;
#176287=DIRECTION ( 'NONE',  ( 0.000000000000000000, 0.000000000000000000, -1.000000000000000000 ) ) ;
#176330=EDGE_CURVE ( 'NONE', #98991, #171186, #170849, .T. ) ;
#176370=DIRECTION ( 'NONE',  ( 0.000000000000000000, -1.776356839400271369E-15, 1.000000000000000000 ) ) ;
#176386=FACE_OUTER_BOUND ( 'NONE', #162931, .T. ) ;
#176406=CARTESIAN_POINT ( 'NONE',  ( 20.85000000000000142, 1.115600667400684642E-11, -167.5000000000000284 ) ) ;
#176415=DIRECTION ( 'NONE',  ( 1.000000000000000000, 0.000000000000000000, -0.000000000000000000 ) ) ;
#176418=DIRECTION ( 'NONE',  ( 0.000000000000000000, 0.000000000000000000, -1.000000000000000000 ) ) ;
#176425=VERTEX_POINT ( 'NONE', #102447 ) ;
#176453=EDGE_CURVE ( 'NONE', #214434, #13316, #162428, .T. ) ;
#176469=CARTESIAN_POINT ( 'NONE',  ( -20.64999999999999858, -8.999999999988846255, -143.3939691226524644 ) ) ;
#176494=EDGE_CURVE ( 'NONE', #83651, #177470, #712, .T. ) ;
#176499=CARTESIAN_POINT ( 'NONE',  ( 21.05000000000000071, 6.540656951712403355, -134.1000000000000227 ) ) ;
#176500=VERTEX_POINT ( 'NONE', #224974 ) ;
#176583=CIRCLE ( 'NONE', #134838, 0.2000000000000057288 ) ;
#176592=EDGE_CURVE ( 'NONE', #196380, #991, #242357, .T. ) ;
#176594=VERTEX_POINT ( 'NONE', #77160 ) ;
#176604=ORIENTED_EDGE ( 'NONE', *, *, #120612, .T. ) ;
#176641=CARTESIAN_POINT ( 'NONE',  ( -21.14999999999999858, 11.65000000001115232, -134.0000000000000000 ) ) ;
#176678=VECTOR ( 'NONE', #173106, 1000.000000000000000 ) ;
#176686=CARTESIAN_POINT ( 'NONE',  ( 22.39999999999999503, 1.115600667400684642E-11, -126.2500000000000284 ) ) ;
#176705=DIRECTION ( 'NONE',  ( -1.000000000000000000, 0.000000000000000000, 0.000000000000000000 ) ) ;
#176720=ORIENTED_EDGE ( 'NONE', *, *, #12428, .F. ) ;
#176743=CARTESIAN_POINT ( 'NONE',  ( 21.07928932188134397, 6.328516656404459262, -133.9011048543456184 ) ) ;
#176759=CARTESIAN_POINT ( 'NONE',  ( 18.59999999999999076, 10.49142135624846439, -158.7500000000000284 ) ) ;
#176768=TOROIDAL_SURFACE ( 'NONE', #201693, 0.2000000000000000111, 0.1000000000000000056 ) ;
#176783=EDGE_CURVE ( 'NONE', #240530, #221551, #146124, .T. ) ;
#176786=DIRECTION ( 'NONE',  ( -1.000000000000000000, 0.000000000000000000, 0.000000000000000000 ) ) ;
#176796=DIRECTION ( 'NONE',  ( 0.000000000000000000, -0.000000000000000000, -1.000000000000000000 ) ) ;
#176851=DIRECTION ( 'NONE',  ( 0.000000000000000000, 0.000000000000000000, -1.000000000000000000 ) ) ;
#176878=LINE ( 'NONE', #116880, #182112 ) ;
#176923=CARTESIAN_POINT ( 'NONE',  ( 23.15000000000000213, -8.999999999988842703, -157.6060308773475640 ) ) ;
#176931=CARTESIAN_POINT ( 'NONE',  ( 21.95218792049437795, 7.201507561257818324, -133.9009715602001052 ) ) ;
#176949=CYLINDRICAL_SURFACE ( 'NONE', #98353, 0.09999999999999939493 ) ;
#176955=EDGE_CURVE ( 'NONE', #112934, #251883, #138286, .T. ) ;
#176988=DIRECTION ( 'NONE',  ( 1.000000000000000000, 0.000000000000000000, 0.000000000000000000 ) ) ;
#177007=EDGE_CURVE ( 'NONE', #165391, #153112, #242350, .T. ) ;
#177028=DIRECTION ( 'NONE',  ( 1.000000000000000000, 0.000000000000000000, 0.000000000000000000 ) ) ;
#177068=FACE_OUTER_BOUND ( 'NONE', #246649, .T. ) ;
#177074=ORIENTED_EDGE ( 'NONE', *, *, #75002, .F. ) ;
#177185=EDGE_CURVE ( 'NONE', #225500, #70632, #84261, .T. ) ;
#177192=ORIENTED_EDGE ( 'NONE', *, *, #163640, .T. ) ;
#177269=ORIENTED_EDGE ( 'NONE', *, *, #205051, .F. ) ;
#177283=TOROIDAL_SURFACE ( 'NONE', #148017, 0.2000000000000000111, 0.1000000000000000056 ) ;
#177330=DIRECTION ( 'NONE',  ( 1.000000000000000000, 0.000000000000000000, 0.000000000000000000 ) ) ;
#177382=ADVANCED_FACE ( 'NONE', ( #217325 ), #256405, .F. ) ;
#177388=EDGE_LOOP ( 'NONE', ( #74844, #77272, #173844, #113575 ) ) ;
#177403=CARTESIAN_POINT ( 'NONE',  ( 18.59999999999999076, 6.650000000011155876, -155.2500000000000284 ) ) ;
#177423=LINE ( 'NONE', #251789, #210833 ) ;
#177424=ADVANCED_FACE ( 'NONE', ( #98640 ), #21969, .T. ) ;
#177452=ORIENTED_EDGE ( 'NONE', *, *, #32247, .F. ) ;
#177461=CIRCLE ( 'NONE', #19205, 0.09999999999998898659 ) ;
#177462=CYLINDRICAL_SURFACE ( 'NONE', #190284, 0.09999999999998898659 ) ;
#177465=LINE ( 'NONE', #256915, #67909 ) ;
#177470=VERTEX_POINT ( 'NONE', #226307 ) ;
#177491=CARTESIAN_POINT ( 'NONE',  ( 20.94999999999999929, -11.64999999998883595, -167.5000000000000000 ) ) ;
#177496=DIRECTION ( 'NONE',  ( 0.000000000000000000, -1.000000000000000000, -1.734723475976807292E-15 ) ) ;
#177500=CARTESIAN_POINT ( 'NONE',  ( 18.59999999999998721, 6.846123162363745074, -171.2377262668498759 ) ) ;
#177550=ORIENTED_EDGE ( 'NONE', *, *, #216681, .T. ) ;
#177556=VECTOR ( 'NONE', #103478, 1000.000000000000000 ) ;
#177560=CIRCLE ( 'NONE', #135991, 0.09999999999998898659 ) ;
#177569=CARTESIAN_POINT ( 'NONE',  ( -20.94999999999999929, -1.835341550213255957, -145.5551512925629822 ) ) ;
#177607=EDGE_CURVE ( 'NONE', #50042, #138896, #190456, .T. ) ;
#177617=VERTEX_POINT ( 'NONE', #230180 ) ;
#177634=CARTESIAN_POINT ( 'NONE',  ( -20.85000000000000142, 1.115600667400684642E-11, -167.5000000000000284 ) ) ;
#177644=CIRCLE ( 'NONE', #181889, 0.09999999999999939493 ) ;
#177662=DIRECTION ( 'NONE',  ( 0.000000000000000000, -0.4999999999999478195, -0.8660254037844686836 ) ) ;
#177699=DIRECTION ( 'NONE',  ( 2.915501640297155269E-16, -1.000000000000000000, 0.000000000000000000 ) ) ;
#177721=DIRECTION ( 'NONE',  ( 1.000000000000000000, 2.952720810173289112E-16, -0.000000000000000000 ) ) ;
#177773=AXIS2_PLACEMENT_3D ( 'NONE', #17891, #117006, #76587 ) ;
#177780=CIRCLE ( 'NONE', #173718, 0.8750000000000007772 ) ;
#177781=DIRECTION ( 'NONE',  ( 1.000000000000000000, 0.000000000000000000, 0.000000000000000000 ) ) ;
#177807=VECTOR ( 'NONE', #177496, 1000.000000000000000 ) ;
#177809=AXIS2_PLACEMENT_3D ( 'NONE', #217955, #159314, #219255 ) ;
#177815=DIRECTION ( 'NONE',  ( -0.000000000000000000, 0.000000000000000000, -1.000000000000000000 ) ) ;
#177824=DIRECTION ( 'NONE',  ( 0.000000000000000000, 0.000000000000000000, 1.000000000000000000 ) ) ;
#177833=ORIENTED_EDGE ( 'NONE', *, *, #91399, .T. ) ;
#177841=ORIENTED_EDGE ( 'NONE', *, *, #164502, .T. ) ;
#177879=CARTESIAN_POINT ( 'NONE',  ( 21.05000000000000071, 10.42338541492406279, -141.4920519238701218 ) ) ;
#177888=CARTESIAN_POINT ( 'NONE',  ( -18.59999999999999787, -1.149570369564537842, -175.3159124845019790 ) ) ;
#177904=ADVANCED_FACE ( 'NONE', ( #146469 ), #106051, .F. ) ;
#177919=CARTESIAN_POINT ( 'NONE',  ( -20.94999999999999929, 1.115600667400684642E-11, -167.5000000000000284 ) ) ;
#177921=LINE ( 'NONE', #1815, #177556 ) ;
#177933=ORIENTED_EDGE ( 'NONE', *, *, #225840, .F. ) ;
#177935=CARTESIAN_POINT ( 'NONE',  ( -23.15000000000000213, 4.250000000011156409, -146.3500000000000227 ) ) ;
#177963=AXIS2_PLACEMENT_3D ( 'NONE', #140365, #161239, #119552 ) ;
#177974=CARTESIAN_POINT ( 'NONE',  ( 18.59999999999999787, 1.115600667400684642E-11, -134.0000000000000000 ) ) ;
#178014=CARTESIAN_POINT ( 'NONE',  ( 18.52928932188133970, 10.27928932189250411, -155.3500000000000227 ) ) ;
#178019=VERTEX_POINT ( 'NONE', #73406 ) ;
#178030=EDGE_CURVE ( 'NONE', #44801, #236473, #130773, .T. ) ;
#178043=ORIENTED_EDGE ( 'NONE', *, *, #218752, .T. ) ;
#178046=CARTESIAN_POINT ( 'NONE',  ( 18.52928932188133970, 10.27928932189249878, -158.7085786437627064 ) ) ;
#178049=DIRECTION ( 'NONE',  ( 1.000000000000000000, 0.000000000000000000, -0.000000000000000000 ) ) ;
#178104=EDGE_LOOP ( 'NONE', ( #10375, #219312, #228596, #135442, #246335 ) ) ;
#178139=AXIS2_PLACEMENT_3D ( 'NONE', #93970, #5, #216493 ) ;
#178157=VERTEX_POINT ( 'NONE', #77211 ) ;
#178170=ORIENTED_EDGE ( 'NONE', *, *, #93152, .T. ) ;
#178186=VERTEX_POINT ( 'NONE', #56354 ) ;
#178204=AXIS2_PLACEMENT_3D ( 'NONE', #80681, #242340, #100235 ) ;
#178210=EDGE_LOOP ( 'NONE', ( #117899, #86966, #201099, #174952, #57428, #120745 ) ) ;
#178222=FACE_OUTER_BOUND ( 'NONE', #82868, .T. ) ;
#178234=EDGE_CURVE ( 'NONE', #105532, #46813, #152845, .T. ) ;
#178251=VERTEX_POINT ( 'NONE', #227970 ) ;
#178253=CARTESIAN_POINT ( 'NONE',  ( -18.47079683080349710, -9.471664105233697839, -141.1088605409922536 ) ) ;
#178254=VERTEX_POINT ( 'NONE', #220595 ) ;
#178256=CARTESIAN_POINT ( 'NONE',  ( -21.05000000000000071, 1.162701749949165642, -142.0000000000000284 ) ) ;
#178260=ORIENTED_EDGE ( 'NONE', *, *, #245462, .F. ) ;
#178272=SPHERICAL_SURFACE ( 'NONE', #152898, 0.1000000000000000056 ) ;
#178274=ORIENTED_EDGE ( 'NONE', *, *, #96210, .F. ) ;
#178275=EDGE_CURVE ( 'NONE', #257831, #58706, #111112, .T. ) ;
#178279=AXIS2_PLACEMENT_3D ( 'NONE', #209345, #192360, #51525 ) ;
#178292=ORIENTED_EDGE ( 'NONE', *, *, #14391, .T. ) ;
#178309=LINE ( 'NONE', #98700, #93164 ) ;
#178360=VECTOR ( 'NONE', #115116, 1000.000000000000114 ) ;
#178380=AXIS2_PLACEMENT_3D ( 'NONE', #257890, #121037, #83113 ) ;
#178430=LINE ( 'NONE', #2306, #138790 ) ;
#178458=CIRCLE ( 'NONE', #7752, 0.09999999999999939493 ) ;
#178467=ORIENTED_EDGE ( 'NONE', *, *, #90946, .F. ) ;
#178471=DIRECTION ( 'NONE',  ( 0.000000000000000000, 0.000000000000000000, -1.000000000000000000 ) ) ;
#178505=ORIENTED_EDGE ( 'NONE', *, *, #34341, .F. ) ;
#178523=AXIS2_PLACEMENT_3D ( 'NONE', #11808, #67899, #164446 ) ;
#178525=CIRCLE ( 'NONE', #37056, 0.5000000000000004441 ) ;
#178563=ORIENTED_EDGE ( 'NONE', *, *, #102024, .T. ) ;
#178571=CIRCLE ( 'NONE', #66103, 0.09999999999999939493 ) ;
#178575=EDGE_CURVE ( 'NONE', #229356, #240051, #240471, .T. ) ;
#178585=DIRECTION ( 'NONE',  ( 0.000000000000000000, -0.4999999999999478195, -0.8660254037844686836 ) ) ;
#178604=FACE_OUTER_BOUND ( 'NONE', #236448, .T. ) ;
#178613=EDGE_LOOP ( 'NONE', ( #182439, #81574, #240063, #143865 ) ) ;
#178615=LINE ( 'NONE', #36543, #130239 ) ;
#178616=ORIENTED_EDGE ( 'NONE', *, *, #55401, .F. ) ;
#178662=EDGE_CURVE ( 'NONE', #245418, #99200, #244642, .T. ) ;
#178672=CIRCLE ( 'NONE', #128566, 0.09999999999998898659 ) ;
#178673=AXIS2_PLACEMENT_3D ( 'NONE', #14347, #92556, #249097 ) ;
#178686=DIRECTION ( 'NONE',  ( -1.000000000000000000, 0.000000000000000000, 0.000000000000000000 ) ) ;
#178688=CARTESIAN_POINT ( 'NONE',  ( -22.50000000000000000, 1.115600667400684642E-11, -133.9000000000000057 ) ) ;
#178703=CARTESIAN_POINT ( 'NONE',  ( 19.97071067811864609, 11.72071067812981404, -158.6500000000000057 ) ) ;
#178708=CIRCLE ( 'NONE', #37213, 0.1000000000000089567 ) ;
#178714=ORIENTED_EDGE ( 'NONE', *, *, #188224, .T. ) ;
#178715=ORIENTED_EDGE ( 'NONE', *, *, #107932, .T. ) ;
#178718=CARTESIAN_POINT ( 'NONE',  ( 21.05000000000000071, 11.65000000001116298, -146.1500000000000341 ) ) ;
#178724=CARTESIAN_POINT ( 'NONE',  ( 20.86777300164945004, 10.33200063080771969, -173.0931674956643178 ) ) ;
#178757=CARTESIAN_POINT ( 'NONE',  ( -23.25000000000000000, 1.115600667400684642E-11, -175.4000000000000341 ) ) ;
#178777=EDGE_CURVE ( 'NONE', #179358, #46322, #219795, .T. ) ;
#178794=LINE ( 'NONE', #173678, #143578 ) ;
#178797=EDGE_CURVE ( 'NONE', #220173, #148410, #215529, .T. ) ;
#178801=AXIS2_PLACEMENT_3D ( 'NONE', #212497, #36440, #57232 ) ;
#178807=ORIENTED_EDGE ( 'NONE', *, *, #57903, .T. ) ;
#178814=ORIENTED_EDGE ( 'NONE', *, *, #36906, .T. ) ;
#178834=DIRECTION ( 'NONE',  ( 0.000000000000000000, 0.000000000000000000, -1.000000000000000000 ) ) ;
#178872=( BOUNDED_SURFACE ( )  B_SPLINE_SURFACE ( 3, 2, ( 
 ( #242081, #24350, #204238 ),
 ( #139100, #218661, #63441 ),
 ( #41353, #2177, #42606 ),
 ( #120893, #201675, #200402 ) ),
 .UNSPECIFIED., .F., .F., .F. ) 
 B_SPLINE_SURFACE_WITH_KNOTS ( ( 4, 4 ),
 ( 3, 3 ),
 ( 0.04058434257139475337, 0.04256401539001599538 ),
 ( 0.000000000000000000, 1.000000000000000000 ),
 .UNSPECIFIED. ) 
 GEOMETRIC_REPRESENTATION_ITEM ( )  RATIONAL_B_SPLINE_SURFACE ( (
 ( 1.000000000000000000, 0.7103081912007809251, 1.000000000000000000),
 ( 1.000000000000000000, 0.7104998333556791223, 1.000000000000000000),
 ( 1.000000000000000000, 0.7107238315754067504, 1.000000000000000000),
 ( 1.000000000000000000, 0.7110073749539717047, 1.000000000000000000) ) ) 
 REPRESENTATION_ITEM ( '' )  SURFACE ( )  );
#178889=LINE ( 'NONE', #62756, #195419 ) ;
#178890=EDGE_CURVE ( 'NONE', #165926, #223519, #220913, .T. ) ;
#178906=CIRCLE ( 'NONE', #87259, 0.09999999999998898659 ) ;
#178907=ORIENTED_EDGE ( 'NONE', *, *, #222749, .F. ) ;
#178914=LINE ( 'NONE', #111526, #142257 ) ;
#178929=DIRECTION ( 'NONE',  ( 1.000000000000000000, 0.000000000000000000, 0.000000000000000000 ) ) ;
#178933=EDGE_CURVE ( 'NONE', #140838, #257284, #190609, .T. ) ;
#178985=VECTOR ( 'NONE', #220930, 1000.000000000000000 ) ;
#178999=CARTESIAN_POINT ( 'NONE',  ( -18.49513951962167368, -9.437725026666546668, -174.2780725750291424 ) ) ;
#179022=DIRECTION ( 'NONE',  ( 1.000000000000000000, 0.000000000000000000, 0.000000000000000000 ) ) ;
#179030=EDGE_CURVE ( 'NONE', #8351, #180099, #165668, .T. ) ;
#179064=AXIS2_PLACEMENT_3D ( 'NONE', #162850, #61158, #140690 ) ;
#179083=FACE_OUTER_BOUND ( 'NONE', #225563, .T. ) ;
#179100=AXIS2_PLACEMENT_3D ( 'NONE', #27856, #248151, #69534 ) ;
#179111=CARTESIAN_POINT ( 'NONE',  ( -21.05000000000000071, 1.250000000011155299, -142.0000000000000284 ) ) ;
#179123=DIRECTION ( 'NONE',  ( 0.000000000000000000, 0.000000000000000000, 1.000000000000000000 ) ) ;
#179167=CARTESIAN_POINT ( 'NONE',  ( 20.95512820512820440, 10.62384868372303615, -141.6649135690876165 ) ) ;
#179172=CARTESIAN_POINT ( 'NONE',  ( -21.04999999999999361, 11.75000000001115374, -140.7838656629781724 ) ) ;
#179187=AXIS2_PLACEMENT_3D ( 'NONE', #207859, #12222, #248242 ) ;
#179193=AXIS2_PLACEMENT_3D ( 'NONE', #115139, #176415, #195974 ) ;
#179208=VERTEX_POINT ( 'NONE', #34321 ) ;
#179233=DIRECTION ( 'NONE',  ( -1.000000000000000000, -0.000000000000000000, -0.000000000000000000 ) ) ;
#179235=EDGE_CURVE ( 'NONE', #42010, #98991, #244934, .T. ) ;
#179254=ORIENTED_EDGE ( 'NONE', *, *, #231466, .T. ) ;
#179275=CIRCLE ( 'NONE', #196013, 0.5999999999999894307 ) ;
#179280=ORIENTED_EDGE ( 'NONE', *, *, #125274, .F. ) ;
#179292=AXIS2_PLACEMENT_3D ( 'NONE', #215636, #94410, #136084 ) ;
#179357=CIRCLE ( 'NONE', #16865, 0.09999999999998898659 ) ;
#179358=VERTEX_POINT ( 'NONE', #118978 ) ;
#179380=ORIENTED_EDGE ( 'NONE', *, *, #95209, .F. ) ;
#179389=CARTESIAN_POINT ( 'NONE',  ( 21.14999999999999858, 1.115600667400684642E-11, -122.3504291924552234 ) ) ;
#179411=DIRECTION ( 'NONE',  ( 0.000000000000000000, 0.000000000000000000, 1.000000000000000000 ) ) ;
#179438=CARTESIAN_POINT ( 'NONE',  ( -20.54999999999999716, -8.730841121484173684, -143.5980747189843783 ) ) ;
#179458=EDGE_CURVE ( 'NONE', #24563, #104087, #232489, .T. ) ;
#179470=ORIENTED_EDGE ( 'NONE', *, *, #145265, .T. ) ;
#179475=ORIENTED_EDGE ( 'NONE', *, *, #178933, .T. ) ;
#179481=DIRECTION ( 'NONE',  ( -1.000000000000000000, -3.265361837132813093E-16, 0.000000000000000000 ) ) ;
#179497=CARTESIAN_POINT ( 'NONE',  ( -21.11833042828115481, 0.007100509070730082022, -127.5543553061452542 ) ) ;
#179517=CARTESIAN_POINT ( 'NONE',  ( 20.95512820512820440, 8.876151316299271343, -142.5586289951409640 ) ) ;
#179530=SPHERICAL_SURFACE ( 'NONE', #4847, 0.1000000000000000056 ) ;
#179540=EDGE_CURVE ( 'NONE', #208712, #35508, #57441, .T. ) ;
#179547=DIRECTION ( 'NONE',  ( 1.000000000000000000, -0.000000000000000000, -0.000000000000000000 ) ) ;
#179593=ORIENTED_EDGE ( 'NONE', *, *, #23832, .F. ) ;
#179609=FACE_OUTER_BOUND ( 'NONE', #217738, .T. ) ;
#179624=ORIENTED_EDGE ( 'NONE', *, *, #131929, .T. ) ;
#179658=FACE_OUTER_BOUND ( 'NONE', #110508, .T. ) ;
#179685=CARTESIAN_POINT ( 'NONE',  ( -18.59999999999999787, -1.249999999988843369, -175.3004807544151049 ) ) ;
#179688=DIRECTION ( 'NONE',  ( 0.000000000000000000, 0.8700118002898322711, -0.4930308989875231696 ) ) ;
#179692=CARTESIAN_POINT ( 'NONE',  ( -20.64999999999999858, 2.000000000011154189, -147.2246219227621111 ) ) ;
#179695=DIRECTION ( 'NONE',  ( 0.000000000000000000, -1.000000000000000000, 0.000000000000000000 ) ) ;
#179725=DIRECTION ( 'NONE',  ( 0.000000000000000000, 0.000000000000000000, -1.000000000000000000 ) ) ;
#179730=EDGE_CURVE ( 'NONE', #23218, #39881, #182776, .T. ) ;
#179757=VECTOR ( 'NONE', #222382, 1000.000000000000000 ) ;
#179760=ORIENTED_EDGE ( 'NONE', *, *, #216766, .F. ) ;
#179777=CARTESIAN_POINT ( 'NONE',  ( -23.15000000000000213, -11.48912529306489816, -164.4000000000000057 ) ) ;
#179879=DIRECTION ( 'NONE',  ( 0.000000000000000000, 0.000000000000000000, -1.000000000000000000 ) ) ;
#179929=EDGE_CURVE ( 'NONE', #201029, #120342, #178708, .T. ) ;
#179954=ORIENTED_EDGE ( 'NONE', *, *, #154474, .T. ) ;
#179967=CARTESIAN_POINT ( 'NONE',  ( 22.50000000000000000, 1.115600667400684642E-11, -134.0000000000000000 ) ) ;
#179979=AXIS2_PLACEMENT_3D ( 'NONE', #123387, #244601, #19481 ) ;
#179999=EDGE_LOOP ( 'NONE', ( #13223, #63747, #19181, #243693 ) ) ;
#180058=VERTEX_POINT ( 'NONE', #219533 ) ;
#180075=ORIENTED_EDGE ( 'NONE', *, *, #189999, .F. ) ;
#180080=ORIENTED_EDGE ( 'NONE', *, *, #227660, .F. ) ;
#180088=CARTESIAN_POINT ( 'NONE',  ( 23.14999999999999503, 11.65000000001116298, -160.4851942293460922 ) ) ;
#180092=AXIS2_PLACEMENT_3D ( 'NONE', #132120, #228669, #211669 ) ;
#180093=EDGE_LOOP ( 'NONE', ( #1019, #231340, #150133, #168930 ) ) ;
#180099=VERTEX_POINT ( 'NONE', #43487 ) ;
#180105=ORIENTED_EDGE ( 'NONE', *, *, #244028, .T. ) ;
#180119=DIRECTION ( 'NONE',  ( 0.000000000000000000, 0.000000000000000000, -1.000000000000000000 ) ) ;
#180184=EDGE_CURVE ( 'NONE', #82520, #175518, #244228, .T. ) ;
#180189=DIRECTION ( 'NONE',  ( 0.000000000000000000, 0.000000000000000000, -1.000000000000000000 ) ) ;
#180195=CARTESIAN_POINT ( 'NONE',  ( -18.59999999999999787, 11.65000000001115232, -122.2500000000000284 ) ) ;
#180198=VERTEX_POINT ( 'NONE', #104694 ) ;
#180205=CIRCLE ( 'NONE', #159361, 7.800000000000001599 ) ;
#180215=CARTESIAN_POINT ( 'NONE',  ( -18.59999999999999787, -9.321008403350132809, -141.2359382490778899 ) ) ;
#180228=DIRECTION ( 'NONE',  ( 0.000000000000000000, -1.000000000000000000, 0.000000000000000000 ) ) ;
#180230=VERTEX_POINT ( 'NONE', #44770 ) ;
#180260=ORIENTED_EDGE ( 'NONE', *, *, #252316, .F. ) ;
#180262=CARTESIAN_POINT ( 'NONE',  ( -23.25000000000000000, -11.74999999998884448, -167.5000000000000000 ) ) ;
#180263=DIRECTION ( 'NONE',  ( 0.000000000000000000, 1.000000000000000000, 0.000000000000000000 ) ) ;
#180288=EDGE_CURVE ( 'NONE', #155942, #196105, #87724, .T. ) ;
#180398=ADVANCED_FACE ( 'NONE', ( #115013 ), #95627, .F. ) ;
#180437=DIRECTION ( 'NONE',  ( 1.000000000000000000, -0.000000000000000000, 0.000000000000000000 ) ) ;
#180450=DIRECTION ( 'NONE',  ( 0.000000000000000000, -0.4930308989874653269, -0.8700118002898649117 ) ) ;
#180462=DIRECTION ( 'NONE',  ( 0.000000000000000000, -0.1350103645451876666, 0.9908441862701600211 ) ) ;
#180473=ORIENTED_EDGE ( 'NONE', *, *, #10164, .T. ) ;
#180492=CIRCLE ( 'NONE', #34765, 0.09999999999999062417 ) ;
#180495=DIRECTION ( 'NONE',  ( 0.000000000000000000, 1.000000000000000000, 0.000000000000000000 ) ) ;
#180503=DIRECTION ( 'NONE',  ( -1.000000000000000000, 0.000000000000000000, 0.000000000000000000 ) ) ;
#180505=CARTESIAN_POINT ( 'NONE',  ( 20.94999999999999574, 1.736257131608553550, -145.5686523290175387 ) ) ;
#180511=TOROIDAL_SURFACE ( 'NONE', #221983, 2.100000000000002309, 0.1000000000000000056 ) ;
#180517=VECTOR ( 'NONE', #104502, 1000.000000000000227 ) ;
#180546=EDGE_LOOP ( 'NONE', ( #116011, #16876, #10725, #730 ) ) ;
#180555=CARTESIAN_POINT ( 'NONE',  ( -21.05000000000000071, 11.60000000001115517, -160.5717967697245285 ) ) ;
#180565=LINE ( 'NONE', #184401, #92931 ) ;
#180572=CARTESIAN_POINT ( 'NONE',  ( -23.15000000000000213, 2.600000000011154278, -154.2753780772379173 ) ) ;
#180578=CIRCLE ( 'NONE', #9878, 0.5000000000000004441 ) ;
#180584=EDGE_CURVE ( 'NONE', #72588, #42134, #225640, .T. ) ;
#180604=DIRECTION ( 'NONE',  ( 0.000000000000000000, 0.9998779222360102414, 0.01562499999996356907 ) ) ;
#180619=CARTESIAN_POINT ( 'NONE',  ( -21.05000000000000071, 1.851028230152016674, -145.6539132694225032 ) ) ;
#180632=CARTESIAN_POINT ( 'NONE',  ( -18.50000000000000000, -1.687074390080403941, -121.1854270334583674 ) ) ;
#180635=CARTESIAN_POINT ( 'NONE',  ( -18.59999999999999787, 9.250000000011157297, -146.2500000000000284 ) ) ;
#180648=ORIENTED_EDGE ( 'NONE', *, *, #244919, .T. ) ;
#180650=DIRECTION ( 'NONE',  ( 0.000000000000000000, 0.000000000000000000, -1.000000000000000000 ) ) ;
#180657=AXIS2_PLACEMENT_3D ( 'NONE', #186213, #167958, #246184 ) ;
#180690=CARTESIAN_POINT ( 'NONE',  ( -23.15000000000000213, 1.115600667400684642E-11, -167.5000000000000284 ) ) ;
#180728=ORIENTED_EDGE ( 'NONE', *, *, #105065, .T. ) ;
#180739=COLOUR_RGB ( '', 0.09019608, 0.27058824, 0.51372549) ;
#180754=VERTEX_POINT ( 'NONE', #96413 ) ;
#180769=CARTESIAN_POINT ( 'NONE',  ( -21.05000000000000071, -0.09999996528894476711, -127.5224478175062472 ) ) ;
#180774=DIRECTION ( 'NONE',  ( 1.000000000000000000, 7.304098846218134667E-16, -0.000000000000000000 ) ) ;
#180775=ORIENTED_EDGE ( 'NONE', *, *, #80788, .T. ) ;
#180795=DIRECTION ( 'NONE',  ( -1.000000000000000000, 0.000000000000000000, 0.000000000000000000 ) ) ;
#180800=VERTEX_POINT ( 'NONE', #255455 ) ;
#180816=DIRECTION ( 'NONE',  ( 0.000000000000000000, 1.000000000000000000, 2.891205793294679805E-16 ) ) ;
#180833=CARTESIAN_POINT ( 'NONE',  ( -18.59999999999999787, 11.75000000001115552, -155.2500000000000284 ) ) ;
#180844=AXIS2_PLACEMENT_3D ( 'NONE', #125164, #6476, #26065 ) ;
#180850=LINE ( 'NONE', #202967, #54079 ) ;
#180897=DIRECTION ( 'NONE',  ( 0.000000000000000000, 1.483188571960168804E-13, -1.000000000000000000 ) ) ;
#180898=EDGE_CURVE ( 'NONE', #35141, #7738, #45755, .T. ) ;
#180922=CARTESIAN_POINT ( 'NONE',  ( 21.11701782572533048, 10.72160911601861244, -146.2450374295112283 ) ) ;
#181006=DIRECTION ( 'NONE',  ( 0.000000000000000000, 0.1350103645451876666, -0.9908441862701600211 ) ) ;
#181015=ORIENTED_EDGE ( 'NONE', *, *, #123579, .F. ) ;
#181041=EDGE_CURVE ( 'NONE', #4950, #76541, #79232, .T. ) ;
#181051=CIRCLE ( 'NONE', #6229, 0.09999999999998902822 ) ;
#181052=VECTOR ( 'NONE', #134366, 1000.000000000000000 ) ;
#181078=FACE_OUTER_BOUND ( 'NONE', #233364, .T. ) ;
#181095=CARTESIAN_POINT ( 'NONE',  ( -23.25000000000000000, -9.599999999988845900, -157.6060308773475924 ) ) ;
#181104=ORIENTED_EDGE ( 'NONE', *, *, #70228, .T. ) ;
#181126=AXIS2_PLACEMENT_3D ( 'NONE', #115207, #153097, #193480 ) ;
#181186=DIRECTION ( 'NONE',  ( -1.000000000000000000, -2.952720810173289112E-16, 0.000000000000000000 ) ) ;
#181255=CARTESIAN_POINT ( 'NONE',  ( 19.88284271247461987, 11.69142135624847256, -158.7500000000000000 ) ) ;
#181293=DIRECTION ( 'NONE',  ( 0.000000000000000000, 0.000000000000000000, -1.000000000000000000 ) ) ;
#181353=DIRECTION ( 'NONE',  ( 0.000000000000000000, 0.000000000000000000, 1.000000000000000000 ) ) ;
#181369=FACE_OUTER_BOUND ( 'NONE', #212722, .T. ) ;
#181385=CIRCLE ( 'NONE', #93874, 0.09999999999999749367 ) ;
#181392=CARTESIAN_POINT ( 'NONE',  ( 18.59999999999999432, -1.299733671219632791, -124.0281295228694347 ) ) ;
#181405=DIRECTION ( 'NONE',  ( 1.000000000000000000, 0.000000000000000000, -0.000000000000000000 ) ) ;
#181425=CARTESIAN_POINT ( 'NONE',  ( 20.94999999999999574, 1.835341550235567887, -145.6551512925629766 ) ) ;
#181450=DIRECTION ( 'NONE',  ( 0.000000000000000000, 0.000000000000000000, -1.000000000000000000 ) ) ;
#181489=CIRCLE ( 'NONE', #89878, 0.09999999999998898659 ) ;
#181493=CARTESIAN_POINT ( 'NONE',  ( -22.47120815636973745, 0.02890382191504723905, -122.3500680112465204 ) ) ;
#181505=CARTESIAN_POINT ( 'NONE',  ( 18.42636655943168833, -9.496944315759476396, -174.1090805711555447 ) ) ;
#181540=ORIENTED_EDGE ( 'NONE', *, *, #9246, .F. ) ;
#181542=AXIS2_PLACEMENT_3D ( 'NONE', #7744, #87250, #71582 ) ;
#181565=DIRECTION ( 'NONE',  ( -1.000000000000000000, -0.000000000000000000, -0.000000000000000000 ) ) ;
#181629=CARTESIAN_POINT ( 'NONE',  ( -18.59999999999999787, 1.835341550235567887, -145.5551512925629822 ) ) ;
#181650=DIRECTION ( 'NONE',  ( -0.000000000000000000, -0.7397360091702755991, -0.6728971962616832059 ) ) ;
#181660=DIRECTION ( 'NONE',  ( 1.000000000000000000, 0.000000000000000000, 0.000000000000000000 ) ) ;
#181708=DIRECTION ( 'NONE',  ( 0.000000000000000000, 0.000000000000000000, 1.000000000000000000 ) ) ;
#181714=CARTESIAN_POINT ( 'NONE',  ( -21.00448002041607864, 11.75000000001115552, -140.8483408623105220 ) ) ;
#181771=ORIENTED_EDGE ( 'NONE', *, *, #88223, .F. ) ;
#181835=LINE ( 'NONE', #154921, #49505 ) ;
#181839=ADVANCED_FACE ( 'NONE', ( #40392 ), #158942, .F. ) ;
#181857=DIRECTION ( 'NONE',  ( -0.000000000000000000, -0.000000000000000000, -1.000000000000000000 ) ) ;
#181866=CARTESIAN_POINT ( 'NONE',  ( 21.14999999999999503, -11.74999999998883560, -122.2500000000000284 ) ) ;
#181875=ORIENTED_EDGE ( 'NONE', *, *, #238209, .T. ) ;
#181884=( BOUNDED_SURFACE ( )  B_SPLINE_SURFACE ( 3, 2, ( 
 ( #224450, #242726, #126644 ),
 ( #45821, #141078, #185336 ),
 ( #64107, #143631, #2825 ),
 ( #122812, #220614, #160666 ),
 ( #27585, #202325, #62816 ),
 ( #125367, #165794, #244009 ) ),
 .UNSPECIFIED., .F., .F., .T. ) 
 B_SPLINE_SURFACE_WITH_KNOTS ( ( 4, 2, 4 ),
 ( 3, 3 ),
 ( 6.719893378901104289E-05, 0.0002757154632485492199, 0.0004842319927080873969 ),
 ( 0.000000000000000000, 1.000000000000000000 ),
 .UNSPECIFIED. ) 
 GEOMETRIC_REPRESENTATION_ITEM ( )  RATIONAL_B_SPLINE_SURFACE ( (
 ( 1.000000000000000000, 0.7250110520819756932, 1.000000000000000000),
 ( 1.000000000000000000, 0.7277932058358369538, 1.000000000000000000),
 ( 1.000000000000000000, 0.7278452872618610403, 1.000000000000000000),
 ( 1.000000000000000000, 0.7221445671548210044, 1.000000000000000000),
 ( 1.000000000000000000, 0.7163662143780332725, 1.000000000000000000),
 ( 1.000000000000000000, 0.7071067811865475727, 1.000000000000000000) ) ) 
 REPRESENTATION_ITEM ( '' )  SURFACE ( )  );
#181889=AXIS2_PLACEMENT_3D ( 'NONE', #257520, #159780, #219731 ) ;
#181890=DIRECTION ( 'NONE',  ( 1.000000000000000000, 0.000000000000000000, -0.000000000000000000 ) ) ;
#181897=LINE ( 'NONE', #26696, #240262 ) ;
#181965=ORIENTED_EDGE ( 'NONE', *, *, #131208, .T. ) ;
#182048=VERTEX_POINT ( 'NONE', #41658 ) ;
#182076=CARTESIAN_POINT ( 'NONE',  ( 18.49999999999999645, -1.835341550213255957, -145.5551512925629822 ) ) ;
#182100=CARTESIAN_POINT ( 'NONE',  ( -18.31572283045127847, -9.548437830874760834, -174.3506256510583796 ) ) ;
#182103=ORIENTED_EDGE ( 'NONE', *, *, #133528, .T. ) ;
#182110=CARTESIAN_POINT ( 'NONE',  ( -23.15000000000000213, -8.999999999988846255, -143.8939691226524644 ) ) ;
#182112=VECTOR ( 'NONE', #38630, 1000.000000000000000 ) ;
#182122=EDGE_CURVE ( 'NONE', #96658, #115258, #58923, .T. ) ;
#182153=FACE_OUTER_BOUND ( 'NONE', #128253, .T. ) ;
#182164=CARTESIAN_POINT ( 'NONE',  ( -23.25000000000000000, -1.164121893230052995, -175.4148480855716059 ) ) ;
#182169=EDGE_CURVE ( 'NONE', #132345, #41773, #9075, .T. ) ;
#182186=CARTESIAN_POINT ( 'NONE',  ( 23.15000000000000213, -11.39257802169451139, -164.4260504201680817 ) ) ;
#182223=ORIENTED_EDGE ( 'NONE', *, *, #41412, .F. ) ;
#182234=VECTOR ( 'NONE', #244214, 1000.000000000000000 ) ;
#182286=AXIS2_PLACEMENT_3D ( 'NONE', #32638, #172150, #116000 ) ;
#182287=CARTESIAN_POINT ( 'NONE',  ( -21.05000000000000071, 1.750000000011155743, -145.6695115579016715 ) ) ;
#182307=ORIENTED_EDGE ( 'NONE', *, *, #205814, .T. ) ;
#182328=EDGE_CURVE ( 'NONE', #173723, #114955, #214818, .T. ) ;
#182354=DIRECTION ( 'NONE',  ( 1.000000000000000000, 0.000000000000000000, 0.000000000000000000 ) ) ;
#182357=AXIS2_PLACEMENT_3D ( 'NONE', #124693, #243338, #145519 ) ;
#182373=CARTESIAN_POINT ( 'NONE',  ( -21.05000000000000071, 1.115600667400684642E-11, -134.0000000000000000 ) ) ;
#182394=ORIENTED_EDGE ( 'NONE', *, *, #177185, .T. ) ;
#182427=CARTESIAN_POINT ( 'NONE',  ( -22.59999985501179154, 11.74986979301414003, -133.9344013302004726 ) ) ;
#182438=CARTESIAN_POINT ( 'NONE',  ( 21.00000000000000000, 9.750000000011153745, -155.2500000000000284 ) ) ;
#182439=ORIENTED_EDGE ( 'NONE', *, *, #171239, .T. ) ;
#182462=ADVANCED_FACE ( 'NONE', ( #140411 ), #178872, .F. ) ;
#182497=VECTOR ( 'NONE', #182688, 1000.000000000000000 ) ;
#182540=ORIENTED_EDGE ( 'NONE', *, *, #161059, .F. ) ;
#182556=ORIENTED_EDGE ( 'NONE', *, *, #129460, .F. ) ;
#182564=AXIS2_PLACEMENT_3D ( 'NONE', #75971, #135921, #34304 ) ;
#182602=ORIENTED_EDGE ( 'NONE', *, *, #124374, .T. ) ;
#182607=CARTESIAN_POINT ( 'NONE',  ( 23.24999999999999289, 5.950000000011163692, -157.1942976949652007 ) ) ;
#182627=DIRECTION ( 'NONE',  ( -1.000000000000000000, 0.000000000000000000, 0.000000000000000000 ) ) ;
#182635=( BOUNDED_SURFACE ( )  B_SPLINE_SURFACE ( 3, 2, ( 
 ( #245362, #240234, #66718 ),
 ( #161989, #84954, #146234 ),
 ( #144946, #225764, #224495 ),
 ( #160716, #163261, #103245 ),
 ( #61581, #201085, #42034 ),
 ( #164543, #141128, #241502 ) ),
 .UNSPECIFIED., .F., .F., .F. ) 
 B_SPLINE_SURFACE_WITH_KNOTS ( ( 4, 2, 4 ),
 ( 3, 3 ),
 ( -1.776356839400250465E-15, 0.7853981633974468357, 1.570796326794895448 ),
 ( 0.000000000000000000, 1.000000000000000000 ),
 .UNSPECIFIED. ) 
 GEOMETRIC_REPRESENTATION_ITEM ( )  RATIONAL_B_SPLINE_SURFACE ( (
 ( 1.000000000000000000, 0.5000000000000260902, 1.000000000000000000),
 ( 1.000000000000000000, 0.4993418825329626332, 1.000000000000000000),
 ( 1.000000000000000000, 0.5278258667064184007, 1.000000000000000000),
 ( 1.000000000000000000, 0.6092287576689454642, 1.000000000000000000),
 ( 1.000000000000000000, 0.6611148371783867050, 1.000000000000000000),
 ( 1.000000000000000000, 0.7071067811865597852, 1.000000000000000000) ) ) 
 REPRESENTATION_ITEM ( '' )  SURFACE ( )  );
#182640=AXIS2_PLACEMENT_3D ( 'NONE', #167587, #111440, #189696 ) ;
#182649=EDGE_LOOP ( 'NONE', ( #193186, #155573, #85548, #67484, #199966, #122952, #124867, #182855, #125471, #97196, #92061, #100490, #66983, #36147 ) ) ;
#182688=DIRECTION ( 'NONE',  ( -1.000000000000000000, -0.000000000000000000, -0.000000000000000000 ) ) ;
#182693=DIRECTION ( 'NONE',  ( 1.000000000000000000, -0.000000000000000000, -0.000000000000000000 ) ) ;
#182695=ORIENTED_EDGE ( 'NONE', *, *, #17564, .F. ) ;
#182706=ORIENTED_EDGE ( 'NONE', *, *, #179540, .T. ) ;
#182726=ORIENTED_EDGE ( 'NONE', *, *, #121609, .T. ) ;
#182740=( BOUNDED_CURVE ( )  B_SPLINE_CURVE ( 3, ( #151381, #253017, #230918, #190512 ),
 .UNSPECIFIED., .F., .F. ) 
 B_SPLINE_CURVE_WITH_KNOTS ( ( 4, 4 ),
 ( 1.570796326794895448, 3.141592653589791784 ),
 .UNSPECIFIED. ) 
 CURVE ( )  GEOMETRIC_REPRESENTATION_ITEM ( )  RATIONAL_B_SPLINE_CURVE ( ( 1.000000000000000000, 0.8047378541243650485, 0.8047378541243650485, 1.000000000000000000 ) ) 
 REPRESENTATION_ITEM ( '' )  );
#182750=ORIENTED_EDGE ( 'NONE', *, *, #255314, .T. ) ;
#182776=CIRCLE ( 'NONE', #186874, 12.77500000000000924 ) ;
#182790=CARTESIAN_POINT ( 'NONE',  ( -21.14999999999999858, -11.74999999998884448, -136.9000000000000341 ) ) ;
#182809=DIRECTION ( 'NONE',  ( -1.000000000000000000, -0.000000000000000000, -0.000000000000000000 ) ) ;
#182810=EDGE_CURVE ( 'NONE', #87157, #257284, #98372, .T. ) ;
#182834=ADVANCED_FACE ( 'NONE', ( #102233 ), #142661, .T. ) ;
#182836=DIRECTION ( 'NONE',  ( -1.000000000000000000, -0.000000000000000000, 0.000000000000000000 ) ) ;
#182855=ORIENTED_EDGE ( 'NONE', *, *, #10574, .T. ) ;
#182873=CARTESIAN_POINT ( 'NONE',  ( 21.05000000000000426, 6.413826288824131971, -134.0857409370334778 ) ) ;
#182886=DIRECTION ( 'NONE',  ( 0.000000000000000000, 0.000000000000000000, -1.000000000000000000 ) ) ;
#182887=CARTESIAN_POINT ( 'NONE',  ( 21.12400247839510925, 10.72148804404153921, -146.2500000000000568 ) ) ;
#182888=EDGE_LOOP ( 'NONE', ( #200166, #235101, #132609, #2483 ) ) ;
#182893=DIRECTION ( 'NONE',  ( 0.000000000000000000, -0.7397360091702744889, 0.6728971962616842051 ) ) ;
#182930=CIRCLE ( 'NONE', #224596, 0.09999999999999939493 ) ;
#182932=CARTESIAN_POINT ( 'NONE',  ( -20.64999999999999858, 7.150000000011155876, -146.3500000000000227 ) ) ;
#182939=DIRECTION ( 'NONE',  ( -0.000000000000000000, 1.000000000000000000, 2.891205793294679805E-16 ) ) ;
#182975=ORIENTED_EDGE ( 'NONE', *, *, #41412, .T. ) ;
#182979=DIRECTION ( 'NONE',  ( 1.000000000000000000, 0.000000000000000000, 0.000000000000000000 ) ) ;
#182999=ADVANCED_FACE ( 'NONE', ( #253010 ), #117208, .T. ) ;
#183045=CIRCLE ( 'NONE', #12194, 0.09999999999998898659 ) ;
#183061=DIRECTION ( 'NONE',  ( -0.000000000000000000, 0.8660254037844411501, 0.4999999999999956701 ) ) ;
#183078=CARTESIAN_POINT ( 'NONE',  ( -22.39999999999999503, 1.114087072463500573E-11, -122.2495671075414094 ) ) ;
#183105=CARTESIAN_POINT ( 'NONE',  ( 21.05000000000000071, -11.29603075032412640, -164.4521008403361577 ) ) ;
#183110=AXIS2_PLACEMENT_3D ( 'NONE', #74048, #12784, #171873 ) ;
#183116=CIRCLE ( 'NONE', #149807, 0.09999999999999939493 ) ;
#183144=ORIENTED_EDGE ( 'NONE', *, *, #214919, .T. ) ;
#183147=DIRECTION ( 'NONE',  ( 1.000000000000000000, 0.000000000000000000, 0.000000000000000000 ) ) ;
#183177=CARTESIAN_POINT ( 'NONE',  ( -18.50000000000000000, 11.65000000001115232, -122.2500000000000284 ) ) ;
#183187=DIRECTION ( 'NONE',  ( 0.000000000000000000, -1.000000000000000000, 0.000000000000000000 ) ) ;
#183195=DIRECTION ( 'NONE',  ( 0.000000000000000000, 0.000000000000000000, -1.000000000000000000 ) ) ;
#183256=FACE_OUTER_BOUND ( 'NONE', #172257, .T. ) ;
#183284=ADVANCED_FACE ( 'NONE', ( #208473 ), #79588, .F. ) ;
#183303=DIRECTION ( 'NONE',  ( 0.000000000000000000, -0.1298341882520079038, -0.9915357197604846018 ) ) ;
#183309=ORIENTED_EDGE ( 'NONE', *, *, #96776, .T. ) ;
#183329=TOROIDAL_SURFACE ( 'NONE', #33336, 0.9750000000000019762, 0.1000000000000000056 ) ;
#183388=ADVANCED_FACE ( 'NONE', ( #122039 ), #138029, .T. ) ;
#183399=ADVANCED_FACE ( 'NONE', ( #67198 ), #24241, .T. ) ;
#183415=EDGE_CURVE ( 'NONE', #76541, #28264, #144143, .T. ) ;
#183448=DIRECTION ( 'NONE',  ( 0.000000000000000000, 0.000000000000000000, -1.000000000000000000 ) ) ;
#183468=CARTESIAN_POINT ( 'NONE',  ( 23.14999999999999503, 11.65000000001116298, -146.1500000000000341 ) ) ;
#183472=ORIENTED_EDGE ( 'NONE', *, *, #213954, .F. ) ;
#183473=DIRECTION ( 'NONE',  ( -1.000000000000000000, 0.000000000000000000, 0.000000000000000000 ) ) ;
#183497=DIRECTION ( 'NONE',  ( 0.000000000000000000, 0.000000000000000000, 1.000000000000000000 ) ) ;
#183521=CARTESIAN_POINT ( 'NONE',  ( 22.42196299218230493, 0.002441673998456600492, -122.3503882973505483 ) ) ;
#183528=ORIENTED_EDGE ( 'NONE', *, *, #5749, .T. ) ;
#183533=DIRECTION ( 'NONE',  ( 0.000000000000000000, 1.000000000000000000, 0.000000000000000000 ) ) ;
#183549=DIRECTION ( 'NONE',  ( 0.000000000000000000, 0.000000000000000000, -1.000000000000000000 ) ) ;
#183567=ADVANCED_FACE ( 'NONE', ( #212772 ), #15875, .F. ) ;
#183576=CARTESIAN_POINT ( 'NONE',  ( -23.15000000000000213, 11.65000000001115588, -155.2500000000000284 ) ) ;
#183578=DIRECTION ( 'NONE',  ( 1.000000000000000000, 0.000000000000000000, 0.000000000000000000 ) ) ;
#183660=ORIENTED_EDGE ( 'NONE', *, *, #17173, .T. ) ;
#183668=CARTESIAN_POINT ( 'NONE',  ( -21.14999999999999858, -0.09999999998884338825, -122.3504291924552092 ) ) ;
#183669=DIRECTION ( 'NONE',  ( 0.000000000000000000, -0.1350103645451904977, 0.9908441862701596881 ) ) ;
#183681=DIRECTION ( 'NONE',  ( -0.000000000000000000, -0.000000000000000000, 1.000000000000000000 ) ) ;
#183723=CARTESIAN_POINT ( 'NONE',  ( -22.50000000000000000, 1.115600667400684642E-11, -134.0000000000000000 ) ) ;
#183740=LINE ( 'NONE', #5062, #53821 ) ;
#183757=DIRECTION ( 'NONE',  ( 1.000000000000000000, -0.000000000000000000, -0.000000000000000000 ) ) ;
#183766=CARTESIAN_POINT ( 'NONE',  ( 20.94999999999999929, 5.400000000011154988, -157.6060308773475640 ) ) ;
#183787=CARTESIAN_POINT ( 'NONE',  ( -20.54999999999999716, 1.115600667400684642E-11, -167.5000000000000284 ) ) ;
#183884=ORIENTED_EDGE ( 'NONE', *, *, #64704, .T. ) ;
#183896=AXIS2_PLACEMENT_3D ( 'NONE', #191719, #254206, #33948 ) ;
#183899=ADVANCED_FACE ( 'NONE', ( #209900 ), #11702, .T. ) ;
#183954=EDGE_CURVE ( 'NONE', #43709, #113685, #75875, .T. ) ;
#183963=EDGE_LOOP ( 'NONE', ( #85903, #35033, #186705, #184734 ) ) ;
#183978=DIRECTION ( 'NONE',  ( -1.000000000000000000, 0.000000000000000000, 0.000000000000000000 ) ) ;
#183998=DIRECTION ( 'NONE',  ( 0.000000000000000000, 0.000000000000000000, -1.000000000000000000 ) ) ;
#184016=VERTEX_POINT ( 'NONE', #36409 ) ;
#184018=FACE_OUTER_BOUND ( 'NONE', #31441, .T. ) ;
#184035=CYLINDRICAL_SURFACE ( 'NONE', #70128, 0.09999999999999939493 ) ;
#184072=CARTESIAN_POINT ( 'NONE',  ( -20.00857864376270001, 9.250000000011157297, -155.1500000000000057 ) ) ;
#184092=ORIENTED_EDGE ( 'NONE', *, *, #246555, .T. ) ;
#184101=DIRECTION ( 'NONE',  ( 0.000000000000000000, -0.000000000000000000, 1.000000000000000000 ) ) ;
#184117=CARTESIAN_POINT ( 'NONE',  ( -21.56666275994539816, 1.115600667400684642E-11, -127.0426315931066910 ) ) ;
#184123=EDGE_CURVE ( 'NONE', #149328, #100941, #234081, .T. ) ;
#184124=CIRCLE ( 'NONE', #71730, 11.80000000000000426 ) ;
#184152=ORIENTED_EDGE ( 'NONE', *, *, #179929, .F. ) ;
#184153=ORIENTED_EDGE ( 'NONE', *, *, #244399, .T. ) ;
#184175=AXIS2_PLACEMENT_3D ( 'NONE', #251443, #35009, #37548 ) ;
#184193=DIRECTION ( 'NONE',  ( 0.7071067811865474617, 0.7071067811865474617, -0.000000000000000000 ) ) ;
#184201=CARTESIAN_POINT ( 'NONE',  ( -23.15000000000000213, 4.350000000011156054, -146.3500000000000227 ) ) ;
#184215=CARTESIAN_POINT ( 'NONE',  ( -21.05000000000000426, -0.02103547652895631712, -127.6955441780524012 ) ) ;
#184220=CARTESIAN_POINT ( 'NONE',  ( -20.00857864376270001, 9.150000000011157653, -146.3500000000000227 ) ) ;
#184221=ADVANCED_FACE ( 'NONE', ( #187140 ), #168883, .T. ) ;
#184238=EDGE_CURVE ( 'NONE', #221150, #173825, #100944, .T. ) ;
#184260=DIRECTION ( 'NONE',  ( 0.000000000000000000, -1.734723475976757554E-14, -1.000000000000000000 ) ) ;
#184279=DIRECTION ( 'NONE',  ( 0.000000000000000000, -3.339342691255721203E-13, 1.000000000000000000 ) ) ;
#184280=CARTESIAN_POINT ( 'NONE',  ( -20.07928932188135107, 9.220710678129810489, -146.3500000000000227 ) ) ;
#184309=FACE_OUTER_BOUND ( 'NONE', #45334, .T. ) ;
#184315=CARTESIAN_POINT ( 'NONE',  ( -20.94999999999999929, 1.116121084443477685E-11, -136.9000000000000057 ) ) ;
#184341=CIRCLE ( 'NONE', #255217, 11.90000000000000391 ) ;
#184363=DIRECTION ( 'NONE',  ( 0.000000000000000000, 1.224646799142185182E-16, 1.000000000000000000 ) ) ;
#184382=CARTESIAN_POINT ( 'NONE',  ( -21.05000000000000071, -0.09999999998884338825, -122.3500000000000085 ) ) ;
#184401=CARTESIAN_POINT ( 'NONE',  ( 18.50000000000000000, -9.499999999988842703, -141.0320693966996828 ) ) ;
#184403=ORIENTED_EDGE ( 'NONE', *, *, #122451, .F. ) ;
#184413=ORIENTED_EDGE ( 'NONE', *, *, #19507, .F. ) ;
#184419=AXIS2_PLACEMENT_3D ( 'NONE', #183105, #202646, #163528 ) ;
#184436=DIRECTION ( 'NONE',  ( 1.000000000000000000, 0.000000000000000000, 0.000000000000000000 ) ) ;
#184454=FACE_OUTER_BOUND ( 'NONE', #254986, .T. ) ;
#184490=CARTESIAN_POINT ( 'NONE',  ( 23.14999999999998437, 1.115600667400684642E-11, -134.0000000000000000 ) ) ;
#184540=AXIS2_PLACEMENT_3D ( 'NONE', #247905, #187946, #109668 ) ;
#184550=VERTEX_POINT ( 'NONE', #189388 ) ;
#184579=CARTESIAN_POINT ( 'NONE',  ( -18.59999999999999787, 1.835341550235567887, -145.5551512925629822 ) ) ;
#184587=CARTESIAN_POINT ( 'NONE',  ( 18.59117750673696534, 10.33248238083634796, -173.0948465439131496 ) ) ;
#184599=EDGE_LOOP ( 'NONE', ( #113728, #2118, #9435, #33397 ) ) ;
#184600=ORIENTED_EDGE ( 'NONE', *, *, #17203, .T. ) ;
#184630=CARTESIAN_POINT ( 'NONE',  ( -20.85000000000000497, 11.75000000001115019, -160.5808527540413024 ) ) ;
#184636=EDGE_LOOP ( 'NONE', ( #62446, #255795, #12330, #173469 ) ) ;
#184638=DIRECTION ( 'NONE',  ( -0.000000000000000000, 1.000000000000000000, -0.000000000000000000 ) ) ;
#184647=CARTESIAN_POINT ( 'NONE',  ( -18.43634282235125710, -9.679787199916876972, -174.1606518854538592 ) ) ;
#184683=CARTESIAN_POINT ( 'NONE',  ( 22.00411653889210228, 0.09903810579702632122, -126.7465571323596123 ) ) ;
#184694=CARTESIAN_POINT ( 'NONE',  ( 20.94999999999999929, -11.64999999998883595, -164.6000000000000227 ) ) ;
#184707=AXIS2_PLACEMENT_3D ( 'NONE', #121360, #219115, #120067 ) ;
#184712=DIRECTION ( 'NONE',  ( 0.000000000000000000, 0.000000000000000000, 1.000000000000000000 ) ) ;
#184716=ORIENTED_EDGE ( 'NONE', *, *, #234358, .T. ) ;
#184719=EDGE_LOOP ( 'NONE', ( #3952, #158181, #24611, #63976 ) ) ;
#184730=EDGE_CURVE ( 'NONE', #165926, #254695, #257842, .T. ) ;
#184734=ORIENTED_EDGE ( 'NONE', *, *, #160945, .F. ) ;
#184743=CARTESIAN_POINT ( 'NONE',  ( -20.85000000000000142, -1.164121893230052995, -175.4148480855716059 ) ) ;
#184767=CARTESIAN_POINT ( 'NONE',  ( -20.86777300164945004, 10.33200063080771969, -173.0931674956643178 ) ) ;
#184800=DIRECTION ( 'NONE',  ( -1.000000000000000000, 0.000000000000000000, 0.000000000000000000 ) ) ;
#184807=CARTESIAN_POINT ( 'NONE',  ( 18.59999999999999432, 1.162701749949165642, -142.1000000000000227 ) ) ;
#184825=CARTESIAN_POINT ( 'NONE',  ( 20.95512820512820440, 10.62384868372303615, -141.6649135690876165 ) ) ;
#184832=DIRECTION ( 'NONE',  ( 0.000000000000000000, -6.308085367188393199E-16, -1.000000000000000000 ) ) ;
#184860=LINE ( 'NONE', #62363, #118258 ) ;
#184869=EDGE_LOOP ( 'NONE', ( #15315, #128825, #153857 ) ) ;
#184880=EDGE_CURVE ( 'NONE', #63952, #175143, #22330, .T. ) ;
#184919=FACE_OUTER_BOUND ( 'NONE', #123264, .T. ) ;
#184925=EDGE_CURVE ( 'NONE', #208289, #64347, #213799, .T. ) ;
#184929=CARTESIAN_POINT ( 'NONE',  ( 18.59999999999999787, -1.835859311432481045, -179.0044391687985410 ) ) ;
#184980=CARTESIAN_POINT ( 'NONE',  ( -18.50000000000000000, 9.150000000011157653, -146.3500000000000227 ) ) ;
#185032=AXIS2_PLACEMENT_3D ( 'NONE', #139263, #153777, #137986 ) ;
#185064=CARTESIAN_POINT ( 'NONE',  ( 18.49351773456749370, -9.443025695134306119, -141.1853255260278104 ) ) ;
#185066=CARTESIAN_POINT ( 'NONE',  ( -23.15000000000000213, 1.115600667400684642E-11, -167.5000000000000284 ) ) ;
#185074=CARTESIAN_POINT ( 'NONE',  ( -20.64999999999999858, -9.399999999988850163, -143.8939691226524644 ) ) ;
#185104=EDGE_CURVE ( 'NONE', #73834, #207677, #192942, .T. ) ;
#185105=DIRECTION ( 'NONE',  ( 0.000000000000000000, 0.000000000000000000, -1.000000000000000000 ) ) ;
#185118=EDGE_LOOP ( 'NONE', ( #255264, #244068, #197978, #123276, #34939, #15954, #55130, #214734 ) ) ;
#185119=CARTESIAN_POINT ( 'NONE',  ( -21.93340585971863632, 7.324147022866478451, -134.0000000000000000 ) ) ;
#185142=DIRECTION ( 'NONE',  ( -0.000000000000000000, 1.000000000000000000, -0.000000000000000000 ) ) ;
#185153=AXIS2_PLACEMENT_3D ( 'NONE', #74916, #153183, #253509 ) ;
#185187=ORIENTED_EDGE ( 'NONE', *, *, #174713, .T. ) ;
#185194=ORIENTED_EDGE ( 'NONE', *, *, #38386, .T. ) ;
#185212=FACE_OUTER_BOUND ( 'NONE', #112110, .T. ) ;
#185282=DIRECTION ( 'NONE',  ( 1.000000000000000000, 0.000000000000000000, 0.000000000000000000 ) ) ;
#185285=DIRECTION ( 'NONE',  ( 0.000000000000000000, -0.1455152366551721865, -0.9893560106964475187 ) ) ;
#185291=DIRECTION ( 'NONE',  ( 0.7071067811865474617, 0.7071067811865474617, 0.000000000000000000 ) ) ;
#185294=DIRECTION ( 'NONE',  ( 0.000000000000000000, 0.9654727137038715545, 0.2605042016806676242 ) ) ;
#185310=VERTEX_POINT ( 'NONE', #140653 ) ;
#185317=AXIS2_PLACEMENT_3D ( 'NONE', #14668, #248104, #250666 ) ;
#185334=CARTESIAN_POINT ( 'NONE',  ( 20.94999999999999929, 1.115600667400684642E-11, -134.0000000000000000 ) ) ;
#185336=CARTESIAN_POINT ( 'NONE',  ( 20.95595624212399954, 10.62389120310529833, -141.6296329141270007 ) ) ;
#185353=DIRECTION ( 'NONE',  ( 0.000000000000000000, -0.4930308989874653269, -0.8700118002898649117 ) ) ;
#185356=CARTESIAN_POINT ( 'NONE',  ( 22.50000000000000000, 11.64957080755595520, -133.9000000000000057 ) ) ;
#185362=ORIENTED_EDGE ( 'NONE', *, *, #168658, .F. ) ;
#185374=ADVANCED_FACE ( 'NONE', ( #184919 ), #1582, .T. ) ;
#185377=CARTESIAN_POINT ( 'NONE',  ( -20.64999999999999858, 1.115600667400684642E-11, -167.5000000000000284 ) ) ;
#185397=DIRECTION ( 'NONE',  ( 0.000000000000000000, 0.000000000000000000, -1.000000000000000000 ) ) ;
#185413=ORIENTED_EDGE ( 'NONE', *, *, #220919, .T. ) ;
#185416=ADVANCED_FACE ( 'NONE', ( #165364 ), #45409, .F. ) ;
#185423=CARTESIAN_POINT ( 'NONE',  ( 18.49999999999999289, 6.450000000011156587, -122.2500000000000284 ) ) ;
#185448=CARTESIAN_POINT ( 'NONE',  ( 18.49999999999999645, -1.135018845899022466, -175.2169768834323520 ) ) ;
#185484=EDGE_CURVE ( 'NONE', #134466, #25818, #209897, .T. ) ;
#185503=CARTESIAN_POINT ( 'NONE',  ( 22.50000000000000000, 0.1000000000111554016, -126.2092204016266379 ) ) ;
#185511=CARTESIAN_POINT ( 'NONE',  ( -21.05000000000000071, -0.09999999998884338825, -127.4593430482987912 ) ) ;
#185517=LINE ( 'NONE', #66853, #27447 ) ;
#185537=CARTESIAN_POINT ( 'NONE',  ( 21.05000000000000426, -0.01681986837451403261, -127.6925747804346116 ) ) ;
#185596=EDGE_CURVE ( 'NONE', #16273, #170246, #71416, .T. ) ;
#185642=DIRECTION ( 'NONE',  ( 0.000000000000000000, 0.000000000000000000, -1.000000000000000000 ) ) ;
#185680=ADVANCED_FACE ( 'NONE', ( #178222 ), #41285, .F. ) ;
#185690=CARTESIAN_POINT ( 'NONE',  ( -22.39999999999999858, 1.115600667400684642E-11, -126.2092204016266379 ) ) ;
#185691=CARTESIAN_POINT ( 'NONE',  ( -21.14999999999999858, 1.115600667400684642E-11, -134.0000000000000000 ) ) ;
#185739=DIRECTION ( 'NONE',  ( -1.000000000000000000, 0.000000000000000000, -0.000000000000000000 ) ) ;
#185746=CARTESIAN_POINT ( 'NONE',  ( 21.05000000000000071, 1.115600667400684642E-11, -134.0000000000000000 ) ) ;
#185757=ORIENTED_EDGE ( 'NONE', *, *, #144866, .T. ) ;
#185781=VERTEX_POINT ( 'NONE', #205446 ) ;
#185853=VECTOR ( 'NONE', #101911, 1000.000000000000000 ) ;
#185860=DIRECTION ( 'NONE',  ( 5.603264701231745086E-32, -1.897661533703520636E-16, 1.000000000000000000 ) ) ;
#185868=CARTESIAN_POINT ( 'NONE',  ( -18.59999999999999787, 11.65000000001115232, -146.1500000000000341 ) ) ;
#185872=CARTESIAN_POINT ( 'NONE',  ( 18.59999999999996945, 10.33248238083634440, -173.0948465439131496 ) ) ;
#185888=EDGE_CURVE ( 'NONE', #237217, #35141, #3387, .T. ) ;
#185901=CIRCLE ( 'NONE', #148505, 0.5000000000000004441 ) ;
#185921=CARTESIAN_POINT ( 'NONE',  ( -18.50000000000000355, -9.399999999988809307, -141.2972597596633193 ) ) ;
#185923=CARTESIAN_POINT ( 'NONE',  ( 20.85000000000000142, 11.75000000001115907, -160.7161343370219129 ) ) ;
#185935=DIRECTION ( 'NONE',  ( -1.000000000000000000, -0.000000000000000000, -0.000000000000000000 ) ) ;
#185942=ORIENTED_EDGE ( 'NONE', *, *, #49680, .F. ) ;
#185954=LINE ( 'NONE', #86829, #117719 ) ;
#185970=FACE_OUTER_BOUND ( 'NONE', #146690, .T. ) ;
#185986=B_SPLINE_CURVE_WITH_KNOTS ( 'NONE', 3,
 ( #209896, #31286, #35136, #110774, #190335, #170811 ),
 .UNSPECIFIED., .F., .F.,
 ( 4, 2, 4 ),
 ( 0.000000000000000000, 0.0001496588209255837190, 0.0002993176418511674379 ),
 .UNSPECIFIED. ) ;
#185996=CARTESIAN_POINT ( 'NONE',  ( 23.24999999999999289, -4.149999999988843058, -134.0000000000000000 ) ) ;
#185998=FACE_OUTER_BOUND ( 'NONE', #188011, .T. ) ;
#186012=EDGE_CURVE ( 'NONE', #91096, #245418, #131135, .T. ) ;
#186029=EDGE_CURVE ( 'NONE', #207656, #158228, #111496, .T. ) ;
#186043=AXIS2_PLACEMENT_3D ( 'NONE', #132109, #252047, #52552 ) ;
#186060=VECTOR ( 'NONE', #225909, 1000.000000000000000 ) ;
#186099=EDGE_CURVE ( 'NONE', #148396, #178251, #47733, .T. ) ;
#186102=CARTESIAN_POINT ( 'NONE',  ( -21.64999999999999858, 7.350000000011155166, -146.2500000000000284 ) ) ;
#186117=CARTESIAN_POINT ( 'NONE',  ( 23.24999999999999289, 6.450000000011156587, -122.2500000000000284 ) ) ;
#186133=AXIS2_PLACEMENT_3D ( 'NONE', #158308, #239096, #201236 ) ;
#186140=AXIS2_PLACEMENT_3D ( 'NONE', #44186, #68888, #224076 ) ;
#186144=ORIENTED_EDGE ( 'NONE', *, *, #256705, .T. ) ;
#186213=CARTESIAN_POINT ( 'NONE',  ( 18.59999999999999076, 6.650000000011155876, -155.1500000000000057 ) ) ;
#186217=CIRCLE ( 'NONE', #27841, 0.1999999999999987899 ) ;
#186239=ORIENTED_EDGE ( 'NONE', *, *, #223430, .T. ) ;
#186261=CARTESIAN_POINT ( 'NONE',  ( -20.54999999999999716, 7.150000000011155876, -146.3500000000000227 ) ) ;
#186270=DIRECTION ( 'NONE',  ( -1.000000000000000000, -0.000000000000000000, -0.000000000000000000 ) ) ;
#186273=AXIS2_PLACEMENT_3D ( 'NONE', #224114, #246263, #127597 ) ;
#186285=DIRECTION ( 'NONE',  ( 1.000000000000000000, -0.000000000000000000, -0.000000000000000000 ) ) ;
#186293=DIRECTION ( 'NONE',  ( 1.000000000000000000, -0.000000000000000000, -0.000000000000000000 ) ) ;
#186310=FACE_OUTER_BOUND ( 'NONE', #257244, .T. ) ;
#186312=ORIENTED_EDGE ( 'NONE', *, *, #172087, .F. ) ;
#186328=DIRECTION ( 'NONE',  ( 0.7071359030027766224, -0.7070776581709024011, 0.000000000000000000 ) ) ;
#186348=ORIENTED_EDGE ( 'NONE', *, *, #23417, .T. ) ;
#186370=DIRECTION ( 'NONE',  ( -0.7070776581709311559, 0.000000000000000000, 0.7071359030027479786 ) ) ;
#186388=EDGE_CURVE ( 'NONE', #101205, #156063, #164649, .T. ) ;
#186413=AXIS2_PLACEMENT_3D ( 'NONE', #116644, #138731, #97033 ) ;
#186438=CARTESIAN_POINT ( 'NONE',  ( 18.49999999999999645, -1.835859311432484375, -179.0044391687985410 ) ) ;
#186450=FACE_OUTER_BOUND ( 'NONE', #187602, .T. ) ;
#186454=ORIENTED_EDGE ( 'NONE', *, *, #96936, .T. ) ;
#186525=FACE_OUTER_BOUND ( 'NONE', #213053, .T. ) ;
#186555=CARTESIAN_POINT ( 'NONE',  ( 18.39999999999999858, -9.499999999988842703, -174.4146583429696875 ) ) ;
#186578=DIRECTION ( 'NONE',  ( 1.000000000000000000, 0.000000000000000000, -0.000000000000000000 ) ) ;
#186581=DIRECTION ( 'NONE',  ( 0.000000000000000000, -0.9893560106964500722, 0.1455152366551550613 ) ) ;
#186589=ADVANCED_FACE ( 'NONE', ( #216382 ), #62460, .F. ) ;
#186606=PLANE ( 'NONE',  #27888 ) ;
#186666=EDGE_CURVE ( 'NONE', #135320, #209723, #11357, .T. ) ;
#186678=EDGE_CURVE ( 'NONE', #96601, #161970, #126710, .T. ) ;
#186682=EDGE_CURVE ( 'NONE', #42519, #109393, #73738, .T. ) ;
#186705=ORIENTED_EDGE ( 'NONE', *, *, #47501, .F. ) ;
#186712=ORIENTED_EDGE ( 'NONE', *, *, #157449, .T. ) ;
#186713=SPHERICAL_SURFACE ( 'NONE', #21232, 0.1000000000000000056 ) ;
#186714=DIRECTION ( 'NONE',  ( 6.938893903907222067E-15, -1.000000000000000000, -0.000000000000000000 ) ) ;
#186759=DIRECTION ( 'NONE',  ( 0.000000000000000000, 0.000000000000000000, -1.000000000000000000 ) ) ;
#186761=ORIENTED_EDGE ( 'NONE', *, *, #76995, .F. ) ;
#186782=VERTEX_POINT ( 'NONE', #131401 ) ;
#186823=VERTEX_POINT ( 'NONE', #192679 ) ;
#186833=DIRECTION ( 'NONE',  ( -0.000000000000000000, -2.891205793294679805E-16, 1.000000000000000000 ) ) ;
#186834=CARTESIAN_POINT ( 'NONE',  ( -22.50000000000000000, 11.65000000001113278, -134.0000000000000284 ) ) ;
#186853=CARTESIAN_POINT ( 'NONE',  ( 20.30466543256828160, 9.304236939266628426, -142.2536626513920339 ) ) ;
#186874=AXIS2_PLACEMENT_3D ( 'NONE', #188748, #10122, #27152 ) ;
#186884=CARTESIAN_POINT ( 'NONE',  ( 18.59999999999999076, 10.25000000001115552, -158.7500000000000284 ) ) ;
#186895=EDGE_CURVE ( 'NONE', #65489, #245081, #256418, .T. ) ;
#186896=CIRCLE ( 'NONE', #203620, 0.09999999999999939493 ) ;
#186964=FACE_OUTER_BOUND ( 'NONE', #182649, .T. ) ;
#186968=EDGE_CURVE ( 'NONE', #196244, #104087, #256821, .T. ) ;
#186971=ORIENTED_EDGE ( 'NONE', *, *, #105891, .F. ) ;
#186995=DIRECTION ( 'NONE',  ( 0.000000000000000000, 0.000000000000000000, -1.000000000000000000 ) ) ;
#187022=AXIS2_PLACEMENT_3D ( 'NONE', #66599, #122736, #142270 ) ;
#187027=AXIS2_PLACEMENT_3D ( 'NONE', #118930, #98029, #198444 ) ;
#187057=DIRECTION ( 'NONE',  ( 0.000000000000000000, 0.000000000000000000, -1.000000000000000000 ) ) ;
#187084=ADVANCED_FACE ( 'NONE', ( #257269 ), #22581, .F. ) ;
#187096=EDGE_LOOP ( 'NONE', ( #127833, #251211, #127160, #121719 ) ) ;
#187097=EDGE_CURVE ( 'NONE', #143423, #149669, #57818, .T. ) ;
#187108=CARTESIAN_POINT ( 'NONE',  ( 21.05000000000000071, 1.162701749949165642, -142.1000000000000227 ) ) ;
#187123=CARTESIAN_POINT ( 'NONE',  ( -21.05000000000000071, 1.835341550235567887, -145.5551512925629822 ) ) ;
#187127=EDGE_LOOP ( 'NONE', ( #110045, #190556, #6468, #231828 ) ) ;
#187140=FACE_OUTER_BOUND ( 'NONE', #116258, .T. ) ;
#187150=LINE ( 'NONE', #245821, #107593 ) ;
#187159=EDGE_LOOP ( 'NONE', ( #236699, #22325, #241843, #45220, #99054 ) ) ;
#187161=ADVANCED_FACE ( 'NONE', ( #98206 ), #222022, .F. ) ;
#187169=VERTEX_POINT ( 'NONE', #17425 ) ;
#187173=CARTESIAN_POINT ( 'NONE',  ( -23.15000000000000213, 2.500000000011154633, -154.2753780772379173 ) ) ;
#187183=DIRECTION ( 'NONE',  ( 0.000000000000000000, -0.9893560106964500722, 0.1455152366551550613 ) ) ;
#187184=FACE_OUTER_BOUND ( 'NONE', #35362, .T. ) ;
#187189=DIRECTION ( 'NONE',  ( -0.000000000000000000, -1.000000000000000000, 6.308085367188393199E-16 ) ) ;
#187201=ORIENTED_EDGE ( 'NONE', *, *, #37815, .T. ) ;
#187208=ORIENTED_EDGE ( 'NONE', *, *, #64187, .T. ) ;
#187229=EDGE_CURVE ( 'NONE', #196380, #50799, #5546, .T. ) ;
#187260=CARTESIAN_POINT ( 'NONE',  ( 18.50000000000000000, -9.499999999988842703, -174.1001893912220737 ) ) ;
#187292=AXIS2_PLACEMENT_3D ( 'NONE', #97107, #98385, #256154 ) ;
#187329=ADVANCED_FACE ( 'NONE', ( #48544 ), #202491, .T. ) ;
#187334=CARTESIAN_POINT ( 'NONE',  ( 19.97071067811865674, 11.72071067812981759, -158.7085786437627064 ) ) ;
#187339=LINE ( 'NONE', #8686, #53685 ) ;
#187342=FACE_OUTER_BOUND ( 'NONE', #174676, .T. ) ;
#187364=ORIENTED_EDGE ( 'NONE', *, *, #98942, .F. ) ;
#187371=VERTEX_POINT ( 'NONE', #147650 ) ;
#187379=CARTESIAN_POINT ( 'NONE',  ( 23.14999999999999503, 11.65000000001116298, -160.4851942293460922 ) ) ;
#187455=CIRCLE ( 'NONE', #158435, 0.09999999999998898659 ) ;
#187461=CARTESIAN_POINT ( 'NONE',  ( -18.59999999999999787, -1.687074390080403941, -121.1854270334583674 ) ) ;
#187465=CARTESIAN_POINT ( 'NONE',  ( -20.94999999999999929, 5.900000000011162093, -157.2809002353436654 ) ) ;
#187490=DIRECTION ( 'NONE',  ( 1.000000000000000000, -7.304098846218135653E-16, -2.111765289898286048E-31 ) ) ;
#187512=EDGE_LOOP ( 'NONE', ( #247934, #20221, #136468, #125255 ) ) ;
#187522=ORIENTED_EDGE ( 'NONE', *, *, #90828, .T. ) ;
#187533=LINE ( 'NONE', #7587, #232020 ) ;
#187550=AXIS2_PLACEMENT_3D ( 'NONE', #205732, #11406, #88329 ) ;
#187594=DIRECTION ( 'NONE',  ( 0.000000000000000000, 1.000000000000000000, 0.000000000000000000 ) ) ;
#187596=CARTESIAN_POINT ( 'NONE',  ( 22.40000000000010161, 1.020945317880167817E-11, -122.2495671075410968 ) ) ;
#187602=EDGE_LOOP ( 'NONE', ( #161430, #10731, #188170, #43986 ) ) ;
#187614=CARTESIAN_POINT ( 'NONE',  ( -23.25000000000000000, 11.65000000001115588, -155.3500000000000227 ) ) ;
#187628=CARTESIAN_POINT ( 'NONE',  ( 18.49999999999999289, 7.120270961708750512, -171.1595630418393625 ) ) ;
#187675=CARTESIAN_POINT ( 'NONE',  ( 21.07928932188134397, 0.09889514566578949673, -127.6714833436012952 ) ) ;
#187703=FACE_OUTER_BOUND ( 'NONE', #184636, .T. ) ;
#187705=ORIENTED_EDGE ( 'NONE', *, *, #136452, .F. ) ;
#187718=ORIENTED_EDGE ( 'NONE', *, *, #216766, .T. ) ;
#187734=CARTESIAN_POINT ( 'NONE',  ( 21.14999999999999858, 11.65000000001115943, -146.1500000000000341 ) ) ;
#187741=ORIENTED_EDGE ( 'NONE', *, *, #171239, .F. ) ;
#187793=DIRECTION ( 'NONE',  ( 1.000000000000000000, 0.000000000000000000, 0.000000000000000000 ) ) ;
#187819=DIRECTION ( 'NONE',  ( -1.000000000000000000, 0.000000000000000000, 0.000000000000000000 ) ) ;
#187844=CARTESIAN_POINT ( 'NONE',  ( -23.25000000000000000, -1.851617760457748618, -179.1031897196036766 ) ) ;
#187855=DIRECTION ( 'NONE',  ( 1.000000000000000000, 0.000000000000000000, 0.000000000000000000 ) ) ;
#187870=FACE_OUTER_BOUND ( 'NONE', #97346, .T. ) ;
#187872=DIRECTION ( 'NONE',  ( -0.000000000000000000, 1.000000000000000000, -0.000000000000000000 ) ) ;
#187889=VERTEX_POINT ( 'NONE', #114466 ) ;
#187908=DIRECTION ( 'NONE',  ( 1.000000000000000000, 0.000000000000000000, -0.000000000000000000 ) ) ;
#187911=AXIS2_PLACEMENT_3D ( 'NONE', #122903, #23822, #182886 ) ;
#187914=CARTESIAN_POINT ( 'NONE',  ( 21.05000000000000071, 8.776282895303626930, -146.1500000000000341 ) ) ;
#187946=DIRECTION ( 'NONE',  ( 0.000000000000000000, -0.000000000000000000, -1.000000000000000000 ) ) ;
#187955=FACE_OUTER_BOUND ( 'NONE', #173627, .T. ) ;
#187961=FACE_OUTER_BOUND ( 'NONE', #85084, .T. ) ;
#187975=CARTESIAN_POINT ( 'NONE',  ( 18.49999999999999289, 10.23906162413259402, -158.7543974345976494 ) ) ;
#187999=CIRCLE ( 'NONE', #129725, 0.09999999999999939493 ) ;
#188011=EDGE_LOOP ( 'NONE', ( #199253, #178274, #84147, #240211 ) ) ;
#188032=EDGE_LOOP ( 'NONE', ( #122649, #5922, #248239, #44723 ) ) ;
#188033=FACE_OUTER_BOUND ( 'NONE', #25715, .T. ) ;
#188061=ORIENTED_EDGE ( 'NONE', *, *, #157097, .F. ) ;
#188116=DIRECTION ( 'NONE',  ( 0.000000000000000000, -0.4791956752371546169, -0.8777080977375152360 ) ) ;
#188122=CARTESIAN_POINT ( 'NONE',  ( 20.44999100639894962, 10.43971070322319683, -141.7590757259705470 ) ) ;
#188156=FACE_OUTER_BOUND ( 'NONE', #82275, .T. ) ;
#188158=VECTOR ( 'NONE', #145630, 1000.000000000000000 ) ;
#188170=ORIENTED_EDGE ( 'NONE', *, *, #103192, .F. ) ;
#188208=CARTESIAN_POINT ( 'NONE',  ( -18.50000000000000000, -9.399999999988850163, -174.3820418481726904 ) ) ;
#188224=EDGE_CURVE ( 'NONE', #68680, #46322, #156807, .T. ) ;
#188259=ORIENTED_EDGE ( 'NONE', *, *, #111082, .T. ) ;
#188261=DIRECTION ( 'NONE',  ( 0.000000000000000000, 0.000000000000000000, -1.000000000000000000 ) ) ;
#188299=EDGE_CURVE ( 'NONE', #217297, #137609, #194405, .T. ) ;
#188324=CARTESIAN_POINT ( 'NONE',  ( 23.14999999999998437, 1.115600667400684642E-11, -134.0000000000000000 ) ) ;
#188327=TOROIDAL_SURFACE ( 'NONE', #75913, 0.4000000000000009104, 0.1000000000000000056 ) ;
#188345=CARTESIAN_POINT ( 'NONE',  ( 23.24999999999999645, 1.115600667400684642E-11, -167.5000000000000284 ) ) ;
#188348=ORIENTED_EDGE ( 'NONE', *, *, #255545, .T. ) ;
#188425=DIRECTION ( 'NONE',  ( -0.000000000000000000, -0.000000000000000000, 1.000000000000000000 ) ) ;
#188443=EDGE_CURVE ( 'NONE', #158190, #140279, #148600, .T. ) ;
#188450=DIRECTION ( 'NONE',  ( 1.000000000000000000, 0.000000000000000000, -0.000000000000000000 ) ) ;
#188453=EDGE_LOOP ( 'NONE', ( #62710, #224595, #227887, #56840 ) ) ;
#188457=DIRECTION ( 'NONE',  ( 0.000000000000000000, 1.000000000000000000, 0.000000000000000000 ) ) ;
#188463=ORIENTED_EDGE ( 'NONE', *, *, #199825, .F. ) ;
#188464=EDGE_CURVE ( 'NONE', #160655, #186823, #111172, .T. ) ;
#188476=EDGE_CURVE ( 'NONE', #159790, #8351, #56973, .T. ) ;
#188477=AXIS2_PLACEMENT_3D ( 'NONE', #129710, #209240, #48884 ) ;
#188504=CARTESIAN_POINT ( 'NONE',  ( -18.51024323315077424, 10.31104185824062469, -173.0204516983106373 ) ) ;
#188511=FACE_OUTER_BOUND ( 'NONE', #7700, .T. ) ;
#188554=DIRECTION ( 'NONE',  ( 1.000000000000000000, 0.000000000000000000, 0.000000000000000000 ) ) ;
#188573=EDGE_LOOP ( 'NONE', ( #7755, #22418, #224287, #197939, #170765, #116564, #46096, #6269, #186761, #241999, #250310, #28706, #226511, #84479, #236390, #95932 ) ) ;
#188587=CARTESIAN_POINT ( 'NONE',  ( 18.54286124688533377, -9.623917578786658211, -174.2412023318627234 ) ) ;
#188617=AXIS2_PLACEMENT_3D ( 'NONE', #88357, #222743, #207055 ) ;
#188633=DIRECTION ( 'NONE',  ( -2.561896900575096011E-15, -0.5907332058517279494, 0.8068669527897025517 ) ) ;
#188650=VECTOR ( 'NONE', #154193, 1000.000000000000000 ) ;
#188669=AXIS2_PLACEMENT_3D ( 'NONE', #84067, #81519, #22891 ) ;
#188748=CARTESIAN_POINT ( 'NONE',  ( -23.25000000000000000, 1.115600667400684642E-11, -167.5000000000000284 ) ) ;
#188753=EDGE_CURVE ( 'NONE', #222155, #229760, #248153, .T. ) ;
#188766=ORIENTED_EDGE ( 'NONE', *, *, #145676, .F. ) ;
#188770=DIRECTION ( 'NONE',  ( 2.952720810173289112E-16, -1.000000000000000000, 0.000000000000000000 ) ) ;
#188779=VERTEX_POINT ( 'NONE', #40776 ) ;
#188782=AXIS2_PLACEMENT_3D ( 'NONE', #190302, #135433, #251536 ) ;
#188812=CARTESIAN_POINT ( 'NONE',  ( 23.14999999999999503, 11.65000000001116298, -146.1500000000000341 ) ) ;
#188841=DIRECTION ( 'NONE',  ( 0.000000000000000000, 0.000000000000000000, -1.000000000000000000 ) ) ;
#188853=CARTESIAN_POINT ( 'NONE',  ( 22.45463910399148943, 1.026727559903908566E-11, -122.3504291898146192 ) ) ;
#188869=VECTOR ( 'NONE', #52033, 1000.000000000000000 ) ;
#188877=CARTESIAN_POINT ( 'NONE',  ( 21.05000000000000071, 6.450000000011156587, -144.0170271704400307 ) ) ;
#188889=DIRECTION ( 'NONE',  ( 1.000000000000000000, 0.000000000000000000, 0.000000000000000000 ) ) ;
#188917=ORIENTED_EDGE ( 'NONE', *, *, #69917, .F. ) ;
#188933=DIRECTION ( 'NONE',  ( -1.000000000000000000, 0.000000000000000000, 0.000000000000000000 ) ) ;
#188935=B_SPLINE_CURVE_WITH_KNOTS ( 'NONE', 3,
 ( #122259, #203065, #21875, #201779, #24464, #60984 ),
 .UNSPECIFIED., .F., .F.,
 ( 4, 2, 4 ),
 ( 0.000000000000000000, 0.0001497467027049249823, 0.0002994934054098499646 ),
 .UNSPECIFIED. ) ;
#189019=ORIENTED_EDGE ( 'NONE', *, *, #127973, .T. ) ;
#189027=VERTEX_POINT ( 'NONE', #211376 ) ;
#189076=AXIS2_PLACEMENT_3D ( 'NONE', #68096, #245465, #249316 ) ;
#189083=CARTESIAN_POINT ( 'NONE',  ( 20.94999999999999574, -1.835341550213255957, -145.5551512925629822 ) ) ;
#189087=VERTEX_POINT ( 'NONE', #11910 ) ;
#189118=ORIENTED_EDGE ( 'NONE', *, *, #244606, .T. ) ;
#189123=DIRECTION ( 'NONE',  ( 1.000000000000000000, -0.000000000000000000, -0.000000000000000000 ) ) ;
#189130=CARTESIAN_POINT ( 'NONE',  ( 21.14999999999999858, 6.650000000011155876, -146.1500000000000341 ) ) ;
#189159=CARTESIAN_POINT ( 'NONE',  ( 20.94999999999999929, 1.115600667400684642E-11, -169.5000000000000284 ) ) ;
#189185=EDGE_CURVE ( 'NONE', #95323, #128128, #177461, .T. ) ;
#189197=CARTESIAN_POINT ( 'NONE',  ( 21.05000005001280172, 8.871279691782060439, -146.1779475882454733 ) ) ;
#189208=CYLINDRICAL_SURFACE ( 'NONE', #34476, 0.5000000000000004441 ) ;
#189218=ORIENTED_EDGE ( 'NONE', *, *, #199545, .F. ) ;
#189259=CARTESIAN_POINT ( 'NONE',  ( 18.49999999999999289, 10.25000000263022670, -158.6871719496316189 ) ) ;
#189293=ADVANCED_FACE ( 'NONE', ( #89813 ), #145939, .T. ) ;
#189306=DIRECTION ( 'NONE',  ( -0.000000000000000000, 0.000000000000000000, 1.000000000000000000 ) ) ;
#189384=ORIENTED_EDGE ( 'NONE', *, *, #135200, .T. ) ;
#189385=ADVANCED_FACE ( 'NONE', ( #205920 ), #144653, .F. ) ;
#189388=CARTESIAN_POINT ( 'NONE',  ( 21.05000000000000071, 1.115600667400684642E-11, -129.6999999999999886 ) ) ;
#189390=DIRECTION ( 'NONE',  ( 1.000000000000000000, 0.000000000000000000, 0.000000000000000000 ) ) ;
#189405=VECTOR ( 'NONE', #107635, 1000.000000000000000 ) ;
#189421=AXIS2_PLACEMENT_3D ( 'NONE', #228575, #227270, #108615 ) ;
#189442=DIRECTION ( 'NONE',  ( 3.265361837132813093E-16, -1.000000000000000000, -0.000000000000000000 ) ) ;
#189451=ORIENTED_EDGE ( 'NONE', *, *, #228711, .T. ) ;
#189491=CARTESIAN_POINT ( 'NONE',  ( 23.14999999999998437, 4.050000000011155343, -134.0000000000000000 ) ) ;
#189524=DIRECTION ( 'NONE',  ( 1.000000000000000000, 0.000000000000000000, 0.000000000000000000 ) ) ;
#189536=CARTESIAN_POINT ( 'NONE',  ( 23.24999999999999645, 1.115600667400684642E-11, -167.5000000000000284 ) ) ;
#189557=ORIENTED_EDGE ( 'NONE', *, *, #199209, .F. ) ;
#189560=DIRECTION ( 'NONE',  ( 1.000000000000000000, 0.000000000000000000, -0.000000000000000000 ) ) ;
#189567=PLANE ( 'NONE',  #205296 ) ;
#189571=EDGE_CURVE ( 'NONE', #59872, #2800, #123628, .T. ) ;
#189600=PLANE ( 'NONE',  #253956 ) ;
#189652=DIRECTION ( 'NONE',  ( 0.000000000000000000, 0.000000000000000000, 1.000000000000000000 ) ) ;
#189655=ORIENTED_EDGE ( 'NONE', *, *, #223906, .T. ) ;
#189658=DIRECTION ( 'NONE',  ( 1.000000000000000000, 0.000000000000000000, 0.000000000000000000 ) ) ;
#189669=ORIENTED_EDGE ( 'NONE', *, *, #173799, .F. ) ;
#189672=LINE ( 'NONE', #150551, #50627 ) ;
#189693=DIRECTION ( 'NONE',  ( 0.000000000000000000, -1.000000000000000000, 0.000000000000000000 ) ) ;
#189696=DIRECTION ( 'NONE',  ( 0.000000000000000000, 0.000000000000000000, -1.000000000000000000 ) ) ;
#189717=ORIENTED_EDGE ( 'NONE', *, *, #176453, .F. ) ;
#189721=DIRECTION ( 'NONE',  ( -1.000000000000000000, -0.000000000000000000, -0.000000000000000000 ) ) ;
#189824=DIRECTION ( 'NONE',  ( 0.000000000000000000, 0.000000000000000000, -1.000000000000000000 ) ) ;
#189867=CARTESIAN_POINT ( 'NONE',  ( -18.59999999999999787, -1.835859311432481045, -179.0044391687985410 ) ) ;
#189870=VERTEX_POINT ( 'NONE', #74813 ) ;
#189913=DIRECTION ( 'NONE',  ( 0.000000000000000000, -1.000000000000000000, -1.897661533703519897E-16 ) ) ;
#189914=DIRECTION ( 'NONE',  ( 0.000000000000000000, -0.9908441862701782288, 0.1350103645450542456 ) ) ;
#189949=ORIENTED_EDGE ( 'NONE', *, *, #23832, .T. ) ;
#189973=LINE ( 'NONE', #88268, #251844 ) ;
#189988=VECTOR ( 'NONE', #147243, 1000.000000000000000 ) ;
#189999=EDGE_CURVE ( 'NONE', #33432, #360, #107162, .T. ) ;
#190093=ORIENTED_EDGE ( 'NONE', *, *, #205273, .F. ) ;
#190095=CYLINDRICAL_SURFACE ( 'NONE', #196232, 0.1000000000000001443 ) ;
#190114=CIRCLE ( 'NONE', #56784, 0.09999999999999939493 ) ;
#190162=DIRECTION ( 'NONE',  ( 0.000000000000000000, -0.6728971962617483760, 0.7397360091702162022 ) ) ;
#190165=DIRECTION ( 'NONE',  ( 1.000000000000000000, 0.000000000000000000, 0.000000000000000000 ) ) ;
#190166=EDGE_LOOP ( 'NONE', ( #169602, #255108, #247952, #136607 ) ) ;
#190170=CARTESIAN_POINT ( 'NONE',  ( -18.50000000000000000, 11.65000000001115232, -155.3500000000000227 ) ) ;
#190177=CARTESIAN_POINT ( 'NONE',  ( -21.05000000000000071, 14.05000000001115623, -139.5136950707610026 ) ) ;
#190205=AXIS2_PLACEMENT_3D ( 'NONE', #188812, #7614, #145824 ) ;
#190213=CARTESIAN_POINT ( 'NONE',  ( 18.42595409746879298, -9.499999812553896916, -140.9993623517468961 ) ) ;
#190235=DIRECTION ( 'NONE',  ( 1.000000000000000000, -0.000000000000000000, 0.000000000000000000 ) ) ;
#190258=EDGE_CURVE ( 'NONE', #159084, #47876, #44885, .T. ) ;
#190284=AXIS2_PLACEMENT_3D ( 'NONE', #130913, #57463, #230012 ) ;
#190291=CARTESIAN_POINT ( 'NONE',  ( 20.94999999999999929, 1.115600667400684642E-11, -171.5000000000000284 ) ) ;
#190302=CARTESIAN_POINT ( 'NONE',  ( 20.94999999999999929, 5.850000000011105428, -144.1324972242779836 ) ) ;
#190335=CARTESIAN_POINT ( 'NONE',  ( 21.08489247129320887, 8.877675190881227252, -146.3500000000000227 ) ) ;
#190370=ORIENTED_EDGE ( 'NONE', *, *, #107230, .F. ) ;
#190378=AXIS2_PLACEMENT_3D ( 'NONE', #23830, #105873, #124199 ) ;
#190419=CARTESIAN_POINT ( 'NONE',  ( -23.15000000000000213, 11.65000000001115588, -160.4851942293460638 ) ) ;
#190455=DIRECTION ( 'NONE',  ( 0.000000000000000000, -1.000000000000000000, 0.000000000000000000 ) ) ;
#190456=CIRCLE ( 'NONE', #203064, 0.09999999999999062417 ) ;
#190495=FACE_OUTER_BOUND ( 'NONE', #209300, .T. ) ;
#190497=CIRCLE ( 'NONE', #136270, 0.09999999999998898659 ) ;
#190504=DIRECTION ( 'NONE',  ( -1.000000000000000000, 0.000000000000000000, 0.000000000000000000 ) ) ;
#190508=ORIENTED_EDGE ( 'NONE', *, *, #2516, .T. ) ;
#190512=CARTESIAN_POINT ( 'NONE',  ( -20.94999999999999929, 11.75000000001115552, -141.0148057706540214 ) ) ;
#190524=AXIS2_PLACEMENT_3D ( 'NONE', #210923, #32316, #111832 ) ;
#190532=DIRECTION ( 'NONE',  ( -1.000000000000000000, 0.000000000000000000, 0.000000000000000000 ) ) ;
#190550=DIRECTION ( 'NONE',  ( 0.000000000000000000, -0.9915357197604853789, 0.1298341882520022694 ) ) ;
#190556=ORIENTED_EDGE ( 'NONE', *, *, #82790, .T. ) ;
#190579=CARTESIAN_POINT ( 'NONE',  ( -20.64999999999999858, 7.250000000011155521, -146.3500000000000227 ) ) ;
#190600=AXIS2_PLACEMENT_3D ( 'NONE', #150005, #229527, #50848 ) ;
#190609=CIRCLE ( 'NONE', #194881, 0.09999999999999939493 ) ;
#190617=DIRECTION ( 'NONE',  ( -1.000000000000000000, -8.673617379884087537E-15, 0.000000000000000000 ) ) ;
#190619=AXIS2_PLACEMENT_3D ( 'NONE', #167787, #30841, #85610 ) ;
#190636=LINE ( 'NONE', #249320, #151981 ) ;
#190653=DIRECTION ( 'NONE',  ( 1.000000000000000000, 7.304098846218134667E-16, 0.000000000000000000 ) ) ;
#190655=CIRCLE ( 'NONE', #194928, 0.09999999999999939493 ) ;
#190687=ORIENTED_EDGE ( 'NONE', *, *, #14067, .T. ) ;
#190691=AXIS2_PLACEMENT_3D ( 'NONE', #103406, #104676, #105973 ) ;
#190696=CARTESIAN_POINT ( 'NONE',  ( 22.50497660315937409, -0.07871793021434793369, -122.2502044951045832 ) ) ;
#190703=DIRECTION ( 'NONE',  ( 8.673617379884087537E-15, -0.000000000000000000, 1.000000000000000000 ) ) ;
#190708=AXIS2_PLACEMENT_3D ( 'NONE', #112505, #9525, #227295 ) ;
#190711=TOROIDAL_SURFACE ( 'NONE', #28397, 0.6000000000000006439, 0.1000000000000000056 ) ;
#190728=CARTESIAN_POINT ( 'NONE',  ( 18.57399277249656322, 10.33112638556969820, -173.0901228926974795 ) ) ;
#190729=ADVANCED_FACE ( 'NONE', ( #238355 ), #62292, .T. ) ;
#190754=FACE_OUTER_BOUND ( 'NONE', #191162, .T. ) ;
#190759=ORIENTED_EDGE ( 'NONE', *, *, #32920, .F. ) ;
#190779=CARTESIAN_POINT ( 'NONE',  ( -20.54999999999999716, -8.999999999988844479, -157.6060308773475924 ) ) ;
#190787=DIRECTION ( 'NONE',  ( 1.000000000000000000, -0.000000000000000000, -0.000000000000000000 ) ) ;
#190794=EDGE_CURVE ( 'NONE', #44063, #105532, #61816, .T. ) ;
#190810=DIRECTION ( 'NONE',  ( 1.000000000000000000, 2.952720810173289112E-16, -0.000000000000000000 ) ) ;
#190819=DIRECTION ( 'NONE',  ( 0.000000000000000000, -0.000000000000000000, 1.000000000000000000 ) ) ;
#190827=DIRECTION ( 'NONE',  ( 0.000000000000000000, -3.122502256758250246E-14, -1.000000000000000000 ) ) ;
#190865=VERTEX_POINT ( 'NONE', #149557 ) ;
#190866=EDGE_LOOP ( 'NONE', ( #47918, #178807, #129490, #172300 ) ) ;
#190875=LINE ( 'NONE', #31804, #96742 ) ;
#190887=CARTESIAN_POINT ( 'NONE',  ( 20.94999999999999929, -8.999999999988842703, -157.6060308773475640 ) ) ;
#190888=ADVANCED_FACE ( 'NONE', ( #94680 ), #152122, .F. ) ;
#190947=CARTESIAN_POINT ( 'NONE',  ( 21.06490991615909181, 10.72489134759826790, -146.2037113535331514 ) ) ;
#190969=CIRCLE ( 'NONE', #107729, 0.1000000000000000472 ) ;
#191007=CARTESIAN_POINT ( 'NONE',  ( -20.94999999999999929, 11.65000000001115232, -167.5000000000000284 ) ) ;
#191029=ORIENTED_EDGE ( 'NONE', *, *, #216083, .F. ) ;
#191039=VECTOR ( 'NONE', #160923, 1000.000000000000000 ) ;
#191058=EDGE_CURVE ( 'NONE', #200852, #206061, #215904, .T. ) ;
#191062=CARTESIAN_POINT ( 'NONE',  ( 20.94999999999999574, 14.00000000001115730, -139.4270925303825663 ) ) ;
#191068=EDGE_CURVE ( 'NONE', #197139, #125446, #78558, .T. ) ;
#191110=CIRCLE ( 'NONE', #174575, 0.09999999999999817368 ) ;
#191112=ORIENTED_EDGE ( 'NONE', *, *, #210694, .T. ) ;
#191145=DIRECTION ( 'NONE',  ( -0.000000000000000000, -0.000000000000000000, 1.000000000000000000 ) ) ;
#191152=DIRECTION ( 'NONE',  ( -0.000000000000000000, -0.000000000000000000, -1.000000000000000000 ) ) ;
#191162=EDGE_LOOP ( 'NONE', ( #145819, #81886, #131389, #209457, #212051 ) ) ;
#191169=AXIS2_PLACEMENT_3D ( 'NONE', #50874, #107009, #125315 ) ;
#191174=DIRECTION ( 'NONE',  ( 0.000000000000000000, -0.000000000000000000, 1.000000000000000000 ) ) ;
#191179=CARTESIAN_POINT ( 'NONE',  ( 18.47688499308725696, -9.464855950272974994, -174.2013477531374406 ) ) ;
#191191=AXIS2_PLACEMENT_3D ( 'NONE', #140662, #123681, #39018 ) ;
#191231=EDGE_LOOP ( 'NONE', ( #130031, #246165, #171326, #135434 ) ) ;
#191234=AXIS2_PLACEMENT_3D ( 'NONE', #194048, #55757, #216141 ) ;
#191301=CIRCLE ( 'NONE', #187022, 11.75000000000000000 ) ;
#191309=EDGE_CURVE ( 'NONE', #206150, #229990, #131661, .T. ) ;
#191340=ORIENTED_EDGE ( 'NONE', *, *, #110290, .T. ) ;
#191370=CARTESIAN_POINT ( 'NONE',  ( -21.05000000000000071, 0.09779029131994597390, -127.7421853895238968 ) ) ;
#191413=EDGE_LOOP ( 'NONE', ( #149188, #129680, #178505, #140532 ) ) ;
#191414=ORIENTED_EDGE ( 'NONE', *, *, #155045, .T. ) ;
#191416=EDGE_LOOP ( 'NONE', ( #96636, #224928, #134840, #148811 ) ) ;
#191430=VECTOR ( 'NONE', #83081, 1000.000000000000000 ) ;
#191449=DIRECTION ( 'NONE',  ( -1.000000000000000000, -0.000000000000000000, -0.000000000000000000 ) ) ;
#191503=VECTOR ( 'NONE', #44198, 1000.000000000000000 ) ;
#191506=CIRCLE ( 'NONE', #70699, 0.09999999999999939493 ) ;
#191530=VECTOR ( 'NONE', #161354, 1000.000000000000000 ) ;
#191547=AXIS2_PLACEMENT_3D ( 'NONE', #122831, #182809, #124113 ) ;
#191549=AXIS2_PLACEMENT_3D ( 'NONE', #80811, #97798, #40467 ) ;
#191578=CARTESIAN_POINT ( 'NONE',  ( 21.00000000000000000, 9.750000000011153745, -155.2500000000000284 ) ) ;
#191605=EDGE_CURVE ( 'NONE', #89005, #8389, #145555, .T. ) ;
#191660=CARTESIAN_POINT ( 'NONE',  ( 20.04142135623730070, 11.65000000001115943, -155.3500000000000227 ) ) ;
#191665=CARTESIAN_POINT ( 'NONE',  ( 23.15000000000000213, -11.48912529306489994, -164.5000000000000000 ) ) ;
#191680=AXIS2_PLACEMENT_3D ( 'NONE', #168049, #50607, #225392 ) ;
#191684=ADVANCED_FACE ( 'NONE', ( #181078 ), #2396, .F. ) ;
#191712=ORIENTED_EDGE ( 'NONE', *, *, #17454, .F. ) ;
#191719=CARTESIAN_POINT ( 'NONE',  ( 18.59999999999999076, 6.450000000011156587, -155.1500000000000057 ) ) ;
#191744=EDGE_CURVE ( 'NONE', #231078, #47961, #247444, .T. ) ;
#191773=CIRCLE ( 'NONE', #21080, 0.2000000000000057288 ) ;
#191824=( BOUNDED_CURVE ( )  B_SPLINE_CURVE ( 3, ( #640, #178046, #235414, #176759 ),
 .UNSPECIFIED., .F., .F. ) 
 B_SPLINE_CURVE_WITH_KNOTS ( ( 4, 4 ),
 ( 3.141592653589793116, 4.712388980384689674 ),
 .UNSPECIFIED. ) 
 CURVE ( )  GEOMETRIC_REPRESENTATION_ITEM ( )  RATIONAL_B_SPLINE_CURVE ( ( 1.000000000000000000, 0.8047378541243649375, 0.8047378541243649375, 1.000000000000000000 ) ) 
 REPRESENTATION_ITEM ( '' )  );
#191850=CARTESIAN_POINT ( 'NONE',  ( -21.05000000000000071, -11.64999999998884483, -136.9000000000000341 ) ) ;
#191851=CARTESIAN_POINT ( 'NONE',  ( 18.52928932304149967, 10.27928932305266407, -158.6762534328032643 ) ) ;
#191889=VECTOR ( 'NONE', #201370, 1000.000000000000000 ) ;
#191901=EDGE_LOOP ( 'NONE', ( #83178, #61530, #75095 ) ) ;
#191914=ADVANCED_FACE ( 'NONE', ( #76497 ), #252567, .T. ) ;
#191915=AXIS2_PLACEMENT_3D ( 'NONE', #201121, #2907, #120346 ) ;
#191954=EDGE_LOOP ( 'NONE', ( #112570, #18262, #179760 ) ) ;
#191976=ORIENTED_EDGE ( 'NONE', *, *, #65002, .T. ) ;
#191980=CARTESIAN_POINT ( 'NONE',  ( 21.12230431290518595, 0.005209851700164400135, -127.5424333467069857 ) ) ;
#191987=CARTESIAN_POINT ( 'NONE',  ( 20.94999999999999929, -8.663551401857999323, -157.9758988819327215 ) ) ;
#192020=DIRECTION ( 'NONE',  ( 2.879366945564059217E-14, -0.9875055080513751582, 0.1575844902526747915 ) ) ;
#192046=EDGE_CURVE ( 'NONE', #64807, #119168, #133105, .T. ) ;
#192083=CARTESIAN_POINT ( 'NONE',  ( 21.05000000000000071, 14.05000000001115623, -161.9863049292391111 ) ) ;
#192092=FACE_BOUND ( 'NONE', #201444, .T. ) ;
#192094=DIRECTION ( 'NONE',  ( -1.000000000000000000, -0.000000000000000000, 0.000000000000000000 ) ) ;
#192110=EDGE_CURVE ( 'NONE', #177470, #15173, #37434, .T. ) ;
#192118=AXIS2_PLACEMENT_3D ( 'NONE', #34987, #153671, #235701 ) ;
#192144=EDGE_CURVE ( 'NONE', #207209, #59363, #53033, .T. ) ;
#192167=VECTOR ( 'NONE', #221186, 1000.000000000000000 ) ;
#192170=ORIENTED_EDGE ( 'NONE', *, *, #188476, .T. ) ;
#192230=CARTESIAN_POINT ( 'NONE',  ( 18.59999999999999787, -1.835341550213255957, -145.5551512925629822 ) ) ;
#192232=VERTEX_POINT ( 'NONE', #223396 ) ;
#192236=DIRECTION ( 'NONE',  ( 0.000000000000000000, -1.000000000000000000, 0.000000000000000000 ) ) ;
#192239=DIRECTION ( 'NONE',  ( 0.000000000000000000, 0.000000000000000000, 1.000000000000000000 ) ) ;
#192257=VERTEX_POINT ( 'NONE', #184280 ) ;
#192278=CARTESIAN_POINT ( 'NONE',  ( -20.64999999999999858, 1.115600667400684642E-11, -167.5000000000000284 ) ) ;
#192290=ORIENTED_EDGE ( 'NONE', *, *, #164978, .T. ) ;
#192328=( NAMED_UNIT ( * ) SI_UNIT ( $, .STERADIAN. ) SOLID_ANGLE_UNIT ( ) );
#192341=DIRECTION ( 'NONE',  ( 1.000000000000000000, 0.000000000000000000, 0.000000000000000000 ) ) ;
#192349=CARTESIAN_POINT ( 'NONE',  ( -20.54999999999999716, -8.999999999988846255, -143.8939691226524644 ) ) ;
#192357=ORIENTED_EDGE ( 'NONE', *, *, #238975, .F. ) ;
#192360=DIRECTION ( 'NONE',  ( 0.000000000000000000, -0.000000000000000000, -1.000000000000000000 ) ) ;
#192369=AXIS2_PLACEMENT_3D ( 'NONE', #219635, #223482, #63123 ) ;
#192371=LINE ( 'NONE', #174133, #211758 ) ;
#192400=CARTESIAN_POINT ( 'NONE',  ( -18.45068461519106506, -9.486506529077926686, -141.0687771689047452 ) ) ;
#192415=ORIENTED_EDGE ( 'NONE', *, *, #43398, .F. ) ;
#192440=ORIENTED_EDGE ( 'NONE', *, *, #235512, .T. ) ;
#192447=EDGE_LOOP ( 'NONE', ( #205475, #230595, #92400, #213154 ) ) ;
#192460=CARTESIAN_POINT ( 'NONE',  ( -22.48970261584618058, 11.65000000001115588, -133.9446305117826341 ) ) ;
#192464=EDGE_CURVE ( 'NONE', #65123, #59718, #141644, .T. ) ;
#192473=ORIENTED_EDGE ( 'NONE', *, *, #163467, .F. ) ;
#192551=CIRCLE ( 'NONE', #100736, 0.09999999999999939493 ) ;
#192554=CIRCLE ( 'NONE', #213380, 0.09999999999998898659 ) ;
#192574=CARTESIAN_POINT ( 'NONE',  ( -21.05000000000000071, -11.48912529306489994, -164.5000000000000000 ) ) ;
#192592=EDGE_LOOP ( 'NONE', ( #244246, #247906, #56989, #35102 ) ) ;
#192595=ORIENTED_EDGE ( 'NONE', *, *, #249384, .F. ) ;
#192605=CARTESIAN_POINT ( 'NONE',  ( 20.94999999999999574, 10.47338541492405994, -141.5786544642485580 ) ) ;
#192621=CIRCLE ( 'NONE', #34253, 0.09999999999998898659 ) ;
#192655=DIRECTION ( 'NONE',  ( 0.000000000000000000, -0.8660254037844411501, -0.4999999999999956146 ) ) ;
#192671=VECTOR ( 'NONE', #200320, 1000.000000000000000 ) ;
#192675=ORIENTED_EDGE ( 'NONE', *, *, #95399, .T. ) ;
#192679=CARTESIAN_POINT ( 'NONE',  ( -20.94999999999999929, 7.120270961708750512, -171.1595630418393625 ) ) ;
#192686=ORIENTED_EDGE ( 'NONE', *, *, #229306, .T. ) ;
#192709=ADVANCED_FACE ( 'NONE', ( #32332 ), #227936, .F. ) ;
#192724=ORIENTED_EDGE ( 'NONE', *, *, #71303, .T. ) ;
#192730=EDGE_CURVE ( 'NONE', #178019, #158625, #71448, .T. ) ;
#192759=LINE ( 'NONE', #132794, #43601 ) ;
#192767=DIRECTION ( 'NONE',  ( 1.000000000000000000, 0.000000000000000000, 0.000000000000000000 ) ) ;
#192785=DIRECTION ( 'NONE',  ( -1.836970198721029934E-16, 1.000000000000000000, 0.000000000000000000 ) ) ;
#192828=CARTESIAN_POINT ( 'NONE',  ( -20.54999999999999716, -9.499999999988846255, -157.6060308773475924 ) ) ;
#192836=ORIENTED_EDGE ( 'NONE', *, *, #71303, .F. ) ;
#192841=AXIS2_PLACEMENT_3D ( 'NONE', #10395, #209878, #194176 ) ;
#192924=CIRCLE ( 'NONE', #213761, 11.90000000000000746 ) ;
#192942=LINE ( 'NONE', #151255, #147156 ) ;
#192947=EDGE_CURVE ( 'NONE', #59363, #63340, #243322, .T. ) ;
#192961=FACE_OUTER_BOUND ( 'NONE', #96650, .T. ) ;
#192994=DIRECTION ( 'NONE',  ( -1.000000000000000000, -0.000000000000000000, 0.000000000000000000 ) ) ;
#193001=CARTESIAN_POINT ( 'NONE',  ( 20.94999999999999574, -11.48912529306490349, -136.9000000000000341 ) ) ;
#193010=DIRECTION ( 'NONE',  ( -0.7071067811865475727, -0.7071067811865475727, 0.000000000000000000 ) ) ;
#193013=AXIS2_PLACEMENT_3D ( 'NONE', #151152, #155014, #230688 ) ;
#193015=AXIS2_PLACEMENT_3D ( 'NONE', #98492, #24159, #180650 ) ;
#193032=DIRECTION ( 'NONE',  ( 1.000000000000000000, 1.875376730785737719E-16, 0.000000000000000000 ) ) ;
#193035=DIRECTION ( 'NONE',  ( 1.000000000000000000, 0.000000000000000000, 0.000000000000000000 ) ) ;
#193039=DIRECTION ( 'NONE',  ( 0.000000000000000000, 1.000000000000000000, 0.000000000000000000 ) ) ;
#193057=DIRECTION ( 'NONE',  ( -1.000000000000000000, 0.000000000000000000, 0.000000000000000000 ) ) ;
#193076=ORIENTED_EDGE ( 'NONE', *, *, #148630, .F. ) ;
#193085=ORIENTED_EDGE ( 'NONE', *, *, #75245, .F. ) ;
#193091=CARTESIAN_POINT ( 'NONE',  ( 19.97071067811864609, 11.72071067812981404, -155.3500000000000227 ) ) ;
#193098=FACE_OUTER_BOUND ( 'NONE', #190166, .T. ) ;
#193099=DIRECTION ( 'NONE',  ( -3.265361837132813093E-16, 1.000000000000000000, 0.000000000000000000 ) ) ;
#193108=CARTESIAN_POINT ( 'NONE',  ( 21.05000000000000071, 5.000000000011153745, -146.4052660189131245 ) ) ;
#193109=ORIENTED_EDGE ( 'NONE', *, *, #6824, .T. ) ;
#193150=B_SPLINE_CURVE_WITH_KNOTS ( 'NONE', 3,
 ( #192605, #73971, #193898, #96049, #233036, #54366, #133900, #213438, #34840, #141604, #222393, #217270, #779, #122050, #99879, #201574, #162474, #82878, #123337, #120790, #219854, #97310 ),
 .UNSPECIFIED., .F., .F.,
 ( 4, 3, 3, 3, 3, 3, 3, 4 ),
 ( 0.000000000000000000, 7.307836821080902015E-06, 4.161455748548337322E-05, 7.576591810647894819E-05, 0.0001098090429817568715, 0.0001438003617351259287, 0.0001777914035423789891, 0.0002117966137403053117 ),
 .UNSPECIFIED. ) ;
#193151=FACE_OUTER_BOUND ( 'NONE', #206235, .T. ) ;
#193153=ORIENTED_EDGE ( 'NONE', *, *, #176453, .T. ) ;
#193161=CIRCLE ( 'NONE', #105809, 11.69999999999998863 ) ;
#193169=DIRECTION ( 'NONE',  ( 0.000000000000000000, 0.000000000000000000, -1.000000000000000000 ) ) ;
#193170=DIRECTION ( 'NONE',  ( 0.000000000000000000, -1.000000000000000000, 0.000000000000000000 ) ) ;
#193172=DIRECTION ( 'NONE',  ( 1.000000000000000000, 0.000000000000000000, 0.000000000000000000 ) ) ;
#193186=ORIENTED_EDGE ( 'NONE', *, *, #144793, .F. ) ;
#193198=ORIENTED_EDGE ( 'NONE', *, *, #21428, .T. ) ;
#193232=ORIENTED_EDGE ( 'NONE', *, *, #212828, .T. ) ;
#193275=AXIS2_PLACEMENT_3D ( 'NONE', #194406, #18306, #133126 ) ;
#193304=DIRECTION ( 'NONE',  ( 2.259780016855445309E-14, 0.9875055080513753802, -0.1575844902526748192 ) ) ;
#193325=DIRECTION ( 'NONE',  ( 0.000000000000000000, 0.000000000000000000, -1.000000000000000000 ) ) ;
#193331=CARTESIAN_POINT ( 'NONE',  ( -23.25000000000000000, -9.682403433465239573, -174.1568433774127982 ) ) ;
#193338=EDGE_CURVE ( 'NONE', #155087, #148690, #80056, .T. ) ;
#193345=EDGE_LOOP ( 'NONE', ( #106326, #215637, #83379, #179 ) ) ;
#193355=ORIENTED_EDGE ( 'NONE', *, *, #231466, .F. ) ;
#193362=CARTESIAN_POINT ( 'NONE',  ( -18.54118089899633048, -9.463537631836938857, -141.0485775978681602 ) ) ;
#193398=ORIENTED_EDGE ( 'NONE', *, *, #225133, .F. ) ;
#193411=DIRECTION ( 'NONE',  ( 1.000000000000000000, 0.000000000000000000, 0.000000000000000000 ) ) ;
#193438=VECTOR ( 'NONE', #31013, 1000.000000000000000 ) ;
#193470=AXIS2_PLACEMENT_3D ( 'NONE', #17650, #135017, #119342 ) ;
#193475=VECTOR ( 'NONE', #197956, 1000.000000000000000 ) ;
#193478=EDGE_CURVE ( 'NONE', #140944, #157963, #29163, .T. ) ;
#193480=DIRECTION ( 'NONE',  ( 0.000000000000000000, 0.000000000000000000, 1.000000000000000000 ) ) ;
#193511=CARTESIAN_POINT ( 'NONE',  ( -20.54999999999999716, 1.115600667400684642E-11, -167.5000000000000284 ) ) ;
#193516=DIRECTION ( 'NONE',  ( 1.000000000000000000, -0.000000000000000000, -0.000000000000000000 ) ) ;
#193520=ORIENTED_EDGE ( 'NONE', *, *, #149056, .F. ) ;
#193521=DIRECTION ( 'NONE',  ( 0.000000000000000000, 0.000000000000000000, -1.000000000000000000 ) ) ;
#193576=VECTOR ( 'NONE', #162044, 1000.000000000000000 ) ;
#193581=DIRECTION ( 'NONE',  ( -0.000000000000000000, -0.000000000000000000, -1.000000000000000000 ) ) ;
#193587=CARTESIAN_POINT ( 'NONE',  ( -21.05000000000000071, -11.64999999998884306, -164.6000000000000227 ) ) ;
#193597=AXIS2_PLACEMENT_3D ( 'NONE', #204948, #103277, #165862 ) ;
#193617=DIRECTION ( 'NONE',  ( 0.000000000000000000, 0.000000000000000000, 1.000000000000000000 ) ) ;
#193632=CARTESIAN_POINT ( 'NONE',  ( 21.05995757104869881, 8.775389244732430427, -146.1949051229912016 ) ) ;
#193654=AXIS2_PLACEMENT_3D ( 'NONE', #230317, #69991, #27020 ) ;
#193673=CARTESIAN_POINT ( 'NONE',  ( -18.59999999999999787, 11.65000000001115232, -155.3500000000000227 ) ) ;
#193686=EDGE_LOOP ( 'NONE', ( #201429, #46550, #237024, #151610 ) ) ;
#193687=ORIENTED_EDGE ( 'NONE', *, *, #9940, .F. ) ;
#193724=DIRECTION ( 'NONE',  ( 1.000000000000000000, 0.000000000000000000, 0.000000000000000000 ) ) ;
#193730=DIRECTION ( 'NONE',  ( 0.000000000000000000, -1.000000000000000000, 0.000000000000000000 ) ) ;
#193732=CARTESIAN_POINT ( 'NONE',  ( 18.46932045258650490, -9.670685200254538927, -174.1738603729967565 ) ) ;
#193736=VECTOR ( 'NONE', #69799, 999.9999999999998863 ) ;
#193804=ORIENTED_EDGE ( 'NONE', *, *, #120083, .F. ) ;
#193817=ORIENTED_EDGE ( 'NONE', *, *, #2039, .T. ) ;
#193825=ORIENTED_EDGE ( 'NONE', *, *, #172201, .T. ) ;
#193844=B_SPLINE_CURVE_WITH_KNOTS ( 'NONE', 3,
 ( #126635, #26264, #202319, #165786, #103199, #45813, #206176, #125359, #181493, #141072, #86195, #201038, #160661, #83614, #220608, #84901 ),
 .UNSPECIFIED., .F., .F.,
 ( 4, 3, 3, 3, 3, 4 ),
 ( 0.000000000000000000, 2.209075297430758666E-05, 5.594258369009635874E-05, 8.979524372342026039E-05, 0.0001236472815274586843, 0.0001574990747609555279 ),
 .UNSPECIFIED. ) ;
#193848=CARTESIAN_POINT ( 'NONE',  ( 23.24999999999999289, 6.650000000011155876, -155.3500000000000227 ) ) ;
#193853=DIRECTION ( 'NONE',  ( 0.000000000000000000, 0.000000000000000000, -1.000000000000000000 ) ) ;
#193860=ADVANCED_FACE ( 'NONE', ( #245295 ), #162670, .T. ) ;
#193894=AXIS2_PLACEMENT_3D ( 'NONE', #116542, #60400, #257273 ) ;
#193898=CARTESIAN_POINT ( 'NONE',  ( 20.95035502843362707, 10.47763832678762164, -141.5762997087363999 ) ) ;
#193916=LINE ( 'NONE', #94793, #193438 ) ;
#193918=ORIENTED_EDGE ( 'NONE', *, *, #248597, .T. ) ;
#193921=EDGE_CURVE ( 'NONE', #68733, #80663, #116870, .T. ) ;
#193936=DIRECTION ( 'NONE',  ( 0.000000000000000000, 0.000000000000000000, -1.000000000000000000 ) ) ;
#193952=CARTESIAN_POINT ( 'NONE',  ( -21.11825140030074266, 6.445407565431249708, -133.9927963793674053 ) ) ;
#193963=EDGE_CURVE ( 'NONE', #147930, #75879, #241946, .T. ) ;
#193981=VECTOR ( 'NONE', #43103, 1000.000000000000000 ) ;
#193986=( GEOMETRIC_REPRESENTATION_CONTEXT ( 3 ) GLOBAL_UNCERTAINTY_ASSIGNED_CONTEXT ( ( #58357 ) ) GLOBAL_UNIT_ASSIGNED_CONTEXT ( ( #175355, #132341, #192328 ) ) REPRESENTATION_CONTEXT ( 'NONE', 'WORKASPACE' ) );
#193990=DIRECTION ( 'NONE',  ( 1.000000000000000000, 0.000000000000000000, 0.000000000000000000 ) ) ;
#194010=ADVANCED_FACE ( 'NONE', ( #174788 ), #71803, .F. ) ;
#194034=CARTESIAN_POINT ( 'NONE',  ( -21.07928932188134041, 0.09889514566555068775, -127.6714833436067238 ) ) ;
#194048=CARTESIAN_POINT ( 'NONE',  ( -23.25000000000000000, 1.115600667400684642E-11, -167.5000000000000284 ) ) ;
#194054=DIRECTION ( 'NONE',  ( 0.000000000000000000, 0.000000000000000000, 1.000000000000000000 ) ) ;
#194081=CARTESIAN_POINT ( 'NONE',  ( 21.05000000000000071, -11.64999999998883595, -164.6000000000000227 ) ) ;
#194108=CARTESIAN_POINT ( 'NONE',  ( 20.95159278453404283, 8.907896337960206523, -142.4847201851092677 ) ) ;
#194117=ORIENTED_EDGE ( 'NONE', *, *, #211156, .F. ) ;
#194120=DIRECTION ( 'NONE',  ( 1.000000000000000000, -0.000000000000000000, -0.000000000000000000 ) ) ;
#194130=EDGE_LOOP ( 'NONE', ( #72033, #237260, #211207, #195178 ) ) ;
#194132=DIRECTION ( 'NONE',  ( 1.000000000000000000, 0.000000000000000000, 0.000000000000000000 ) ) ;
#194176=DIRECTION ( 'NONE',  ( 0.000000000000000000, 0.000000000000000000, -1.000000000000000000 ) ) ;
#194177=EDGE_LOOP ( 'NONE', ( #114451, #158223, #35556, #172808 ) ) ;
#194201=CIRCLE ( 'NONE', #248334, 0.2000000000000057288 ) ;
#194231=CARTESIAN_POINT ( 'NONE',  ( 20.94999999999999574, -11.64999999998883595, -136.9000000000000341 ) ) ;
#194240=CARTESIAN_POINT ( 'NONE',  ( 18.49999999999998934, 6.550000000011156231, -155.1500000000000057 ) ) ;
#194289=EDGE_CURVE ( 'NONE', #18380, #110751, #171574, .T. ) ;
#194310=DIRECTION ( 'NONE',  ( -1.000000000000000000, 0.000000000000000000, 0.000000000000000000 ) ) ;
#194311=ORIENTED_EDGE ( 'NONE', *, *, #9950, .T. ) ;
#194344=ORIENTED_EDGE ( 'NONE', *, *, #70228, .F. ) ;
#194348=DIRECTION ( 'NONE',  ( -1.000000000000000000, 0.000000000000000000, 0.000000000000000000 ) ) ;
#194359=LINE ( 'NONE', #53535, #134808 ) ;
#194370=DIRECTION ( 'NONE',  ( 1.000000000000000000, 0.000000000000000000, 0.000000000000000000 ) ) ;
#194377=CARTESIAN_POINT ( 'NONE',  ( -23.25000000000000000, -8.999999999988844479, -157.6060308773475924 ) ) ;
#194399=ORIENTED_EDGE ( 'NONE', *, *, #86659, .F. ) ;
#194405=CIRCLE ( 'NONE', #152720, 0.09999999999998898659 ) ;
#194406=CARTESIAN_POINT ( 'NONE',  ( 21.05000000000000071, -8.999999999988842703, -157.6060308773475640 ) ) ;
#194464=DIRECTION ( 'NONE',  ( 1.000000000000000000, 2.952720810173289112E-16, -0.000000000000000000 ) ) ;
#194467=ADVANCED_FACE ( 'NONE', ( #155851 ), #117248, .T. ) ;
#194473=EDGE_CURVE ( 'NONE', #248851, #111708, #154579, .T. ) ;
#194493=ORIENTED_EDGE ( 'NONE', *, *, #26467, .T. ) ;
#194501=DIRECTION ( 'NONE',  ( -1.000000000000000000, -0.000000000000000000, -0.000000000000000000 ) ) ;
#194532=AXIS2_PLACEMENT_3D ( 'NONE', #185691, #25353, #186995 ) ;
#194538=CIRCLE ( 'NONE', #144406, 0.09999999999999939493 ) ;
#194550=CARTESIAN_POINT ( 'NONE',  ( 21.14999999999999858, 1.115600667400684642E-11, -127.4593430482987912 ) ) ;
#194552=ORIENTED_EDGE ( 'NONE', *, *, #240316, .T. ) ;
#194555=DIRECTION ( 'NONE',  ( 1.000000000000000000, 0.000000000000000000, 0.000000000000000000 ) ) ;
#194582=DIRECTION ( 'NONE',  ( 1.000000000000000000, 0.000000000000000000, 0.000000000000000000 ) ) ;
#194678=CARTESIAN_POINT ( 'NONE',  ( 23.14999999999999858, 5.000000000011153745, -155.5947339810869323 ) ) ;
#194683=CARTESIAN_POINT ( 'NONE',  ( 20.94999999999999929, -8.999999999988842703, -158.1060308773475640 ) ) ;
#194690=VERTEX_POINT ( 'NONE', #131428 ) ;
#194700=ORIENTED_EDGE ( 'NONE', *, *, #3763, .F. ) ;
#194735=EDGE_CURVE ( 'NONE', #117471, #16854, #75746, .T. ) ;
#194793=TOROIDAL_SURFACE ( 'NONE', #202957, 0.2000000000000000111, 0.1000000000000000056 ) ;
#194827=EDGE_CURVE ( 'NONE', #89589, #146074, #150740, .T. ) ;
#194829=EDGE_LOOP ( 'NONE', ( #93996, #42707, #29033 ) ) ;
#194872=ORIENTED_EDGE ( 'NONE', *, *, #218514, .T. ) ;
#194881=AXIS2_PLACEMENT_3D ( 'NONE', #100930, #196225, #159686 ) ;
#194885=CARTESIAN_POINT ( 'NONE',  ( -20.64999999999999858, 4.250000000011156409, -155.1500000000000057 ) ) ;
#194914=ORIENTED_EDGE ( 'NONE', *, *, #255904, .F. ) ;
#194927=DIRECTION ( 'NONE',  ( 0.000000000000000000, 1.000000000000000000, 0.000000000000000000 ) ) ;
#194928=AXIS2_PLACEMENT_3D ( 'NONE', #73887, #76399, #33486 ) ;
#194940=AXIS2_PLACEMENT_3D ( 'NONE', #47385, #124387, #203906 ) ;
#194958=AXIS2_PLACEMENT_3D ( 'NONE', #172440, #91577, #14630 ) ;
#194973=CARTESIAN_POINT ( 'NONE',  ( -20.00857864376270001, 9.350000000011156942, -155.1500000000000057 ) ) ;
#195012=ORIENTED_EDGE ( 'NONE', *, *, #170777, .F. ) ;
#195025=CARTESIAN_POINT ( 'NONE',  ( 21.08621493067296626, 6.349294291182826733, -133.9438051605239082 ) ) ;
#195064=CIRCLE ( 'NONE', #128405, 0.09999999999998902822 ) ;
#195091=CARTESIAN_POINT ( 'NONE',  ( -23.25000000000000000, 1.115600667400684642E-11, -175.4000000000000341 ) ) ;
#195157=DIRECTION ( 'NONE',  ( 1.000000000000000000, 0.000000000000000000, 0.000000000000000000 ) ) ;
#195178=ORIENTED_EDGE ( 'NONE', *, *, #223786, .F. ) ;
#195190=ORIENTED_EDGE ( 'NONE', *, *, #29312, .F. ) ;
#195211=DIRECTION ( 'NONE',  ( 0.000000000000000000, 0.000000000000000000, -1.000000000000000000 ) ) ;
#195213=CARTESIAN_POINT ( 'NONE',  ( 22.37643362114956247, 7.625789993969535274, -133.9009186263186564 ) ) ;
#195229=ORIENTED_EDGE ( 'NONE', *, *, #204712, .T. ) ;
#195249=ORIENTED_EDGE ( 'NONE', *, *, #48100, .F. ) ;
#195252=CARTESIAN_POINT ( 'NONE',  ( -21.05000000000000071, 6.304961112695769643, -134.0213855659371234 ) ) ;
#195259=EDGE_LOOP ( 'NONE', ( #255433, #111087, #187705, #172452 ) ) ;
#195277=EDGE_CURVE ( 'NONE', #227344, #250075, #254910, .T. ) ;
#195286=DIRECTION ( 'NONE',  ( 0.000000000000000000, 1.000000000000000000, -0.000000000000000000 ) ) ;
#195296=DIRECTION ( 'NONE',  ( -6.938893903907209445E-14, -0.9999176327611370985, -0.01283462868040260302 ) ) ;
#195310=CARTESIAN_POINT ( 'NONE',  ( -18.50000000000000000, -9.399999999988850163, -141.2972597596633193 ) ) ;
#195326=DIRECTION ( 'NONE',  ( 1.000000000000000000, 0.000000000000000000, 0.000000000000000000 ) ) ;
#195338=CIRCLE ( 'NONE', #20360, 0.1000000000000096922 ) ;
#195348=AXIS2_PLACEMENT_3D ( 'NONE', #193511, #254702, #171405 ) ;
#195373=ORIENTED_EDGE ( 'NONE', *, *, #60445, .T. ) ;
#195398=EDGE_CURVE ( 'NONE', #187371, #111708, #205256, .T. ) ;
#195419=VECTOR ( 'NONE', #202268, 1000.000000000000000 ) ;
#195420=DIRECTION ( 'NONE',  ( 0.000000000000000000, 0.000000000000000000, -1.000000000000000000 ) ) ;
#195447=DIRECTION ( 'NONE',  ( 0.000000000000000000, -0.8660254037844411501, -0.4999999999999956701 ) ) ;
#195455=ORIENTED_EDGE ( 'NONE', *, *, #66823, .T. ) ;
#195466=ORIENTED_EDGE ( 'NONE', *, *, #138846, .T. ) ;
#195483=DIRECTION ( 'NONE',  ( 0.000000000000000000, -0.000000000000000000, 1.000000000000000000 ) ) ;
#195485=ORIENTED_EDGE ( 'NONE', *, *, #163785, .F. ) ;
#195511=ORIENTED_EDGE ( 'NONE', *, *, #56070, .F. ) ;
#195515=ADVANCED_FACE ( 'NONE', ( #90403 ), #201008, .T. ) ;
#195536=AXIS2_PLACEMENT_3D ( 'NONE', #114456, #137847, #16653 ) ;
#195543=ORIENTED_EDGE ( 'NONE', *, *, #53244, .T. ) ;
#195555=ORIENTED_EDGE ( 'NONE', *, *, #29689, .T. ) ;
#195586=CARTESIAN_POINT ( 'NONE',  ( -20.54999999999999716, 2.000000000011154189, -146.7246219227621111 ) ) ;
#195621=FACE_OUTER_BOUND ( 'NONE', #52308, .T. ) ;
#195632=DIRECTION ( 'NONE',  ( 0.000000000000000000, 0.000000000000000000, -1.000000000000000000 ) ) ;
#195640=VERTEX_POINT ( 'NONE', #232518 ) ;
#195646=EDGE_CURVE ( 'NONE', #5925, #197139, #9450, .T. ) ;
#195651=ORIENTED_EDGE ( 'NONE', *, *, #120012, .F. ) ;
#195681=ORIENTED_EDGE ( 'NONE', *, *, #12066, .F. ) ;
#195688=DIRECTION ( 'NONE',  ( 0.000000000000000000, -0.1298341882520022694, -0.9915357197604853789 ) ) ;
#195720=DIRECTION ( 'NONE',  ( 4.408576920032447355E-17, -0.1350103645451876666, -0.9908441862701600211 ) ) ;
#195780=ORIENTED_EDGE ( 'NONE', *, *, #171993, .T. ) ;
#195802=FACE_OUTER_BOUND ( 'NONE', #30306, .T. ) ;
#195842=DIRECTION ( 'NONE',  ( -3.265361837132813093E-16, 1.000000000000000000, 0.000000000000000000 ) ) ;
#195875=CARTESIAN_POINT ( 'NONE',  ( -23.15000000000000213, 1.115600667400684642E-11, -138.1500000000000057 ) ) ;
#195876=CARTESIAN_POINT ( 'NONE',  ( -20.94999999999999929, 7.021664781911246322, -171.1335654018973003 ) ) ;
#195885=ORIENTED_EDGE ( 'NONE', *, *, #167132, .T. ) ;
#195890=EDGE_CURVE ( 'NONE', #92094, #170589, #1566, .T. ) ;
#195914=CIRCLE ( 'NONE', #212475, 4.300000000000025580 ) ;
#195954=DIRECTION ( 'NONE',  ( 0.000000000000000000, 0.9654727137038726648, -0.2605042016806632943 ) ) ;
#195959=ORIENTED_EDGE ( 'NONE', *, *, #172170, .T. ) ;
#195974=DIRECTION ( 'NONE',  ( 0.000000000000000000, 0.000000000000000000, -1.000000000000000000 ) ) ;
#196013=AXIS2_PLACEMENT_3D ( 'NONE', #119589, #96133, #17886 ) ;
#196020=VERTEX_POINT ( 'NONE', #141729 ) ;
#196066=CIRCLE ( 'NONE', #133515, 0.5000000000000004441 ) ;
#196075=CARTESIAN_POINT ( 'NONE',  ( 21.30000000000002558, 1.115650265596050101E-11, -138.0500000000000114 ) ) ;
#196076=ORIENTED_EDGE ( 'NONE', *, *, #164698, .F. ) ;
#196080=CARTESIAN_POINT ( 'NONE',  ( 23.14999999999999858, 5.500000000011153745, -155.0947339810869323 ) ) ;
#196084=AXIS2_PLACEMENT_3D ( 'NONE', #103965, #225199, #179695 ) ;
#196086=ADVANCED_FACE ( 'NONE', ( #59602 ), #151976, .F. ) ;
#196089=EDGE_LOOP ( 'NONE', ( #71656, #255970, #31461, #137112 ) ) ;
#196093=CARTESIAN_POINT ( 'NONE',  ( -21.05000000000000071, -11.48912529306489994, -164.6000000000000227 ) ) ;
#196105=VERTEX_POINT ( 'NONE', #101271 ) ;
#196161=ORIENTED_EDGE ( 'NONE', *, *, #147724, .F. ) ;
#196168=AXIS2_PLACEMENT_3D ( 'NONE', #180195, #120248, #161925 ) ;
#196172=ORIENTED_EDGE ( 'NONE', *, *, #6824, .F. ) ;
#196183=FACE_OUTER_BOUND ( 'NONE', #54925, .T. ) ;
#196225=DIRECTION ( 'NONE',  ( 0.000000000000000000, 0.000000000000000000, 1.000000000000000000 ) ) ;
#196232=AXIS2_PLACEMENT_3D ( 'NONE', #106677, #227933, #49287 ) ;
#196244=VERTEX_POINT ( 'NONE', #83010 ) ;
#196272=TOROIDAL_SURFACE ( 'NONE', #254513, 11.65000000000000036, 0.1000000000000000056 ) ;
#196285=CARTESIAN_POINT ( 'NONE',  ( 21.07971444708685738, 6.329792081637700463, -133.9121765636821237 ) ) ;
#196369=CARTESIAN_POINT ( 'NONE',  ( -20.99749315643149217, 11.75000000001115197, -160.4851942312420761 ) ) ;
#196375=ORIENTED_EDGE ( 'NONE', *, *, #45085, .T. ) ;
#196380=VERTEX_POINT ( 'NONE', #178014 ) ;
#196383=CARTESIAN_POINT ( 'NONE',  ( -20.54999999999999716, 4.350000000011156054, -146.3500000000000227 ) ) ;
#196388=CARTESIAN_POINT ( 'NONE',  ( -21.07094088545368393, 0.09889370256337755294, -127.6798327780828686 ) ) ;
#196397=CARTESIAN_POINT ( 'NONE',  ( -22.50000000000000000, 11.64957080755595520, -133.9000000000000057 ) ) ;
#196398=ADVANCED_FACE ( 'NONE', ( #175449 ), #100970, .T. ) ;
#196402=DIRECTION ( 'NONE',  ( -1.000000000000000000, -0.000000000000000000, -0.000000000000000000 ) ) ;
#196412=AXIS2_PLACEMENT_3D ( 'NONE', #36474, #118569, #235915 ) ;
#196461=DIRECTION ( 'NONE',  ( 1.000000000000000000, -0.000000000000000000, -0.000000000000000000 ) ) ;
#196511=FACE_OUTER_BOUND ( 'NONE', #221593, .T. ) ;
#196535=ADVANCED_FACE ( 'NONE', ( #124454 ), #51159, .T. ) ;
#196595=CARTESIAN_POINT ( 'NONE',  ( 23.25000000000000000, -9.599999999988842347, -157.6060308773475640 ) ) ;
#196602=ORIENTED_EDGE ( 'NONE', *, *, #140216, .F. ) ;
#196618=CARTESIAN_POINT ( 'NONE',  ( -20.94999999999999929, 11.65000000001115232, -160.7161343370219129 ) ) ;
#196631=CIRCLE ( 'NONE', #50877, 0.2000000000000057288 ) ;
#196636=VERTEX_POINT ( 'NONE', #130859 ) ;
#196637=DIRECTION ( 'NONE',  ( 0.000000000000000000, -1.734723475976997999E-14, 1.000000000000000000 ) ) ;
#196638=ADVANCED_FACE ( 'NONE', ( #10931 ), #189567, .F. ) ;
#196748=TOROIDAL_SURFACE ( 'NONE', #176126, 11.65000000000000036, 0.1000000000000000056 ) ;
#196756=ORIENTED_EDGE ( 'NONE', *, *, #124144, .F. ) ;
#196757=FACE_OUTER_BOUND ( 'NONE', #159855, .T. ) ;
#196789=CYLINDRICAL_SURFACE ( 'NONE', #53288, 0.09999999999999892308 ) ;
#196854=CARTESIAN_POINT ( 'NONE',  ( -20.94999999999999929, 1.115600667400684642E-11, -167.5000000000000284 ) ) ;
#196867=CIRCLE ( 'NONE', #251018, 0.09999999999999939493 ) ;
#196875=LINE ( 'NONE', #241160, #5625 ) ;
#196897=AXIS2_PLACEMENT_3D ( 'NONE', #255633, #156626, #236117 ) ;
#196909=EDGE_CURVE ( 'NONE', #118509, #27654, #203678, .T. ) ;
#196945=ORIENTED_EDGE ( 'NONE', *, *, #172087, .T. ) ;
#196954=DIRECTION ( 'NONE',  ( 0.000000000000000000, 0.000000000000000000, -1.000000000000000000 ) ) ;
#196961=ORIENTED_EDGE ( 'NONE', *, *, #87305, .F. ) ;
#196992=DIRECTION ( 'NONE',  ( 1.000000000000000000, 0.000000000000000000, 0.000000000000000000 ) ) ;
#197043=ORIENTED_EDGE ( 'NONE', *, *, #222621, .T. ) ;
#197054=EDGE_CURVE ( 'NONE', #113973, #220002, #28940, .T. ) ;
#197060=DIRECTION ( 'NONE',  ( 0.000000000000000000, 0.8660254037844309360, -0.5000000000000134337 ) ) ;
#197074=ORIENTED_EDGE ( 'NONE', *, *, #98701, .T. ) ;
#197076=DIRECTION ( 'NONE',  ( -1.000000000000000000, 0.000000000000000000, 0.000000000000000000 ) ) ;
#197092=ORIENTED_EDGE ( 'NONE', *, *, #178933, .F. ) ;
#197109=ORIENTED_EDGE ( 'NONE', *, *, #99089, .F. ) ;
#197135=TOROIDAL_SURFACE ( 'NONE', #147640, 0.2000000000000000111, 0.1000000000000000056 ) ;
#197139=VERTEX_POINT ( 'NONE', #191850 ) ;
#197180=CIRCLE ( 'NONE', #184707, 3.999999999999999112 ) ;
#197186=CARTESIAN_POINT ( 'NONE',  ( -18.39999999999999858, -9.519327731081281385, -140.9729763765593589 ) ) ;
#197191=MANIFOLD_SOLID_BREP ( 'Stock-MAS-200-1', #157355 ) ;
#197198=ORIENTED_EDGE ( 'NONE', *, *, #170133, .T. ) ;
#197202=CARTESIAN_POINT ( 'NONE',  ( 23.14999999999999858, 3.900000000011155432, -167.5000000000000284 ) ) ;
#197212=CARTESIAN_POINT ( 'NONE',  ( 18.49999999999998934, 19.85039924724470950, -136.2803030578013761 ) ) ;
#197241=AXIS2_PLACEMENT_3D ( 'NONE', #116297, #195842, #53735 ) ;
#197243=EDGE_LOOP ( 'NONE', ( #76400, #19180 ) ) ;
#197286=CARTESIAN_POINT ( 'NONE',  ( 21.04116576186311605, 10.62466307876251292, -146.3285817686277994 ) ) ;
#197302=ADVANCED_FACE ( 'NONE', ( #140831 ), #161697, .F. ) ;
#197309=DIRECTION ( 'NONE',  ( 1.000000000000000000, 0.000000000000000000, 0.000000000000000000 ) ) ;
#197325=ORIENTED_EDGE ( 'NONE', *, *, #58183, .T. ) ;
#197350=CIRCLE ( 'NONE', #89011, 7.800000000000001599 ) ;
#197412=CARTESIAN_POINT ( 'NONE',  ( -20.97625342178436725, 11.60000000083177696, -140.9282032298017953 ) ) ;
#197419=AXIS2_PLACEMENT_3D ( 'NONE', #171559, #210653, #45486 ) ;
#197457=DIRECTION ( 'NONE',  ( -1.000000000000000000, 0.000000000000000000, 0.000000000000000000 ) ) ;
#197476=STYLED_ITEM ( 'NONE', ( #37900 ), #197191 ) ;
#197481=VERTEX_POINT ( 'NONE', #113250 ) ;
#197487=TOROIDAL_SURFACE ( 'NONE', #222408, 2.100000000000002309, 0.1000000000000000056 ) ;
#197489=VECTOR ( 'NONE', #111626, 1000.000000000000000 ) ;
#197539=ORIENTED_EDGE ( 'NONE', *, *, #257998, .T. ) ;
#197567=AXIS2_PLACEMENT_3D ( 'NONE', #130537, #232237, #193099 ) ;
#197577=CYLINDRICAL_SURFACE ( 'NONE', #37769, 0.09999999999998898659 ) ;
#197614=VECTOR ( 'NONE', #150882, 1000.000000000000000 ) ;
#197648=CARTESIAN_POINT ( 'NONE',  ( -21.04386569057595580, 11.75000000001099210, -160.6428373517797752 ) ) ;
#197694=AXIS2_PLACEMENT_3D ( 'NONE', #5242, #240044, #24868 ) ;
#197712=CIRCLE ( 'NONE', #147279, 0.09999999999999939493 ) ;
#197727=VERTEX_POINT ( 'NONE', #113906 ) ;
#197796=CARTESIAN_POINT ( 'NONE',  ( 22.50014994444007499, 11.74971973190328178, -133.9169198432811072 ) ) ;
#197821=TOROIDAL_SURFACE ( 'NONE', #235241, 0.2000000000000000111, 0.1000000000000000056 ) ;
#197831=CARTESIAN_POINT ( 'NONE',  ( -18.59999999999999787, 9.250000000011157297, -155.1500000000000057 ) ) ;
#197835=DIRECTION ( 'NONE',  ( -6.938893903907222067E-15, 1.000000000000000000, 0.000000000000000000 ) ) ;
#197839=EDGE_CURVE ( 'NONE', #194690, #7738, #39498, .T. ) ;
#197840=DIRECTION ( 'NONE',  ( -1.000000000000000000, -0.000000000000000000, -0.000000000000000000 ) ) ;
#197842=AXIS2_PLACEMENT_3D ( 'NONE', #16493, #133850, #111725 ) ;
#197866=EDGE_LOOP ( 'NONE', ( #208595, #226071, #54980 ) ) ;
#197880=VECTOR ( 'NONE', #243516, 1000.000000000000000 ) ;
#197890=CIRCLE ( 'NONE', #110606, 0.1999999999999987899 ) ;
#197902=CARTESIAN_POINT ( 'NONE',  ( 21.14261333020286671, 10.71569264926606202, -146.2500000000002274 ) ) ;
#197914=CARTESIAN_POINT ( 'NONE',  ( 20.94999999999999929, -1.362429037182151470, -175.3888812479212334 ) ) ;
#197920=ORIENTED_EDGE ( 'NONE', *, *, #79017, .F. ) ;
#197939=ORIENTED_EDGE ( 'NONE', *, *, #73247, .F. ) ;
#197956=DIRECTION ( 'NONE',  ( -1.000000000000000000, -0.000000000000000000, 0.000000000000000000 ) ) ;
#197978=ORIENTED_EDGE ( 'NONE', *, *, #57803, .F. ) ;
#197993=PLANE ( 'NONE',  #112202 ) ;
#197999=DIRECTION ( 'NONE',  ( 0.000000000000000000, 0.000000000000000000, -1.000000000000000000 ) ) ;
#198007=AXIS2_PLACEMENT_3D ( 'NONE', #141737, #81732, #3503 ) ;
#198014=FACE_OUTER_BOUND ( 'NONE', #223223, .T. ) ;
#198032=EDGE_CURVE ( 'NONE', #24563, #42426, #163315, .T. ) ;
#198044=CIRCLE ( 'NONE', #252201, 11.65000000000000036 ) ;
#198152=CARTESIAN_POINT ( 'NONE',  ( -20.15000000000000568, 9.291421356248463326, -146.2500000000000284 ) ) ;
#198190=EDGE_CURVE ( 'NONE', #95993, #240051, #214594, .T. ) ;
#198204=FACE_OUTER_BOUND ( 'NONE', #161917, .T. ) ;
#198238=VERTEX_POINT ( 'NONE', #144563 ) ;
#198265=ORIENTED_EDGE ( 'NONE', *, *, #124144, .T. ) ;
#198278=ORIENTED_EDGE ( 'NONE', *, *, #158573, .F. ) ;
#198298=VERTEX_POINT ( 'NONE', #222820 ) ;
#198300=EDGE_LOOP ( 'NONE', ( #192724, #222351, #254079, #59465 ) ) ;
#198306=AXIS2_PLACEMENT_3D ( 'NONE', #145682, #126115, #183549 ) ;
#198308=ORIENTED_EDGE ( 'NONE', *, *, #36981, .T. ) ;
#198321=CARTESIAN_POINT ( 'NONE',  ( -21.05000000000000071, 1.115600667400684642E-11, -138.2999999999999829 ) ) ;
#198330=DIRECTION ( 'NONE',  ( -0.7071067811865475727, -0.7071067811865475727, 0.000000000000000000 ) ) ;
#198352=ORIENTED_EDGE ( 'NONE', *, *, #201004, .F. ) ;
#198371=DIRECTION ( 'NONE',  ( -0.7071067811865388020, 0.7071067811865561215, 0.000000000000000000 ) ) ;
#198377=FACE_OUTER_BOUND ( 'NONE', #249730, .T. ) ;
#198434=DIRECTION ( 'NONE',  ( 0.000000000000000000, -0.8700118002898359348, 0.4930308989875165082 ) ) ;
#198435=ADVANCED_FACE ( 'NONE', ( #162891 ), #2196, .T. ) ;
#198444=DIRECTION ( 'NONE',  ( 0.000000000000000000, 0.000000000000000000, 1.000000000000000000 ) ) ;
#198470=CARTESIAN_POINT ( 'NONE',  ( 23.14999999999999503, 14.10000000001115694, -161.8997023888606748 ) ) ;
#198494=CARTESIAN_POINT ( 'NONE',  ( 20.85000000000000142, -1.149570369564537842, -175.3159124845019790 ) ) ;
#198516=CARTESIAN_POINT ( 'NONE',  ( -18.50000000000000000, -9.399999999988850163, -174.3820418481726904 ) ) ;
#198530=CARTESIAN_POINT ( 'NONE',  ( 20.94999999999999574, 1.250000000011155299, -142.0000000000000284 ) ) ;
#198550=ORIENTED_EDGE ( 'NONE', *, *, #211240, .F. ) ;
#198569=DIRECTION ( 'NONE',  ( 0.000000000000000000, -0.9999631594459056361, -0.008583690987124413183 ) ) ;
#198653=EDGE_LOOP ( 'NONE', ( #98452, #133888, #6950, #216895, #221305 ) ) ;
#198663=ADVANCED_FACE ( 'NONE', ( #135270 ), #89304, .T. ) ;
#198701=AXIS2_PLACEMENT_3D ( 'NONE', #9618, #189560, #10922 ) ;
#198723=DIRECTION ( 'NONE',  ( -0.000000000000000000, -1.000000000000000000, 0.000000000000000000 ) ) ;
#198781=DIRECTION ( 'NONE',  ( -2.578261006436900068E-14, 0.1350103645451904977, -0.9908441862701597991 ) ) ;
#198811=EDGE_CURVE ( 'NONE', #34631, #243100, #181489, .T. ) ;
#198829=EDGE_LOOP ( 'NONE', ( #169068, #95858, #37733, #104704 ) ) ;
#198832=DIRECTION ( 'NONE',  ( 0.000000000000000000, 0.9915357197604973694, -0.1298341882519105928 ) ) ;
#198845=ORIENTED_EDGE ( 'NONE', *, *, #137099, .F. ) ;
#198847=CARTESIAN_POINT ( 'NONE',  ( -18.59999999999999787, -1.736705739456431807, -179.0174225876237415 ) ) ;
#198859=VECTOR ( 'NONE', #30842, 1000.000000000000114 ) ;
#198872=DIRECTION ( 'NONE',  ( 0.7070776581709139474, -0.7071359030027652981, -2.453168425935592377E-14 ) ) ;
#198873=CARTESIAN_POINT ( 'NONE',  ( -20.94999999999999929, -1.249999999988843369, -142.0000000000000284 ) ) ;
#198889=VECTOR ( 'NONE', #1605, 1000.000000000000000 ) ;
#198897=ORIENTED_EDGE ( 'NONE', *, *, #79017, .T. ) ;
#198917=EDGE_CURVE ( 'NONE', #241842, #169539, #218021, .T. ) ;
#198925=ORIENTED_EDGE ( 'NONE', *, *, #222121, .T. ) ;
#198942=DIRECTION ( 'NONE',  ( 0.000000000000000000, 0.000000000000000000, 1.000000000000000000 ) ) ;
#198955=ORIENTED_EDGE ( 'NONE', *, *, #218296, .T. ) ;
#198989=EDGE_LOOP ( 'NONE', ( #110986, #30343, #158828, #94059 ) ) ;
#199039=LINE ( 'NONE', #116932, #192671 ) ;
#199077=DIRECTION ( 'NONE',  ( -2.342056488767301376E-15, -0.1350103645451904977, 0.9908441862701596881 ) ) ;
#199091=CARTESIAN_POINT ( 'NONE',  ( 22.49999999999999645, 11.64957080755595520, -133.9000000000000057 ) ) ;
#199094=CARTESIAN_POINT ( 'NONE',  ( -23.15000000000000213, 2.600000000011156054, -147.2246219227621111 ) ) ;
#199178=AXIS2_PLACEMENT_3D ( 'NONE', #74580, #231070, #53688 ) ;
#199180=AXIS2_PLACEMENT_3D ( 'NONE', #99261, #164402, #24909 ) ;
#199199=ORIENTED_EDGE ( 'NONE', *, *, #183415, .T. ) ;
#199209=EDGE_CURVE ( 'NONE', #257284, #41279, #143481, .T. ) ;
#199217=CARTESIAN_POINT ( 'NONE',  ( -18.59999999999999787, -1.736257131586239844, -145.5686523290175387 ) ) ;
#199228=EDGE_LOOP ( 'NONE', ( #3622, #157171, #253619, #33068 ) ) ;
#199251=CARTESIAN_POINT ( 'NONE',  ( -18.59999999999999787, -26.43935341558978891, -152.1415086075074896 ) ) ;
#199253=ORIENTED_EDGE ( 'NONE', *, *, #119450, .T. ) ;
#199268=ORIENTED_EDGE ( 'NONE', *, *, #20852, .T. ) ;
#199284=EDGE_CURVE ( 'NONE', #250075, #126194, #18258, .T. ) ;
#199329=AXIS2_PLACEMENT_3D ( 'NONE', #174968, #194501, #74573 ) ;
#199368=VERTEX_POINT ( 'NONE', #241173 ) ;
#199460=ORIENTED_EDGE ( 'NONE', *, *, #78836, .T. ) ;
#199466=FACE_OUTER_BOUND ( 'NONE', #1799, .T. ) ;
#199514=ADVANCED_FACE ( 'NONE', ( #89770 ), #204585, .F. ) ;
#199517=FACE_OUTER_BOUND ( 'NONE', #251153, .T. ) ;
#199518=DIRECTION ( 'NONE',  ( 0.000000000000000000, 0.000000000000000000, 1.000000000000000000 ) ) ;
#199531=ORIENTED_EDGE ( 'NONE', *, *, #102325, .F. ) ;
#199539=DIRECTION ( 'NONE',  ( 0.000000000000000000, 0.000000000000000000, 1.000000000000000000 ) ) ;
#199545=EDGE_CURVE ( 'NONE', #137609, #128950, #152062, .T. ) ;
#199561=CARTESIAN_POINT ( 'NONE',  ( 20.93975676684922504, 10.31104185824063535, -173.0204516983106089 ) ) ;
#199592=DIRECTION ( 'NONE',  ( 0.000000000000000000, 0.000000000000000000, 1.000000000000000000 ) ) ;
#199599=ORIENTED_EDGE ( 'NONE', *, *, #90479, .T. ) ;
#199604=CARTESIAN_POINT ( 'NONE',  ( -21.05000000000000071, 1.116121084443477685E-11, -136.9000000000000057 ) ) ;
#199619=ORIENTED_EDGE ( 'NONE', *, *, #182810, .F. ) ;
#199621=EDGE_LOOP ( 'NONE', ( #36731, #178715, #43824, #182975 ) ) ;
#199630=CARTESIAN_POINT ( 'NONE',  ( -21.52071067811865746, 7.779289321892505882, -146.3500000000000227 ) ) ;
#199696=EDGE_CURVE ( 'NONE', #42010, #159384, #143835, .T. ) ;
#199714=CARTESIAN_POINT ( 'NONE',  ( -23.25000000000000000, 5.950000000011167245, -157.1942976949652007 ) ) ;
#199715=ORIENTED_EDGE ( 'NONE', *, *, #219274, .F. ) ;
#199765=AXIS2_PLACEMENT_3D ( 'NONE', #214736, #115645, #195211 ) ;
#199781=ADVANCED_FACE ( 'NONE', ( #79186 ), #227234, .F. ) ;
#199813=ADVANCED_FACE ( 'NONE', ( #221261 ), #161326, .T. ) ;
#199825=EDGE_CURVE ( 'NONE', #104663, #130320, #118929, .T. ) ;
#199909=VERTEX_POINT ( 'NONE', #29534 ) ;
#199963=CIRCLE ( 'NONE', #45823, 4.149999999999999467 ) ;
#199966=ORIENTED_EDGE ( 'NONE', *, *, #185596, .T. ) ;
#199969=CYLINDRICAL_SURFACE ( 'NONE', #90760, 0.5000000000000004441 ) ;
#199989=DIRECTION ( 'NONE',  ( -0.7071067811865474617, -0.7071067811865474617, -0.000000000000000000 ) ) ;
#200029=EDGE_LOOP ( 'NONE', ( #198550, #238882, #31157, #16393 ) ) ;
#200034=( NAMED_UNIT ( * ) SI_UNIT ( $, .STERADIAN. ) SOLID_ANGLE_UNIT ( ) );
#200048=ORIENTED_EDGE ( 'NONE', *, *, #179235, .T. ) ;
#200057=CARTESIAN_POINT ( 'NONE',  ( 23.24999999999999645, 5.600000000011153389, -122.2500000000000284 ) ) ;
#200122=ORIENTED_EDGE ( 'NONE', *, *, #47769, .T. ) ;
#200162=LINE ( 'NONE', #154638, #122546 ) ;
#200166=ORIENTED_EDGE ( 'NONE', *, *, #249286, .T. ) ;
#200169=DIRECTION ( 'NONE',  ( 0.7071359030027680737, 0.7070776581709111719, 0.000000000000000000 ) ) ;
#200174=CARTESIAN_POINT ( 'NONE',  ( -18.59999999999999787, 11.65000000001115232, -141.0148057706540214 ) ) ;
#200191=CIRCLE ( 'NONE', #87742, 0.5000000000000004441 ) ;
#200194=AXIS2_PLACEMENT_3D ( 'NONE', #222792, #159019, #101542 ) ;
#200207=LINE ( 'NONE', #195091, #208802 ) ;
#200209=AXIS2_PLACEMENT_3D ( 'NONE', #125354, #7980, #26261 ) ;
#200218=ORIENTED_EDGE ( 'NONE', *, *, #127661, .F. ) ;
#200309=ORIENTED_EDGE ( 'NONE', *, *, #60838, .F. ) ;
#200314=LINE ( 'NONE', #106318, #61420 ) ;
#200319=DIRECTION ( 'NONE',  ( 0.000000000000000000, 0.000000000000000000, -1.000000000000000000 ) ) ;
#200320=DIRECTION ( 'NONE',  ( 1.000000000000000000, -0.000000000000000000, -0.000000000000000000 ) ) ;
#200325=CARTESIAN_POINT ( 'NONE',  ( -21.05000000000000071, -0.01771943329720805649, -127.5589153115293186 ) ) ;
#200356=CARTESIAN_POINT ( 'NONE',  ( -18.40000000000000213, -9.499999999988851584, -141.0320693966996828 ) ) ;
#200384=CIRCLE ( 'NONE', #121313, 0.5000000000000004441 ) ;
#200402=CARTESIAN_POINT ( 'NONE',  ( 21.00023020733438628, 6.390869245278875788, -134.0000000000000000 ) ) ;
#200413=CARTESIAN_POINT ( 'NONE',  ( -21.55000000000000426, 7.750000000011159074, -155.2500000000000284 ) ) ;
#200425=ORIENTED_EDGE ( 'NONE', *, *, #148646, .F. ) ;
#200427=CARTESIAN_POINT ( 'NONE',  ( 20.94999999999999929, 4.850467289730772791, -146.0342674090016999 ) ) ;
#200440=DIRECTION ( 'NONE',  ( 2.952720810173289112E-16, -1.000000000000000000, 0.000000000000000000 ) ) ;
#200443=CARTESIAN_POINT ( 'NONE',  ( 19.92426406871192412, 11.75000000001116085, -158.8500000000000227 ) ) ;
#200447=VERTEX_POINT ( 'NONE', #112600 ) ;
#200460=EDGE_CURVE ( 'NONE', #172429, #44452, #231719, .T. ) ;
#200512=CARTESIAN_POINT ( 'NONE',  ( 22.44352723754029810, 0.009277095054436620969, -122.3502786546513050 ) ) ;
#200528=LINE ( 'NONE', #257882, #228045 ) ;
#200535=VERTEX_POINT ( 'NONE', #94299 ) ;
#200543=CARTESIAN_POINT ( 'NONE',  ( -23.25000000000000000, 11.75000000001115552, -155.3500000000000227 ) ) ;
#200545=ORIENTED_EDGE ( 'NONE', *, *, #53738, .T. ) ;
#200599=CIRCLE ( 'NONE', #88134, 0.09999999999999939493 ) ;
#200654=VERTEX_POINT ( 'NONE', #166832 ) ;
#200694=CARTESIAN_POINT ( 'NONE',  ( 21.05000000000000071, 5.400000000011154988, -146.4052660189131245 ) ) ;
#200725=ORIENTED_EDGE ( 'NONE', *, *, #55536, .F. ) ;
#200740=ADVANCED_FACE ( 'NONE', ( #74146 ), #235974, .T. ) ;
#200767=CARTESIAN_POINT ( 'NONE',  ( 23.14999999999999503, 11.75000000001116263, -160.4851942293460638 ) ) ;
#200778=CARTESIAN_POINT ( 'NONE',  ( -18.50000000000000000, -1.736257131586239844, -145.5686523290175387 ) ) ;
#200830=DIRECTION ( 'NONE',  ( 0.000000000000000000, -1.000000000000000000, 0.000000000000000000 ) ) ;
#200841=ORIENTED_EDGE ( 'NONE', *, *, #128612, .F. ) ;
#200849=DIRECTION ( 'NONE',  ( 1.000000000000000000, 0.000000000000000000, 0.000000000000000000 ) ) ;
#200852=VERTEX_POINT ( 'NONE', #50357 ) ;
#200858=DIRECTION ( 'NONE',  ( 0.000000000000000000, 0.000000000000000000, -1.000000000000000000 ) ) ;
#200869=ORIENTED_EDGE ( 'NONE', *, *, #248597, .F. ) ;
#200873=EDGE_CURVE ( 'NONE', #142216, #208289, #110352, .T. ) ;
#200875=ORIENTED_EDGE ( 'NONE', *, *, #201077, .F. ) ;
#200903=AXIS2_PLACEMENT_3D ( 'NONE', #137981, #100128, #136705 ) ;
#200907=DIRECTION ( 'NONE',  ( 0.000000000000000000, 1.000000000000000000, 0.000000000000000000 ) ) ;
#200929=CIRCLE ( 'NONE', #21865, 0.09999999999999939493 ) ;
#200942=CYLINDRICAL_SURFACE ( 'NONE', #207871, 0.09999999999999939493 ) ;
#200946=DIRECTION ( 'NONE',  ( 0.000000000000000000, 0.9908441862701600211, -0.1350103645451876666 ) ) ;
#200949=CARTESIAN_POINT ( 'NONE',  ( -22.39999999999999858, -0.09999999998884338825, -122.3504291924552234 ) ) ;
#200981=CIRCLE ( 'NONE', #230010, 0.09999999999998898659 ) ;
#201004=EDGE_CURVE ( 'NONE', #256904, #12568, #132491, .T. ) ;
#201008=TOROIDAL_SURFACE ( 'NONE', #251043, 0.2000000000000000111, 0.1000000000000000056 ) ;
#201029=VERTEX_POINT ( 'NONE', #115486 ) ;
#201038=CARTESIAN_POINT ( 'NONE',  ( -22.44366136229477249, 0.009341569497225218552, -122.3502814425261107 ) ) ;
#201040=ORIENTED_EDGE ( 'NONE', *, *, #202191, .F. ) ;
#201042=LINE ( 'NONE', #22433, #185853 ) ;
#201044=DIRECTION ( 'NONE',  ( 0.000000000000000000, 0.9908441862701600211, -0.1350103645451876666 ) ) ;
#201064=CARTESIAN_POINT ( 'NONE',  ( -18.59999999999999787, 9.350000000011156942, -146.1500000000000341 ) ) ;
#201074=CYLINDRICAL_SURFACE ( 'NONE', #126212, 0.09999999999999939493 ) ;
#201077=EDGE_CURVE ( 'NONE', #44736, #231425, #98747, .T. ) ;
#201085=CARTESIAN_POINT ( 'NONE',  ( 20.96428641294273021, 11.75000000001150013, -160.6748931779423231 ) ) ;
#201099=ORIENTED_EDGE ( 'NONE', *, *, #244732, .T. ) ;
#201114=AXIS2_PLACEMENT_3D ( 'NONE', #59790, #58513, #18126 ) ;
#201121=CARTESIAN_POINT ( 'NONE',  ( 23.14999999999999503, 6.450000000011156587, -122.2500000000000284 ) ) ;
#201130=ORIENTED_EDGE ( 'NONE', *, *, #33269, .F. ) ;
#201135=CARTESIAN_POINT ( 'NONE',  ( -21.05000000000000071, -1.261786168553869603, -142.0864989635454947 ) ) ;
#201179=ORIENTED_EDGE ( 'NONE', *, *, #130895, .T. ) ;
#201192=VECTOR ( 'NONE', #230295, 1000.000000000000000 ) ;
#201234=LINE ( 'NONE', #240380, #131320 ) ;
#201236=DIRECTION ( 'NONE',  ( 0.000000000000000000, 0.000000000000000000, 1.000000000000000000 ) ) ;
#201315=CARTESIAN_POINT ( 'NONE',  ( 21.05000000000000071, 6.540656951712400691, -134.1000000000000227 ) ) ;
#201329=DIRECTION ( 'NONE',  ( -0.000000000000000000, 0.000000000000000000, -1.000000000000000000 ) ) ;
#201334=SPHERICAL_SURFACE ( 'NONE', #99910, 0.1000000000000000056 ) ;
#201335=VECTOR ( 'NONE', #63800, 1000.000000000000000 ) ;
#201342=FACE_OUTER_BOUND ( 'NONE', #39878, .T. ) ;
#201353=AXIS2_PLACEMENT_3D ( 'NONE', #188345, #111380, #70997 ) ;
#201361=LINE ( 'NONE', #125676, #250520 ) ;
#201370=DIRECTION ( 'NONE',  ( 1.000000000000000000, 7.304098846218134667E-16, -0.000000000000000000 ) ) ;
#201376=CIRCLE ( 'NONE', #143100, 2.000000000000001776 ) ;
#201383=ORIENTED_EDGE ( 'NONE', *, *, #160958, .T. ) ;
#201391=ORIENTED_EDGE ( 'NONE', *, *, #216933, .T. ) ;
#201411=CIRCLE ( 'NONE', #251479, 0.09999999999998898659 ) ;
#201412=EDGE_LOOP ( 'NONE', ( #11596, #88425, #138955, #39301 ) ) ;
#201417=CARTESIAN_POINT ( 'NONE',  ( 21.14999999999999858, 11.65000000001116298, -122.2500000000000284 ) ) ;
#201429=ORIENTED_EDGE ( 'NONE', *, *, #41408, .T. ) ;
#201439=LINE ( 'NONE', #198873, #13044 ) ;
#201444=EDGE_LOOP ( 'NONE', ( #102870, #42948 ) ) ;
#201445=DIRECTION ( 'NONE',  ( -1.000000000000000000, -0.000000000000000000, 0.000000000000000000 ) ) ;
#201451=FACE_OUTER_BOUND ( 'NONE', #104251, .T. ) ;
#201484=ORIENTED_EDGE ( 'NONE', *, *, #98942, .T. ) ;
#201497=AXIS2_PLACEMENT_3D ( 'NONE', #19569, #161662, #144622 ) ;
#201503=AXIS2_PLACEMENT_3D ( 'NONE', #160569, #122723, #60139 ) ;
#201555=ORIENTED_EDGE ( 'NONE', *, *, #38950, .T. ) ;
#201561=ORIENTED_EDGE ( 'NONE', *, *, #230608, .F. ) ;
#201569=DIRECTION ( 'NONE',  ( 0.000000000000000000, 0.000000000000000000, -1.000000000000000000 ) ) ;
#201574=CARTESIAN_POINT ( 'NONE',  ( 20.95568717954149562, 10.60199405390297400, -141.6025083682686727 ) ) ;
#201600=CARTESIAN_POINT ( 'NONE',  ( -21.04999999999999716, -0.01465611850265158278, -127.5033134142315987 ) ) ;
#201613=EDGE_LOOP ( 'NONE', ( #7668, #158725 ) ) ;
#201631=ADVANCED_FACE ( 'NONE', ( #185212 ), #199969, .F. ) ;
#201649=CARTESIAN_POINT ( 'NONE',  ( -18.52309608778520200, -9.642476320044035987, -174.2145963411697096 ) ) ;
#201650=CARTESIAN_POINT ( 'NONE',  ( 20.94999999999999929, 1.835341550235569663, -145.5551512925629822 ) ) ;
#201651=CARTESIAN_POINT ( 'NONE',  ( 21.14999999999999503, 11.65000000001116298, -134.1000000000000227 ) ) ;
#201654=CIRCLE ( 'NONE', #105952, 11.75000000000001066 ) ;
#201675=CARTESIAN_POINT ( 'NONE',  ( 21.07016717456945187, 6.320940838111423155, -134.0000000000000000 ) ) ;
#201693=AXIS2_PLACEMENT_3D ( 'NONE', #184579, #89320, #165024 ) ;
#201705=CARTESIAN_POINT ( 'NONE',  ( 20.94999999999999929, 6.846123162363745074, -171.2377262668498759 ) ) ;
#201727=VERTEX_POINT ( 'NONE', #191665 ) ;
#201744=DIRECTION ( 'NONE',  ( -1.000000000000000000, 7.304098846218134667E-16, 2.111765289898285610E-31 ) ) ;
#201755=CARTESIAN_POINT ( 'NONE',  ( 21.12769345151713196, 10.71928767695172624, -146.2474803461975057 ) ) ;
#201760=DIRECTION ( 'NONE',  ( 0.000000000000000000, 0.000000000000000000, 1.000000000000000000 ) ) ;
#201779=CARTESIAN_POINT ( 'NONE',  ( 20.97224591636399538, 10.62515341617478271, -146.2499259046635984 ) ) ;
#201856=DIRECTION ( 'NONE',  ( 1.000000000000000000, 2.952720810173289112E-16, -0.000000000000000000 ) ) ;
#201904=EDGE_LOOP ( 'NONE', ( #31121, #71393, #206273, #143918 ) ) ;
#201906=DIRECTION ( 'NONE',  ( 0.000000000000000000, 0.000000000000000000, 1.000000000000000000 ) ) ;
#201988=CARTESIAN_POINT ( 'NONE',  ( -23.25000000000000000, -1.835859311432481045, -179.0044391687985410 ) ) ;
#202014=DIRECTION ( 'NONE',  ( 0.000000000000000000, 0.000000000000000000, -1.000000000000000000 ) ) ;
#202016=DIRECTION ( 'NONE',  ( 1.000000000000000000, 0.000000000000000000, 0.000000000000000000 ) ) ;
#202069=LINE ( 'NONE', #200778, #253225 ) ;
#202095=EDGE_CURVE ( 'NONE', #159233, #180230, #157648, .T. ) ;
#202096=DIRECTION ( 'NONE',  ( 0.000000000000000000, 7.993605777301153912E-15, 1.000000000000000000 ) ) ;
#202101=EDGE_LOOP ( 'NONE', ( #147741, #243791, #217076, #242720 ) ) ;
#202123=EDGE_LOOP ( 'NONE', ( #72957, #114959, #209930, #251605 ) ) ;
#202152=CARTESIAN_POINT ( 'NONE',  ( -18.59999999999999787, 7.021664781911246322, -171.3335654018973173 ) ) ;
#202161=EDGE_LOOP ( 'NONE', ( #30234, #218867, #133230, #54683 ) ) ;
#202165=EDGE_LOOP ( 'NONE', ( #58242, #257447, #84440, #210326 ) ) ;
#202191=EDGE_CURVE ( 'NONE', #212047, #101749, #170125, .T. ) ;
#202213=FACE_OUTER_BOUND ( 'NONE', #89411, .T. ) ;
#202216=ORIENTED_EDGE ( 'NONE', *, *, #93877, .T. ) ;
#202219=ADVANCED_FACE ( 'NONE', ( #227877 ), #89634, .F. ) ;
#202237=DIRECTION ( 'NONE',  ( 0.000000000000000000, 0.000000000000000000, 1.000000000000000000 ) ) ;
#202268=DIRECTION ( 'NONE',  ( -0.000000000000000000, -0.000000000000000000, 1.000000000000000000 ) ) ;
#202283=CARTESIAN_POINT ( 'NONE',  ( -21.14999999999999858, 1.115600667400684642E-11, -127.7414213562373106 ) ) ;
#202293=ORIENTED_EDGE ( 'NONE', *, *, #132824, .F. ) ;
#202316=TOROIDAL_SURFACE ( 'NONE', #144037, 7.800000000000000711, 0.1000000000000000056 ) ;
#202319=CARTESIAN_POINT ( 'NONE',  ( -22.49917693094574389, 0.08522996423282774847, -122.3502042154693612 ) ) ;
#202323=CARTESIAN_POINT ( 'NONE',  ( 20.85000000000000142, 1.115600667400684642E-11, -175.3000000000000398 ) ) ;
#202325=CARTESIAN_POINT ( 'NONE',  ( 21.04999999999999716, 10.50253167713776392, -141.5588298170757184 ) ) ;
#202365=FACE_OUTER_BOUND ( 'NONE', #132500, .T. ) ;
#202369=AXIS2_PLACEMENT_3D ( 'NONE', #59664, #21857, #2267 ) ;
#202422=ADVANCED_FACE ( 'NONE', ( #145445 ), #122479, .T. ) ;
#202470=FACE_OUTER_BOUND ( 'NONE', #147382, .T. ) ;
#202472=EDGE_CURVE ( 'NONE', #154148, #149376, #232828, .T. ) ;
#202476=DIRECTION ( 'NONE',  ( 0.000000000000000000, -0.8660254037844459241, -0.4999999999999873990 ) ) ;
#202491=CYLINDRICAL_SURFACE ( 'NONE', #102203, 0.09999999999999939493 ) ;
#202501=AXIS2_PLACEMENT_3D ( 'NONE', #156695, #35469, #155417 ) ;
#202503=ORIENTED_EDGE ( 'NONE', *, *, #70853, .T. ) ;
#202526=SPHERICAL_SURFACE ( 'NONE', #218280, 0.1000000000000000056 ) ;
#202544=CARTESIAN_POINT ( 'NONE',  ( 20.97438252431638972, 8.925423506087151182, -142.4723706890108303 ) ) ;
#202555=DIRECTION ( 'NONE',  ( 0.000000000000000000, 0.000000000000000000, -1.000000000000000000 ) ) ;
#202565=EDGE_CURVE ( 'NONE', #157661, #141295, #82733, .T. ) ;
#202646=DIRECTION ( 'NONE',  ( 0.000000000000000000, 0.2605042016806715099, 0.9654727137038706664 ) ) ;
#202658=VERTEX_POINT ( 'NONE', #177879 ) ;
#202702=DIRECTION ( 'NONE',  ( 0.000000000000000000, 0.000000000000000000, -1.000000000000000000 ) ) ;
#202743=DIRECTION ( 'NONE',  ( 1.000000000000000000, 0.000000000000000000, 0.000000000000000000 ) ) ;
#202751=ORIENTED_EDGE ( 'NONE', *, *, #119203, .F. ) ;
#202766=VECTOR ( 'NONE', #64542, 1000.000000000000000 ) ;
#202799=VERTEX_POINT ( 'NONE', #112467 ) ;
#202808=CARTESIAN_POINT ( 'NONE',  ( -20.85000000000000142, -11.64999999998884483, -167.5000000000000284 ) ) ;
#202815=AXIS2_PLACEMENT_3D ( 'NONE', #171231, #233735, #211601 ) ;
#202848=DIRECTION ( 'NONE',  ( 1.000000000000000000, 3.265361837132813093E-16, -0.000000000000000000 ) ) ;
#202861=DIRECTION ( 'NONE',  ( 0.000000000000000000, 0.000000000000000000, 1.000000000000000000 ) ) ;
#202910=DIRECTION ( 'NONE',  ( -1.000000000000000000, -3.265361837132813093E-16, 0.000000000000000000 ) ) ;
#202932=CARTESIAN_POINT ( 'NONE',  ( -18.46154800491012082, -9.480206274230850383, -174.1574508383815214 ) ) ;
#202957=AXIS2_PLACEMENT_3D ( 'NONE', #222786, #104119, #123715 ) ;
#202967=CARTESIAN_POINT ( 'NONE',  ( -21.55000000000000426, 7.708578643773852157, -155.2500000000000284 ) ) ;
#202992=CARTESIAN_POINT ( 'NONE',  ( 20.94999999999999929, 1.115600667400684642E-11, -167.5000000000000284 ) ) ;
#203005=VERTEX_POINT ( 'NONE', #97997 ) ;
#203023=CARTESIAN_POINT ( 'NONE',  ( -23.25000000000000000, 1.115600667400684642E-11, -138.1500000000000057 ) ) ;
#203041=CARTESIAN_POINT ( 'NONE',  ( -22.39999999999999858, 1.115600667400684642E-11, -133.9000000000000057 ) ) ;
#203044=DIRECTION ( 'NONE',  ( 0.000000000000000000, 0.000000000000000000, -1.000000000000000000 ) ) ;
#203050=EDGE_CURVE ( 'NONE', #160572, #197727, #178889, .T. ) ;
#203056=ORIENTED_EDGE ( 'NONE', *, *, #127990, .F. ) ;
#203059=EDGE_CURVE ( 'NONE', #199909, #141516, #166381, .T. ) ;
#203064=AXIS2_PLACEMENT_3D ( 'NONE', #11142, #95786, #93231 ) ;
#203065=CARTESIAN_POINT ( 'NONE',  ( 21.08489834409762054, 10.62232389474667293, -146.3499999999999659 ) ) ;
#203070=CARTESIAN_POINT ( 'NONE',  ( 22.48508240969612615, 0.04627641452807085970, -122.3499892684264552 ) ) ;
#203107=ORIENTED_EDGE ( 'NONE', *, *, #145470, .T. ) ;
#203110=DIRECTION ( 'NONE',  ( 0.000000000000000000, 0.000000000000000000, 1.000000000000000000 ) ) ;
#203125=ORIENTED_EDGE ( 'NONE', *, *, #245753, .T. ) ;
#203135=CIRCLE ( 'NONE', #107467, 0.09999999999998898659 ) ;
#203151=DIRECTION ( 'NONE',  ( 0.000000000000000000, -0.1350103645451876944, 0.9908441862701601321 ) ) ;
#203158=DIRECTION ( 'NONE',  ( -1.000000000000000000, -0.000000000000000000, 0.000000000000000000 ) ) ;
#203176=CARTESIAN_POINT ( 'NONE',  ( -18.50000000000000000, 7.021664781911246322, -171.1335654018973003 ) ) ;
#203184=CIRCLE ( 'NONE', #53166, 0.09999999999998898659 ) ;
#203229=DIRECTION ( 'NONE',  ( 0.000000000000000000, 0.000000000000000000, -1.000000000000000000 ) ) ;
#203242=CARTESIAN_POINT ( 'NONE',  ( -21.95218792049438861, 0.09902843981107177507, -126.7984924387533567 ) ) ;
#203258=EDGE_CURVE ( 'NONE', #18380, #144444, #241381, .T. ) ;
#203291=EDGE_CURVE ( 'NONE', #17738, #142484, #49609, .T. ) ;
#203336=ORIENTED_EDGE ( 'NONE', *, *, #184925, .T. ) ;
#203349=DIRECTION ( 'NONE',  ( 0.000000000000000000, 0.000000000000000000, -1.000000000000000000 ) ) ;
#203373=CARTESIAN_POINT ( 'NONE',  ( 21.05000000000000426, 0.01471785653553484702, -127.6552765959085036 ) ) ;
#203419=EDGE_CURVE ( 'NONE', #217669, #133237, #183116, .T. ) ;
#203440=SPHERICAL_SURFACE ( 'NONE', #212610, 0.1000000000000000056 ) ;
#203475=DIRECTION ( 'NONE',  ( -1.000000000000000000, -3.265361837132813093E-16, 0.000000000000000000 ) ) ;
#203521=DIRECTION ( 'NONE',  ( 0.000000000000000000, 0.1350103645451876666, 0.9908441862701600211 ) ) ;
#203542=EDGE_CURVE ( 'NONE', #47883, #26579, #79016, .T. ) ;
#203603=DIRECTION ( 'NONE',  ( 1.000000000000000000, 0.000000000000000000, 0.000000000000000000 ) ) ;
#203620=AXIS2_PLACEMENT_3D ( 'NONE', #151132, #48159, #32497 ) ;
#203670=VERTEX_POINT ( 'NONE', #29453 ) ;
#203673=CARTESIAN_POINT ( 'NONE',  ( -2.995603634470829482E-16, -11.74999999998884448, -155.2500000000000284 ) ) ;
#203675=CARTESIAN_POINT ( 'NONE',  ( 20.94999999999999929, -11.48912529306489994, -164.6000000000000227 ) ) ;
#203678=LINE ( 'NONE', #124156, #247182 ) ;
#203697=LINE ( 'NONE', #167168, #37970 ) ;
#203698=CARTESIAN_POINT ( 'NONE',  ( -22.39999999999999858, 1.115600667400684642E-11, -126.2092204016266379 ) ) ;
#203772=EDGE_LOOP ( 'NONE', ( #80732, #177269, #88764, #224480 ) ) ;
#203776=DIRECTION ( 'NONE',  ( -1.000000000000000000, -2.952720810173289112E-16, 0.000000000000000000 ) ) ;
#203789=DIRECTION ( 'NONE',  ( -1.000000000000000000, -0.000000000000000000, -0.000000000000000000 ) ) ;
#203796=EDGE_LOOP ( 'NONE', ( #20341, #164703, #117745, #66832 ) ) ;
#203799=ORIENTED_EDGE ( 'NONE', *, *, #68917, .F. ) ;
#203807=CARTESIAN_POINT ( 'NONE',  ( 21.05000000000000071, 0.09779029131994770863, -127.7421853895238968 ) ) ;
#203859=DIRECTION ( 'NONE',  ( 1.000000000000000000, 0.000000000000000000, 0.000000000000000000 ) ) ;
#203865=AXIS2_PLACEMENT_3D ( 'NONE', #59575, #93609, #74080 ) ;
#203906=DIRECTION ( 'NONE',  ( 0.000000000000000000, 0.000000000000000000, 1.000000000000000000 ) ) ;
#203942=CARTESIAN_POINT ( 'NONE',  ( 23.25000000000000000, 11.75000000001116263, -155.3500000000000227 ) ) ;
#203945=ORIENTED_EDGE ( 'NONE', *, *, #130440, .F. ) ;
#204033=ADVANCED_FACE ( 'NONE', ( #57636 ), #207879, .T. ) ;
#204061=CARTESIAN_POINT ( 'NONE',  ( -18.50000000000000000, -1.164121893230052995, -175.2148480855716173 ) ) ;
#204065=DIRECTION ( 'NONE',  ( -1.000000000000000000, 7.304098846218135653E-16, -4.607487905232624742E-31 ) ) ;
#204168=ORIENTED_EDGE ( 'NONE', *, *, #9175, .F. ) ;
#204176=CARTESIAN_POINT ( 'NONE',  ( -21.29999999999995808, 1.115650265596050101E-11, -129.9500000000000171 ) ) ;
#204180=CARTESIAN_POINT ( 'NONE',  ( 23.25000000000000355, -22.45632476061176774, -140.7938984477316353 ) ) ;
#204197=ORIENTED_EDGE ( 'NONE', *, *, #62413, .T. ) ;
#204217=FACE_OUTER_BOUND ( 'NONE', #40191, .T. ) ;
#204220=DIRECTION ( 'NONE',  ( -1.000000000000000000, -0.000000000000000000, 0.000000000000000000 ) ) ;
#204238=CARTESIAN_POINT ( 'NONE',  ( 22.39999999999999858, 7.790779598384538041, -134.0000000000000000 ) ) ;
#204257=ORIENTED_EDGE ( 'NONE', *, *, #2109, .F. ) ;
#204283=DIRECTION ( 'NONE',  ( -3.265361837132813093E-16, 1.000000000000000000, -0.000000000000000000 ) ) ;
#204322=CARTESIAN_POINT ( 'NONE',  ( -20.90851465518106167, 10.32532329027886320, -173.0699343018359855 ) ) ;
#204350=CARTESIAN_POINT ( 'NONE',  ( 23.14999999999999858, 1.115600667400684642E-11, -169.5000000000000284 ) ) ;
#204388=CARTESIAN_POINT ( 'NONE',  ( -21.05000000000000071, 1.835341550235569663, -145.5551512925629822 ) ) ;
#204394=VECTOR ( 'NONE', #177824, 1000.000000000000000 ) ;
#204420=ORIENTED_EDGE ( 'NONE', *, *, #132824, .T. ) ;
#204423=SPHERICAL_SURFACE ( 'NONE', #62790, 0.1000000000000000056 ) ;
#204440=LINE ( 'NONE', #105313, #59646 ) ;
#204573=ORIENTED_EDGE ( 'NONE', *, *, #61683, .F. ) ;
#204585=CYLINDRICAL_SURFACE ( 'NONE', #60446, 11.80000000000000426 ) ;
#204615=CARTESIAN_POINT ( 'NONE',  ( 18.40000000000000568, -9.499999999988844479, -140.9993620971801533 ) ) ;
#204631=CARTESIAN_POINT ( 'NONE',  ( 21.05000000000000071, -0.02138556592653190550, -127.6950388873150075 ) ) ;
#204663=CARTESIAN_POINT ( 'NONE',  ( 23.14999999999999503, 6.650000000011155876, -155.3500000000000227 ) ) ;
#204677=DIRECTION ( 'NONE',  ( -0.000000000000000000, -0.000000000000000000, 1.000000000000000000 ) ) ;
#204692=AXIS2_PLACEMENT_3D ( 'NONE', #7648, #70214, #209696 ) ;
#204712=EDGE_CURVE ( 'NONE', #40935, #45962, #1203, .T. ) ;
#204722=CIRCLE ( 'NONE', #8933, 12.87499999999999822 ) ;
#204723=DIRECTION ( 'NONE',  ( 0.000000000000000000, 0.000000000000000000, -1.000000000000000000 ) ) ;
#204734=EDGE_CURVE ( 'NONE', #52565, #85287, #253987, .T. ) ;
#204736=EDGE_LOOP ( 'NONE', ( #195959, #106640, #174503, #79562 ) ) ;
#204748=DIRECTION ( 'NONE',  ( 0.000000000000000000, 0.000000000000000000, 1.000000000000000000 ) ) ;
#204782=LINE ( 'NONE', #143533, #182497 ) ;
#204790=ORIENTED_EDGE ( 'NONE', *, *, #52959, .F. ) ;
#204791=ORIENTED_EDGE ( 'NONE', *, *, #56481, .F. ) ;
#204794=DIRECTION ( 'NONE',  ( -1.000000000000000000, 0.000000000000000000, 0.000000000000000000 ) ) ;
#204811=EDGE_CURVE ( 'NONE', #200447, #121012, #51885, .T. ) ;
#204820=VERTEX_POINT ( 'NONE', #7660 ) ;
#204821=CARTESIAN_POINT ( 'NONE',  ( 21.14999999999999858, -11.64999999998883595, -134.0000000000000000 ) ) ;
#204827=AXIS2_PLACEMENT_3D ( 'NONE', #231532, #227653, #128571 ) ;
#204836=EDGE_CURVE ( 'NONE', #43656, #202799, #89, .T. ) ;
#204854=CARTESIAN_POINT ( 'NONE',  ( -20.85000000000000142, 0.1610488207298751417, -167.2158101556397867 ) ) ;
#204866=ORIENTED_EDGE ( 'NONE', *, *, #133002, .F. ) ;
#204944=DIRECTION ( 'NONE',  ( -1.000000000000000000, -1.836970198721029934E-16, -0.000000000000000000 ) ) ;
#204948=CARTESIAN_POINT ( 'NONE',  ( 20.85000000000000142, -11.64999999998883595, -167.5000000000000284 ) ) ;
#204952=ORIENTED_EDGE ( 'NONE', *, *, #136510, .F. ) ;
#204968=VECTOR ( 'NONE', #17841, 1000.000000000000000 ) ;
#204971=ORIENTED_EDGE ( 'NONE', *, *, #193478, .F. ) ;
#204975=CARTESIAN_POINT ( 'NONE',  ( -21.05000000000000071, 1.851028230152016674, -145.6539132694225032 ) ) ;
#205028=ORIENTED_EDGE ( 'NONE', *, *, #117263, .T. ) ;
#205051=EDGE_CURVE ( 'NONE', #117707, #49547, #180850, .T. ) ;
#205068=PLANE ( 'NONE',  #241834 ) ;
#205077=DIRECTION ( 'NONE',  ( 0.000000000000000000, 0.000000000000000000, -1.000000000000000000 ) ) ;
#205092=CARTESIAN_POINT ( 'NONE',  ( 20.53930447207977039, 8.977148687535430938, -142.4425071415754189 ) ) ;
#205133=CYLINDRICAL_SURFACE ( 'NONE', #69491, 0.09999999999999817368 ) ;
#205134=VERTEX_POINT ( 'NONE', #98692 ) ;
#205157=DIRECTION ( 'NONE',  ( 0.000000000000000000, 0.000000000000000000, -1.000000000000000000 ) ) ;
#205174=CARTESIAN_POINT ( 'NONE',  ( -22.59999970745345976, -0.009356377315856832799, -122.2494867923307993 ) ) ;
#205201=ORIENTED_EDGE ( 'NONE', *, *, #163640, .F. ) ;
#205211=DIRECTION ( 'NONE',  ( 1.000000000000000000, 0.000000000000000000, 0.000000000000000000 ) ) ;
#205242=CARTESIAN_POINT ( 'NONE',  ( 23.14999999999999503, 6.650000000011155876, -146.2500000000000284 ) ) ;
#205256=CIRCLE ( 'NONE', #184419, 0.09999999999999971412 ) ;
#205270=CIRCLE ( 'NONE', #192841, 0.09999999999998898659 ) ;
#205273=EDGE_CURVE ( 'NONE', #217297, #21635, #208422, .T. ) ;
#205277=DIRECTION ( 'NONE',  ( 0.000000000000000000, 0.000000000000000000, 1.000000000000000000 ) ) ;
#205288=CARTESIAN_POINT ( 'NONE',  ( -23.15000000000000213, 1.115600667400684642E-11, -134.0000000000000000 ) ) ;
#205289=ORIENTED_EDGE ( 'NONE', *, *, #115068, .F. ) ;
#205290=DIRECTION ( 'NONE',  ( -1.000000000000000000, 0.000000000000000000, 0.000000000000000000 ) ) ;
#205296=AXIS2_PLACEMENT_3D ( 'NONE', #172610, #231271, #252090 ) ;
#205306=AXIS2_PLACEMENT_3D ( 'NONE', #189536, #74756, #177699 ) ;
#205316=ORIENTED_EDGE ( 'NONE', *, *, #204712, .F. ) ;
#205319=CIRCLE ( 'NONE', #72267, 0.09999999999999939493 ) ;
#205415=CARTESIAN_POINT ( 'NONE',  ( 20.00000000000000355, 11.75000000001116263, -158.6500000000000341 ) ) ;
#205417=VERTEX_POINT ( 'NONE', #571 ) ;
#205420=TOROIDAL_SURFACE ( 'NONE', #109575, 12.97499999999999609, 0.1000000000000000056 ) ;
#205427=CIRCLE ( 'NONE', #242858, 0.09999999999999939493 ) ;
#205444=ADVANCED_FACE ( 'NONE', ( #95816 ), #37913, .T. ) ;
#205445=EDGE_LOOP ( 'NONE', ( #216466, #177833, #148226, #179280, #221858 ) ) ;
#205446=CARTESIAN_POINT ( 'NONE',  ( 20.94999999999999574, 5.900000000011102586, -144.2190997646564483 ) ) ;
#205475=ORIENTED_EDGE ( 'NONE', *, *, #70742, .T. ) ;
#205491=CARTESIAN_POINT ( 'NONE',  ( -18.44232395689728676, -9.552282557040124189, -174.3422519848069783 ) ) ;
#205538=CARTESIAN_POINT ( 'NONE',  ( -20.64999999999999858, -8.730841121484170131, -157.9019252810156786 ) ) ;
#205557=( BOUNDED_CURVE ( )  B_SPLINE_CURVE ( 3, ( #235743, #136636, #160091, #196618 ),
 .UNSPECIFIED., .F., .T. ) 
 B_SPLINE_CURVE_WITH_KNOTS ( ( 4, 4 ),
 ( 3.141592653589793116, 4.712388980384689674 ),
 .UNSPECIFIED. ) 
 CURVE ( )  GEOMETRIC_REPRESENTATION_ITEM ( )  RATIONAL_B_SPLINE_CURVE ( ( 1.000000000000000000, 0.8047378541243649375, 0.8047378541243649375, 1.000000000000000000 ) ) 
 REPRESENTATION_ITEM ( '' )  );
#205568=DIRECTION ( 'NONE',  ( 0.000000000000000000, 0.000000000000000000, -1.000000000000000000 ) ) ;
#205578=DIRECTION ( 'NONE',  ( 0.000000000000000000, 0.000000000000000000, 1.000000000000000000 ) ) ;
#205602=DIRECTION ( 'NONE',  ( 0.000000000000000000, 0.000000000000000000, 1.000000000000000000 ) ) ;
#205606=CARTESIAN_POINT ( 'NONE',  ( -20.89878130938411616, 10.32747123227773045, -173.0774032850249569 ) ) ;
#205610=EDGE_CURVE ( 'NONE', #80694, #245081, #46243, .T. ) ;
#205630=CARTESIAN_POINT ( 'NONE',  ( -20.94999999999999929, -1.261786168553869603, -142.0864989635454947 ) ) ;
#205648=DIRECTION ( 'NONE',  ( -1.000000000000000000, 0.000000000000000000, 0.000000000000000000 ) ) ;
#205668=ORIENTED_EDGE ( 'NONE', *, *, #82790, .F. ) ;
#205676=ADVANCED_FACE ( 'NONE', ( #168713 ), #248200, .T. ) ;
#205721=CARTESIAN_POINT ( 'NONE',  ( -18.39999999999999858, -9.682403433465239573, -174.1568433774127982 ) ) ;
#205727=ORIENTED_EDGE ( 'NONE', *, *, #95693, .F. ) ;
#205728=ORIENTED_EDGE ( 'NONE', *, *, #84445, .T. ) ;
#205732=CARTESIAN_POINT ( 'NONE',  ( 20.94999999999999929, 1.835341550235569663, -145.5551512925629822 ) ) ;
#205734=CARTESIAN_POINT ( 'NONE',  ( 20.85000000000000142, -11.74999999998883560, -164.5000000000000000 ) ) ;
#205738=DIRECTION ( 'NONE',  ( 1.000000000000000000, 3.265361837132813093E-16, -0.000000000000000000 ) ) ;
#205755=ADVANCED_FACE ( 'NONE', ( #176386 ), #255849, .F. ) ;
#205771=AXIS2_PLACEMENT_3D ( 'NONE', #208189, #127352, #8689 ) ;
#205814=EDGE_CURVE ( 'NONE', #136758, #98196, #180205, .T. ) ;
#205815=ORIENTED_EDGE ( 'NONE', *, *, #36357, .T. ) ;
#205835=DIRECTION ( 'NONE',  ( -0.000000000000000000, 0.000000000000000000, -1.000000000000000000 ) ) ;
#205836=DIRECTION ( 'NONE',  ( 0.000000000000000000, -1.000000000000000000, -5.551115123125768187E-14 ) ) ;
#205846=ORIENTED_EDGE ( 'NONE', *, *, #228412, .T. ) ;
#205848=DIRECTION ( 'NONE',  ( -1.000000000000000000, -3.265361837132813093E-16, 0.000000000000000000 ) ) ;
#205857=ORIENTED_EDGE ( 'NONE', *, *, #71657, .F. ) ;
#205873=AXIS2_PLACEMENT_3D ( 'NONE', #61025, #101393, #119749 ) ;
#205905=FACE_OUTER_BOUND ( 'NONE', #22029, .T. ) ;
#205915=ORIENTED_EDGE ( 'NONE', *, *, #53963, .F. ) ;
#205920=FACE_OUTER_BOUND ( 'NONE', #31546, .T. ) ;
#205927=CARTESIAN_POINT ( 'NONE',  ( 21.05000000000000071, -0.08559286335101129461, -127.5863372651308225 ) ) ;
#205946=CARTESIAN_POINT ( 'NONE',  ( -21.45000000000000284, 7.708578643773852157, -146.3500000000000227 ) ) ;
#205961=CARTESIAN_POINT ( 'NONE',  ( -18.50000000000000000, -1.362429037182155023, -175.3888812479212334 ) ) ;
#205969=AXIS2_PLACEMENT_3D ( 'NONE', #247008, #108788, #44976 ) ;
#205997=AXIS2_PLACEMENT_3D ( 'NONE', #206497, #27898, #107387 ) ;
#205998=ADVANCED_FACE ( 'NONE', ( #242739 ), #196748, .T. ) ;
#206027=VECTOR ( 'NONE', #13981, 1000.000000000000000 ) ;
#206030=VERTEX_POINT ( 'NONE', #250452 ) ;
#206035=EDGE_LOOP ( 'NONE', ( #182556, #141213, #204257, #60352 ) ) ;
#206051=VERTEX_POINT ( 'NONE', #49688 ) ;
#206056=DIRECTION ( 'NONE',  ( 0.000000000000000000, 1.000000000000000000, 0.000000000000000000 ) ) ;
#206061=VERTEX_POINT ( 'NONE', #52236 ) ;
#206065=ADVANCED_FACE ( 'NONE', ( #251741 ), #189208, .F. ) ;
#206071=VECTOR ( 'NONE', #202702, 1000.000000000000000 ) ;
#206079=ADVANCED_FACE ( 'NONE', ( #211337 ), #70571, .F. ) ;
#206082=CARTESIAN_POINT ( 'NONE',  ( 18.49999999999999289, 10.20857864377385127, -158.6500000000000057 ) ) ;
#206083=EDGE_LOOP ( 'NONE', ( #2117, #164016, #69527, #2455 ) ) ;
#206097=ORIENTED_EDGE ( 'NONE', *, *, #80459, .T. ) ;
#206136=DIRECTION ( 'NONE',  ( -1.000000000000000000, -7.304098846218133681E-16, 4.217023435051677994E-16 ) ) ;
#206150=VERTEX_POINT ( 'NONE', #215181 ) ;
#206176=CARTESIAN_POINT ( 'NONE',  ( -22.48479450179659977, 0.04699158119804078271, -122.3500015537484131 ) ) ;
#206181=CYLINDRICAL_SURFACE ( 'NONE', #144628, 0.09999999999998898659 ) ;
#206184=CARTESIAN_POINT ( 'NONE',  ( 21.05000000000000071, 8.776282889879928106, -146.1762151410683543 ) ) ;
#206194=ORIENTED_EDGE ( 'NONE', *, *, #18524, .F. ) ;
#206199=DIRECTION ( 'NONE',  ( 0.000000000000000000, 1.000000000000000000, 0.000000000000000000 ) ) ;
#206216=CARTESIAN_POINT ( 'NONE',  ( 21.05000000000000071, 10.48443348965288635, -141.4568058014919245 ) ) ;
#206220=DIRECTION ( 'NONE',  ( 0.000000000000000000, 0.000000000000000000, -1.000000000000000000 ) ) ;
#206223=EDGE_CURVE ( 'NONE', #96734, #198238, #54769, .T. ) ;
#206229=PRODUCT_DEFINITION ( 'UNKNOWN', '', #11353, #45242 ) ;
#206230=DIRECTION ( 'NONE',  ( 0.000000000000000000, 0.000000000000000000, -1.000000000000000000 ) ) ;
#206235=EDGE_LOOP ( 'NONE', ( #31589, #128770, #111047 ) ) ;
#206241=FACE_OUTER_BOUND ( 'NONE', #95252, .T. ) ;
#206245=LINE ( 'NONE', #27645, #216746 ) ;
#206273=ORIENTED_EDGE ( 'NONE', *, *, #75300, .T. ) ;
#206295=ORIENTED_EDGE ( 'NONE', *, *, #60070, .T. ) ;
#206300=ORIENTED_EDGE ( 'NONE', *, *, #161059, .T. ) ;
#206310=DIRECTION ( 'NONE',  ( 1.000000000000000000, 0.000000000000000000, -0.000000000000000000 ) ) ;
#206359=CIRCLE ( 'NONE', #68999, 0.09999999999999971412 ) ;
#206370=DIRECTION ( 'NONE',  ( 0.000000000000000000, 2.891205793294679805E-16, -1.000000000000000000 ) ) ;
#206400=VERTEX_POINT ( 'NONE', #187628 ) ;
#206402=CARTESIAN_POINT ( 'NONE',  ( 20.22894356738451194, 9.278498222849622223, -142.2685229062465169 ) ) ;
#206435=EDGE_LOOP ( 'NONE', ( #133387, #219896, #153943, #232456 ) ) ;
#206481=CARTESIAN_POINT ( 'NONE',  ( -22.39999999999999858, 1.115486826172573664E-11, -122.3504291924552234 ) ) ;
#206497=CARTESIAN_POINT ( 'NONE',  ( 20.94999999999999929, 1.115600667400684642E-11, -167.5000000000000284 ) ) ;
#206534=CARTESIAN_POINT ( 'NONE',  ( 20.94999999999999574, 11.62071067812981795, -160.6315833476590456 ) ) ;
#206587=EDGE_CURVE ( 'NONE', #39562, #42519, #154753, .T. ) ;
#206591=EDGE_LOOP ( 'NONE', ( #12216, #134812, #96000, #86067 ) ) ;
#206595=CIRCLE ( 'NONE', #90060, 3.999999999999999112 ) ;
#206650=DIRECTION ( 'NONE',  ( -0.000000000000000000, -0.000000000000000000, -1.000000000000000000 ) ) ;
#206667=DIRECTION ( 'NONE',  ( 1.000000000000000000, -0.000000000000000000, -0.000000000000000000 ) ) ;
#206690=DIRECTION ( 'NONE',  ( -1.000000000000000000, -7.304098846218134667E-16, 4.217023435051678980E-16 ) ) ;
#206706=CYLINDRICAL_SURFACE ( 'NONE', #32512, 0.09999999999999939493 ) ;
#206708=ORIENTED_EDGE ( 'NONE', *, *, #39337, .F. ) ;
#206731=AXIS2_PLACEMENT_3D ( 'NONE', #80046, #160926, #219583 ) ;
#206743=ORIENTED_EDGE ( 'NONE', *, *, #47547, .F. ) ;
#206757=ADVANCED_FACE ( 'NONE', ( #89152 ), #35648, .T. ) ;
#206758=CARTESIAN_POINT ( 'NONE',  ( 23.15000000000000213, -9.499999999988844479, -157.6060308773475640 ) ) ;
#206776=CARTESIAN_POINT ( 'NONE',  ( 20.93284271247462414, 11.75000000001116085, -160.4851942293460638 ) ) ;
#206787=CARTESIAN_POINT ( 'NONE',  ( 22.60000000000000142, 11.74956712350054744, -133.8991416309013118 ) ) ;
#206789=CARTESIAN_POINT ( 'NONE',  ( -18.33682934331484304, -9.511185591082512047, -174.4056547686735428 ) ) ;
#206796=DIRECTION ( 'NONE',  ( 1.000000000000000000, 0.000000000000000000, 0.000000000000000000 ) ) ;
#206826=CARTESIAN_POINT ( 'NONE',  ( 22.00356870068456061, 9.582273870969723154E-12, -126.7457576382395388 ) ) ;
#206833=EDGE_CURVE ( 'NONE', #226065, #154105, #109110, .T. ) ;
#206834=CARTESIAN_POINT ( 'NONE',  ( -20.64999999999999858, 4.350000000011156054, -146.2500000000000284 ) ) ;
#206837=CIRCLE ( 'NONE', #223569, 0.1000000000000002554 ) ;
#206847=CARTESIAN_POINT ( 'NONE',  ( 21.00000000000000000, 9.750000000011153745, -146.3500000000000227 ) ) ;
#206872=CARTESIAN_POINT ( 'NONE',  ( 18.43630871534866955, -9.679800874791860466, -174.1606320679840394 ) ) ;
#206943=ORIENTED_EDGE ( 'NONE', *, *, #90782, .T. ) ;
#206971=VECTOR ( 'NONE', #190787, 1000.000000000000000 ) ;
#206977=DIRECTION ( 'NONE',  ( 0.000000000000000000, 1.000000000000000000, 0.000000000000000000 ) ) ;
#207014=ORIENTED_EDGE ( 'NONE', *, *, #115068, .T. ) ;
#207023=ORIENTED_EDGE ( 'NONE', *, *, #104114, .T. ) ;
#207053=ORIENTED_EDGE ( 'NONE', *, *, #220098, .T. ) ;
#207055=DIRECTION ( 'NONE',  ( 0.000000000000000000, 0.000000000000000000, -1.000000000000000000 ) ) ;
#207064=ADVANCED_FACE ( 'NONE', ( #163276, #242786 ), #124152, .T. ) ;
#207097=DIRECTION ( 'NONE',  ( 0.000000000000000000, 0.000000000000000000, 1.000000000000000000 ) ) ;
#207138=DIRECTION ( 'NONE',  ( 0.000000000000000000, 0.000000000000000000, 1.000000000000000000 ) ) ;
#207209=VERTEX_POINT ( 'NONE', #159131 ) ;
#207216=CARTESIAN_POINT ( 'NONE',  ( 18.50000000000000000, -9.399999999988823518, -141.2972597596632909 ) ) ;
#207225=DIRECTION ( 'NONE',  ( 1.000000000000000000, 0.000000000000000000, 0.000000000000000000 ) ) ;
#207235=DIRECTION ( 'NONE',  ( 2.659396599871503635E-15, 0.6132151058540549204, -0.7899159663865520375 ) ) ;
#207241=CIRCLE ( 'NONE', #53092, 0.2000000000000057288 ) ;
#207280=DIRECTION ( 'NONE',  ( -0.000000000000000000, -0.000000000000000000, 1.000000000000000000 ) ) ;
#207285=DIRECTION ( 'NONE',  ( 1.000000000000000000, -0.000000000000000000, -0.000000000000000000 ) ) ;
#207304=ORIENTED_EDGE ( 'NONE', *, *, #242156, .T. ) ;
#207306=CIRCLE ( 'NONE', #182357, 0.09999999999999939493 ) ;
#207315=ORIENTED_EDGE ( 'NONE', *, *, #117563, .F. ) ;
#207330=ORIENTED_EDGE ( 'NONE', *, *, #104156, .T. ) ;
#207413=VECTOR ( 'NONE', #246705, 1000.000000000000114 ) ;
#207414=CARTESIAN_POINT ( 'NONE',  ( 21.33487959338958362, 6.725558151922348848, -134.0000000000000000 ) ) ;
#207456=ORIENTED_EDGE ( 'NONE', *, *, #127973, .F. ) ;
#207458=DIRECTION ( 'NONE',  ( 1.000000000000000000, 0.000000000000000000, 0.000000000000000000 ) ) ;
#207477=EDGE_CURVE ( 'NONE', #180058, #182048, #72873, .T. ) ;
#207489=AXIS2_PLACEMENT_3D ( 'NONE', #13935, #256313, #252517 ) ;
#207491=ADVANCED_FACE ( 'NONE', ( #89817 ), #91115, .T. ) ;
#207523=CARTESIAN_POINT ( 'NONE',  ( -21.05000000000000071, 11.65000000001115232, -134.1000000000000227 ) ) ;
#207640=ADVANCED_FACE ( 'NONE', ( #242172 ), #20584, .F. ) ;
#207656=VERTEX_POINT ( 'NONE', #24443 ) ;
#207667=AXIS2_PLACEMENT_3D ( 'NONE', #65398, #224464, #47097 ) ;
#207677=VERTEX_POINT ( 'NONE', #239619 ) ;
#207687=AXIS2_PLACEMENT_3D ( 'NONE', #97981, #257034, #237531 ) ;
#207701=CARTESIAN_POINT ( 'NONE',  ( 20.97107704358301916, 8.875478152032441059, -142.5589732293892951 ) ) ;
#207703=CARTESIAN_POINT ( 'NONE',  ( 20.94999999999999574, -1.835341550213255957, -145.5551512925629822 ) ) ;
#207735=CARTESIAN_POINT ( 'NONE',  ( -20.94999999999999929, -11.48912529306489994, -164.4000000000000057 ) ) ;
#207744=ORIENTED_EDGE ( 'NONE', *, *, #256337, .T. ) ;
#207777=ADVANCED_FACE ( 'NONE', ( #152088 ), #7405, .T. ) ;
#207838=EDGE_LOOP ( 'NONE', ( #79995, #188917, #226940, #33595, #247620 ) ) ;
#207859=CARTESIAN_POINT ( 'NONE',  ( 20.94999999999999929, 10.72371710471867701, -141.6649135690876165 ) ) ;
#207871=AXIS2_PLACEMENT_3D ( 'NONE', #220518, #40630, #197076 ) ;
#207874=EDGE_CURVE ( 'NONE', #41050, #239914, #34680, .T. ) ;
#207879=TOROIDAL_SURFACE ( 'NONE', #187027, 0.2000000000000000111, 0.1000000000000000056 ) ;
#207982=DIRECTION ( 'NONE',  ( 1.000000000000000000, 0.000000000000000000, -0.000000000000000000 ) ) ;
#208009=DIRECTION ( 'NONE',  ( -5.603264701231743991E-32, 1.897661533703520143E-16, -1.000000000000000000 ) ) ;
#208047=CARTESIAN_POINT ( 'NONE',  ( -23.15000000000000213, 11.65000000001115588, -146.1500000000000341 ) ) ;
#208065=FACE_BOUND ( 'NONE', #54393, .T. ) ;
#208087=EDGE_LOOP ( 'NONE', ( #109995, #210670, #13 ) ) ;
#208098=CYLINDRICAL_SURFACE ( 'NONE', #170870, 0.5000000000000004441 ) ;
#208175=DIRECTION ( 'NONE',  ( -0.000000000000000000, 0.000000000000000000, -1.000000000000000000 ) ) ;
#208177=EDGE_LOOP ( 'NONE', ( #173398, #203336, #87311, #17944 ) ) ;
#208187=CARTESIAN_POINT ( 'NONE',  ( -21.44999999999999929, 7.250000000011155521, -146.3500000000000227 ) ) ;
#208189=CARTESIAN_POINT ( 'NONE',  ( -23.15000000000000213, -11.64999999998884483, -164.4000000000000057 ) ) ;
#208197=DIRECTION ( 'NONE',  ( 1.000000000000000000, -0.000000000000000000, -0.000000000000000000 ) ) ;
#208208=CARTESIAN_POINT ( 'NONE',  ( 18.49999999999999645, 1.115600667400684642E-11, -167.5000000000000284 ) ) ;
#208228=CARTESIAN_POINT ( 'NONE',  ( -23.25000000000000000, 11.65000000001115588, -155.2500000000000284 ) ) ;
#208249=DIRECTION ( 'NONE',  ( 1.000000000000000000, -0.000000000000000000, -0.000000000000000000 ) ) ;
#208289=VERTEX_POINT ( 'NONE', #49768 ) ;
#208336=CARTESIAN_POINT ( 'NONE',  ( 23.14999999999999858, 11.65000000001116298, -160.4851942293460922 ) ) ;
#208361=ORIENTED_EDGE ( 'NONE', *, *, #237466, .F. ) ;
#208375=ORIENTED_EDGE ( 'NONE', *, *, #94418, .F. ) ;
#208418=AXIS2_PLACEMENT_3D ( 'NONE', #257382, #13697, #213177 ) ;
#208421=ORIENTED_EDGE ( 'NONE', *, *, #187229, .F. ) ;
#208422=CIRCLE ( 'NONE', #133555, 7.791421356237310469 ) ;
#208439=ORIENTED_EDGE ( 'NONE', *, *, #241667, .F. ) ;
#208443=CARTESIAN_POINT ( 'NONE',  ( 22.49999999999999645, 0.1000000000111554016, -122.3504291924552092 ) ) ;
#208473=FACE_OUTER_BOUND ( 'NONE', #103568, .T. ) ;
#208476=ORIENTED_EDGE ( 'NONE', *, *, #202472, .F. ) ;
#208488=AXIS2_PLACEMENT_3D ( 'NONE', #25687, #127350, #105167 ) ;
#208501=ORIENTED_EDGE ( 'NONE', *, *, #164841, .T. ) ;
#208515=DIRECTION ( 'NONE',  ( 0.000000000000000000, 1.000000000000000000, 0.000000000000000000 ) ) ;
#208549=DIRECTION ( 'NONE',  ( 0.000000000000000000, 0.000000000000000000, -1.000000000000000000 ) ) ;
#208557=VERTEX_POINT ( 'NONE', #56991 ) ;
#208558=AXIS2_PLACEMENT_3D ( 'NONE', #45411, #87086, #188770 ) ;
#208564=ORIENTED_EDGE ( 'NONE', *, *, #10542, .T. ) ;
#208583=CARTESIAN_POINT ( 'NONE',  ( 18.43565242384934066, -9.519327731081286714, -140.9729763765593589 ) ) ;
#208593=CARTESIAN_POINT ( 'NONE',  ( 20.95512820512820440, 8.876151316299271343, -146.1500000000000341 ) ) ;
#208595=ORIENTED_EDGE ( 'NONE', *, *, #84352, .F. ) ;
#208659=( BOUNDED_CURVE ( )  B_SPLINE_CURVE ( 3, ( #133383, #34303, #212914, #209058 ),
 .UNSPECIFIED., .F., .T. ) 
 B_SPLINE_CURVE_WITH_KNOTS ( ( 4, 4 ),
 ( 1.570796326794896558, 3.141592653589793116 ),
 .UNSPECIFIED. ) 
 CURVE ( )  GEOMETRIC_REPRESENTATION_ITEM ( )  RATIONAL_B_SPLINE_CURVE ( ( 1.000000000000000000, 0.8047378541243649375, 0.8047378541243649375, 1.000000000000000000 ) ) 
 REPRESENTATION_ITEM ( '' )  );
#208712=VERTEX_POINT ( 'NONE', #8610 ) ;
#208729=DIRECTION ( 'NONE',  ( -1.000000000000000000, 0.000000000000000000, 0.000000000000000000 ) ) ;
#208746=VERTEX_POINT ( 'NONE', #93808 ) ;
#208763=CARTESIAN_POINT ( 'NONE',  ( 21.13461538461538680, 8.885417037985614996, -146.3500000000000227 ) ) ;
#208774=DIRECTION ( 'NONE',  ( 0.000000000000000000, 0.000000000000000000, 1.000000000000000000 ) ) ;
#208777=DIRECTION ( 'NONE',  ( -4.701977403289178058E-30, 1.734723475976807094E-14, -1.000000000000000000 ) ) ;
#208799=DIRECTION ( 'NONE',  ( -1.000000000000000000, -0.000000000000000000, -0.000000000000000000 ) ) ;
#208802=VECTOR ( 'NONE', #16452, 1000.000000000000000 ) ;
#208855=DIRECTION ( 'NONE',  ( 1.000000000000000000, 0.000000000000000000, 0.000000000000000000 ) ) ;
#208891=CYLINDRICAL_SURFACE ( 'NONE', #240377, 2.000000000000001776 ) ;
#208913=ADVANCED_FACE ( 'NONE', ( #196757 ), #3692, .T. ) ;
#208915=ORIENTED_EDGE ( 'NONE', *, *, #24728, .T. ) ;
#208922=ORIENTED_EDGE ( 'NONE', *, *, #146931, .T. ) ;
#208950=CARTESIAN_POINT ( 'NONE',  ( -21.08479644141222664, 6.345038657743036659, -133.9414455574358556 ) ) ;
#208969=AXIS2_PLACEMENT_3D ( 'NONE', #65323, #50871, #243960 ) ;
#208999=FACE_OUTER_BOUND ( 'NONE', #188453, .T. ) ;
#209001=EDGE_CURVE ( 'NONE', #169538, #94099, #89641, .T. ) ;
#209052=ADVANCED_FACE ( 'NONE', ( #152229 ), #197135, .T. ) ;
#209058=CARTESIAN_POINT ( 'NONE',  ( 18.49999999999999289, 10.20857864377385127, -158.6500000000000057 ) ) ;
#209061=DIRECTION ( 'NONE',  ( 0.000000000000000000, 0.000000000000000000, -1.000000000000000000 ) ) ;
#209182=LINE ( 'NONE', #150508, #234702 ) ;
#209218=EDGE_CURVE ( 'NONE', #214434, #246557, #98592, .T. ) ;
#209237=LINE ( 'NONE', #11045, #168271 ) ;
#209240=DIRECTION ( 'NONE',  ( -1.000000000000000000, -0.000000000000000000, 0.000000000000000000 ) ) ;
#209243=EDGE_CURVE ( 'NONE', #99799, #205134, #180578, .T. ) ;
#209278=ORIENTED_EDGE ( 'NONE', *, *, #164841, .F. ) ;
#209281=CARTESIAN_POINT ( 'NONE',  ( -21.05000000000000071, 5.850000000011108092, -144.1324972242779836 ) ) ;
#209300=EDGE_LOOP ( 'NONE', ( #39322, #1376, #19081, #14691 ) ) ;
#209317=DIRECTION ( 'NONE',  ( 1.000000000000000000, 2.952720810173289112E-16, -0.000000000000000000 ) ) ;
#209345=CARTESIAN_POINT ( 'NONE',  ( 23.14999999999999858, -3.899999999988843502, -167.5000000000000284 ) ) ;
#209364=DIRECTION ( 'NONE',  ( -1.000000000000000000, -3.265361837132813093E-16, 0.000000000000000000 ) ) ;
#209373=EDGE_CURVE ( 'NONE', #140569, #83407, #213457, .T. ) ;
#209421=ORIENTED_EDGE ( 'NONE', *, *, #146931, .F. ) ;
#209434=AXIS2_PLACEMENT_3D ( 'NONE', #203041, #43974, #100069 ) ;
#209435=CARTESIAN_POINT ( 'NONE',  ( 18.39999999999999858, -9.682403433465241349, -174.1568433774127982 ) ) ;
#209457=ORIENTED_EDGE ( 'NONE', *, *, #7426, .F. ) ;
#209463=CARTESIAN_POINT ( 'NONE',  ( 18.59999999999999076, 6.450000000011156587, -144.0170271704400307 ) ) ;
#209468=CARTESIAN_POINT ( 'NONE',  ( -20.91682497891422798, 10.32263460347359363, -173.0605957968672328 ) ) ;
#209518=AXIS2_PLACEMENT_3D ( 'NONE', #116569, #254744, #17461 ) ;
#209543=DIRECTION ( 'NONE',  ( 0.000000000000000000, 1.000000000000000000, -6.308085367188393199E-16 ) ) ;
#209567=DIRECTION ( 'NONE',  ( 0.000000000000000000, 0.1568667991644863147, 0.9876197685951252359 ) ) ;
#209603=DIRECTION ( 'NONE',  ( 0.000000000000000000, 0.000000000000000000, -1.000000000000000000 ) ) ;
#209617=EDGE_LOOP ( 'NONE', ( #205028, #228625, #159241, #158450, #156471, #152341, #94371, #151756, #255635, #183660, #131219 ) ) ;
#209653=CIRCLE ( 'NONE', #217994, 0.09999999999999939493 ) ;
#209674=VECTOR ( 'NONE', #133182, 1000.000000000000000 ) ;
#209688=ADVANCED_FACE ( 'NONE', ( #5303 ), #219238, .F. ) ;
#209696=DIRECTION ( 'NONE',  ( 0.000000000000000000, 0.000000000000000000, -1.000000000000000000 ) ) ;
#209699=CIRCLE ( 'NONE', #168045, 0.09999999999998898659 ) ;
#209706=DIRECTION ( 'NONE',  ( 1.000000000000000000, -0.000000000000000000, -0.000000000000000000 ) ) ;
#209715=CIRCLE ( 'NONE', #122224, 0.09999999999999939493 ) ;
#209723=VERTEX_POINT ( 'NONE', #99281 ) ;
#209745=LINE ( 'NONE', #251432, #20355 ) ;
#209771=CARTESIAN_POINT ( 'NONE',  ( 18.43473516226068298, -9.494942282747075524, -141.0458986833495203 ) ) ;
#209820=CARTESIAN_POINT ( 'NONE',  ( -21.05000000000000426, 6.477046381801004671, -134.1000000000000227 ) ) ;
#209830=CARTESIAN_POINT ( 'NONE',  ( -23.25000000000000000, 1.115600667400684642E-11, -167.5000000000000284 ) ) ;
#209843=EDGE_CURVE ( 'NONE', #21693, #72588, #35054, .T. ) ;
#209845=B_SPLINE_CURVE_WITH_KNOTS ( 'NONE', 3,
 ( #153289, #214496, #16328, #95818, #15041, #175410 ),
 .UNSPECIFIED., .F., .F.,
 ( 4, 2, 4 ),
 ( 0.000000000000000000, 0.0001568709654583421050, 0.0003137419309166842099 ),
 .UNSPECIFIED. ) ;
#209878=DIRECTION ( 'NONE',  ( 0.000000000000000000, -1.000000000000000000, 6.308085367188393199E-16 ) ) ;
#209896=CARTESIAN_POINT ( 'NONE',  ( 20.95512820512820440, 8.876151316299271343, -146.1500000000000341 ) ) ;
#209897=CIRCLE ( 'NONE', #5844, 4.049999999999998934 ) ;
#209900=FACE_OUTER_BOUND ( 'NONE', #129996, .T. ) ;
#209929=EDGE_LOOP ( 'NONE', ( #159543, #57544, #231671, #153363 ) ) ;
#209930=ORIENTED_EDGE ( 'NONE', *, *, #130024, .F. ) ;
#209945=DIRECTION ( 'NONE',  ( 0.000000000000000000, 0.8660254037844352659, -0.5000000000000058842 ) ) ;
#209947=DIRECTION ( 'NONE',  ( 1.000000000000000000, -0.000000000000000000, -0.000000000000000000 ) ) ;
#209995=DIRECTION ( 'NONE',  ( 1.000000000000000000, 0.000000000000000000, 0.000000000000000000 ) ) ;
#210005=EDGE_CURVE ( 'NONE', #257831, #215317, #172164, .T. ) ;
#210017=AXIS2_PLACEMENT_3D ( 'NONE', #19357, #98850, #257906 ) ;
#210019=AXIS2_PLACEMENT_3D ( 'NONE', #156835, #131133, #16038 ) ;
#210033=DIRECTION ( 'NONE',  ( -1.000000000000000000, -3.265361837132813093E-16, 0.000000000000000000 ) ) ;
#210047=CARTESIAN_POINT ( 'NONE',  ( -23.15000000000000213, -11.64999999998884483, -164.4000000000000057 ) ) ;
#210061=DIRECTION ( 'NONE',  ( 1.000000000000000000, 0.000000000000000000, 0.000000000000000000 ) ) ;
#210071=VECTOR ( 'NONE', #53770, 1000.000000000000000 ) ;
#210078=CARTESIAN_POINT ( 'NONE',  ( 21.05000000000000071, 10.72371710471867701, -141.6649135690876165 ) ) ;
#210079=CARTESIAN_POINT ( 'NONE',  ( 21.05000000000000071, 8.815201804577958100, -142.4205374966838633 ) ) ;
#210095=AXIS2_PLACEMENT_3D ( 'NONE', #62210, #218689, #242115 ) ;
#210117=TOROIDAL_SURFACE ( 'NONE', #126893, 0.2000000000000000111, 0.1000000000000000056 ) ;
#210172=CARTESIAN_POINT ( 'NONE',  ( -21.64999999999999858, 7.250000000011148416, -155.1500000000000057 ) ) ;
#210174=CIRCLE ( 'NONE', #39315, 2.000000000000001776 ) ;
#210175=AXIS2_PLACEMENT_3D ( 'NONE', #111616, #191174, #193724 ) ;
#210190=DIRECTION ( 'NONE',  ( 0.000000000000000000, 0.000000000000000000, -1.000000000000000000 ) ) ;
#210214=EDGE_CURVE ( 'NONE', #227883, #163431, #210174, .T. ) ;
#210245=CARTESIAN_POINT ( 'NONE',  ( -21.04999999999999716, -9.599999999988844124, -141.0320693966996828 ) ) ;
#210247=CARTESIAN_POINT ( 'NONE',  ( 21.07928932188134397, 0.09889514566555242248, -127.6714833436067238 ) ) ;
#210267=CARTESIAN_POINT ( 'NONE',  ( 20.97565083910961548, 10.47461740128996510, -141.5779431765885477 ) ) ;
#210274=AXIS2_PLACEMENT_3D ( 'NONE', #103018, #185142, #224256 ) ;
#210278=CARTESIAN_POINT ( 'NONE',  ( -20.95000000000000284, 11.65000000001115232, -160.4851942293460638 ) ) ;
#210315=AXIS2_PLACEMENT_3D ( 'NONE', #140311, #179481, #55621 ) ;
#210316=ORIENTED_EDGE ( 'NONE', *, *, #249016, .F. ) ;
#210326=ORIENTED_EDGE ( 'NONE', *, *, #102024, .F. ) ;
#210372=B_SPLINE_CURVE_WITH_KNOTS ( 'NONE', 3,
 ( #12464, #73727, #68577, #168994, #252320, #91974, #34596, #167697, #50267, #110254 ),
 .UNSPECIFIED., .F., .F.,
 ( 4, 3, 3, 4 ),
 ( 0.000000000000000000, 0.0002000000000008733344, 0.001000000000082982470, 0.001967863649483324578 ),
 .UNSPECIFIED. ) ;
#210384=ADVANCED_FACE ( 'NONE', ( #14032 ), #220707, .T. ) ;
#210440=AXIS2_PLACEMENT_3D ( 'NONE', #123512, #4814, #84321 ) ;
#210466=ORIENTED_EDGE ( 'NONE', *, *, #1643, .F. ) ;
#210476=EDGE_CURVE ( 'NONE', #83171, #180198, #214427, .T. ) ;
#210511=EDGE_LOOP ( 'NONE', ( #250496, #158583, #244415, #85081 ) ) ;
#210540=DIRECTION ( 'NONE',  ( -1.000000000000000000, 0.000000000000000000, 0.000000000000000000 ) ) ;
#210548=DIRECTION ( 'NONE',  ( 0.000000000000000000, 0.000000000000000000, -1.000000000000000000 ) ) ;
#210573=DIRECTION ( 'NONE',  ( 0.000000000000000000, 0.000000000000000000, -1.000000000000000000 ) ) ;
#210616=ORIENTED_EDGE ( 'NONE', *, *, #255932, .F. ) ;
#210621=ORIENTED_EDGE ( 'NONE', *, *, #128232, .F. ) ;
#210635=ADVANCED_FACE ( 'NONE', ( #90663 ), #175380, .F. ) ;
#210641=CARTESIAN_POINT ( 'NONE',  ( -20.05000000000000426, 9.250000000011157297, -155.1500000000000057 ) ) ;
#210653=DIRECTION ( 'NONE',  ( 0.000000000000000000, -0.5907332058517320572, 0.8068669527896995541 ) ) ;
#210663=DIRECTION ( 'NONE',  ( 0.000000000000000000, 0.000000000000000000, 1.000000000000000000 ) ) ;
#210670=ORIENTED_EDGE ( 'NONE', *, *, #184925, .F. ) ;
#210694=EDGE_CURVE ( 'NONE', #91733, #15173, #253123, .T. ) ;
#210707=ADVANCED_FACE ( 'NONE', ( #39718 ), #237885, .F. ) ;
#210722=CARTESIAN_POINT ( 'NONE',  ( 18.54271179734065456, -9.624084290087184357, -174.2409648527008983 ) ) ;
#210725=EDGE_LOOP ( 'NONE', ( #161123, #114252, #64374, #237859, #216080 ) ) ;
#210739=AXIS2_PLACEMENT_3D ( 'NONE', #108247, #187793, #229479 ) ;
#210761=ORIENTED_EDGE ( 'NONE', *, *, #169271, .F. ) ;
#210799=CARTESIAN_POINT ( 'NONE',  ( -23.24999999999999645, -9.599999999988845900, -174.2001893912220680 ) ) ;
#210806=DIRECTION ( 'NONE',  ( 0.000000000000000000, -0.3738317757009718689, 0.9274965247785342815 ) ) ;
#210833=VECTOR ( 'NONE', #255590, 1000.000000000000000 ) ;
#210837=DIRECTION ( 'NONE',  ( 1.000000000000000000, 0.000000000000000000, -0.000000000000000000 ) ) ;
#210876=DIRECTION ( 'NONE',  ( 0.000000000000000000, 0.000000000000000000, 1.000000000000000000 ) ) ;
#210896=LINE ( 'NONE', #94792, #97160 ) ;
#210922=CARTESIAN_POINT ( 'NONE',  ( -21.12757541349819590, 0.005161215820883788274, -127.5266194287484609 ) ) ;
#210923=CARTESIAN_POINT ( 'NONE',  ( 20.94999999999999929, 1.115600667400684642E-11, -167.5000000000000284 ) ) ;
#210957=DIRECTION ( 'NONE',  ( -2.952720810173288619E-16, 1.000000000000000000, 0.000000000000000000 ) ) ;
#210999=ADVANCED_FACE ( 'NONE', ( #152950 ), #232472, .F. ) ;
#211022=CARTESIAN_POINT ( 'NONE',  ( -20.00857864376270001, 9.150000000011157653, -155.1500000000000057 ) ) ;
#211034=EDGE_CURVE ( 'NONE', #91128, #87157, #81312, .T. ) ;
#211043=DIRECTION ( 'NONE',  ( 0.000000000000000000, 0.000000000000000000, 1.000000000000000000 ) ) ;
#211072=FACE_OUTER_BOUND ( 'NONE', #158595, .T. ) ;
#211156=EDGE_CURVE ( 'NONE', #175543, #52387, #77239, .T. ) ;
#211176=VECTOR ( 'NONE', #136585, 1000.000000000000000 ) ;
#211207=ORIENTED_EDGE ( 'NONE', *, *, #121490, .F. ) ;
#211227=ORIENTED_EDGE ( 'NONE', *, *, #163647, .F. ) ;
#211239=ORIENTED_EDGE ( 'NONE', *, *, #66649, .F. ) ;
#211240=EDGE_CURVE ( 'NONE', #160655, #106067, #56551, .T. ) ;
#211249=DIRECTION ( 'NONE',  ( 0.000000000000000000, -0.000000000000000000, 1.000000000000000000 ) ) ;
#211270=DIRECTION ( 'NONE',  ( 0.000000000000000000, 0.000000000000000000, -1.000000000000000000 ) ) ;
#211328=DIRECTION ( 'NONE',  ( 0.000000000000000000, 0.000000000000000000, -1.000000000000000000 ) ) ;
#211337=FACE_OUTER_BOUND ( 'NONE', #129345, .T. ) ;
#211343=CARTESIAN_POINT ( 'NONE',  ( 22.49806830649814060, 11.64988965485023620, -133.9225356836745107 ) ) ;
#211376=CARTESIAN_POINT ( 'NONE',  ( -18.39999999999999858, -9.499999999988849808, -141.0320693966996828 ) ) ;
#211386=CARTESIAN_POINT ( 'NONE',  ( -18.50000000000000000, -9.399999999988850163, -174.4146583429696875 ) ) ;
#211395=CARTESIAN_POINT ( 'NONE',  ( 18.50000000000000000, -9.399999999988843058, -141.2972597596633193 ) ) ;
#211400=CARTESIAN_POINT ( 'NONE',  ( 20.85000000000000142, -1.835859311432481045, -179.0044391687985410 ) ) ;
#211406=CARTESIAN_POINT ( 'NONE',  ( -20.54999999999999716, -8.999999999988844479, -157.6060308773475924 ) ) ;
#211409=CARTESIAN_POINT ( 'NONE',  ( 20.84999999999999432, 7.021664781911246322, -171.3335654018973173 ) ) ;
#211452=CARTESIAN_POINT ( 'NONE',  ( 18.59999999999999076, 1.835341550235567887, -145.6551512925629766 ) ) ;
#211468=CIRCLE ( 'NONE', #70022, 0.09999999999998898659 ) ;
#211489=ORIENTED_EDGE ( 'NONE', *, *, #14862, .F. ) ;
#211491=CIRCLE ( 'NONE', #119338, 0.4000000000000114575 ) ;
#211562=ORIENTED_EDGE ( 'NONE', *, *, #14391, .F. ) ;
#211601=DIRECTION ( 'NONE',  ( 0.000000000000000000, 0.9908441862701782288, -0.1350103645450542456 ) ) ;
#211620=VERTEX_POINT ( 'NONE', #125985 ) ;
#211650=ORIENTED_EDGE ( 'NONE', *, *, #198917, .F. ) ;
#211651=CARTESIAN_POINT ( 'NONE',  ( 23.14999999999999503, 11.65000000001116298, -155.3500000000000227 ) ) ;
#211656=DIRECTION ( 'NONE',  ( 0.000000000000000000, 0.000000000000000000, -1.000000000000000000 ) ) ;
#211669=DIRECTION ( 'NONE',  ( 1.000000000000000000, 0.000000000000000000, 0.000000000000000000 ) ) ;
#211672=DIRECTION ( 'NONE',  ( 1.000000000000000000, 0.000000000000000000, 0.000000000000000000 ) ) ;
#211680=CIRCLE ( 'NONE', #199180, 0.09999999999998807065 ) ;
#211695=AXIS2_PLACEMENT_3D ( 'NONE', #245612, #171258, #248178 ) ;
#211703=LINE ( 'NONE', #73488, #91672 ) ;
#211708=ORIENTED_EDGE ( 'NONE', *, *, #139476, .F. ) ;
#211715=ADVANCED_FACE ( 'NONE', ( #116695 ), #12488, .T. ) ;
#211756=CIRCLE ( 'NONE', #170099, 0.09999999999998898659 ) ;
#211758=VECTOR ( 'NONE', #108967, 999.9999999999998863 ) ;
#211782=ORIENTED_EDGE ( 'NONE', *, *, #145478, .T. ) ;
#211812=DIRECTION ( 'NONE',  ( -1.000000000000000000, 0.000000000000000000, 0.000000000000000000 ) ) ;
#211853=CARTESIAN_POINT ( 'NONE',  ( 20.94999999999999929, 6.650000000011155876, -155.2500000000000284 ) ) ;
#211861=CARTESIAN_POINT ( 'NONE',  ( 20.94999999999999929, 8.876614585098254295, -142.3850804788447135 ) ) ;
#211874=ORIENTED_EDGE ( 'NONE', *, *, #252813, .F. ) ;
#211891=CIRCLE ( 'NONE', #124400, 7.720710678118692272 ) ;
#211910=CARTESIAN_POINT ( 'NONE',  ( 20.94999999999999929, -9.399999999988844834, -157.6060308773475640 ) ) ;
#211911=CYLINDRICAL_SURFACE ( 'NONE', #124390, 11.75000000000001066 ) ;
#211918=DIRECTION ( 'NONE',  ( 0.000000000000000000, 1.000000000000000000, 0.000000000000000000 ) ) ;
#211931=EDGE_LOOP ( 'NONE', ( #81469, #22859, #96283, #162480 ) ) ;
#211932=ORIENTED_EDGE ( 'NONE', *, *, #36589, .F. ) ;
#211934=CARTESIAN_POINT ( 'NONE',  ( -18.55807992284871943, 10.32898536001801304, -173.0826683222764757 ) ) ;
#211943=DIRECTION ( 'NONE',  ( 0.000000000000000000, 0.000000000000000000, -1.000000000000000000 ) ) ;
#211964=DIRECTION ( 'NONE',  ( 1.000000000000000000, 0.000000000000000000, 0.000000000000000000 ) ) ;
#211974=EDGE_CURVE ( 'NONE', #224742, #125106, #219265, .T. ) ;
#212011=VECTOR ( 'NONE', #176418, 1000.000000000000000 ) ;
#212016=ADVANCED_FACE ( 'NONE', ( #121428 ), #118843, .T. ) ;
#212025=LINE ( 'NONE', #35953, #197489 ) ;
#212039=CARTESIAN_POINT ( 'NONE',  ( -22.39999999999999503, 7.790779598384560245, -133.9000000000000057 ) ) ;
#212043=DIRECTION ( 'NONE',  ( 1.000000000000000000, 0.000000000000000000, 0.000000000000000000 ) ) ;
#212047=VERTEX_POINT ( 'NONE', #221746 ) ;
#212051=ORIENTED_EDGE ( 'NONE', *, *, #28306, .F. ) ;
#212055=DIRECTION ( 'NONE',  ( -1.000000000000000000, -2.952720810173289112E-16, 0.000000000000000000 ) ) ;
#212088=DIRECTION ( 'NONE',  ( 0.000000000000000000, 0.000000000000000000, -1.000000000000000000 ) ) ;
#212138=CARTESIAN_POINT ( 'NONE',  ( -23.25000000000000000, 1.115600667400684642E-11, -169.6000000000000227 ) ) ;
#212149=ORIENTED_EDGE ( 'NONE', *, *, #124575, .T. ) ;
#212168=ORIENTED_EDGE ( 'NONE', *, *, #67634, .T. ) ;
#212176=CARTESIAN_POINT ( 'NONE',  ( -21.55000000000000426, 7.708578643773852157, -146.3500000000000227 ) ) ;
#212203=CARTESIAN_POINT ( 'NONE',  ( -21.05000000000000071, 0.03175835306687004034, -127.7411528769171980 ) ) ;
#212295=EDGE_LOOP ( 'NONE', ( #100200, #178814 ) ) ;
#212342=CARTESIAN_POINT ( 'NONE',  ( -20.64999999999999858, 1.115600667400684642E-11, -169.4000000000000625 ) ) ;
#212362=VERTEX_POINT ( 'NONE', #199217 ) ;
#212365=AXIS2_PLACEMENT_3D ( 'NONE', #57075, #234443, #140475 ) ;
#212393=AXIS2_PLACEMENT_3D ( 'NONE', #185377, #208799, #109676 ) ;
#212462=ORIENTED_EDGE ( 'NONE', *, *, #29607, .F. ) ;
#212475=AXIS2_PLACEMENT_3D ( 'NONE', #55612, #218550, #201569 ) ;
#212497=CARTESIAN_POINT ( 'NONE',  ( 21.05000000000000071, 5.000000000011153745, -155.0947339810869323 ) ) ;
#212563=CARTESIAN_POINT ( 'NONE',  ( 20.94999999999999929, -8.999999999988842703, -157.6060308773475640 ) ) ;
#212606=ORIENTED_EDGE ( 'NONE', *, *, #86285, .T. ) ;
#212610=AXIS2_PLACEMENT_3D ( 'NONE', #84724, #88595, #103029 ) ;
#212660=CYLINDRICAL_SURFACE ( 'NONE', #178139, 0.09999999999999939493 ) ;
#212662=DIRECTION ( 'NONE',  ( -1.000000000000000000, -2.952720810173289112E-16, 0.000000000000000000 ) ) ;
#212663=CARTESIAN_POINT ( 'NONE',  ( -18.59999999999999787, -1.835859311432481045, -179.0044391687985410 ) ) ;
#212678=AXIS2_PLACEMENT_3D ( 'NONE', #193108, #14487, #93982 ) ;
#212684=EDGE_CURVE ( 'NONE', #219363, #51801, #32216, .T. ) ;
#212687=CARTESIAN_POINT ( 'NONE',  ( 23.25000000000000000, -11.74999999998883560, -164.4000000000000057 ) ) ;
#212692=ADVANCED_FACE ( 'NONE', ( #89511 ), #150786, .T. ) ;
#212721=CARTESIAN_POINT ( 'NONE',  ( -18.59999999999999787, -1.164121893230052995, -175.4148480855716059 ) ) ;
#212722=EDGE_LOOP ( 'NONE', ( #44560, #110075, #223414, #30273 ) ) ;
#212723=VECTOR ( 'NONE', #45157, 1000.000000000000000 ) ;
#212772=FACE_OUTER_BOUND ( 'NONE', #21512, .T. ) ;
#212776=DIRECTION ( 'NONE',  ( -1.000000000000000000, -0.000000000000000000, 0.000000000000000000 ) ) ;
#212826=AXIS2_PLACEMENT_3D ( 'NONE', #167608, #188425, #25521 ) ;
#212828=EDGE_CURVE ( 'NONE', #16273, #162055, #174072, .T. ) ;
#212843=VERTEX_POINT ( 'NONE', #84031 ) ;
#212858=CIRCLE ( 'NONE', #100393, 0.5000000000000004441 ) ;
#212908=DIRECTION ( 'NONE',  ( 1.000000000000000000, -0.000000000000000000, -0.000000000000000000 ) ) ;
#212914=CARTESIAN_POINT ( 'NONE',  ( 18.49999999999999289, 10.20857864377384239, -158.7671572875253787 ) ) ;
#212938=DIRECTION ( 'NONE',  ( 0.000000000000000000, 0.000000000000000000, -1.000000000000000000 ) ) ;
#212968=ORIENTED_EDGE ( 'NONE', *, *, #132156, .T. ) ;
#212971=CIRCLE ( 'NONE', #154727, 0.09999999999999363565 ) ;
#212996=CARTESIAN_POINT ( 'NONE',  ( 18.59999999999996945, 10.33248238083634440, -173.0948465439131496 ) ) ;
#212997=CARTESIAN_POINT ( 'NONE',  ( 21.09551895715245706, 10.62143732718000244, -146.2371246658989890 ) ) ;
#213021=AXIS2_PLACEMENT_3D ( 'NONE', #82979, #162577, #223800 ) ;
#213053=EDGE_LOOP ( 'NONE', ( #179380, #33949, #14537, #55755 ) ) ;
#213065=DIRECTION ( 'NONE',  ( -0.000000000000000000, 1.000000000000000000, -0.000000000000000000 ) ) ;
#213094=CIRCLE ( 'NONE', #175529, 0.09999999999999939493 ) ;
#213125=AXIS2_PLACEMENT_3D ( 'NONE', #5927, #85449, #165028 ) ;
#213154=ORIENTED_EDGE ( 'NONE', *, *, #6121, .F. ) ;
#213170=DIRECTION ( 'NONE',  ( 1.000000000000000000, 0.000000000000000000, 0.000000000000000000 ) ) ;
#213177=DIRECTION ( 'NONE',  ( 0.000000000000000000, 0.000000000000000000, -1.000000000000000000 ) ) ;
#213198=CARTESIAN_POINT ( 'NONE',  ( 20.94999999999999929, -8.999999999988842703, -158.0060308773475697 ) ) ;
#213209=ORIENTED_EDGE ( 'NONE', *, *, #164502, .F. ) ;
#213244=ORIENTED_EDGE ( 'NONE', *, *, #239965, .F. ) ;
#213276=CARTESIAN_POINT ( 'NONE',  ( 18.60000000000000142, -9.480686695267808162, -174.4411151687578752 ) ) ;
#213278=ORIENTED_EDGE ( 'NONE', *, *, #19503, .F. ) ;
#213304=ORIENTED_EDGE ( 'NONE', *, *, #76428, .F. ) ;
#213310=EDGE_CURVE ( 'NONE', #69302, #106574, #6811, .T. ) ;
#213359=CARTESIAN_POINT ( 'NONE',  ( -21.05000000000000071, 11.60000000001115339, -160.5717967697245285 ) ) ;
#213361=VERTEX_POINT ( 'NONE', #231025 ) ;
#213380=AXIS2_PLACEMENT_3D ( 'NONE', #201064, #4140, #241481 ) ;
#213381=CARTESIAN_POINT ( 'NONE',  ( -21.93340585898186390, 1.115541036281197940E-11, -126.6758529778672369 ) ) ;
#213406=ORIENTED_EDGE ( 'NONE', *, *, #9175, .T. ) ;
#213437=DIRECTION ( 'NONE',  ( 1.000000000000000000, 3.469446951953704435E-14, -2.003086131649669752E-14 ) ) ;
#213438=CARTESIAN_POINT ( 'NONE',  ( 20.95325940946048249, 10.52339007070744614, -141.5644621292400984 ) ) ;
#213449=AXIS2_PLACEMENT_3D ( 'NONE', #154664, #235436, #58074 ) ;
#213457=B_SPLINE_CURVE_WITH_KNOTS ( 'NONE', 3,
 ( #86754, #163757, #102451, #162481, #52449, #3368, #25533, #151601, #31656, #243267, #244557, #111163, #43806, #65934, #106315, #190728, #12086, #184587, #185872 ),
 .UNSPECIFIED., .F., .F.,
 ( 4, 3, 3, 3, 3, 3, 4 ),
 ( -2.000416914663624153E-06, 4.235164736271501695E-22, 4.714008503747322393E-05, 9.979203887779870851E-05, 0.0001372215519229730426, 0.0001635031576221134507, 0.0001900083748504316744 ),
 .UNSPECIFIED. ) ;
#213465=DIRECTION ( 'NONE',  ( 0.000000000000000000, 0.8700118002898321601, -0.4930308989875230030 ) ) ;
#213469=VECTOR ( 'NONE', #50188, 1000.000000000000000 ) ;
#213548=DIRECTION ( 'NONE',  ( 0.000000000000000000, 0.000000000000000000, -1.000000000000000000 ) ) ;
#213564=LINE ( 'NONE', #15392, #240235 ) ;
#213644=ORIENTED_EDGE ( 'NONE', *, *, #56858, .F. ) ;
#213664=CARTESIAN_POINT ( 'NONE',  ( -21.05000000000000071, 6.258316057343182415, -133.9342983896779344 ) ) ;
#213674=CYLINDRICAL_SURFACE ( 'NONE', #226986, 7.899999999999990585 ) ;
#213678=FACE_OUTER_BOUND ( 'NONE', #133773, .T. ) ;
#213689=AXIS2_PLACEMENT_3D ( 'NONE', #145272, #183147, #245677 ) ;
#213694=CARTESIAN_POINT ( 'NONE',  ( 18.59999999999999787, 1.866714910068465239, -145.7526752462820241 ) ) ;
#213710=EDGE_CURVE ( 'NONE', #236521, #151746, #61969, .T. ) ;
#213727=CIRCLE ( 'NONE', #109667, 0.09999999999998898659 ) ;
#213734=ORIENTED_EDGE ( 'NONE', *, *, #122314, .T. ) ;
#213738=ORIENTED_EDGE ( 'NONE', *, *, #205814, .F. ) ;
#213761=AXIS2_PLACEMENT_3D ( 'NONE', #31745, #91682, #214204 ) ;
#213762=AXIS2_PLACEMENT_3D ( 'NONE', #153409, #54249, #176796 ) ;
#213766=FACE_OUTER_BOUND ( 'NONE', #61451, .T. ) ;
#213776=EDGE_LOOP ( 'NONE', ( #165546, #29713, #134766, #225583 ) ) ;
#213799=CIRCLE ( 'NONE', #251392, 0.09999999999999939493 ) ;
#213865=DIRECTION ( 'NONE',  ( -1.000000000000000000, -0.000000000000000000, -0.000000000000000000 ) ) ;
#213912=CARTESIAN_POINT ( 'NONE',  ( 20.95429402530550433, 8.876194151113340425, -142.5230866979379698 ) ) ;
#213954=EDGE_CURVE ( 'NONE', #220244, #196380, #4568, .T. ) ;
#213997=FACE_OUTER_BOUND ( 'NONE', #35357, .T. ) ;
#214006=CARTESIAN_POINT ( 'NONE',  ( 23.24999999999999289, 6.650000000011155876, -146.3500000000000227 ) ) ;
#214008=ORIENTED_EDGE ( 'NONE', *, *, #180584, .T. ) ;
#214012=FACE_OUTER_BOUND ( 'NONE', #197866, .T. ) ;
#214014=ORIENTED_EDGE ( 'NONE', *, *, #164497, .T. ) ;
#214038=CIRCLE ( 'NONE', #168295, 11.70000000000001528 ) ;
#214059=CARTESIAN_POINT ( 'NONE',  ( -20.64999999999999858, 1.115600667400684642E-11, -146.8750000000000000 ) ) ;
#214107=EDGE_CURVE ( 'NONE', #226140, #199368, #12111, .T. ) ;
#214114=CARTESIAN_POINT ( 'NONE',  ( 18.59999999999999076, 10.20857864377385127, -155.3500000000000227 ) ) ;
#214121=AXIS2_PLACEMENT_3D ( 'NONE', #23834, #102027, #65487 ) ;
#214153=EDGE_CURVE ( 'NONE', #134395, #117471, #119878, .T. ) ;
#214156=EDGE_LOOP ( 'NONE', ( #156541, #213738, #171977, #230750, #36438 ) ) ;
#214204=DIRECTION ( 'NONE',  ( 0.000000000000000000, 0.000000000000000000, 1.000000000000000000 ) ) ;
#214225=DIRECTION ( 'NONE',  ( 1.000000000000000000, 0.000000000000000000, 0.000000000000000000 ) ) ;
#214233=DIRECTION ( 'NONE',  ( 1.000000000000000000, 0.000000000000000000, 0.000000000000000000 ) ) ;
#214240=DIRECTION ( 'NONE',  ( 0.000000000000000000, 0.000000000000000000, -1.000000000000000000 ) ) ;
#214250=EDGE_CURVE ( 'NONE', #195640, #92142, #155689, .T. ) ;
#214292=ORIENTED_EDGE ( 'NONE', *, *, #72718, .T. ) ;
#214302=AXIS2_PLACEMENT_3D ( 'NONE', #109351, #53256, #11578 ) ;
#214307=AXIS2_PLACEMENT_3D ( 'NONE', #246692, #189306, #70666 ) ;
#214324=ORIENTED_EDGE ( 'NONE', *, *, #225399, .T. ) ;
#214326=CARTESIAN_POINT ( 'NONE',  ( 21.05000000000000071, 6.477552182504828338, -134.0999999652991050 ) ) ;
#214370=DIRECTION ( 'NONE',  ( 0.000000000000000000, 0.4999999999999478195, 0.8660254037844686836 ) ) ;
#214394=EDGE_LOOP ( 'NONE', ( #50103, #122473, #178563, #204573 ) ) ;
#214400=DIRECTION ( 'NONE',  ( 1.000000000000000000, 0.000000000000000000, 0.000000000000000000 ) ) ;
#214409=CARTESIAN_POINT ( 'NONE',  ( 23.14999999999999858, 5.950000000011160139, -157.1942976949652007 ) ) ;
#214414=ORIENTED_EDGE ( 'NONE', *, *, #248374, .T. ) ;
#214427=CIRCLE ( 'NONE', #231215, 0.09999999999999817368 ) ;
#214434=VERTEX_POINT ( 'NONE', #25158 ) ;
#214496=CARTESIAN_POINT ( 'NONE',  ( -22.45305610364634674, -0.1008583690875579225, -122.2504328765106294 ) ) ;
#214505=AXIS2_PLACEMENT_3D ( 'NONE', #105178, #81777, #21849 ) ;
#214531=ADVANCED_FACE ( 'NONE', ( #88940 ), #65852, .T. ) ;
#214540=EDGE_LOOP ( 'NONE', ( #226896, #12429 ) ) ;
#214543=ADVANCED_FACE ( 'NONE', ( #30281 ), #90218, .T. ) ;
#214557=CARTESIAN_POINT ( 'NONE',  ( 21.08198257630413508, 6.336596734026219480, -133.9273566762154246 ) ) ;
#214562=CARTESIAN_POINT ( 'NONE',  ( 18.48197441911520400, -9.517954794694846399, -174.3902116422105735 ) ) ;
#214582=DIRECTION ( 'NONE',  ( 0.000000000000000000, 0.000000000000000000, -1.000000000000000000 ) ) ;
#214594=CIRCLE ( 'NONE', #227072, 0.9750000000000036415 ) ;
#214625=EDGE_CURVE ( 'NONE', #247963, #178157, #57652, .T. ) ;
#214634=AXIS2_PLACEMENT_3D ( 'NONE', #140119, #102257, #85269 ) ;
#214643=CARTESIAN_POINT ( 'NONE',  ( -23.25000000000000000, -11.74999999998884448, -164.4000000000000057 ) ) ;
#214644=ORIENTED_EDGE ( 'NONE', *, *, #162341, .T. ) ;
#214656=DIRECTION ( 'NONE',  ( 0.000000000000000000, 0.000000000000000000, -1.000000000000000000 ) ) ;
#214657=CARTESIAN_POINT ( 'NONE',  ( -20.00857864376270001, 9.150000000011157653, -155.1500000000000057 ) ) ;
#214734=ORIENTED_EDGE ( 'NONE', *, *, #45737, .T. ) ;
#214736=CARTESIAN_POINT ( 'NONE',  ( -21.05000000000000071, -1.835341550213255957, -145.5551512925629822 ) ) ;
#214776=ORIENTED_EDGE ( 'NONE', *, *, #2809, .F. ) ;
#214777=DIRECTION ( 'NONE',  ( 1.000000000000000000, 3.265361837132813093E-16, -0.000000000000000000 ) ) ;
#214785=DIRECTION ( 'NONE',  ( -1.000000000000000000, -3.265361837132813093E-16, 0.000000000000000000 ) ) ;
#214790=VERTEX_POINT ( 'NONE', #198321 ) ;
#214792=CARTESIAN_POINT ( 'NONE',  ( 21.05000000000000071, 5.000000000011153745, -155.0947339810869323 ) ) ;
#214818=LINE ( 'NONE', #253938, #254726 ) ;
#214819=EDGE_CURVE ( 'NONE', #171180, #96601, #195064, .T. ) ;
#214852=CARTESIAN_POINT ( 'NONE',  ( -18.50000000000000000, 9.350000000011156942, -146.3500000000000227 ) ) ;
#214918=CARTESIAN_POINT ( 'NONE',  ( -20.94999999999999929, 1.261786168576181755, -142.0864989635454947 ) ) ;
#214919=EDGE_CURVE ( 'NONE', #256904, #11722, #170144, .T. ) ;
#214947=CARTESIAN_POINT ( 'NONE',  ( -21.00023020733438273, 6.390869245278866018, -134.0000000000000000 ) ) ;
#214968=EDGE_LOOP ( 'NONE', ( #57811, #18003, #227595, #26821, #25346 ) ) ;
#214998=AXIS2_PLACEMENT_3D ( 'NONE', #83917, #185642, #222165 ) ;
#215035=DIRECTION ( 'NONE',  ( 1.000000000000000000, 0.000000000000000000, 0.000000000000000000 ) ) ;
#215084=ADVANCED_FACE ( 'NONE', ( #61067 ), #160207, .T. ) ;
#215100=LINE ( 'NONE', #11795, #92309 ) ;
#215113=DIRECTION ( 'NONE',  ( -0.000000000000000000, -0.000000000000000000, 1.000000000000000000 ) ) ;
#215153=CARTESIAN_POINT ( 'NONE',  ( 21.05000000000000071, 1.115600667400684642E-11, -167.5000000000000284 ) ) ;
#215158=LINE ( 'NONE', #219000, #112099 ) ;
#215181=CARTESIAN_POINT ( 'NONE',  ( -23.25000000000000000, -9.599999999988847676, -143.8939691226524644 ) ) ;
#215249=ADVANCED_FACE ( 'NONE', ( #63639 ), #104026, .T. ) ;
#215259=CARTESIAN_POINT ( 'NONE',  ( -21.14999999999999858, -0.09999999998884338825, -127.7500000000000284 ) ) ;
#215278=EDGE_LOOP ( 'NONE', ( #136046, #138849, #58821, #249091 ) ) ;
#215288=CARTESIAN_POINT ( 'NONE',  ( 23.24999999999999645, 2.100000000011158274, -167.5000000000000284 ) ) ;
#215290=CIRCLE ( 'NONE', #227752, 0.4000000000000114575 ) ;
#215307=ORIENTED_EDGE ( 'NONE', *, *, #105230, .T. ) ;
#215317=VERTEX_POINT ( 'NONE', #28410 ) ;
#215331=CIRCLE ( 'NONE', #69608, 0.9750000000000036415 ) ;
#215337=ORIENTED_EDGE ( 'NONE', *, *, #206223, .F. ) ;
#215349=AXIS2_PLACEMENT_3D ( 'NONE', #208208, #29588, #109081 ) ;
#215364=CARTESIAN_POINT ( 'NONE',  ( -23.25000000000000000, -11.74999999998884448, -137.1000000000000227 ) ) ;
#215369=FACE_OUTER_BOUND ( 'NONE', #138207, .T. ) ;
#215372=ADVANCED_FACE ( 'NONE', ( #165314 ), #204423, .T. ) ;
#215428=EDGE_CURVE ( 'NONE', #247963, #17731, #137587, .T. ) ;
#215483=CARTESIAN_POINT ( 'NONE',  ( -23.15000000000000213, -8.999999999988846255, -143.3939691226524644 ) ) ;
#215495=ADVANCED_FACE ( 'NONE', ( #163408 ), #236824, .F. ) ;
#215496=ORIENTED_EDGE ( 'NONE', *, *, #12349, .T. ) ;
#215506=CARTESIAN_POINT ( 'NONE',  ( 21.05000000000000071, 1.115600667400684642E-11, -146.1500000000000341 ) ) ;
#215529=CIRCLE ( 'NONE', #248854, 3.999999999999999112 ) ;
#215552=AXIS2_PLACEMENT_3D ( 'NONE', #168866, #230079, #51406 ) ;
#215561=CARTESIAN_POINT ( 'NONE',  ( 23.14999999999999858, 6.650000000011155876, -146.3500000000000227 ) ) ;
#215568=CARTESIAN_POINT ( 'NONE',  ( -18.39999999999999858, -9.599999999988849453, -174.1001893912220737 ) ) ;
#215575=DIRECTION ( 'NONE',  ( 0.000000000000000000, 0.000000000000000000, -1.000000000000000000 ) ) ;
#215597=EDGE_LOOP ( 'NONE', ( #203125, #26457, #137680 ) ) ;
#215616=DIRECTION ( 'NONE',  ( -1.000000000000000000, 0.000000000000000000, 0.000000000000000000 ) ) ;
#215631=CARTESIAN_POINT ( 'NONE',  ( -21.64999999999999858, 7.350000000011155166, -155.2500000000000284 ) ) ;
#215636=CARTESIAN_POINT ( 'NONE',  ( 19.75857864376268935, 11.65000000001115943, -158.8500000000000227 ) ) ;
#215637=ORIENTED_EDGE ( 'NONE', *, *, #151029, .T. ) ;
#215642=ORIENTED_EDGE ( 'NONE', *, *, #111327, .T. ) ;
#215710=ADVANCED_FACE ( 'NONE', ( #70747 ), #150271, .T. ) ;
#215746=CARTESIAN_POINT ( 'NONE',  ( -21.14999999999999858, -0.09999999998884338825, -122.3504291924552234 ) ) ;
#215776=DIRECTION ( 'NONE',  ( 0.000000000000000000, 1.000000000000000000, 0.000000000000000000 ) ) ;
#215778=CARTESIAN_POINT ( 'NONE',  ( 20.94999999999999929, 5.000000000011153745, -155.0947339810869323 ) ) ;
#215813=ORIENTED_EDGE ( 'NONE', *, *, #134256, .T. ) ;
#215829=CARTESIAN_POINT ( 'NONE',  ( 21.11927991906888025, 6.448493118502571342, -133.9909163205261109 ) ) ;
#215844=CARTESIAN_POINT ( 'NONE',  ( 18.49999999999998934, 6.450000000011156587, -144.0170271704400307 ) ) ;
#215854=ORIENTED_EDGE ( 'NONE', *, *, #82875, .T. ) ;
#215865=VECTOR ( 'NONE', #49715, 1000.000000000000000 ) ;
#215892=CARTESIAN_POINT ( 'NONE',  ( -21.59142135623730852, 7.850000000011158718, -155.1500000000000057 ) ) ;
#215902=AXIS2_PLACEMENT_3D ( 'NONE', #138477, #218019, #220618 ) ;
#215904=CIRCLE ( 'NONE', #24416, 0.1000000000000106914 ) ;
#215910=DIRECTION ( 'NONE',  ( 1.000000000000000000, 0.000000000000000000, 0.000000000000000000 ) ) ;
#215915=ORIENTED_EDGE ( 'NONE', *, *, #59247, .T. ) ;
#215918=CARTESIAN_POINT ( 'NONE',  ( -21.05315837450580574, 11.75000000001115197, -160.6583560043927434 ) ) ;
#215931=ORIENTED_EDGE ( 'NONE', *, *, #99391, .F. ) ;
#215937=VECTOR ( 'NONE', #194310, 1000.000000000000000 ) ;
#215942=CARTESIAN_POINT ( 'NONE',  ( -22.00356870067200177, 1.197144702919310711E-11, -126.7457576382269480 ) ) ;
#215971=ORIENTED_EDGE ( 'NONE', *, *, #216681, .F. ) ;
#216041=CARTESIAN_POINT ( 'NONE',  ( -21.14999999999999858, 1.115600667400684642E-11, -127.4593430482987912 ) ) ;
#216050=CARTESIAN_POINT ( 'NONE',  ( -18.43473496883411045, -9.494952410988167557, -141.0458715722282648 ) ) ;
#216059=AXIS2_PLACEMENT_3D ( 'NONE', #257940, #2367, #122339 ) ;
#216070=CARTESIAN_POINT ( 'NONE',  ( -20.54999999999999716, 7.250000000011155521, -146.2500000000000284 ) ) ;
#216080=ORIENTED_EDGE ( 'NONE', *, *, #193921, .F. ) ;
#216083=EDGE_CURVE ( 'NONE', #194690, #56718, #67902, .T. ) ;
#216104=ORIENTED_EDGE ( 'NONE', *, *, #105928, .F. ) ;
#216111=FACE_OUTER_BOUND ( 'NONE', #71974, .T. ) ;
#216137=AXIS2_PLACEMENT_3D ( 'NONE', #250153, #88479, #53234 ) ;
#216141=DIRECTION ( 'NONE',  ( 0.000000000000000000, 0.000000000000000000, -1.000000000000000000 ) ) ;
#216174=ORIENTED_EDGE ( 'NONE', *, *, #112123, .F. ) ;
#216212=CARTESIAN_POINT ( 'NONE',  ( -22.47071067811865319, 7.720074744509219933, -133.9009075452974002 ) ) ;
#216236=PLANE ( 'NONE',  #99424 ) ;
#216242=CARTESIAN_POINT ( 'NONE',  ( -21.05000000000000071, -11.64999999998884306, -164.4000000000000057 ) ) ;
#216248=ADVANCED_FACE ( 'NONE', ( #175555 ), #248899, .T. ) ;
#216258=AXIS2_PLACEMENT_3D ( 'NONE', #13453, #112557, #233788 ) ;
#216372=DIRECTION ( 'NONE',  ( -1.000000000000000000, 0.000000000000000000, 0.000000000000000000 ) ) ;
#216382=FACE_OUTER_BOUND ( 'NONE', #217220, .T. ) ;
#216387=CARTESIAN_POINT ( 'NONE',  ( -20.64999999999999858, 4.350000000011156054, -146.3500000000000227 ) ) ;
#216395=CARTESIAN_POINT ( 'NONE',  ( -22.49999999999999645, 11.74956712350054744, -133.8991416309012834 ) ) ;
#216415=CARTESIAN_POINT ( 'NONE',  ( -21.05000000000000071, 1.835341550235567887, -145.5551512925629822 ) ) ;
#216430=ORIENTED_EDGE ( 'NONE', *, *, #72163, .T. ) ;
#216442=CARTESIAN_POINT ( 'NONE',  ( -21.44999999999999929, 7.150000000011155876, -155.1500000000000057 ) ) ;
#216464=CIRCLE ( 'NONE', #104003, 3.899999999999987033 ) ;
#216466=ORIENTED_EDGE ( 'NONE', *, *, #136809, .T. ) ;
#216490=DIRECTION ( 'NONE',  ( -1.000000000000000000, -0.000000000000000000, -0.000000000000000000 ) ) ;
#216493=DIRECTION ( 'NONE',  ( 0.000000000000000000, 1.000000000000000000, 0.000000000000000000 ) ) ;
#216498=DIRECTION ( 'NONE',  ( -1.000000000000000000, 0.000000000000000000, -0.000000000000000000 ) ) ;
#216501=DIRECTION ( 'NONE',  ( 2.715809747126116508E-16, -1.000000000000000000, 0.000000000000000000 ) ) ;
#216508=SURFACE_STYLE_USAGE ( .BOTH. , #155292 ) ;
#216511=AXIS2_PLACEMENT_3D ( 'NONE', #101349, #163956, #221329 ) ;
#216523=CARTESIAN_POINT ( 'NONE',  ( 20.94788355080264353, 10.30207779525982659, -172.9895520716782755 ) ) ;
#216560=ORIENTED_EDGE ( 'NONE', *, *, #115109, .F. ) ;
#216590=EDGE_LOOP ( 'NONE', ( #237776, #70625, #11500 ) ) ;
#216601=ORIENTED_EDGE ( 'NONE', *, *, #112348, .T. ) ;
#216612=EDGE_LOOP ( 'NONE', ( #179475, #32323, #135132 ) ) ;
#216637=ADVANCED_FACE ( 'NONE', ( #60082 ), #180511, .T. ) ;
#216642=VECTOR ( 'NONE', #201329, 1000.000000000000000 ) ;
#216662=AXIS2_PLACEMENT_3D ( 'NONE', #220281, #34275, #23376 ) ;
#216681=EDGE_CURVE ( 'NONE', #120136, #43801, #126338, .T. ) ;
#216682=DIRECTION ( 'NONE',  ( 0.000000000000000000, 0.000000000000000000, 1.000000000000000000 ) ) ;
#216695=VECTOR ( 'NONE', #82465, 1000.000000000000000 ) ;
#216709=VERTEX_POINT ( 'NONE', #221708 ) ;
#216724=ORIENTED_EDGE ( 'NONE', *, *, #35396, .T. ) ;
#216746=VECTOR ( 'NONE', #181565, 1000.000000000000000 ) ;
#216766=EDGE_CURVE ( 'NONE', #219189, #71001, #205427, .T. ) ;
#216768=FACE_OUTER_BOUND ( 'NONE', #144304, .T. ) ;
#216815=DIRECTION ( 'NONE',  ( -1.000000000000000000, -2.952720810173289112E-16, 0.000000000000000000 ) ) ;
#216831=AXIS2_PLACEMENT_3D ( 'NONE', #109281, #110580, #193990 ) ;
#216841=CARTESIAN_POINT ( 'NONE',  ( 20.94999999999999574, -1.835341550213255957, -145.5551512925629822 ) ) ;
#216842=CARTESIAN_POINT ( 'NONE',  ( 21.06280952165543141, 10.62713230061201841, -146.2040538867793771 ) ) ;
#216850=DIRECTION ( 'NONE',  ( 1.000000000000000000, -0.000000000000000000, 0.000000000000000000 ) ) ;
#216861=ORIENTED_EDGE ( 'NONE', *, *, #3763, .T. ) ;
#216866=CIRCLE ( 'NONE', #50264, 0.09999999999999939493 ) ;
#216886=ORIENTED_EDGE ( 'NONE', *, *, #1790, .T. ) ;
#216890=CARTESIAN_POINT ( 'NONE',  ( -22.50000000000000000, 7.790779598384560245, -133.9000000000000057 ) ) ;
#216895=ORIENTED_EDGE ( 'NONE', *, *, #159451, .T. ) ;
#216896=FACE_OUTER_BOUND ( 'NONE', #145618, .T. ) ;
#216916=VERTEX_POINT ( 'NONE', #252840 ) ;
#216933=EDGE_CURVE ( 'NONE', #178157, #176425, #59866, .T. ) ;
#216963=CARTESIAN_POINT ( 'NONE',  ( -20.94684162548871242, 11.75000000001115197, -140.8416439955713031 ) ) ;
#216973=ORIENTED_EDGE ( 'NONE', *, *, #13120, .F. ) ;
#216983=CIRCLE ( 'NONE', #162873, 0.1000000000000033223 ) ;
#217009=AXIS2_PLACEMENT_3D ( 'NONE', #170659, #127631, #132785 ) ;
#217020=FACE_OUTER_BOUND ( 'NONE', #115185, .T. ) ;
#217031=VERTEX_POINT ( 'NONE', #118495 ) ;
#217072=DIRECTION ( 'NONE',  ( 1.000000000000000000, -0.000000000000000000, -0.000000000000000000 ) ) ;
#217076=ORIENTED_EDGE ( 'NONE', *, *, #112198, .T. ) ;
#217098=ORIENTED_EDGE ( 'NONE', *, *, #194289, .T. ) ;
#217102=DIRECTION ( 'NONE',  ( 0.000000000000000000, -0.4930308989874718772, -0.8700118002898612479 ) ) ;
#217128=ADVANCED_FACE ( 'NONE', ( #222689 ), #21955, .T. ) ;
#217132=CARTESIAN_POINT ( 'NONE',  ( 18.59999999999999432, -1.835859311432481045, -179.0044391687985410 ) ) ;
#217170=VERTEX_POINT ( 'NONE', #192574 ) ;
#217187=CARTESIAN_POINT ( 'NONE',  ( 18.59999999999999432, -1.261786168553869603, -142.0864989635454947 ) ) ;
#217214=CARTESIAN_POINT ( 'NONE',  ( -18.59999999999999787, 6.846123162363745074, -171.2377262668498759 ) ) ;
#217220=EDGE_LOOP ( 'NONE', ( #105940, #90196, #39599, #245020 ) ) ;
#217227=VERTEX_POINT ( 'NONE', #251242 ) ;
#217262=ORIENTED_EDGE ( 'NONE', *, *, #60769, .F. ) ;
#217270=CARTESIAN_POINT ( 'NONE',  ( 20.95496329884391784, 10.56743320610419623, -141.5743099322848479 ) ) ;
#217292=ORIENTED_EDGE ( 'NONE', *, *, #34104, .F. ) ;
#217297=VERTEX_POINT ( 'NONE', #253811 ) ;
#217307=DIRECTION ( 'NONE',  ( 4.408576920032447355E-17, -0.1350103645451876666, 0.9908441862701600211 ) ) ;
#217325=FACE_OUTER_BOUND ( 'NONE', #123419, .T. ) ;
#217377=CARTESIAN_POINT ( 'NONE',  ( 22.39999999999999858, 7.790779598384538929, -133.9000000000000057 ) ) ;
#217412=DIRECTION ( 'NONE',  ( 0.000000000000000000, 0.000000000000000000, -1.000000000000000000 ) ) ;
#217441=DIRECTION ( 'NONE',  ( 0.000000000000000000, 0.9908441862701782288, 0.1350103645450542456 ) ) ;
#217514=VECTOR ( 'NONE', #34177, 1000.000000000000000 ) ;
#217522=DIRECTION ( 'NONE',  ( -0.000000000000000000, -1.000000000000000000, -0.000000000000000000 ) ) ;
#217537=AXIS2_PLACEMENT_3D ( 'NONE', #44688, #244143, #124227 ) ;
#217545=ORIENTED_EDGE ( 'NONE', *, *, #253648, .F. ) ;
#217570=FACE_OUTER_BOUND ( 'NONE', #131810, .T. ) ;
#217572=ORIENTED_EDGE ( 'NONE', *, *, #71335, .F. ) ;
#217600=DIRECTION ( 'NONE',  ( 0.000000000000000000, 0.000000000000000000, -1.000000000000000000 ) ) ;
#217606=DIRECTION ( 'NONE',  ( 0.000000000000000000, 0.000000000000000000, 1.000000000000000000 ) ) ;
#217623=EDGE_CURVE ( 'NONE', #177617, #120136, #151886, .T. ) ;
#217641=DIRECTION ( 'NONE',  ( 0.000000000000000000, -1.000000000000000000, 0.000000000000000000 ) ) ;
#217669=VERTEX_POINT ( 'NONE', #8502 ) ;
#217671=ADVANCED_FACE ( 'NONE', ( #52743 ), #210117, .F. ) ;
#217711=CARTESIAN_POINT ( 'NONE',  ( -21.05000000000000071, 1.115650877919449575E-11, -171.6000000000000227 ) ) ;
#217724=CIRCLE ( 'NONE', #151120, 0.09999999999999363565 ) ;
#217738=EDGE_LOOP ( 'NONE', ( #196945, #206708, #175594, #61794 ) ) ;
#217748=DIRECTION ( 'NONE',  ( -0.000000000000000000, -0.1350103645451876666, 0.9908441862701600211 ) ) ;
#217769=ORIENTED_EDGE ( 'NONE', *, *, #45737, .F. ) ;
#217794=CARTESIAN_POINT ( 'NONE',  ( -23.25000000000000000, 1.910280373842936141, -146.6313678551989597 ) ) ;
#217801=ORIENTED_EDGE ( 'NONE', *, *, #74067, .T. ) ;
#217810=ADVANCED_FACE ( 'NONE', ( #116583 ), #93155, .F. ) ;
#217825=ORIENTED_EDGE ( 'NONE', *, *, #49097, .T. ) ;
#217848=ORIENTED_EDGE ( 'NONE', *, *, #186666, .T. ) ;
#217874=CIRCLE ( 'NONE', #17975, 0.09999999999998898659 ) ;
#217910=DIRECTION ( 'NONE',  ( 0.7071067811865475727, 0.7071067811865475727, -0.000000000000000000 ) ) ;
#217918=LINE ( 'NONE', #116294, #69511 ) ;
#217924=EDGE_LOOP ( 'NONE', ( #175513, #59394, #137841, #192836, #45751 ) ) ;
#217951=DIRECTION ( 'NONE',  ( 4.504528286903032433E-15, -0.1298341882520124002, -0.9915357197604841577 ) ) ;
#217955=CARTESIAN_POINT ( 'NONE',  ( -20.54999999999999716, -11.74999999998884448, -150.7500000000000284 ) ) ;
#217978=EDGE_CURVE ( 'NONE', #158228, #227353, #147350, .T. ) ;
#217991=CARTESIAN_POINT ( 'NONE',  ( 20.94999999999999574, 1.162701749949165642, -142.1000000000000227 ) ) ;
#217994=AXIS2_PLACEMENT_3D ( 'NONE', #75265, #72699, #152238 ) ;
#218019=DIRECTION ( 'NONE',  ( -0.000000000000000000, 0.01283462868039629209, -0.9999176327611372095 ) ) ;
#218020=CARTESIAN_POINT ( 'NONE',  ( 18.41416235934317314, -9.499999999988842703, -174.1001893912220169 ) ) ;
#218021=LINE ( 'NONE', #257121, #139753 ) ;
#218032=ORIENTED_EDGE ( 'NONE', *, *, #161265, .T. ) ;
#218044=AXIS2_PLACEMENT_3D ( 'NONE', #246514, #183978, #9192 ) ;
#218064=CIRCLE ( 'NONE', #26571, 0.1000000000000028644 ) ;
#218074=VERTEX_POINT ( 'NONE', #109840 ) ;
#218094=CIRCLE ( 'NONE', #101555, 0.1000000000000094008 ) ;
#218101=LINE ( 'NONE', #235126, #88987 ) ;
#218133=ADVANCED_FACE ( 'NONE', ( #92852 ), #55542, .F. ) ;
#218135=ORIENTED_EDGE ( 'NONE', *, *, #98270, .F. ) ;
#218139=ORIENTED_EDGE ( 'NONE', *, *, #13514, .F. ) ;
#218151=ORIENTED_EDGE ( 'NONE', *, *, #6164, .T. ) ;
#218156=ORIENTED_EDGE ( 'NONE', *, *, #186968, .F. ) ;
#218167=CARTESIAN_POINT ( 'NONE',  ( -23.15000000000000213, -8.596261682231830292, -158.0498724828497359 ) ) ;
#218170=DIRECTION ( 'NONE',  ( -1.000000000000000000, 0.000000000000000000, 0.000000000000000000 ) ) ;
#218199=CIRCLE ( 'NONE', #226581, 0.09999999999999178990 ) ;
#218223=ADVANCED_FACE ( 'NONE', ( #215369 ), #255743, .T. ) ;
#218243=CARTESIAN_POINT ( 'NONE',  ( -21.14999999999999858, 11.75000000001115197, -140.7838656629781724 ) ) ;
#218258=EDGE_CURVE ( 'NONE', #208746, #24271, #218064, .T. ) ;
#218277=( LENGTH_UNIT ( ) NAMED_UNIT ( * ) SI_UNIT ( .MILLI., .METRE. ) );
#218280=AXIS2_PLACEMENT_3D ( 'NONE', #162136, #42181, #142538 ) ;
#218284=LINE ( 'NONE', #137470, #191039 ) ;
#218294=EDGE_CURVE ( 'NONE', #247600, #192232, #238946, .T. ) ;
#218296=EDGE_CURVE ( 'NONE', #41545, #174999, #163128, .T. ) ;
#218322=AXIS2_PLACEMENT_3D ( 'NONE', #212342, #174539, #114502 ) ;
#218326=ADVANCED_FACE ( 'NONE', ( #100529 ), #230757, .F. ) ;
#218402=ORIENTED_EDGE ( 'NONE', *, *, #182810, .T. ) ;
#218404=CIRCLE ( 'NONE', #156108, 0.1000000000000001027 ) ;
#218408=TOROIDAL_SURFACE ( 'NONE', #251758, 4.099999999999999645, 0.1000000000000000056 ) ;
#218415=CIRCLE ( 'NONE', #126684, 0.09999999999999864553 ) ;
#218423=EDGE_LOOP ( 'NONE', ( #116729, #187364, #128532, #109818 ) ) ;
#218427=VECTOR ( 'NONE', #131043, 1000.000000000000000 ) ;
#218456=EDGE_LOOP ( 'NONE', ( #232218, #203799, #162821, #132166 ) ) ;
#218486=VECTOR ( 'NONE', #103989, 1000.000000000000000 ) ;
#218514=EDGE_CURVE ( 'NONE', #142484, #69302, #151669, .T. ) ;
#218550=DIRECTION ( 'NONE',  ( 1.000000000000000000, 0.000000000000000000, 0.000000000000000000 ) ) ;
#218578=ORIENTED_EDGE ( 'NONE', *, *, #95062, .F. ) ;
#218589=FACE_OUTER_BOUND ( 'NONE', #202161, .T. ) ;
#218595=EDGE_CURVE ( 'NONE', #128950, #90426, #8062, .T. ) ;
#218610=CARTESIAN_POINT ( 'NONE',  ( -18.50000000000001066, -9.421308209727802918, -141.2423632140505561 ) ) ;
#218619=CIRCLE ( 'NONE', #210274, 0.09999999999998898659 ) ;
#218635=CARTESIAN_POINT ( 'NONE',  ( 22.59999985501178799, 11.74986979301414181, -133.9344013302005294 ) ) ;
#218643=AXIS2_PLACEMENT_3D ( 'NONE', #17188, #97958, #156 ) ;
#218646=EDGE_CURVE ( 'NONE', #115616, #196105, #251771, .T. ) ;
#218661=CARTESIAN_POINT ( 'NONE',  ( 22.00356870140399579, 7.254242362511003961, -134.0000000000000000 ) ) ;
#218665=ORIENTED_EDGE ( 'NONE', *, *, #213310, .T. ) ;
#218673=ORIENTED_EDGE ( 'NONE', *, *, #154586, .F. ) ;
#218678=VECTOR ( 'NONE', #222665, 1000.000000000000000 ) ;
#218684=CARTESIAN_POINT ( 'NONE',  ( 18.49999999999999289, 11.75000000001115907, -142.1000000000000227 ) ) ;
#218689=DIRECTION ( 'NONE',  ( -0.000000000000000000, -0.000000000000000000, 1.000000000000000000 ) ) ;
#218690=CARTESIAN_POINT ( 'NONE',  ( 23.24999999999999289, 11.65000000001116298, -122.2500000000000284 ) ) ;
#218693=DIRECTION ( 'NONE',  ( -2.940209281316621016E-16, 1.000000000000000000, -4.704334850106593625E-15 ) ) ;
#218711=VERTEX_POINT ( 'NONE', #222409 ) ;
#218720=EDGE_LOOP ( 'NONE', ( #232625, #85177, #168258, #251104 ) ) ;
#218727=DIRECTION ( 'NONE',  ( -4.336808689941752679E-15, 0.8660254037844482555, 0.4999999999999837907 ) ) ;
#218752=EDGE_CURVE ( 'NONE', #8211, #97103, #129760, .T. ) ;
#218791=DIRECTION ( 'NONE',  ( 1.000000000000000000, 0.000000000000000000, 0.000000000000000000 ) ) ;
#218816=PLANE ( 'NONE',  #95900 ) ;
#218822=AXIS2_PLACEMENT_3D ( 'NONE', #255421, #76833, #55967 ) ;
#218833=EDGE_CURVE ( 'NONE', #209723, #152770, #71093, .T. ) ;
#218834=CARTESIAN_POINT ( 'NONE',  ( -2.995603634470829482E-16, -11.74999999998884448, -146.2500000000000284 ) ) ;
#218850=ORIENTED_EDGE ( 'NONE', *, *, #49680, .T. ) ;
#218860=TOROIDAL_SURFACE ( 'NONE', #127115, 7.800000000000000711, 0.1000000000000000056 ) ;
#218867=ORIENTED_EDGE ( 'NONE', *, *, #45224, .F. ) ;
#218911=ORIENTED_EDGE ( 'NONE', *, *, #75139, .T. ) ;
#218990=EDGE_LOOP ( 'NONE', ( #85070, #193232, #76123, #211489 ) ) ;
#218999=CARTESIAN_POINT ( 'NONE',  ( 23.25000000000000000, -11.74999999998883560, -122.2500000000000284 ) ) ;
#219000=CARTESIAN_POINT ( 'NONE',  ( -21.05000000000000071, 5.900000000011162093, -157.2809002353436654 ) ) ;
#219004=CYLINDRICAL_SURFACE ( 'NONE', #30810, 4.049999999999998046 ) ;
#219016=ORIENTED_EDGE ( 'NONE', *, *, #185484, .T. ) ;
#219020=AXIS2_PLACEMENT_3D ( 'NONE', #250810, #216815, #113875 ) ;
#219042=CYLINDRICAL_SURFACE ( 'NONE', #136995, 0.09999999999998898659 ) ;
#219114=VECTOR ( 'NONE', #41221, 1000.000000000000000 ) ;
#219115=DIRECTION ( 'NONE',  ( -1.000000000000000000, -2.952720810173289112E-16, 0.000000000000000000 ) ) ;
#219116=EDGE_LOOP ( 'NONE', ( #233850, #126104, #174864 ) ) ;
#219126=CIRCLE ( 'NONE', #7324, 0.5000000000000004441 ) ;
#219155=DIRECTION ( 'NONE',  ( 0.000000000000000000, 1.000000000000000000, -1.224646799147353207E-16 ) ) ;
#219157=ADVANCED_FACE ( 'NONE', ( #29128 ), #229848, .F. ) ;
#219173=DIRECTION ( 'NONE',  ( -1.000000000000000000, 0.000000000000000000, 0.000000000000000000 ) ) ;
#219180=ADVANCED_FACE ( 'NONE', ( #208999 ), #130746, .T. ) ;
#219184=ADVANCED_FACE ( 'NONE', ( #190754 ), #107322, .T. ) ;
#219189=VERTEX_POINT ( 'NONE', #66918 ) ;
#219238=CYLINDRICAL_SURFACE ( 'NONE', #55822, 0.09999999999998898659 ) ;
#219247=DIRECTION ( 'NONE',  ( 0.000000000000000000, 0.000000000000000000, 1.000000000000000000 ) ) ;
#219255=DIRECTION ( 'NONE',  ( 0.000000000000000000, 0.000000000000000000, -1.000000000000000000 ) ) ;
#219265=CIRCLE ( 'NONE', #48571, 1.900000000000012790 ) ;
#219274=EDGE_CURVE ( 'NONE', #82520, #99517, #218619, .T. ) ;
#219306=AXIS2_PLACEMENT_3D ( 'NONE', #92844, #171158, #189390 ) ;
#219312=ORIENTED_EDGE ( 'NONE', *, *, #95062, .T. ) ;
#219332=ORIENTED_EDGE ( 'NONE', *, *, #134225, .T. ) ;
#219333=DIRECTION ( 'NONE',  ( -1.000000000000000000, -2.952720810173289112E-16, 0.000000000000000000 ) ) ;
#219342=AXIS2_PLACEMENT_3D ( 'NONE', #230365, #51700, #210806 ) ;
#219363=VERTEX_POINT ( 'NONE', #186438 ) ;
#219366=CARTESIAN_POINT ( 'NONE',  ( 23.24999999999999645, 5.000000000011153745, -155.0947339810869323 ) ) ;
#219472=ORIENTED_EDGE ( 'NONE', *, *, #252316, .T. ) ;
#219479=ORIENTED_EDGE ( 'NONE', *, *, #51382, .F. ) ;
#219492=FACE_OUTER_BOUND ( 'NONE', #125250, .T. ) ;
#219505=FACE_OUTER_BOUND ( 'NONE', #4345, .T. ) ;
#219521=ORIENTED_EDGE ( 'NONE', *, *, #20376, .F. ) ;
#219525=CARTESIAN_POINT ( 'NONE',  ( 21.07928932188134397, 0.09889514566555242248, -127.6714833436067238 ) ) ;
#219533=CARTESIAN_POINT ( 'NONE',  ( -20.94999999999999929, 1.835341550235567887, -145.6551512925629766 ) ) ;
#219536=CARTESIAN_POINT ( 'NONE',  ( -20.94999999999999929, 11.60000000001115339, -140.9282032302755852 ) ) ;
#219575=ADVANCED_FACE ( 'NONE', ( #81997 ), #25926, .T. ) ;
#219583=DIRECTION ( 'NONE',  ( 1.000000000000000000, 0.000000000000000000, 0.000000000000000000 ) ) ;
#219592=EDGE_CURVE ( 'NONE', #224075, #59451, #206359, .T. ) ;
#219625=DIRECTION ( 'NONE',  ( 0.000000000000000000, 0.000000000000000000, -1.000000000000000000 ) ) ;
#219629=CARTESIAN_POINT ( 'NONE',  ( -18.59999999999999787, 1.115600667400684642E-11, -134.0000000000000000 ) ) ;
#219632=LINE ( 'NONE', #41031, #129557 ) ;
#219635=CARTESIAN_POINT ( 'NONE',  ( 23.15000000000000213, -11.74999999998883560, -146.1500000000000341 ) ) ;
#219639=LINE ( 'NONE', #159688, #9519 ) ;
#219645=AXIS2_PLACEMENT_3D ( 'NONE', #187123, #110125, #7159 ) ;
#219652=AXIS2_PLACEMENT_3D ( 'NONE', #23518, #1327, #181293 ) ;
#219654=DIRECTION ( 'NONE',  ( 0.000000000000000000, 0.000000000000000000, -1.000000000000000000 ) ) ;
#219677=ORIENTED_EDGE ( 'NONE', *, *, #223430, .F. ) ;
#219720=LINE ( 'NONE', #20259, #40378 ) ;
#219728=AXIS2_PLACEMENT_3D ( 'NONE', #233522, #190550, #195688 ) ;
#219731=DIRECTION ( 'NONE',  ( -1.000000000000000000, 0.000000000000000000, 0.000000000000000000 ) ) ;
#219756=ORIENTED_EDGE ( 'NONE', *, *, #30530, .T. ) ;
#219782=ORIENTED_EDGE ( 'NONE', *, *, #771, .F. ) ;
#219795=CIRCLE ( 'NONE', #24015, 0.09999999999998898659 ) ;
#219850=DIRECTION ( 'NONE',  ( 1.000000000000000000, -0.000000000000000000, -0.000000000000000000 ) ) ;
#219851=ORIENTED_EDGE ( 'NONE', *, *, #160945, .T. ) ;
#219854=CARTESIAN_POINT ( 'NONE',  ( 20.95539060131842746, 10.62386215766679776, -141.6537338136562028 ) ) ;
#219856=CARTESIAN_POINT ( 'NONE',  ( -23.25000000000000000, 5.950000000011163692, -157.1942976949652007 ) ) ;
#219869=CYLINDRICAL_SURFACE ( 'NONE', #199765, 0.09999999999998898659 ) ;
#219871=ADVANCED_FACE ( 'NONE', ( #103513 ), #119062, .T. ) ;
#219873=CARTESIAN_POINT ( 'NONE',  ( 22.47071067811865319, 7.720074744509199505, -133.9009075452974002 ) ) ;
#219878=AXIS2_PLACEMENT_3D ( 'NONE', #135820, #255738, #75864 ) ;
#219896=ORIENTED_EDGE ( 'NONE', *, *, #58183, .F. ) ;
#219908=CARTESIAN_POINT ( 'NONE',  ( 18.49999999999998934, 10.25000000001115552, -158.7500000000000284 ) ) ;
#219913=CARTESIAN_POINT ( 'NONE',  ( -18.58693740092134306, -9.406432150241803569, -141.1248164565013781 ) ) ;
#219935=ORIENTED_EDGE ( 'NONE', *, *, #86899, .T. ) ;
#219961=DIRECTION ( 'NONE',  ( 1.000000000000000000, -0.000000000000000000, -0.000000000000000000 ) ) ;
#219989=DIRECTION ( 'NONE',  ( 0.000000000000000000, 0.000000000000000000, -1.000000000000000000 ) ) ;
#219990=CARTESIAN_POINT ( 'NONE',  ( 18.59999999999999076, 10.20857864377385127, -158.7500000000000284 ) ) ;
#219996=VECTOR ( 'NONE', #189442, 1000.000000000000000 ) ;
#220000=( BOUNDED_SURFACE ( )  B_SPLINE_SURFACE ( 3, 2, ( 
 ( #206481, #183078, #42278 ),
 ( #147801, #4414, #102205 ),
 ( #22733, #121824, #205174 ),
 ( #3121, #83912, #85208 ) ),
 .UNSPECIFIED., .F., .F., .F. ) 
 B_SPLINE_SURFACE_WITH_KNOTS ( ( 4, 4 ),
 ( 3, 3 ),
 ( 1.355252715606880543E-20, 0.0003124336117481268005 ),
 ( 0.000000000000000000, 1.000000000000000000 ),
 .UNSPECIFIED. ) 
 GEOMETRIC_REPRESENTATION_ITEM ( )  RATIONAL_B_SPLINE_SURFACE ( (
 ( 1.000000000000000000, 0.7040654476016472429, 1.000000000000000000),
 ( 1.000000000000000000, 0.7039193538781700621, 1.000000000000000000),
 ( 1.000000000000000000, 0.7089171279145592974, 1.000000000000000000),
 ( 1.000000000000000000, 0.7071067811865506814, 1.000000000000000000) ) ) 
 REPRESENTATION_ITEM ( '' )  SURFACE ( )  );
#220002=VERTEX_POINT ( 'NONE', #188208 ) ;
#220022=AXIS2_PLACEMENT_3D ( 'NONE', #249917, #174279, #212088 ) ;
#220046=CARTESIAN_POINT ( 'NONE',  ( 23.14999999999999858, 4.813084112160684214, -155.5584822434762202 ) ) ;
#220066=ORIENTED_EDGE ( 'NONE', *, *, #47547, .T. ) ;
#220080=VECTOR ( 'NONE', #24971, 1000.000000000000000 ) ;
#220098=EDGE_CURVE ( 'NONE', #229760, #231169, #239864, .T. ) ;
#220103=AXIS2_PLACEMENT_3D ( 'NONE', #169399, #248904, #132812 ) ;
#220115=CARTESIAN_POINT ( 'NONE',  ( 21.05000000000000071, -11.64999999998883595, -136.9000000000000341 ) ) ;
#220134=VERTEX_POINT ( 'NONE', #111239 ) ;
#220138=ORIENTED_EDGE ( 'NONE', *, *, #117742, .T. ) ;
#220168=SPHERICAL_SURFACE ( 'NONE', #28029, 0.1000000000000000056 ) ;
#220169=CIRCLE ( 'NONE', #157668, 0.2000000000000000944 ) ;
#220173=VERTEX_POINT ( 'NONE', #172549 ) ;
#220189=DIRECTION ( 'NONE',  ( 0.000000000000000000, 1.000000000000000000, -6.308085367188393199E-16 ) ) ;
#220198=LINE ( 'NONE', #84477, #76167 ) ;
#220224=ORIENTED_EDGE ( 'NONE', *, *, #61038, .T. ) ;
#220244=VERTEX_POINT ( 'NONE', #39436 ) ;
#220245=DIRECTION ( 'NONE',  ( 0.000000000000000000, 0.000000000000000000, -1.000000000000000000 ) ) ;
#220262=DIRECTION ( 'NONE',  ( -2.915501640297154283E-16, 1.000000000000000000, 0.000000000000000000 ) ) ;
#220281=CARTESIAN_POINT ( 'NONE',  ( 20.94999999999999929, 1.115600667400684642E-11, -167.5000000000000284 ) ) ;
#220299=EDGE_CURVE ( 'NONE', #79795, #159346, #201042, .T. ) ;
#220346=ORIENTED_EDGE ( 'NONE', *, *, #120018, .T. ) ;
#220359=CARTESIAN_POINT ( 'NONE',  ( -22.39999999999999858, 7.790779598384560245, -134.0000000000000000 ) ) ;
#220361=LINE ( 'NONE', #41733, #223886 ) ;
#220433=DIRECTION ( 'NONE',  ( 1.000000000000000000, 0.000000000000000000, -0.000000000000000000 ) ) ;
#220481=CARTESIAN_POINT ( 'NONE',  ( -20.15000000000000568, 9.291421356248463326, -146.3500000000000227 ) ) ;
#220518=CARTESIAN_POINT ( 'NONE',  ( 21.14999999999999858, -0.09999999998884338825, -134.0000000000000000 ) ) ;
#220522=AXIS2_PLACEMENT_3D ( 'NONE', #41219, #164985, #3322 ) ;
#220575=CARTESIAN_POINT ( 'NONE',  ( -23.15000000000000213, 1.115649653272650466E-11, -171.5000000000000284 ) ) ;
#220582=AXIS2_PLACEMENT_3D ( 'NONE', #219990, #103872, #106434 ) ;
#220595=CARTESIAN_POINT ( 'NONE',  ( 20.94999999999999929, 1.115600667400684642E-11, -146.9749999999999943 ) ) ;
#220608=CARTESIAN_POINT ( 'NONE',  ( -22.41119224318417125, 1.115600667400684642E-11, -122.3504291924552234 ) ) ;
#220614=CARTESIAN_POINT ( 'NONE',  ( 21.05000000000000071, 10.54375127550676616, -141.5563878086650504 ) ) ;
#220618=DIRECTION ( 'NONE',  ( -3.469446951953604722E-14, -0.9999176327611370985, -0.01283462868040260302 ) ) ;
#220634=FACE_OUTER_BOUND ( 'NONE', #33616, .T. ) ;
#220707=( BOUNDED_SURFACE ( )  B_SPLINE_SURFACE ( 3, 2, ( 
 ( #111845, #135231, #93549 ),
 ( #252616, #114404, #253899 ),
 ( #193952, #136508, #75306 ),
 ( #154840, #115691, #195252 ),
 ( #16609, #96102, #255137 ),
 ( #76548, #156129, #235619 ) ),
 .UNSPECIFIED., .F., .F., .F. ) 
 B_SPLINE_SURFACE_WITH_KNOTS ( ( 4, 2, 4 ),
 ( 3, 3 ),
 ( 0.0001300404313046710908, 0.0003183318589266656172, 0.0005066232865486601164 ),
 ( 0.000000000000000000, 1.000000000000000000 ),
 .UNSPECIFIED. ) 
 GEOMETRIC_REPRESENTATION_ITEM ( )  RATIONAL_B_SPLINE_SURFACE ( (
 ( 1.000000000000000000, 0.7071067811865475727, 1.000000000000000000),
 ( 1.000000000000000000, 0.7625113560542993163, 1.000000000000000000),
 ( 1.000000000000000000, 0.8126073484684785964, 1.000000000000000000),
 ( 1.000000000000000000, 0.8923049332736345818, 1.000000000000000000),
 ( 1.000000000000000000, 0.9231914937766407814, 1.000000000000000000),
 ( 1.000000000000000000, 0.9238795325112909573, 1.000000000000000000) ) ) 
 REPRESENTATION_ITEM ( '' )  SURFACE ( )  );
#220708=CARTESIAN_POINT ( 'NONE',  ( 21.13461538461538680, 10.61458296203669427, -146.2500000000000568 ) ) ;
#220743=EDGE_LOOP ( 'NONE', ( #163364, #3233, #226165, #138103 ) ) ;
#220745=VERTEX_POINT ( 'NONE', #23419 ) ;
#220754=VERTEX_POINT ( 'NONE', #187614 ) ;
#220816=ORIENTED_EDGE ( 'NONE', *, *, #79604, .T. ) ;
#220828=CARTESIAN_POINT ( 'NONE',  ( -21.03571358705729466, 11.75000000001115374, -140.8251068220585864 ) ) ;
#220873=DIRECTION ( 'NONE',  ( 1.000000000000000000, 0.000000000000000000, 0.000000000000000000 ) ) ;
#220904=CARTESIAN_POINT ( 'NONE',  ( 21.05000000000000071, 8.776282895303632259, -142.5586289951409640 ) ) ;
#220913=LINE ( 'NONE', #138782, #232310 ) ;
#220919=EDGE_CURVE ( 'NONE', #227883, #188779, #213564, .T. ) ;
#220926=EDGE_LOOP ( 'NONE', ( #219935, #195555, #95653, #60508 ) ) ;
#220930=DIRECTION ( 'NONE',  ( -0.000000000000000000, -0.000000000000000000, 1.000000000000000000 ) ) ;
#220990=CARTESIAN_POINT ( 'NONE',  ( 20.94999999999999929, 1.115600667400684642E-11, -167.5000000000000284 ) ) ;
#221001=LINE ( 'NONE', #22845, #173661 ) ;
#221009=CARTESIAN_POINT ( 'NONE',  ( -20.64999999999999858, 2.000000000011154189, -154.2753780772379173 ) ) ;
#221026=AXIS2_PLACEMENT_3D ( 'NONE', #254586, #120281, #78533 ) ;
#221032=ORIENTED_EDGE ( 'NONE', *, *, #128591, .T. ) ;
#221045=EDGE_CURVE ( 'NONE', #247963, #222383, #17928, .T. ) ;
#221046=ORIENTED_EDGE ( 'NONE', *, *, #172170, .F. ) ;
#221077=FACE_OUTER_BOUND ( 'NONE', #114903, .T. ) ;
#221128=CARTESIAN_POINT ( 'NONE',  ( 19.75857864376268935, 11.75000000001116440, -158.7500000000000284 ) ) ;
#221135=CIRCLE ( 'NONE', #158641, 0.09999999999998898659 ) ;
#221150=VERTEX_POINT ( 'NONE', #83009 ) ;
#221161=ORIENTED_EDGE ( 'NONE', *, *, #59936, .F. ) ;
#221185=ORIENTED_EDGE ( 'NONE', *, *, #124829, .T. ) ;
#221186=DIRECTION ( 'NONE',  ( -1.000000000000000000, -0.000000000000000000, -0.000000000000000000 ) ) ;
#221190=ADVANCED_FACE ( 'NONE', ( #47750 ), #244478, .F. ) ;
#221196=CARTESIAN_POINT ( 'NONE',  ( -23.25000000000000000, 2.600000000011156054, -154.2753780772379173 ) ) ;
#221198=DIRECTION ( 'NONE',  ( -1.000000000000000000, 0.000000000000000000, 0.000000000000000000 ) ) ;
#221206=CIRCLE ( 'NONE', #8844, 0.5000000000000004441 ) ;
#221251=LINE ( 'NONE', #218684, #63150 ) ;
#221261=FACE_OUTER_BOUND ( 'NONE', #194130, .T. ) ;
#221264=VECTOR ( 'NONE', #144687, 1000.000000000000000 ) ;
#221300=CARTESIAN_POINT ( 'NONE',  ( 20.85000000000000142, 11.75000000001115907, -160.7161343370219129 ) ) ;
#221304=ADVANCED_FACE ( 'NONE', ( #128597 ), #112883, .T. ) ;
#221305=ORIENTED_EDGE ( 'NONE', *, *, #96776, .F. ) ;
#221329=DIRECTION ( 'NONE',  ( -0.8660254037844653530, 0.000000000000000000, 0.4999999999999539257 ) ) ;
#221378=AXIS2_PLACEMENT_3D ( 'NONE', #111265, #189524, #228660 ) ;
#221388=ORIENTED_EDGE ( 'NONE', *, *, #171763, .T. ) ;
#221391=CARTESIAN_POINT ( 'NONE',  ( 21.05000000000000071, 1.115600667400684642E-11, -167.5000000000000284 ) ) ;
#221417=CARTESIAN_POINT ( 'NONE',  ( -18.58735405345342784, -9.566478620325446158, -174.3227146462660357 ) ) ;
#221430=CARTESIAN_POINT ( 'NONE',  ( -21.14999999999999858, 1.115600667400684642E-11, -127.4593430482987912 ) ) ;
#221447=ORIENTED_EDGE ( 'NONE', *, *, #25651, .F. ) ;
#221452=DIRECTION ( 'NONE',  ( 0.000000000000000000, 0.1350103645451876666, -0.9908441862701600211 ) ) ;
#221469=CIRCLE ( 'NONE', #183896, 0.09999999999999939493 ) ;
#221490=CARTESIAN_POINT ( 'NONE',  ( 21.05000000000000071, 5.000000000011153745, -155.0947339810869323 ) ) ;
#221513=CARTESIAN_POINT ( 'NONE',  ( -22.49533356619863866, 11.65000000631534149, -133.9348774196772354 ) ) ;
#221541=CYLINDRICAL_SURFACE ( 'NONE', #233958, 4.000000000000003553 ) ;
#221551=VERTEX_POINT ( 'NONE', #205242 ) ;
#221560=LINE ( 'NONE', #121249, #63964 ) ;
#221593=EDGE_LOOP ( 'NONE', ( #159375, #41921, #59046 ) ) ;
#221635=VERTEX_POINT ( 'NONE', #249542 ) ;
#221655=AXIS2_PLACEMENT_3D ( 'NONE', #107726, #245967, #131140 ) ;
#221708=CARTESIAN_POINT ( 'NONE',  ( 18.59999999999999076, 6.550000000011156231, -144.0170271704400307 ) ) ;
#221730=CARTESIAN_POINT ( 'NONE',  ( 19.97071067811864609, 11.72071067812981404, -158.6500000000000057 ) ) ;
#221737=FACE_OUTER_BOUND ( 'NONE', #160037, .T. ) ;
#221746=CARTESIAN_POINT ( 'NONE',  ( 23.14999999999999503, 11.65000000001116298, -160.5851942293460866 ) ) ;
#221759=CARTESIAN_POINT ( 'NONE',  ( -20.54999999999999716, 9.350000000011156942, -155.2500000000000284 ) ) ;
#221797=CARTESIAN_POINT ( 'NONE',  ( 23.14999999999999503, 6.450000000011156587, -146.3500000000000227 ) ) ;
#221817=ORIENTED_EDGE ( 'NONE', *, *, #180898, .T. ) ;
#221822=ADVANCED_FACE ( 'NONE', ( #117390 ), #160398, .F. ) ;
#221842=EDGE_CURVE ( 'NONE', #152529, #212362, #202069, .T. ) ;
#221856=EDGE_LOOP ( 'NONE', ( #123702, #27310, #28319, #136500 ) ) ;
#221858=ORIENTED_EDGE ( 'NONE', *, *, #55401, .T. ) ;
#221877=DIRECTION ( 'NONE',  ( 0.000000000000000000, 0.000000000000000000, 1.000000000000000000 ) ) ;
#221879=CARTESIAN_POINT ( 'NONE',  ( -20.94999999999999929, -11.48912529306490349, -136.9000000000000341 ) ) ;
#221886=DIRECTION ( 'NONE',  ( 1.441126678808781001E-14, 0.9876197685951252359, 0.1568667991644863424 ) ) ;
#221902=EDGE_CURVE ( 'NONE', #48580, #105943, #78441, .T. ) ;
#221939=CYLINDRICAL_SURFACE ( 'NONE', #191915, 0.09999999999999939493 ) ;
#221943=CARTESIAN_POINT ( 'NONE',  ( 21.05000000000000071, 5.000000000011153745, -155.4947339810869380 ) ) ;
#221946=DIRECTION ( 'NONE',  ( 1.000000000000000000, 0.000000000000000000, 0.000000000000000000 ) ) ;
#221965=FACE_OUTER_BOUND ( 'NONE', #193345, .T. ) ;
#221978=ADVANCED_FACE ( 'NONE', ( #205905 ), #24309, .T. ) ;
#221983=AXIS2_PLACEMENT_3D ( 'NONE', #160508, #240025, #61377 ) ;
#222013=AXIS2_PLACEMENT_3D ( 'NONE', #109061, #212043, #30850 ) ;
#222022=CYLINDRICAL_SURFACE ( 'NONE', #93867, 0.1000000000000098310 ) ;
#222035=ORIENTED_EDGE ( 'NONE', *, *, #83281, .F. ) ;
#222059=CARTESIAN_POINT ( 'NONE',  ( 21.05000000000000071, -11.64999999998883595, -134.0000000000000000 ) ) ;
#222070=EDGE_LOOP ( 'NONE', ( #130586, #205668, #180260, #102669 ) ) ;
#222074=CARTESIAN_POINT ( 'NONE',  ( 20.77766267348356166, 10.44904239062959839, -141.5927089158778642 ) ) ;
#222107=CARTESIAN_POINT ( 'NONE',  ( -18.50000000000000000, -9.499999999988849808, -122.2500000000000284 ) ) ;
#222121=EDGE_CURVE ( 'NONE', #208712, #8349, #41061, .T. ) ;
#222155=VERTEX_POINT ( 'NONE', #70288 ) ;
#222158=DIRECTION ( 'NONE',  ( -1.000000000000000000, -0.000000000000000000, -0.000000000000000000 ) ) ;
#222159=CARTESIAN_POINT ( 'NONE',  ( -2.995603634470829482E-16, -11.74999999998884448, -158.7500000000000284 ) ) ;
#222162=DIRECTION ( 'NONE',  ( 0.000000000000000000, 0.000000000000000000, -1.000000000000000000 ) ) ;
#222165=DIRECTION ( 'NONE',  ( -1.000000000000000000, 0.000000000000000000, 0.000000000000000000 ) ) ;
#222280=DIRECTION ( 'NONE',  ( 0.000000000000000000, 0.9274965247785529332, 0.3738317757009255171 ) ) ;
#222302=DIRECTION ( 'NONE',  ( 0.000000000000000000, 2.168404344970946942E-15, 1.000000000000000000 ) ) ;
#222351=ORIENTED_EDGE ( 'NONE', *, *, #178234, .F. ) ;
#222371=VERTEX_POINT ( 'NONE', #203023 ) ;
#222382=DIRECTION ( 'NONE',  ( 1.000000000000000000, -0.000000000000000000, -0.000000000000000000 ) ) ;
#222383=VERTEX_POINT ( 'NONE', #24426 ) ;
#222393=CARTESIAN_POINT ( 'NONE',  ( 20.95462737510932882, 10.55678195165489441, -141.5699500565623055 ) ) ;
#222404=ORIENTED_EDGE ( 'NONE', *, *, #118735, .F. ) ;
#222408=AXIS2_PLACEMENT_3D ( 'NONE', #58757, #233581, #35407 ) ;
#222409=CARTESIAN_POINT ( 'NONE',  ( 21.13461538461538325, 10.61458296203669249, -146.3500000000000227 ) ) ;
#222411=DIRECTION ( 'NONE',  ( -1.000000000000000000, -0.000000000000000000, 0.000000000000000000 ) ) ;
#222441=LINE ( 'NONE', #204180, #10939 ) ;
#222466=EDGE_CURVE ( 'NONE', #159346, #245418, #187339, .T. ) ;
#222472=CARTESIAN_POINT ( 'NONE',  ( -18.48179518608866445, -9.518325300483311935, -174.3897055767653512 ) ) ;
#222485=EDGE_CURVE ( 'NONE', #156163, #116539, #152828, .T. ) ;
#222502=AXIS2_PLACEMENT_3D ( 'NONE', #40146, #218727, #139185 ) ;
#222517=EDGE_CURVE ( 'NONE', #116136, #177617, #170379, .T. ) ;
#222534=AXIS2_PLACEMENT_3D ( 'NONE', #76264, #198781, #117970 ) ;
#222585=DIRECTION ( 'NONE',  ( 0.000000000000000000, -2.664535259100396996E-15, 1.000000000000000000 ) ) ;
#222594=VERTEX_POINT ( 'NONE', #171649 ) ;
#222614=CARTESIAN_POINT ( 'NONE',  ( 22.49806830649814060, 0.07746431633666325811, -122.3501103451609424 ) ) ;
#222619=VERTEX_POINT ( 'NONE', #208187 ) ;
#222621=EDGE_CURVE ( 'NONE', #91601, #225500, #99456, .T. ) ;
#222632=FACE_OUTER_BOUND ( 'NONE', #126946, .T. ) ;
#222648=TOROIDAL_SURFACE ( 'NONE', #110236, 0.6000000000000009770, 0.1000000000000000056 ) ;
#222665=DIRECTION ( 'NONE',  ( -1.000000000000000000, -7.304098846218134667E-16, 0.000000000000000000 ) ) ;
#222682=AXIS2_PLACEMENT_3D ( 'NONE', #179692, #40199, #21893 ) ;
#222689=FACE_OUTER_BOUND ( 'NONE', #119493, .T. ) ;
#222708=AXIS2_PLACEMENT_3D ( 'NONE', #171209, #249423, #109885 ) ;
#222743=DIRECTION ( 'NONE',  ( 1.000000000000000000, 0.000000000000000000, 0.000000000000000000 ) ) ;
#222749=EDGE_CURVE ( 'NONE', #223519, #194690, #232217, .T. ) ;
#222762=ORIENTED_EDGE ( 'NONE', *, *, #152535, .T. ) ;
#222786=CARTESIAN_POINT ( 'NONE',  ( -20.94999999999999929, -1.162701749926853712, -142.1000000000000227 ) ) ;
#222790=DIRECTION ( 'NONE',  ( 1.000000000000000000, 0.000000000000000000, 0.000000000000000000 ) ) ;
#222792=CARTESIAN_POINT ( 'NONE',  ( -20.94999999999999929, -1.835341550213255957, -145.5551512925629822 ) ) ;
#222820=CARTESIAN_POINT ( 'NONE',  ( -23.25000000000000000, 4.350000000011156054, -155.3500000000000227 ) ) ;
#222833=CARTESIAN_POINT ( 'NONE',  ( 22.59999999999999432, 0.1008583691098678542, -122.2504328765106152 ) ) ;
#222845=ORIENTED_EDGE ( 'NONE', *, *, #148815, .F. ) ;
#222889=AXIS2_PLACEMENT_3D ( 'NONE', #210172, #133195, #190617 ) ;
#222895=CARTESIAN_POINT ( 'NONE',  ( 21.14999999999999858, 1.115600667400684642E-11, -146.1500000000000341 ) ) ;
#222907=DIRECTION ( 'NONE',  ( 1.000000000000000000, -0.000000000000000000, -0.000000000000000000 ) ) ;
#222963=LINE ( 'NONE', #178757, #96896 ) ;
#222995=ORIENTED_EDGE ( 'NONE', *, *, #245230, .T. ) ;
#223048=ORIENTED_EDGE ( 'NONE', *, *, #224582, .F. ) ;
#223088=AXIS2_PLACEMENT_3D ( 'NONE', #35850, #211918, #192341 ) ;
#223095=ORIENTED_EDGE ( 'NONE', *, *, #18746, .F. ) ;
#223096=DIRECTION ( 'NONE',  ( 0.000000000000000000, 1.000000000000000000, 2.891205793294679805E-16 ) ) ;
#223108=DIRECTION ( 'NONE',  ( 1.000000000000000000, 0.000000000000000000, 0.000000000000000000 ) ) ;
#223118=AXIS2_PLACEMENT_3D ( 'NONE', #68543, #209317, #8568 ) ;
#223123=AXIS2_PLACEMENT_3D ( 'NONE', #106053, #159986, #21746 ) ;
#223129=CIRCLE ( 'NONE', #173123, 0.09999999999998898659 ) ;
#223135=DIRECTION ( 'NONE',  ( 0.000000000000000000, 1.000000000000000000, 1.265107689135680095E-16 ) ) ;
#223143=VERTEX_POINT ( 'NONE', #176469 ) ;
#223178=CARTESIAN_POINT ( 'NONE',  ( 18.59999999999999076, 1.115600667400684642E-11, -167.5000000000000284 ) ) ;
#223213=ORIENTED_EDGE ( 'NONE', *, *, #74399, .F. ) ;
#223223=EDGE_LOOP ( 'NONE', ( #210621, #240508, #234723, #154064 ) ) ;
#223243=ADVANCED_FACE ( 'NONE', ( #73090 ), #190711, .T. ) ;
#223253=CARTESIAN_POINT ( 'NONE',  ( -23.15000000000000213, 1.115600667400684642E-11, -154.6250000000000284 ) ) ;
#223295=DIRECTION ( 'NONE',  ( 1.000000000000000000, 0.000000000000000000, 0.000000000000000000 ) ) ;
#223309=EDGE_CURVE ( 'NONE', #237217, #27502, #124239, .T. ) ;
#223324=FACE_OUTER_BOUND ( 'NONE', #243610, .T. ) ;
#223396=CARTESIAN_POINT ( 'NONE',  ( 18.49999999999999645, 1.162701749949165642, -142.1000000000000227 ) ) ;
#223399=CARTESIAN_POINT ( 'NONE',  ( 23.14999999999998437, -11.74999999998884448, -134.0000000000000000 ) ) ;
#223406=AXIS2_PLACEMENT_3D ( 'NONE', #50460, #130004, #209567 ) ;
#223414=ORIENTED_EDGE ( 'NONE', *, *, #214919, .F. ) ;
#223430=EDGE_CURVE ( 'NONE', #51735, #229756, #149371, .T. ) ;
#223442=CARTESIAN_POINT ( 'NONE',  ( -21.05000000000000071, -1.835341550213255957, -145.5551512925629822 ) ) ;
#223482=DIRECTION ( 'NONE',  ( -2.952720810173289112E-16, 1.000000000000000000, 0.000000000000000000 ) ) ;
#223508=CARTESIAN_POINT ( 'NONE',  ( 23.14999999999999858, 4.775700934590591196, -155.6512318959540551 ) ) ;
#223519=VERTEX_POINT ( 'NONE', #179389 ) ;
#223544=CIRCLE ( 'NONE', #256828, 0.09999999999998898659 ) ;
#223552=DIRECTION ( 'NONE',  ( 1.000000000000000000, 0.000000000000000000, 0.000000000000000000 ) ) ;
#223558=CARTESIAN_POINT ( 'NONE',  ( 18.50000000000000000, -9.399999999988843058, -174.3820418481727188 ) ) ;
#223564=DIRECTION ( 'NONE',  ( 0.000000000000000000, 0.000000000000000000, -1.000000000000000000 ) ) ;
#223566=DIRECTION ( 'NONE',  ( 1.000000000000000000, 0.000000000000000000, 0.000000000000000000 ) ) ;
#223569=AXIS2_PLACEMENT_3D ( 'NONE', #232391, #186833, #148998 ) ;
#223598=ORIENTED_EDGE ( 'NONE', *, *, #85609, .T. ) ;
#223609=DIRECTION ( 'NONE',  ( 0.000000000000000000, 0.000000000000000000, 1.000000000000000000 ) ) ;
#223634=CARTESIAN_POINT ( 'NONE',  ( -20.94999999999999929, 1.115600667400684642E-11, -167.5000000000000284 ) ) ;
#223664=DIRECTION ( 'NONE',  ( 1.000000000000000000, 0.000000000000000000, -0.000000000000000000 ) ) ;
#223668=TOROIDAL_SURFACE ( 'NONE', #223123, 0.2000000000000000111, 0.1000000000000000056 ) ;
#223677=ADVANCED_FACE ( 'NONE', ( #216896 ), #37017, .T. ) ;
#223692=DIRECTION ( 'NONE',  ( 0.000000000000000000, 0.000000000000000000, 1.000000000000000000 ) ) ;
#223723=ORIENTED_EDGE ( 'NONE', *, *, #180288, .T. ) ;
#223786=EDGE_CURVE ( 'NONE', #89589, #83182, #18708, .T. ) ;
#223796=AXIS2_PLACEMENT_3D ( 'NONE', #116958, #136494, #97353 ) ;
#223800=DIRECTION ( 'NONE',  ( 0.000000000000000000, 0.000000000000000000, 1.000000000000000000 ) ) ;
#223808=DIRECTION ( 'NONE',  ( 1.000000000000000000, -0.000000000000000000, -0.000000000000000000 ) ) ;
#223828=DIRECTION ( 'NONE',  ( -1.000000000000000000, -2.952720810173289112E-16, 0.000000000000000000 ) ) ;
#223837=CARTESIAN_POINT ( 'NONE',  ( 19.97071067811864609, 11.72071067812981404, -158.7500000000000284 ) ) ;
#223847=CARTESIAN_POINT ( 'NONE',  ( 18.39999999999999858, -9.499999999988844479, -174.4221498493304239 ) ) ;
#223854=ORIENTED_EDGE ( 'NONE', *, *, #9379, .F. ) ;
#223858=CARTESIAN_POINT ( 'NONE',  ( 23.14999999999999503, 11.65000000001116298, -146.2500000000000284 ) ) ;
#223863=CARTESIAN_POINT ( 'NONE',  ( -23.15000000000000213, 1.115600667400684642E-11, -167.5000000000000284 ) ) ;
#223878=LINE ( 'NONE', #101329, #154863 ) ;
#223886=VECTOR ( 'NONE', #136954, 1000.000000000000000 ) ;
#223906=EDGE_CURVE ( 'NONE', #253143, #199368, #99500, .T. ) ;
#223913=ORIENTED_EDGE ( 'NONE', *, *, #62770, .T. ) ;
#223918=DIRECTION ( 'NONE',  ( -7.304098846218201720E-16, 1.000000000000000000, 0.000000000000000000 ) ) ;
#223924=DIRECTION ( 'NONE',  ( 1.000000000000000000, 3.469446951953704435E-14, -2.003086131649669752E-14 ) ) ;
#223946=CYLINDRICAL_SURFACE ( 'NONE', #205873, 0.09999999999999817368 ) ;
#223951=DIRECTION ( 'NONE',  ( 0.000000000000000000, 0.000000000000000000, 1.000000000000000000 ) ) ;
#223984=DIRECTION ( 'NONE',  ( 0.000000000000000000, 0.8700118002898321601, -0.4930308989875230585 ) ) ;
#224001=ORIENTED_EDGE ( 'NONE', *, *, #157741, .F. ) ;
#224022=VECTOR ( 'NONE', #75353, 1000.000000000000000 ) ;
#224059=DIRECTION ( 'NONE',  ( 1.000000000000000000, -0.000000000000000000, -0.000000000000000000 ) ) ;
#224075=VERTEX_POINT ( 'NONE', #248020 ) ;
#224076=DIRECTION ( 'NONE',  ( -1.000000000000000000, 0.000000000000000000, 0.000000000000000000 ) ) ;
#224095=VERTEX_POINT ( 'NONE', #253156 ) ;
#224103=CARTESIAN_POINT ( 'NONE',  ( -20.94999999999999929, -11.29603075032412995, -137.0478991596638991 ) ) ;
#224113=AXIS2_PLACEMENT_3D ( 'NONE', #146062, #45687, #204748 ) ;
#224114=CARTESIAN_POINT ( 'NONE',  ( -18.59999999999999787, 1.115600667400684642E-11, -134.0000000000000000 ) ) ;
#224119=ORIENTED_EDGE ( 'NONE', *, *, #255759, .T. ) ;
#224143=AXIS2_PLACEMENT_3D ( 'NONE', #174097, #171516, #193617 ) ;
#224151=LINE ( 'NONE', #143334, #153182 ) ;
#224158=AXIS2_PLACEMENT_3D ( 'NONE', #165700, #200946, #203521 ) ;
#224186=FACE_OUTER_BOUND ( 'NONE', #179999, .T. ) ;
#224188=DIRECTION ( 'NONE',  ( 0.7071359030028113724, 0.000000000000000000, 0.7070776581708677622 ) ) ;
#224200=CARTESIAN_POINT ( 'NONE',  ( 21.04999999999999361, -0.01759718699768685404, -127.5592291063394725 ) ) ;
#224208=CIRCLE ( 'NONE', #111799, 0.09999999999999939493 ) ;
#224215=DIRECTION ( 'NONE',  ( 1.000000000000000000, 0.000000000000000000, 0.000000000000000000 ) ) ;
#224233=CARTESIAN_POINT ( 'NONE',  ( -22.47071067811865319, 7.720074744509219933, -133.9009075452974002 ) ) ;
#224253=EDGE_CURVE ( 'NONE', #125106, #73834, #183045, .T. ) ;
#224254=AXIS2_PLACEMENT_3D ( 'NONE', #219908, #144202, #165071 ) ;
#224256=DIRECTION ( 'NONE',  ( 0.000000000000000000, 0.000000000000000000, -1.000000000000000000 ) ) ;
#224259=CARTESIAN_POINT ( 'NONE',  ( -20.94999999999999929, 11.60000000001115517, -160.5717967697245285 ) ) ;
#224275=CIRCLE ( 'NONE', #111874, 0.09999999999999939493 ) ;
#224277=ORIENTED_EDGE ( 'NONE', *, *, #128764, .T. ) ;
#224279=VECTOR ( 'NONE', #109323, 1000.000000000000000 ) ;
#224287=ORIENTED_EDGE ( 'NONE', *, *, #12259, .F. ) ;
#224303=EDGE_CURVE ( 'NONE', #180800, #31307, #41400, .T. ) ;
#224360=CARTESIAN_POINT ( 'NONE',  ( -20.94999999999999929, -1.164121893230052995, -175.4148480855716059 ) ) ;
#224362=VECTOR ( 'NONE', #182939, 1000.000000000000000 ) ;
#224370=FACE_OUTER_BOUND ( 'NONE', #42770, .T. ) ;
#224381=ORIENTED_EDGE ( 'NONE', *, *, #256300, .T. ) ;
#224450=CARTESIAN_POINT ( 'NONE',  ( 21.05000000000000071, 10.72371710471868056, -141.6649135690876449 ) ) ;
#224458=FACE_OUTER_BOUND ( 'NONE', #31594, .T. ) ;
#224464=DIRECTION ( 'NONE',  ( 1.000000000000000000, -0.000000000000000000, -0.000000000000000000 ) ) ;
#224467=DIRECTION ( 'NONE',  ( 1.000000000000000000, 0.000000000000000000, -0.000000000000000000 ) ) ;
#224468=CARTESIAN_POINT ( 'NONE',  ( -21.44999999999999929, 7.350000000011155166, -155.2500000000000284 ) ) ;
#224480=ORIENTED_EDGE ( 'NONE', *, *, #186029, .F. ) ;
#224489=CARTESIAN_POINT ( 'NONE',  ( -18.50000000000000000, 9.250000000011157297, -155.2500000000000284 ) ) ;
#224495=CARTESIAN_POINT ( 'NONE',  ( 20.94560253601876809, 11.75000000001115907, -160.5100835125150809 ) ) ;
#224496=ADVANCED_FACE ( 'NONE', ( #149930 ), #132926, .T. ) ;
#224506=AXIS2_PLACEMENT_3D ( 'NONE', #57999, #81400, #176705 ) ;
#224527=AXIS2_PLACEMENT_3D ( 'NONE', #222107, #124329, #246828 ) ;
#224547=CARTESIAN_POINT ( 'NONE',  ( -23.25000000000000000, 11.65000000001115588, -134.0000000000000000 ) ) ;
#224568=DIRECTION ( 'NONE',  ( 0.000000000000000000, -1.000000000000000000, 0.000000000000000000 ) ) ;
#224582=EDGE_CURVE ( 'NONE', #141490, #177470, #185986, .T. ) ;
#224595=ORIENTED_EDGE ( 'NONE', *, *, #225628, .T. ) ;
#224596=AXIS2_PLACEMENT_3D ( 'NONE', #61951, #64515, #205290 ) ;
#224597=DIRECTION ( 'NONE',  ( -1.000000000000000000, 0.000000000000000000, 0.000000000000000000 ) ) ;
#224615=CARTESIAN_POINT ( 'NONE',  ( -20.94999999999999929, 1.115600667400684642E-11, -167.5000000000000284 ) ) ;
#224667=CARTESIAN_POINT ( 'NONE',  ( 20.77526135991795186, 8.932009016637321608, -142.4685685427219539 ) ) ;
#224742=VERTEX_POINT ( 'NONE', #81883 ) ;
#224792=CARTESIAN_POINT ( 'NONE',  ( -20.94999999999999929, 1.115600667400684642E-11, -155.8000000000000398 ) ) ;
#224794=DIRECTION ( 'NONE',  ( 6.484947573744954877E-15, 0.9274965247785529332, -0.3738317757009255171 ) ) ;
#224852=CARTESIAN_POINT ( 'NONE',  ( 23.14999999999998437, 1.115650265596050101E-11, -129.9500000000000171 ) ) ;
#224875=ORIENTED_EDGE ( 'NONE', *, *, #147284, .F. ) ;
#224878=VERTEX_POINT ( 'NONE', #32243 ) ;
#224928=ORIENTED_EDGE ( 'NONE', *, *, #239965, .T. ) ;
#224943=CIRCLE ( 'NONE', #253995, 0.09999999999999939493 ) ;
#224961=AXIS2_PLACEMENT_3D ( 'NONE', #115189, #55171, #134727 ) ;
#224965=EDGE_LOOP ( 'NONE', ( #194914, #191414, #149250, #254804, #177074 ) ) ;
#224970=CARTESIAN_POINT ( 'NONE',  ( 20.04142135391667168, 11.75000000001116263, -158.7025068656295446 ) ) ;
#224974=CARTESIAN_POINT ( 'NONE',  ( -22.59999999999999787, 0.1008583691098682150, -122.2504328765106294 ) ) ;
#225026=ORIENTED_EDGE ( 'NONE', *, *, #125274, .T. ) ;
#225042=CARTESIAN_POINT ( 'NONE',  ( -18.36527282682077100, -9.500000599987968641, -174.4221489645001952 ) ) ;
#225093=DIRECTION ( 'NONE',  ( 0.000000000000000000, 0.4930308989875230585, 0.8700118002898322711 ) ) ;
#225115=ORIENTED_EDGE ( 'NONE', *, *, #130866, .T. ) ;
#225133=EDGE_CURVE ( 'NONE', #95988, #213361, #58004, .T. ) ;
#225167=ADVANCED_FACE ( 'NONE', ( #167280 ), #250622, .T. ) ;
#225199=DIRECTION ( 'NONE',  ( 1.000000000000000000, 2.952720810173289112E-16, -0.000000000000000000 ) ) ;
#225211=ADVANCED_FACE ( 'NONE', ( #125551 ), #205068, .F. ) ;
#225226=SPHERICAL_SURFACE ( 'NONE', #72651, 0.1000000000000000056 ) ;
#225272=ORIENTED_EDGE ( 'NONE', *, *, #30549, .T. ) ;
#225290=AXIS2_PLACEMENT_3D ( 'NONE', #9714, #110103, #189652 ) ;
#225323=CARTESIAN_POINT ( 'NONE',  ( 20.94999999999999929, 5.000000000011153745, -155.0947339810869323 ) ) ;
#225328=AXIS2_PLACEMENT_3D ( 'NONE', #211022, #28586, #188889 ) ;
#225333=CARTESIAN_POINT ( 'NONE',  ( -23.25000000000000000, 1.115600667400684642E-11, -134.0000000000000000 ) ) ;
#225359=DIRECTION ( 'NONE',  ( 1.000000000000000000, 3.265361837132813093E-16, -0.000000000000000000 ) ) ;
#225365=CARTESIAN_POINT ( 'NONE',  ( -21.05000000000000071, 11.62071067812980907, -140.8684166523410681 ) ) ;
#225392=DIRECTION ( 'NONE',  ( 0.000000000000000000, 0.000000000000000000, -1.000000000000000000 ) ) ;
#225399=EDGE_CURVE ( 'NONE', #55107, #26254, #116946, .T. ) ;
#225452=FACE_OUTER_BOUND ( 'NONE', #46704, .T. ) ;
#225453=CARTESIAN_POINT ( 'NONE',  ( -20.94999999999999929, -1.835341550213257733, -145.5551512925629822 ) ) ;
#225475=CIRCLE ( 'NONE', #225290, 0.09999999999998898659 ) ;
#225476=AXIS2_PLACEMENT_3D ( 'NONE', #251108, #253684, #72512 ) ;
#225497=ORIENTED_EDGE ( 'NONE', *, *, #188443, .F. ) ;
#225500=VERTEX_POINT ( 'NONE', #120157 ) ;
#225512=DIRECTION ( 'NONE',  ( 0.000000000000000000, 1.265107689135680095E-16, -1.000000000000000000 ) ) ;
#225554=ADVANCED_FACE ( 'NONE', ( #144796 ), #148684, .F. ) ;
#225563=EDGE_LOOP ( 'NONE', ( #135078, #68941, #152669 ) ) ;
#225583=ORIENTED_EDGE ( 'NONE', *, *, #155124, .F. ) ;
#225597=ORIENTED_EDGE ( 'NONE', *, *, #9330, .T. ) ;
#225623=ADVANCED_BREP_SHAPE_REPRESENTATION ( '', ( #197191, #2425 ), #193986 ) ;
#225628=EDGE_CURVE ( 'NONE', #63952, #224878, #249072, .T. ) ;
#225640=LINE ( 'NONE', #199714, #91738 ) ;
#225658=CARTESIAN_POINT ( 'NONE',  ( 20.85000000000000142, 0.1610488207298751417, -167.2158101556397867 ) ) ;
#225663=FACE_OUTER_BOUND ( 'NONE', #34643, .T. ) ;
#225664=DIRECTION ( 'NONE',  ( 2.978066053179067751E-16, -1.000000000000000000, 0.000000000000000000 ) ) ;
#225672=DIRECTION ( 'NONE',  ( 0.000000000000000000, 0.000000000000000000, 1.000000000000000000 ) ) ;
#225691=CARTESIAN_POINT ( 'NONE',  ( 20.94999999999999574, -11.39257802169451672, -137.0739495798319467 ) ) ;
#225717=CARTESIAN_POINT ( 'NONE',  ( 21.13461538461538680, 8.885417037985613220, -146.2500000000000568 ) ) ;
#225744=ORIENTED_EDGE ( 'NONE', *, *, #157689, .T. ) ;
#225763=EDGE_CURVE ( 'NONE', #20940, #116282, #230021, .T. ) ;
#225764=CARTESIAN_POINT ( 'NONE',  ( 21.04386569057559697, 11.75000000001105427, -160.6428373517805710 ) ) ;
#225797=DIRECTION ( 'NONE',  ( 0.000000000000000000, 0.000000000000000000, 1.000000000000000000 ) ) ;
#225831=EDGE_CURVE ( 'NONE', #243619, #178254, #5139, .T. ) ;
#225840=EDGE_CURVE ( 'NONE', #195640, #134466, #237198, .T. ) ;
#225842=ORIENTED_EDGE ( 'NONE', *, *, #243426, .T. ) ;
#225874=AXIS2_PLACEMENT_3D ( 'NONE', #166892, #207285, #246396 ) ;
#225894=ORIENTED_EDGE ( 'NONE', *, *, #38022, .T. ) ;
#225899=ADVANCED_FACE ( 'NONE', ( #61114 ), #3705, .T. ) ;
#225908=CARTESIAN_POINT ( 'NONE',  ( 21.04999999999999716, -0.03753606327451243507, -127.6677277260643564 ) ) ;
#225909=DIRECTION ( 'NONE',  ( -1.000000000000000000, -7.304098846218135653E-16, 4.607487905232624742E-31 ) ) ;
#225910=FACE_OUTER_BOUND ( 'NONE', #71683, .T. ) ;
#225924=EDGE_CURVE ( 'NONE', #99917, #174669, #126260, .T. ) ;
#225925=CARTESIAN_POINT ( 'NONE',  ( 20.12481660106788084, 9.526343992285099205, -142.2261416690962506 ) ) ;
#225953=DIRECTION ( 'NONE',  ( 0.000000000000000000, 1.734723475976807292E-15, -1.000000000000000000 ) ) ;
#225955=DIRECTION ( 'NONE',  ( 0.000000000000000000, 1.000000000000000000, 0.000000000000000000 ) ) ;
#225968=EDGE_LOOP ( 'NONE', ( #29455, #59088, #161010, #214776 ) ) ;
#225974=AXIS2_PLACEMENT_3D ( 'NONE', #71579, #230640, #247623 ) ;
#225985=ORIENTED_EDGE ( 'NONE', *, *, #164436, .T. ) ;
#226035=ORIENTED_EDGE ( 'NONE', *, *, #61688, .T. ) ;
#226049=ADVANCED_FACE ( 'NONE', ( #90947 ), #131359, .T. ) ;
#226060=VECTOR ( 'NONE', #156067, 999.9999999999998863 ) ;
#226063=FACE_OUTER_BOUND ( 'NONE', #257913, .T. ) ;
#226065=VERTEX_POINT ( 'NONE', #50515 ) ;
#226071=ORIENTED_EDGE ( 'NONE', *, *, #218294, .T. ) ;
#226085=VERTEX_POINT ( 'NONE', #11433 ) ;
#226117=CARTESIAN_POINT ( 'NONE',  ( -21.14999999999999858, -11.64999999998884483, -134.0000000000000000 ) ) ;
#226140=VERTEX_POINT ( 'NONE', #229193 ) ;
#226156=ADVANCED_FACE ( 'NONE', ( #93512 ), #164349, .T. ) ;
#226165=ORIENTED_EDGE ( 'NONE', *, *, #80788, .F. ) ;
#226167=CARTESIAN_POINT ( 'NONE',  ( -22.50000000000000000, 11.65000000001115588, -134.0000000000000284 ) ) ;
#226180=DIRECTION ( 'NONE',  ( 0.000000000000000000, 0.000000000000000000, -1.000000000000000000 ) ) ;
#226184=DIRECTION ( 'NONE',  ( -3.890533409366484652E-14, -0.1298341882520124002, -0.9915357197604841577 ) ) ;
#226200=FACE_OUTER_BOUND ( 'NONE', #104068, .T. ) ;
#226204=DIRECTION ( 'NONE',  ( 0.000000000000000000, 0.000000000000000000, -1.000000000000000000 ) ) ;
#226211=DIRECTION ( 'NONE',  ( 0.000000000000000000, -0.1350103645451876666, -0.9908441862701600211 ) ) ;
#226245=LINE ( 'NONE', #187173, #213469 ) ;
#226246=CARTESIAN_POINT ( 'NONE',  ( -18.59999999999999787, -1.362429037182155023, -175.3888812479212334 ) ) ;
#226307=CARTESIAN_POINT ( 'NONE',  ( 21.13461538461538325, 8.885417037985616773, -146.3500000000000227 ) ) ;
#226335=DIRECTION ( 'NONE',  ( 1.000000000000000000, 1.836970198721029934E-16, -0.000000000000000000 ) ) ;
#226341=DIRECTION ( 'NONE',  ( -1.000000000000000000, -1.875376730785737719E-16, -0.000000000000000000 ) ) ;
#226360=AXIS2_PLACEMENT_3D ( 'NONE', #165612, #146020, #126465 ) ;
#226366=FACE_OUTER_BOUND ( 'NONE', #119740, .T. ) ;
#226375=DIRECTION ( 'NONE',  ( 0.000000000000000000, -0.8700118002898321601, 0.4930308989875230030 ) ) ;
#226382=VECTOR ( 'NONE', #86006, 1000.000000000000000 ) ;
#226463=FACE_OUTER_BOUND ( 'NONE', #13520, .T. ) ;
#226467=EDGE_CURVE ( 'NONE', #205134, #218074, #38983, .T. ) ;
#226468=CARTESIAN_POINT ( 'NONE',  ( -20.85000000000000142, 6.933893972137497030, -171.2856458343736108 ) ) ;
#226477=AXIS2_PLACEMENT_3D ( 'NONE', #31837, #168801, #248286 ) ;
#226495=EDGE_LOOP ( 'NONE', ( #252913, #87445, #242985, #65640, #26166 ) ) ;
#226499=LINE ( 'NONE', #186117, #76615 ) ;
#226504=CARTESIAN_POINT ( 'NONE',  ( -20.64999999999999858, 4.350000000011156054, -146.3500000000000227 ) ) ;
#226509=PLANE ( 'NONE',  #139239 ) ;
#226511=ORIENTED_EDGE ( 'NONE', *, *, #217623, .T. ) ;
#226514=AXIS2_PLACEMENT_3D ( 'NONE', #183468, #100039, #59625 ) ;
#226519=ORIENTED_EDGE ( 'NONE', *, *, #223309, .F. ) ;
#226554=AXIS2_PLACEMENT_3D ( 'NONE', #113913, #39553, #35697 ) ;
#226563=ORIENTED_EDGE ( 'NONE', *, *, #15321, .F. ) ;
#226581=AXIS2_PLACEMENT_3D ( 'NONE', #205538, #141724, #7354 ) ;
#226613=CIRCLE ( 'NONE', #105800, 0.09999999999998898659 ) ;
#226638=CONICAL_SURFACE ( 'NONE', #167848, 7.750000000000034639, 0.7853981633974531640 ) ;
#226642=CARTESIAN_POINT ( 'NONE',  ( -23.15000000000000213, 2.000000000011154189, -154.8753780772379116 ) ) ;
#226676=DIRECTION ( 'NONE',  ( 0.000000000000000000, 0.000000000000000000, -1.000000000000000000 ) ) ;
#226682=EDGE_CURVE ( 'NONE', #247600, #175543, #145159, .T. ) ;
#226692=CARTESIAN_POINT ( 'NONE',  ( -18.39999999999999858, -9.499999999988849808, -174.1001893912220737 ) ) ;
#226733=EDGE_LOOP ( 'NONE', ( #138990, #10016, #158471, #219521 ) ) ;
#226747=EDGE_CURVE ( 'NONE', #111708, #99517, #101659, .T. ) ;
#226847=AXIS2_PLACEMENT_3D ( 'NONE', #107922, #170524, #30993 ) ;
#226853=EDGE_LOOP ( 'NONE', ( #64629, #186348, #190687, #80594 ) ) ;
#226893=ORIENTED_EDGE ( 'NONE', *, *, #197054, .T. ) ;
#226896=ORIENTED_EDGE ( 'NONE', *, *, #198190, .T. ) ;
#226902=ORIENTED_EDGE ( 'NONE', *, *, #30056, .T. ) ;
#226905=CARTESIAN_POINT ( 'NONE',  ( -23.25000000000000000, -9.599999999988838795, -157.6060308773475924 ) ) ;
#226936=TOROIDAL_SURFACE ( 'NONE', #2052, 2.100000000000002309, 0.1000000000000000056 ) ;
#226940=ORIENTED_EDGE ( 'NONE', *, *, #129444, .F. ) ;
#226945=DIRECTION ( 'NONE',  ( 0.000000000000000000, 0.000000000000000000, -1.000000000000000000 ) ) ;
#226962=ORIENTED_EDGE ( 'NONE', *, *, #126776, .T. ) ;
#226965=DIRECTION ( 'NONE',  ( -0.000000000000000000, -0.000000000000000000, 1.000000000000000000 ) ) ;
#226986=AXIS2_PLACEMENT_3D ( 'NONE', #209830, #50716, #195420 ) ;
#227039=DIRECTION ( 'NONE',  ( 1.000000000000000000, 0.000000000000000000, -0.000000000000000000 ) ) ;
#227072=AXIS2_PLACEMENT_3D ( 'NONE', #182438, #205835, #123741 ) ;
#227079=CARTESIAN_POINT ( 'NONE',  ( 18.49999999999999289, 10.20857864377384416, -158.6500000000000057 ) ) ;
#227147=CYLINDRICAL_SURFACE ( 'NONE', #31404, 0.1000000000000098310 ) ;
#227152=ORIENTED_EDGE ( 'NONE', *, *, #46523, .T. ) ;
#227177=CARTESIAN_POINT ( 'NONE',  ( 19.99999999999998934, 11.75000000001115552, -155.3500000000000227 ) ) ;
#227216=CARTESIAN_POINT ( 'NONE',  ( -23.25000000000000000, -11.74999999998884448, -122.2500000000000284 ) ) ;
#227234=TOROIDAL_SURFACE ( 'NONE', #198007, 11.70000000000000639, 0.1000000000000000056 ) ;
#227243=ORIENTED_EDGE ( 'NONE', *, *, #157449, .F. ) ;
#227246=ORIENTED_EDGE ( 'NONE', *, *, #176592, .F. ) ;
#227270=DIRECTION ( 'NONE',  ( 1.000000000000000000, -0.000000000000000000, -0.000000000000000000 ) ) ;
#227275=ORIENTED_EDGE ( 'NONE', *, *, #94, .T. ) ;
#227295=DIRECTION ( 'NONE',  ( 0.000000000000000000, 1.000000000000000000, 0.000000000000000000 ) ) ;
#227299=FACE_OUTER_BOUND ( 'NONE', #138626, .T. ) ;
#227344=VERTEX_POINT ( 'NONE', #239669 ) ;
#227349=EDGE_LOOP ( 'NONE', ( #86840, #242624, #69123, #53968 ) ) ;
#227353=VERTEX_POINT ( 'NONE', #78010 ) ;
#227357=AXIS2_PLACEMENT_3D ( 'NONE', #235178, #56508, #77365 ) ;
#227379=ORIENTED_EDGE ( 'NONE', *, *, #111327, .F. ) ;
#227487=ORIENTED_EDGE ( 'NONE', *, *, #224303, .T. ) ;
#227496=FACE_OUTER_BOUND ( 'NONE', #144842, .T. ) ;
#227510=ORIENTED_EDGE ( 'NONE', *, *, #128612, .T. ) ;
#227515=DIRECTION ( 'NONE',  ( -3.265361837132813093E-16, 1.000000000000000000, 0.000000000000000000 ) ) ;
#227543=AXIS2_PLACEMENT_3D ( 'NONE', #55396, #95820, #254855 ) ;
#227578=CARTESIAN_POINT ( 'NONE',  ( 20.94999999999999929, 4.813084112160684214, -155.5584822434762202 ) ) ;
#227591=AXIS2_PLACEMENT_3D ( 'NONE', #50563, #110557, #147108 ) ;
#227595=ORIENTED_EDGE ( 'NONE', *, *, #222485, .T. ) ;
#227621=CARTESIAN_POINT ( 'NONE',  ( -18.57399277249657032, 10.33112638556969465, -173.0901228926974795 ) ) ;
#227648=ORIENTED_EDGE ( 'NONE', *, *, #120612, .F. ) ;
#227653=DIRECTION ( 'NONE',  ( 0.000000000000000000, 0.000000000000000000, 1.000000000000000000 ) ) ;
#227660=EDGE_CURVE ( 'NONE', #128128, #55661, #59387, .T. ) ;
#227662=CARTESIAN_POINT ( 'NONE',  ( -18.44362607810622023, -9.490496158073668198, -141.0579538668471855 ) ) ;
#227667=EDGE_CURVE ( 'NONE', #196105, #107215, #68742, .T. ) ;
#227669=CARTESIAN_POINT ( 'NONE',  ( -20.54999999999999716, 4.350000000011156054, -155.1500000000000057 ) ) ;
#227691=CARTESIAN_POINT ( 'NONE',  ( 20.94999999999999574, -11.64999999998883595, -137.0000000000000000 ) ) ;
#227705=DIRECTION ( 'NONE',  ( 1.000000000000000000, 0.000000000000000000, 0.000000000000000000 ) ) ;
#227710=CARTESIAN_POINT ( 'NONE',  ( 18.47149038651510367, -9.671457157995551057, -174.1727863347384471 ) ) ;
#227727=DIRECTION ( 'NONE',  ( 0.000000000000000000, 0.000000000000000000, -1.000000000000000000 ) ) ;
#227752=AXIS2_PLACEMENT_3D ( 'NONE', #190779, #151650, #231181 ) ;
#227769=CARTESIAN_POINT ( 'NONE',  ( 20.94999999999999929, 5.400000000011154988, -146.4052660189131245 ) ) ;
#227855=AXIS2_PLACEMENT_3D ( 'NONE', #12078, #248087, #131997 ) ;
#227867=B_SPLINE_CURVE_WITH_KNOTS ( 'NONE', 3,
 ( #220904, #137512, #97081, #117971 ),
 .UNSPECIFIED., .F., .F.,
 ( 4, 4 ),
 ( 0.000000000000000000, 0.0002118541922231684618 ),
 .UNSPECIFIED. ) ;
#227875=DIRECTION ( 'NONE',  ( 0.000000000000000000, 0.4999999999999478195, 0.8660254037844686836 ) ) ;
#227877=FACE_OUTER_BOUND ( 'NONE', #216590, .T. ) ;
#227883=VERTEX_POINT ( 'NONE', #420 ) ;
#227887=ORIENTED_EDGE ( 'NONE', *, *, #252813, .T. ) ;
#227920=CARTESIAN_POINT ( 'NONE',  ( -21.10320863425827298, 0.02502225123826237740, -127.5997226135408056 ) ) ;
#227922=DIRECTION ( 'NONE',  ( -1.000000000000000000, -0.000000000000000000, -0.000000000000000000 ) ) ;
#227930=CIRCLE ( 'NONE', #98702, 0.1000000000000102612 ) ;
#227933=DIRECTION ( 'NONE',  ( 0.7071067811865475727, 0.7071067811865475727, 0.000000000000000000 ) ) ;
#227936=CYLINDRICAL_SURFACE ( 'NONE', #104395, 0.09999999999998898659 ) ;
#227944=CARTESIAN_POINT ( 'NONE',  ( -22.37643362114956602, 0.09908137369253962323, -126.3742100060416220 ) ) ;
#227946=ORIENTED_EDGE ( 'NONE', *, *, #93600, .T. ) ;
#227950=DIRECTION ( 'NONE',  ( 0.000000000000000000, -0.8660254037844383745, 0.5000000000000003331 ) ) ;
#227970=CARTESIAN_POINT ( 'NONE',  ( 18.59999999999999787, -1.263275465206102233, -175.4018646667464338 ) ) ;
#228036=CIRCLE ( 'NONE', #11371, 0.09999999999999939493 ) ;
#228040=AXIS2_PLACEMENT_3D ( 'NONE', #184201, #5554, #145076 ) ;
#228042=EDGE_LOOP ( 'NONE', ( #66851, #81201, #129619, #254410, #234804 ) ) ;
#228045=VECTOR ( 'NONE', #41480, 1000.000000000000000 ) ;
#228051=CARTESIAN_POINT ( 'NONE',  ( -20.64999999999999858, 2.000000000011154189, -146.7246219227621111 ) ) ;
#228061=ORIENTED_EDGE ( 'NONE', *, *, #186895, .F. ) ;
#228069=EDGE_CURVE ( 'NONE', #60110, #186782, #22586, .T. ) ;
#228087=EDGE_CURVE ( 'NONE', #220745, #105532, #45980, .T. ) ;
#228099=ORIENTED_EDGE ( 'NONE', *, *, #225831, .F. ) ;
#228115=VERTEX_POINT ( 'NONE', #168554 ) ;
#228137=ORIENTED_EDGE ( 'NONE', *, *, #106982, .T. ) ;
#228174=DIRECTION ( 'NONE',  ( 1.000000000000000000, -0.000000000000000000, 0.000000000000000000 ) ) ;
#228188=ORIENTED_EDGE ( 'NONE', *, *, #25067, .F. ) ;
#228203=EDGE_CURVE ( 'NONE', #213361, #194690, #171118, .T. ) ;
#228212=AXIS2_PLACEMENT_3D ( 'NONE', #51142, #188116, #168606 ) ;
#228242=DIRECTION ( 'NONE',  ( 1.000000000000000000, 0.000000000000000000, -0.000000000000000000 ) ) ;
#228250=LINE ( 'NONE', #186555, #83590 ) ;
#228280=VECTOR ( 'NONE', #249380, 1000.000000000000000 ) ;
#228298=CARTESIAN_POINT ( 'NONE',  ( 20.94999999999999929, -9.399999999988846611, -143.8939691226524644 ) ) ;
#228299=ORIENTED_EDGE ( 'NONE', *, *, #179730, .T. ) ;
#228321=CARTESIAN_POINT ( 'NONE',  ( 21.06277459767432703, 8.872862438279403463, -146.2039991923570881 ) ) ;
#228399=AXIS2_PLACEMENT_3D ( 'NONE', #167483, #164892, #26684 ) ;
#228407=DIRECTION ( 'NONE',  ( 0.000000000000000000, 0.1575844902526876978, 0.9875055080513731598 ) ) ;
#228412=EDGE_CURVE ( 'NONE', #154251, #87157, #124896, .T. ) ;
#228415=DIRECTION ( 'NONE',  ( -0.000000000000000000, -0.000000000000000000, -1.000000000000000000 ) ) ;
#228429=EDGE_LOOP ( 'NONE', ( #40607, #99155, #50404, #119030 ) ) ;
#228532=AXIS2_PLACEMENT_3D ( 'NONE', #74330, #228242, #132997 ) ;
#228534=AXIS2_PLACEMENT_3D ( 'NONE', #33753, #92382, #254020 ) ;
#228561=CARTESIAN_POINT ( 'NONE',  ( 22.39999999999999858, 0.1000000000111554016, -126.2092204016266379 ) ) ;
#228575=CARTESIAN_POINT ( 'NONE',  ( -21.05000000000000071, -1.835341550213255957, -145.5551512925629822 ) ) ;
#228576=AXIS2_PLACEMENT_3D ( 'NONE', #192230, #154414, #250889 ) ;
#228583=ORIENTED_EDGE ( 'NONE', *, *, #80459, .F. ) ;
#228588=EDGE_CURVE ( 'NONE', #114955, #203670, #131298, .T. ) ;
#228596=ORIENTED_EDGE ( 'NONE', *, *, #202095, .F. ) ;
#228625=ORIENTED_EDGE ( 'NONE', *, *, #113986, .T. ) ;
#228626=DIRECTION ( 'NONE',  ( 0.000000000000000000, 0.000000000000000000, -1.000000000000000000 ) ) ;
#228660=DIRECTION ( 'NONE',  ( 0.000000000000000000, 0.000000000000000000, -1.000000000000000000 ) ) ;
#228669=DIRECTION ( 'NONE',  ( 0.000000000000000000, 1.000000000000000000, 0.000000000000000000 ) ) ;
#228684=CARTESIAN_POINT ( 'NONE',  ( 21.05000000000000071, 1.115600667400684642E-11, -134.0000000000000000 ) ) ;
#228711=EDGE_CURVE ( 'NONE', #155422, #184016, #152523, .T. ) ;
#228735=ORIENTED_EDGE ( 'NONE', *, *, #243643, .F. ) ;
#228739=CARTESIAN_POINT ( 'NONE',  ( 21.05000000000000071, -12.41227409413852811, -164.5000000000000000 ) ) ;
#228783=ORIENTED_EDGE ( 'NONE', *, *, #207874, .T. ) ;
#228807=CYLINDRICAL_SURFACE ( 'NONE', #219645, 0.09999999999998898659 ) ;
#228832=CYLINDRICAL_SURFACE ( 'NONE', #182640, 4.049999999999998046 ) ;
#228859=ORIENTED_EDGE ( 'NONE', *, *, #256294, .F. ) ;
#228875=EDGE_CURVE ( 'NONE', #253862, #37772, #252572, .T. ) ;
#228913=EDGE_CURVE ( 'NONE', #93478, #86414, #98275, .T. ) ;
#228919=ORIENTED_EDGE ( 'NONE', *, *, #253648, .T. ) ;
#228925=CARTESIAN_POINT ( 'NONE',  ( -18.50000000000000000, -1.835859311432484375, -179.0044391687985410 ) ) ;
#228933=AXIS2_PLACEMENT_3D ( 'NONE', #224468, #66696, #165814 ) ;
#228938=ORIENTED_EDGE ( 'NONE', *, *, #236277, .F. ) ;
#228945=CARTESIAN_POINT ( 'NONE',  ( -23.15000000000000213, 11.65000000001115588, -146.1500000000000341 ) ) ;
#228959=VECTOR ( 'NONE', #131159, 1000.000000000000000 ) ;
#228960=AXIS2_PLACEMENT_3D ( 'NONE', #207735, #73374, #232439 ) ;
#228961=ORIENTED_EDGE ( 'NONE', *, *, #68575, .T. ) ;
#228989=AXIS2_PLACEMENT_3D ( 'NONE', #80525, #58398, #156284 ) ;
#229047=CARTESIAN_POINT ( 'NONE',  ( -20.94999675878240808, 10.29307482169070731, -172.9586421466940465 ) ) ;
#229066=CARTESIAN_POINT ( 'NONE',  ( 23.24999999999999645, -2.099999999988846344, -167.5000000000000284 ) ) ;
#229083=EDGE_LOOP ( 'NONE', ( #191112, #112554, #108040, #54933 ) ) ;
#229132=DIRECTION ( 'NONE',  ( 1.000000000000000000, -0.000000000000000000, -0.000000000000000000 ) ) ;
#229133=EDGE_CURVE ( 'NONE', #113603, #249928, #16140, .T. ) ;
#229193=CARTESIAN_POINT ( 'NONE',  ( -20.64999999999999858, 7.250000000011155521, -146.3500000000000227 ) ) ;
#229219=DIRECTION ( 'NONE',  ( -1.000000000000000000, -0.000000000000000000, -0.000000000000000000 ) ) ;
#229231=DIRECTION ( 'NONE',  ( 1.000000000000000000, 0.000000000000000000, 0.000000000000000000 ) ) ;
#229232=CIRCLE ( 'NONE', #187550, 0.09999999999999996392 ) ;
#229245=DIRECTION ( 'NONE',  ( 3.265361837132813093E-16, -1.000000000000000000, -0.000000000000000000 ) ) ;
#229250=DIRECTION ( 'NONE',  ( 0.000000000000000000, 0.000000000000000000, -1.000000000000000000 ) ) ;
#229251=AXIS2_PLACEMENT_3D ( 'NONE', #6095, #183473, #205578 ) ;
#229277=DIRECTION ( 'NONE',  ( 0.000000000000000000, -0.4930308989874653269, -0.8700118002898649117 ) ) ;
#229288=CIRCLE ( 'NONE', #95975, 0.1000000000000002554 ) ;
#229300=EDGE_CURVE ( 'NONE', #159966, #170648, #73599, .T. ) ;
#229306=EDGE_CURVE ( 'NONE', #100003, #4224, #230909, .T. ) ;
#229332=EDGE_CURVE ( 'NONE', #60099, #222619, #206837, .T. ) ;
#229340=DIRECTION ( 'NONE',  ( -0.000000000000000000, -1.000000000000000000, -1.734723475976807292E-15 ) ) ;
#229342=CARTESIAN_POINT ( 'NONE',  ( 18.51565452909268217, -9.352859338823158453, -141.1949093212308810 ) ) ;
#229356=VERTEX_POINT ( 'NONE', #237513 ) ;
#229389=CARTESIAN_POINT ( 'NONE',  ( -21.05000000000000782, 6.332272273946818686, -134.0375360632857280 ) ) ;
#229401=DIRECTION ( 'NONE',  ( 0.000000000000000000, -6.308085367188393199E-16, -1.000000000000000000 ) ) ;
#229458=VERTEX_POINT ( 'NONE', #118857 ) ;
#229479=DIRECTION ( 'NONE',  ( 0.000000000000000000, 0.000000000000000000, -1.000000000000000000 ) ) ;
#229498=CARTESIAN_POINT ( 'NONE',  ( -20.64999999999999858, 2.500000000011154633, -154.2753780772379173 ) ) ;
#229513=CYLINDRICAL_SURFACE ( 'NONE', #102462, 0.09999999999999939493 ) ;
#229527=DIRECTION ( 'NONE',  ( 1.000000000000000000, 0.000000000000000000, -0.000000000000000000 ) ) ;
#229533=DIRECTION ( 'NONE',  ( 0.000000000000000000, 6.938893903907270030E-14, 1.000000000000000000 ) ) ;
#229555=FACE_OUTER_BOUND ( 'NONE', #5872, .T. ) ;
#229588=CARTESIAN_POINT ( 'NONE',  ( 18.49999999999999645, 1.115600667400684642E-11, -167.5000000000000284 ) ) ;
#229599=CARTESIAN_POINT ( 'NONE',  ( -20.54999999999999716, 1.115600667400684642E-11, -165.5000000000000284 ) ) ;
#229632=CARTESIAN_POINT ( 'NONE',  ( 21.05000000000000071, 10.42338541492406279, -141.4920519238701218 ) ) ;
#229686=ADVANCED_FACE ( 'NONE', ( #46983 ), #115429, .T. ) ;
#229688=DIRECTION ( 'NONE',  ( 0.000000000000000000, 0.000000000000000000, -1.000000000000000000 ) ) ;
#229750=DIRECTION ( 'NONE',  ( 0.000000000000000000, 0.000000000000000000, -1.000000000000000000 ) ) ;
#229756=VERTEX_POINT ( 'NONE', #165698 ) ;
#229760=VERTEX_POINT ( 'NONE', #245220 ) ;
#229767=CARTESIAN_POINT ( 'NONE',  ( 21.05000000000000071, 6.650000000011155876, -144.0170271704400307 ) ) ;
#229773=ORIENTED_EDGE ( 'NONE', *, *, #152515, .F. ) ;
#229798=DIRECTION ( 'NONE',  ( -0.7071067811865475727, -0.7071067811865475727, 0.000000000000000000 ) ) ;
#229833=CARTESIAN_POINT ( 'NONE',  ( -20.64999999999999858, -9.399999999988846611, -157.6060308773475924 ) ) ;
#229848=CYLINDRICAL_SURFACE ( 'NONE', #189421, 0.09999999999998898659 ) ;
#229849=CARTESIAN_POINT ( 'NONE',  ( 18.59999999999999432, 1.637172712981537659, -145.5821533654720383 ) ) ;
#229850=CARTESIAN_POINT ( 'NONE',  ( 20.12500000000000000, 9.750000000011153745, -155.2500000000000284 ) ) ;
#229864=ORIENTED_EDGE ( 'NONE', *, *, #185888, .F. ) ;
#229870=AXIS2_PLACEMENT_3D ( 'NONE', #153645, #154901, #118322 ) ;
#229883=EDGE_CURVE ( 'NONE', #237934, #26254, #232173, .T. ) ;
#229894=CARTESIAN_POINT ( 'NONE',  ( 21.05000000000000071, -8.999999999988844479, -143.8939691226524644 ) ) ;
#229924=EDGE_LOOP ( 'NONE', ( #38150, #2972, #19113, #226563 ) ) ;
#229947=DIRECTION ( 'NONE',  ( 0.000000000000000000, 0.000000000000000000, -1.000000000000000000 ) ) ;
#229984=CIRCLE ( 'NONE', #175837, 2.000000000000001776 ) ;
#229990=VERTEX_POINT ( 'NONE', #181095 ) ;
#230010=AXIS2_PLACEMENT_3D ( 'NONE', #48153, #88549, #85970 ) ;
#230012=DIRECTION ( 'NONE',  ( 0.000000000000000000, 0.000000000000000000, -1.000000000000000000 ) ) ;
#230016=ORIENTED_EDGE ( 'NONE', *, *, #62770, .F. ) ;
#230020=AXIS2_PLACEMENT_3D ( 'NONE', #60646, #202743, #41131 ) ;
#230021=CIRCLE ( 'NONE', #254907, 0.09999999999998898659 ) ;
#230069=ORIENTED_EDGE ( 'NONE', *, *, #109882, .F. ) ;
#230079=DIRECTION ( 'NONE',  ( -1.000000000000000000, 0.000000000000000000, 0.000000000000000000 ) ) ;
#230082=ORIENTED_EDGE ( 'NONE', *, *, #106340, .F. ) ;
#230083=EDGE_CURVE ( 'NONE', #214790, #110751, #103138, .T. ) ;
#230092=DIRECTION ( 'NONE',  ( -1.000000000000000000, 0.000000000000000000, 0.000000000000000000 ) ) ;
#230095=LINE ( 'NONE', #11051, #28646 ) ;
#230128=AXIS2_PLACEMENT_3D ( 'NONE', #71596, #11617, #72891 ) ;
#230136=DIRECTION ( 'NONE',  ( -0.1538461538461510236, 0.9880948137434718559, 0.000000000000000000 ) ) ;
#230155=ORIENTED_EDGE ( 'NONE', *, *, #204811, .T. ) ;
#230180=CARTESIAN_POINT ( 'NONE',  ( -20.94999999999999929, 11.65000000001115232, -160.7161343370219129 ) ) ;
#230188=DIRECTION ( 'NONE',  ( -0.000000000000000000, 0.8660254037844502539, 0.4999999999999799605 ) ) ;
#230211=AXIS2_PLACEMENT_3D ( 'NONE', #253328, #39464, #16041 ) ;
#230241=CARTESIAN_POINT ( 'NONE',  ( -21.59780538579341425, 6.847090529954407145, -133.9010213304020454 ) ) ;
#230266=CARTESIAN_POINT ( 'NONE',  ( -23.25000000000000000, -1.835859311432481045, -179.1044391687985353 ) ) ;
#230267=ADVANCED_FACE ( 'NONE', ( #131036 ), #119945, .F. ) ;
#230281=CARTESIAN_POINT ( 'NONE',  ( 18.43709777086140988, -9.682403433465239573, -174.1568433774128835 ) ) ;
#230286=EDGE_CURVE ( 'NONE', #35759, #83651, #27791, .T. ) ;
#230295=DIRECTION ( 'NONE',  ( 1.000000000000000000, 0.000000000000000000, 0.000000000000000000 ) ) ;
#230317=CARTESIAN_POINT ( 'NONE',  ( -18.59999999999999787, 1.115600667400684642E-11, -167.5000000000000284 ) ) ;
#230329=ORIENTED_EDGE ( 'NONE', *, *, #84884, .F. ) ;
#230343=DIRECTION ( 'NONE',  ( 1.000000000000000000, 0.000000000000000000, -0.000000000000000000 ) ) ;
#230365=CARTESIAN_POINT ( 'NONE',  ( 23.14999999999999858, 4.775700934590584090, -145.8487681040459734 ) ) ;
#230376=CARTESIAN_POINT ( 'NONE',  ( 20.94999999999999929, 1.115600667400684642E-11, -167.5000000000000284 ) ) ;
#230377=EDGE_CURVE ( 'NONE', #238921, #170648, #211491, .T. ) ;
#230393=ORIENTED_EDGE ( 'NONE', *, *, #172243, .T. ) ;
#230402=VERTEX_POINT ( 'NONE', #223399 ) ;
#230418=ORIENTED_EDGE ( 'NONE', *, *, #73020, .F. ) ;
#230444=FACE_OUTER_BOUND ( 'NONE', #238002, .T. ) ;
#230456=CARTESIAN_POINT ( 'NONE',  ( 21.05000000000000071, 1.115600667400684642E-11, -171.5000000000000284 ) ) ;
#230491=CARTESIAN_POINT ( 'NONE',  ( -21.11101077989000174, 0.01528526892543027871, -127.5763152652739052 ) ) ;
#230497=DIRECTION ( 'NONE',  ( 0.000000000000000000, 0.000000000000000000, -1.000000000000000000 ) ) ;
#230507=AXIS2_PLACEMENT_3D ( 'NONE', #238147, #222411, #141621 ) ;
#230559=AXIS2_PLACEMENT_3D ( 'NONE', #211406, #113586, #152749 ) ;
#230569=AXIS2_PLACEMENT_3D ( 'NONE', #56523, #52687, #34458 ) ;
#230575=AXIS2_PLACEMENT_3D ( 'NONE', #42121, #129033, #64230 ) ;
#230587=LINE ( 'NONE', #54496, #164121 ) ;
#230595=ORIENTED_EDGE ( 'NONE', *, *, #223906, .F. ) ;
#230608=EDGE_CURVE ( 'NONE', #219363, #18611, #165312, .T. ) ;
#230640=DIRECTION ( 'NONE',  ( 0.000000000000000000, 1.000000000000000000, 0.000000000000000000 ) ) ;
#230681=EDGE_LOOP ( 'NONE', ( #93050, #98810, #190093, #206097 ) ) ;
#230686=FACE_OUTER_BOUND ( 'NONE', #58351, .T. ) ;
#230688=DIRECTION ( 'NONE',  ( 0.000000000000000000, 0.000000000000000000, 1.000000000000000000 ) ) ;
#230697=EDGE_LOOP ( 'NONE', ( #144656, #198845, #228938, #151188 ) ) ;
#230699=CIRCLE ( 'NONE', #214121, 0.1000000000000102612 ) ;
#230724=ADVANCED_FACE ( 'NONE', ( #15962 ), #158058, .F. ) ;
#230730=VECTOR ( 'NONE', #90157, 1000.000000000000000 ) ;
#230741=ORIENTED_EDGE ( 'NONE', *, *, #179458, .T. ) ;
#230746=DIRECTION ( 'NONE',  ( -1.000000000000000000, 0.000000000000000000, 0.000000000000000000 ) ) ;
#230750=ORIENTED_EDGE ( 'NONE', *, *, #39366, .F. ) ;
#230756=ORIENTED_EDGE ( 'NONE', *, *, #73215, .T. ) ;
#230757=CONICAL_SURFACE ( 'NONE', #109929, 4.299999999999970512, 0.7853981633974466137 ) ;
#230767=ORIENTED_EDGE ( 'NONE', *, *, #112051, .F. ) ;
#230770=ORIENTED_EDGE ( 'NONE', *, *, #224253, .T. ) ;
#230795=ORIENTED_EDGE ( 'NONE', *, *, #75300, .F. ) ;
#230803=CARTESIAN_POINT ( 'NONE',  ( -20.85000000000000142, 1.115600667400684642E-11, -167.5000000000000284 ) ) ;
#230817=ORIENTED_EDGE ( 'NONE', *, *, #238851, .F. ) ;
#230830=DIRECTION ( 'NONE',  ( 0.000000000000000000, 0.000000000000000000, -1.000000000000000000 ) ) ;
#230839=ORIENTED_EDGE ( 'NONE', *, *, #245753, .F. ) ;
#230849=CARTESIAN_POINT ( 'NONE',  ( -21.05000000000000071, -11.29603075032412995, -137.0478991596638991 ) ) ;
#230850=CARTESIAN_POINT ( 'NONE',  ( -23.25000000000000000, 10.33248238083634440, -173.0948465439131496 ) ) ;
#230853=CARTESIAN_POINT ( 'NONE',  ( -23.15000000000000213, -11.41227409413852811, -164.5000000000000000 ) ) ;
#230854=EDGE_CURVE ( 'NONE', #35141, #56718, #231977, .T. ) ;
#230860=TOROIDAL_SURFACE ( 'NONE', #51726, 11.65000000000000036, 0.1000000000000000056 ) ;
#230863=DIRECTION ( 'NONE',  ( 0.000000000000000000, -0.000000000000000000, -1.000000000000000000 ) ) ;
#230873=DIRECTION ( 'NONE',  ( 1.000000000000000000, -0.000000000000000000, -0.000000000000000000 ) ) ;
#230875=CIRCLE ( 'NONE', #247402, 0.09999999999998898659 ) ;
#230899=CARTESIAN_POINT ( 'NONE',  ( 21.14999999999999858, -0.09999999998884338825, -127.4593430482987912 ) ) ;
#230909=B_SPLINE_CURVE_WITH_KNOTS ( 'NONE', 3,
 ( #151578, #49869, #208950, #111135, #88981, #107273, #90264, #48583 ),
 .UNSPECIFIED., .F., .F.,
 ( 4, 2, 2, 4 ),
 ( 0.000000000000000000, 6.534141206311710429E-05, 0.0001306828241262342086, 0.0002613656482524441852 ),
 .UNSPECIFIED. ) ;
#230918=CARTESIAN_POINT ( 'NONE',  ( -21.06715728752538652, 11.75000000001115197, -141.0148057706540214 ) ) ;
#230956=FACE_OUTER_BOUND ( 'NONE', #23752, .T. ) ;
#230965=DIRECTION ( 'NONE',  ( -1.000000000000000000, 9.012599976028471648E-15, 6.882867235861662930E-14 ) ) ;
#230989=ORIENTED_EDGE ( 'NONE', *, *, #229300, .F. ) ;
#231010=DIRECTION ( 'NONE',  ( 0.000000000000000000, -0.6728971962617388280, -0.7397360091702248619 ) ) ;
#231025=CARTESIAN_POINT ( 'NONE',  ( 22.39999999999999503, -0.1008583690875579364, -122.2504328765106294 ) ) ;
#231050=EDGE_LOOP ( 'NONE', ( #37040, #200869, #110536, #129197 ) ) ;
#231070=DIRECTION ( 'NONE',  ( 0.000000000000000000, 1.000000000000000000, 0.000000000000000000 ) ) ;
#231078=VERTEX_POINT ( 'NONE', #242601 ) ;
#231089=ORIENTED_EDGE ( 'NONE', *, *, #123296, .F. ) ;
#231110=DIRECTION ( 'NONE',  ( 0.000000000000000000, 0.000000000000000000, -1.000000000000000000 ) ) ;
#231128=TOROIDAL_SURFACE ( 'NONE', #185317, 12.77500000000000036, 0.1000000000000000056 ) ;
#231131=ADVANCED_FACE ( 'NONE', ( #246464 ), #161824, .T. ) ;
#231143=VECTOR ( 'NONE', #12322, 1000.000000000000000 ) ;
#231166=ORIENTED_EDGE ( 'NONE', *, *, #110661, .T. ) ;
#231169=VERTEX_POINT ( 'NONE', #73001 ) ;
#231181=DIRECTION ( 'NONE',  ( 0.000000000000000000, -2.211772431870365684E-13, -1.000000000000000000 ) ) ;
#231189=FACE_OUTER_BOUND ( 'NONE', #182888, .T. ) ;
#231208=DIRECTION ( 'NONE',  ( -1.000000000000000000, 0.000000000000000000, 0.000000000000000000 ) ) ;
#231215=AXIS2_PLACEMENT_3D ( 'NONE', #119556, #199077, #99942 ) ;
#231271=DIRECTION ( 'NONE',  ( 0.000000000000000000, 0.4999999999999956701, -0.8660254037844411501 ) ) ;
#231293=AXIS2_PLACEMENT_3D ( 'NONE', #80900, #157940, #78340 ) ;
#231327=ORIENTED_EDGE ( 'NONE', *, *, #81973, .T. ) ;
#231340=ORIENTED_EDGE ( 'NONE', *, *, #213310, .F. ) ;
#231362=ORIENTED_EDGE ( 'NONE', *, *, #117581, .F. ) ;
#231363=CARTESIAN_POINT ( 'NONE',  ( -21.05000000000000071, -11.48912529306489994, -164.4000000000000057 ) ) ;
#231365=CARTESIAN_POINT ( 'NONE',  ( 20.94999999999999574, 1.115600667400684642E-11, -134.0000000000000000 ) ) ;
#231378=ORIENTED_EDGE ( 'NONE', *, *, #237261, .T. ) ;
#231398=DIRECTION ( 'NONE',  ( 1.000000000000000000, 2.952720810173289112E-16, -0.000000000000000000 ) ) ;
#231425=VERTEX_POINT ( 'NONE', #3685 ) ;
#231466=EDGE_CURVE ( 'NONE', #133237, #16470, #162785, .T. ) ;
#231488=DIRECTION ( 'NONE',  ( -1.000000000000000000, 0.000000000000000000, 0.000000000000000000 ) ) ;
#231501=FACE_OUTER_BOUND ( 'NONE', #45949, .T. ) ;
#231519=DIRECTION ( 'NONE',  ( -6.938893903907222067E-15, 1.000000000000000000, 2.891205793294679805E-16 ) ) ;
#231526=CARTESIAN_POINT ( 'NONE',  ( -1.739115166359751170E-14, 11.65000000001114699, -158.8500000000000227 ) ) ;
#231532=CARTESIAN_POINT ( 'NONE',  ( 20.94999999999999929, 8.776282895303632259, -146.1500000000000341 ) ) ;
#231537=CARTESIAN_POINT ( 'NONE',  ( -18.46856557590793813, -9.474215907775338508, -141.1019862408823542 ) ) ;
#231538=DIRECTION ( 'NONE',  ( 0.000000000000000000, 0.000000000000000000, -1.000000000000000000 ) ) ;
#231539=ADVANCED_FACE ( 'NONE', ( #230444 ), #92203, .T. ) ;
#231542=CYLINDRICAL_SURFACE ( 'NONE', #13582, 0.09999999999999939493 ) ;
#231610=ORIENTED_EDGE ( 'NONE', *, *, #73162, .F. ) ;
#231631=CARTESIAN_POINT ( 'NONE',  ( -18.59999999999999787, -9.399999999988851940, -174.3820418481726904 ) ) ;
#231663=FACE_OUTER_BOUND ( 'NONE', #84359, .T. ) ;
#231671=ORIENTED_EDGE ( 'NONE', *, *, #256933, .F. ) ;
#231719=CIRCLE ( 'NONE', #15239, 12.87500000000000000 ) ;
#231749=CARTESIAN_POINT ( 'NONE',  ( -18.59999999999999787, 7.021664781911246322, -171.3335654018973173 ) ) ;
#231752=EDGE_LOOP ( 'NONE', ( #27969, #179624, #247665, #164954 ) ) ;
#231759=ORIENTED_EDGE ( 'NONE', *, *, #15855, .F. ) ;
#231785=CYLINDRICAL_SURFACE ( 'NONE', #26120, 0.1000000000000098310 ) ;
#231803=DIRECTION ( 'NONE',  ( 0.000000000000000000, 1.000000000000000000, 0.000000000000000000 ) ) ;
#231828=ORIENTED_EDGE ( 'NONE', *, *, #178234, .T. ) ;
#231888=AXIS2_PLACEMENT_3D ( 'NONE', #177634, #1516, #240151 ) ;
#231902=VERTEX_POINT ( 'NONE', #234962 ) ;
#231936=CARTESIAN_POINT ( 'NONE',  ( 23.14999999999999503, 6.650000000011155876, -155.1500000000000057 ) ) ;
#231960=CARTESIAN_POINT ( 'NONE',  ( 23.14999999999999858, 1.115600667400684642E-11, -167.5000000000000284 ) ) ;
#231977=CIRCLE ( 'NONE', #90276, 0.09999999999999939493 ) ;
#231998=CARTESIAN_POINT ( 'NONE',  ( 18.54116936837188945, -9.463564198361279267, -141.0485424908882806 ) ) ;
#232020=VECTOR ( 'NONE', #166696, 1000.000000000000000 ) ;
#232021=DIRECTION ( 'NONE',  ( 2.342056488767301376E-15, -0.1350103645451904977, -0.9908441862701596881 ) ) ;
#232022=ORIENTED_EDGE ( 'NONE', *, *, #130440, .T. ) ;
#232051=ORIENTED_EDGE ( 'NONE', *, *, #128232, .T. ) ;
#232064=FACE_OUTER_BOUND ( 'NONE', #47694, .T. ) ;
#232082=ORIENTED_EDGE ( 'NONE', *, *, #101839, .F. ) ;
#232088=DIRECTION ( 'NONE',  ( 1.000000000000000000, 0.000000000000000000, 0.000000000000000000 ) ) ;
#232116=EDGE_LOOP ( 'NONE', ( #253566, #104924, #189384, #76490 ) ) ;
#232147=CIRCLE ( 'NONE', #144809, 0.2000000000000057288 ) ;
#232158=DIRECTION ( 'NONE',  ( 1.000000000000000000, -0.000000000000000000, -0.000000000000000000 ) ) ;
#232173=CIRCLE ( 'NONE', #61466, 0.09999999999998898659 ) ;
#232190=DIRECTION ( 'NONE',  ( 1.000000000000000000, -0.000000000000000000, -0.000000000000000000 ) ) ;
#232192=DIRECTION ( 'NONE',  ( 1.000000000000000000, 0.000000000000000000, 0.000000000000000000 ) ) ;
#232203=ADVANCED_FACE ( 'NONE', ( #224370 ), #23648, .T. ) ;
#232212=ORIENTED_EDGE ( 'NONE', *, *, #124243, .T. ) ;
#232215=EDGE_CURVE ( 'NONE', #185310, #92859, #45231, .T. ) ;
#232217=CIRCLE ( 'NONE', #111387, 0.1000000000000028644 ) ;
#232218=ORIENTED_EDGE ( 'NONE', *, *, #86659, .T. ) ;
#232236=CARTESIAN_POINT ( 'NONE',  ( 23.24999999999999645, 1.115600667400684642E-11, -167.5000000000000284 ) ) ;
#232237=DIRECTION ( 'NONE',  ( 1.000000000000000000, 3.265361837132813093E-16, -0.000000000000000000 ) ) ;
#232250=CARTESIAN_POINT ( 'NONE',  ( -22.39999999999999858, 1.115600667400684642E-11, -127.7500000000000284 ) ) ;
#232263=EDGE_LOOP ( 'NONE', ( #154880, #237884, #103912, #16449 ) ) ;
#232284=ORIENTED_EDGE ( 'NONE', *, *, #249633, .F. ) ;
#232299=VECTOR ( 'NONE', #172155, 1000.000000000000000 ) ;
#232310=VECTOR ( 'NONE', #158427, 1000.000000000000000 ) ;
#232333=ORIENTED_EDGE ( 'NONE', *, *, #189571, .F. ) ;
#232346=ORIENTED_EDGE ( 'NONE', *, *, #19503, .T. ) ;
#232391=CARTESIAN_POINT ( 'NONE',  ( -21.44999999999999929, 7.350000000011155166, -146.3500000000000227 ) ) ;
#232397=DIRECTION ( 'NONE',  ( 0.000000000000000000, 0.000000000000000000, 1.000000000000000000 ) ) ;
#232414=ORIENTED_EDGE ( 'NONE', *, *, #176330, .T. ) ;
#232429=CARTESIAN_POINT ( 'NONE',  ( -18.59999999999999787, 11.65000000001115232, -140.9148057706540271 ) ) ;
#232439=DIRECTION ( 'NONE',  ( 0.000000000000000000, 0.000000000000000000, 1.000000000000000000 ) ) ;
#232456=ORIENTED_EDGE ( 'NONE', *, *, #130895, .F. ) ;
#232472=PLANE ( 'NONE',  #160489 ) ;
#232489=CIRCLE ( 'NONE', #99347, 0.1000000000000001860 ) ;
#232490=ORIENTED_EDGE ( 'NONE', *, *, #142950, .F. ) ;
#232518=CARTESIAN_POINT ( 'NONE',  ( 21.30000000000002558, 1.115600667400684642E-11, -138.0500000000000114 ) ) ;
#232565=DIRECTION ( 'NONE',  ( -2.952720810173289112E-16, 1.000000000000000000, 0.000000000000000000 ) ) ;
#232602=DIRECTION ( 'NONE',  ( 1.000000000000000000, -0.000000000000000000, 0.000000000000000000 ) ) ;
#232622=CIRCLE ( 'NONE', #141201, 0.1000000000000094008 ) ;
#232625=ORIENTED_EDGE ( 'NONE', *, *, #198811, .T. ) ;
#232640=CARTESIAN_POINT ( 'NONE',  ( 23.14999999999999858, 1.115600667400684642E-11, -167.5000000000000284 ) ) ;
#232714=VERTEX_POINT ( 'NONE', #239483 ) ;
#232750=VECTOR ( 'NONE', #93101, 1000.000000000000000 ) ;
#232774=CARTESIAN_POINT ( 'NONE',  ( 21.10710606213542562, 8.776894023904366904, -146.2409965263994422 ) ) ;
#232828=CIRCLE ( 'NONE', #12071, 0.09999999999999817368 ) ;
#232831=CARTESIAN_POINT ( 'NONE',  ( -18.47653818581421703, -9.465280387751800362, -141.1259608161398944 ) ) ;
#232840=CARTESIAN_POINT ( 'NONE',  ( -23.15000000000000213, 1.115600667400684642E-11, -171.4000000000000341 ) ) ;
#232854=ORIENTED_EDGE ( 'NONE', *, *, #238486, .F. ) ;
#232888=CARTESIAN_POINT ( 'NONE',  ( -20.54999999999999716, -8.999999999988844479, -157.6060308773475924 ) ) ;
#232905=CARTESIAN_POINT ( 'NONE',  ( -20.94999999999999929, 1.115600667400684642E-11, -167.5000000000000284 ) ) ;
#232916=DIRECTION ( 'NONE',  ( 1.000000000000000000, 0.000000000000000000, 0.000000000000000000 ) ) ;
#232925=CIRCLE ( 'NONE', #191234, 2.099999999999990763 ) ;
#232949=CIRCLE ( 'NONE', #66342, 0.09999999999999864553 ) ;
#232963=CARTESIAN_POINT ( 'NONE',  ( -20.85000000000000142, 11.75000000001115197, -160.7161343370219129 ) ) ;
#232967=FACE_OUTER_BOUND ( 'NONE', #36619, .T. ) ;
#232975=DIRECTION ( 'NONE',  ( 0.000000000000000000, 0.008583690987127625890, 0.9999631594459055250 ) ) ;
#232979=AXIS2_PLACEMENT_3D ( 'NONE', #58539, #62418, #217606 ) ;
#232981=ORIENTED_EDGE ( 'NONE', *, *, #113183, .F. ) ;
#232985=ORIENTED_EDGE ( 'NONE', *, *, #178, .T. ) ;
#233036=CARTESIAN_POINT ( 'NONE',  ( 20.95132126680579887, 10.48994987015794322, -141.5703245384345053 ) ) ;
#233056=CARTESIAN_POINT ( 'NONE',  ( 21.05000000000000071, 5.000000000011153745, -155.0947339810869323 ) ) ;
#233072=ORIENTED_EDGE ( 'NONE', *, *, #167967, .F. ) ;
#233077=CARTESIAN_POINT ( 'NONE',  ( -21.08035267497491816, 0.08268862478717949049, -127.6682931602169901 ) ) ;
#233105=CARTESIAN_POINT ( 'NONE',  ( 18.49999999999999289, 10.49142135624846439, -158.8500000000000227 ) ) ;
#233107=DIRECTION ( 'NONE',  ( -1.000000000000000000, -2.952720810173289112E-16, 0.000000000000000000 ) ) ;
#233117=VECTOR ( 'NONE', #180263, 1000.000000000000000 ) ;
#233147=FACE_OUTER_BOUND ( 'NONE', #135935, .T. ) ;
#233183=DIRECTION ( 'NONE',  ( 0.000000000000000000, 1.000000000000000000, 0.000000000000000000 ) ) ;
#233199=ORIENTED_EDGE ( 'NONE', *, *, #241362, .T. ) ;
#233252=AXIS2_PLACEMENT_3D ( 'NONE', #92684, #236052, #156556 ) ;
#233293=DIRECTION ( 'NONE',  ( 0.000000000000000000, 0.000000000000000000, 1.000000000000000000 ) ) ;
#233296=ORIENTED_EDGE ( 'NONE', *, *, #235385, .F. ) ;
#233326=ADVANCED_FACE ( 'NONE', ( #149072 ), #30404, .T. ) ;
#233364=EDGE_LOOP ( 'NONE', ( #225026, #202751, #53290, #204866 ) ) ;
#233366=DIRECTION ( 'NONE',  ( 0.000000000000000000, 0.000000000000000000, 1.000000000000000000 ) ) ;
#233385=CARTESIAN_POINT ( 'NONE',  ( 23.14999999999999503, 11.65000000001116298, -122.2500000000000284 ) ) ;
#233390=CARTESIAN_POINT ( 'NONE',  ( -23.15000000000000213, -11.64999999998884483, -164.4000000000000057 ) ) ;
#233404=CIRCLE ( 'NONE', #162649, 0.09999999999998898659 ) ;
#233457=ADVANCED_FACE ( 'NONE', ( #41648 ), #59877, .T. ) ;
#233486=CARTESIAN_POINT ( 'NONE',  ( -20.15000000000000568, 9.291421356248463326, -155.1500000000000057 ) ) ;
#233502=CARTESIAN_POINT ( 'NONE',  ( 20.85000000000000142, 1.115600667400684642E-11, -175.4000000000000341 ) ) ;
#233503=CARTESIAN_POINT ( 'NONE',  ( 20.95263205890659108, 8.895740107905192318, -142.4895084069416384 ) ) ;
#233508=CARTESIAN_POINT ( 'NONE',  ( 23.25000000000000000, -8.596261682231833845, -143.4501275171502925 ) ) ;
#233522=CARTESIAN_POINT ( 'NONE',  ( -23.25000000000000000, -1.249999999988843369, -175.3004807544151049 ) ) ;
#233532=EDGE_CURVE ( 'NONE', #180099, #122938, #70949, .T. ) ;
#233536=ORIENTED_EDGE ( 'NONE', *, *, #48514, .T. ) ;
#233551=CARTESIAN_POINT ( 'NONE',  ( 18.59999999999999076, -1.249999999988843369, -142.0000000000000284 ) ) ;
#233571=AXIS2_PLACEMENT_3D ( 'NONE', #34604, #209364, #234055 ) ;
#233581=DIRECTION ( 'NONE',  ( -1.000000000000000000, -2.952720810173289112E-16, 0.000000000000000000 ) ) ;
#233607=VERTEX_POINT ( 'NONE', #242381 ) ;
#233653=ADVANCED_FACE ( 'NONE', ( #28531 ), #143287, .T. ) ;
#233696=ADVANCED_FACE ( 'NONE', ( #88421 ), #94859, .F. ) ;
#233733=DIRECTION ( 'NONE',  ( 1.000000000000000000, 0.000000000000000000, 0.000000000000000000 ) ) ;
#233735=DIRECTION ( 'NONE',  ( 0.000000000000000000, -0.1350103645451904977, -0.9908441862701596881 ) ) ;
#233764=FACE_OUTER_BOUND ( 'NONE', #41704, .T. ) ;
#233773=VECTOR ( 'NONE', #59693, 1000.000000000000000 ) ;
#233788=DIRECTION ( 'NONE',  ( 0.000000000000000000, -1.000000000000000000, 0.000000000000000000 ) ) ;
#233794=CYLINDRICAL_SURFACE ( 'NONE', #247022, 0.09999999999998898659 ) ;
#233841=EDGE_CURVE ( 'NONE', #37324, #206150, #179275, .T. ) ;
#233847=ORIENTED_EDGE ( 'NONE', *, *, #109882, .T. ) ;
#233850=ORIENTED_EDGE ( 'NONE', *, *, #76724, .T. ) ;
#233854=FACE_OUTER_BOUND ( 'NONE', #195259, .T. ) ;
#233886=CARTESIAN_POINT ( 'NONE',  ( 21.13422380239053311, 6.493326514816903483, -134.0000000000000284 ) ) ;
#233893=EDGE_LOOP ( 'NONE', ( #205815, #202293, #80996, #68526 ) ) ;
#233896=CARTESIAN_POINT ( 'NONE',  ( 21.05563370358598263, 10.72423035585766549, -146.1830908159630837 ) ) ;
#233958=AXIS2_PLACEMENT_3D ( 'NONE', #164176, #83309, #202014 ) ;
#233987=LINE ( 'NONE', #51476, #124584 ) ;
#234008=SURFACE_SIDE_STYLE ('',( #76209 ) ) ;
#234015=DIRECTION ( 'NONE',  ( 1.000000000000000000, -0.000000000000000000, -0.000000000000000000 ) ) ;
#234029=CARTESIAN_POINT ( 'NONE',  ( 21.14999999999999858, 8.786607556611267356, -146.2500000000000284 ) ) ;
#234043=DIRECTION ( 'NONE',  ( 0.000000000000000000, 0.000000000000000000, -1.000000000000000000 ) ) ;
#234046=DIRECTION ( 'NONE',  ( -0.7071067811865474617, -0.7071067811865474617, -0.000000000000000000 ) ) ;
#234055=DIRECTION ( 'NONE',  ( 0.000000000000000000, 1.000000000000000000, 0.000000000000000000 ) ) ;
#234067=CARTESIAN_POINT ( 'NONE',  ( 23.14999999999999858, 1.115600667400684642E-11, -167.5000000000000284 ) ) ;
#234070=CYLINDRICAL_SURFACE ( 'NONE', #84494, 0.09999999999999939493 ) ;
#234081=CIRCLE ( 'NONE', #121685, 0.09999999999999230338 ) ;
#234121=CARTESIAN_POINT ( 'NONE',  ( 21.08035267497491105, 6.331706839794169817, -133.9173113752239033 ) ) ;
#234127=CARTESIAN_POINT ( 'NONE',  ( 18.48413544395656416, -9.664304033616613054, -174.1831049930383131 ) ) ;
#234132=AXIS2_PLACEMENT_3D ( 'NONE', #173151, #214785, #231803 ) ;
#234189=EDGE_CURVE ( 'NONE', #60099, #117707, #151998, .T. ) ;
#234197=EDGE_CURVE ( 'NONE', #174969, #91096, #171298, .T. ) ;
#234227=ORIENTED_EDGE ( 'NONE', *, *, #72163, .F. ) ;
#234243=CARTESIAN_POINT ( 'NONE',  ( -18.50000000000000000, 11.75000000001115197, -122.2500000000000284 ) ) ;
#234270=CIRCLE ( 'NONE', #117764, 0.1000000000000096922 ) ;
#234291=EDGE_CURVE ( 'NONE', #216916, #91733, #219632, .T. ) ;
#234304=EDGE_CURVE ( 'NONE', #6309, #149328, #55395, .T. ) ;
#234309=DIRECTION ( 'NONE',  ( 1.000000000000000000, -0.000000000000000000, -0.000000000000000000 ) ) ;
#234358=EDGE_CURVE ( 'NONE', #67207, #84586, #201361, .T. ) ;
#234393=SPHERICAL_SURFACE ( 'NONE', #229870, 0.1000000000000000056 ) ;
#234416=CYLINDRICAL_SURFACE ( 'NONE', #42090, 0.09999999999999939493 ) ;
#234424=ORIENTED_EDGE ( 'NONE', *, *, #230083, .F. ) ;
#234443=DIRECTION ( 'NONE',  ( -1.000000000000000000, -0.000000000000000000, 0.000000000000000000 ) ) ;
#234460=CARTESIAN_POINT ( 'NONE',  ( -21.05000000000000071, 1.360870587203197646, -142.0729979270909951 ) ) ;
#234478=EDGE_LOOP ( 'NONE', ( #183528, #60987, #103232, #210316 ) ) ;
#234481=CARTESIAN_POINT ( 'NONE',  ( 20.95483826173899899, 8.876166204781142710, -142.5462755528995444 ) ) ;
#234567=AXIS2_PLACEMENT_3D ( 'NONE', #111651, #205602, #88205 ) ;
#234614=ORIENTED_EDGE ( 'NONE', *, *, #2109, .T. ) ;
#234615=DIRECTION ( 'NONE',  ( 0.000000000000000000, -0.000000000000000000, 1.000000000000000000 ) ) ;
#234627=ORIENTED_EDGE ( 'NONE', *, *, #122180, .T. ) ;
#234702=VECTOR ( 'NONE', #130934, 999.9999999999998863 ) ;
#234704=AXIS2_PLACEMENT_3D ( 'NONE', #232640, #253448, #74860 ) ;
#234723=ORIENTED_EDGE ( 'NONE', *, *, #105065, .F. ) ;
#234775=CARTESIAN_POINT ( 'NONE',  ( 20.94999999999999929, -1.835341550213257733, -145.5551512925629822 ) ) ;
#234780=CARTESIAN_POINT ( 'NONE',  ( 22.39999999999999503, 0.1000000000111554016, -127.7500000000000284 ) ) ;
#234795=EDGE_CURVE ( 'NONE', #86831, #90426, #1476, .T. ) ;
#234804=ORIENTED_EDGE ( 'NONE', *, *, #47686, .F. ) ;
#234926=DIRECTION ( 'NONE',  ( 0.000000000000000000, 0.4999999999999608646, 0.8660254037844612451 ) ) ;
#234930=CIRCLE ( 'NONE', #218322, 0.09999999999998898659 ) ;
#234938=ORIENTED_EDGE ( 'NONE', *, *, #104048, .F. ) ;
#234962=CARTESIAN_POINT ( 'NONE',  ( 23.14999999999999503, 11.75000000001116263, -146.1500000000000341 ) ) ;
#234965=AXIS2_PLACEMENT_3D ( 'NONE', #29130, #146437, #143877 ) ;
#234969=VECTOR ( 'NONE', #107475, 1000.000000000000000 ) ;
#234974=ORIENTED_EDGE ( 'NONE', *, *, #94096, .T. ) ;
#235020=DIRECTION ( 'NONE',  ( 3.616040088954497272E-32, -1.224646799147352961E-16, 1.000000000000000000 ) ) ;
#235028=ORIENTED_EDGE ( 'NONE', *, *, #194827, .T. ) ;
#235036=ORIENTED_EDGE ( 'NONE', *, *, #147901, .T. ) ;
#235062=DIRECTION ( 'NONE',  ( 0.000000000000000000, 0.000000000000000000, -1.000000000000000000 ) ) ;
#235063=DIRECTION ( 'NONE',  ( 1.000000000000000000, -0.000000000000000000, -0.000000000000000000 ) ) ;
#235085=DIRECTION ( 'NONE',  ( 1.000000000000000000, 2.952720810173289112E-16, -0.000000000000000000 ) ) ;
#235101=ORIENTED_EDGE ( 'NONE', *, *, #211156, .T. ) ;
#235126=CARTESIAN_POINT ( 'NONE',  ( -23.25000000000000000, -11.64999999998884483, -164.5000000000000000 ) ) ;
#235131=CIRCLE ( 'NONE', #47840, 0.09999999999998898659 ) ;
#235146=ADVANCED_FACE ( 'NONE', ( #55158 ), #73509, .F. ) ;
#235178=CARTESIAN_POINT ( 'NONE',  ( 20.94999999999999574, 1.115600667400684642E-11, -134.0000000000000000 ) ) ;
#235217=CARTESIAN_POINT ( 'NONE',  ( 22.39999999999999503, 1.115600667400684642E-11, -126.2092204016266379 ) ) ;
#235241=AXIS2_PLACEMENT_3D ( 'NONE', #86093, #187819, #154790 ) ;
#235243=VECTOR ( 'NONE', #16991, 1000.000000000000000 ) ;
#235252=VERTEX_POINT ( 'NONE', #141160 ) ;
#235254=CARTESIAN_POINT ( 'NONE',  ( -21.05439746398122836, 11.75000000001115197, -140.9899164874850044 ) ) ;
#235264=CARTESIAN_POINT ( 'NONE',  ( 20.94999999999999929, 5.000000000011153745, -155.0947339810869323 ) ) ;
#235298=AXIS2_PLACEMENT_3D ( 'NONE', #38815, #238275, #40121 ) ;
#235322=ORIENTED_EDGE ( 'NONE', *, *, #64935, .T. ) ;
#235334=ADVANCED_FACE ( 'NONE', ( #40800 ), #221939, .T. ) ;
#235347=ORIENTED_EDGE ( 'NONE', *, *, #32987, .F. ) ;
#235351=DIRECTION ( 'NONE',  ( 1.000000000000000000, 3.265361837132813093E-16, -0.000000000000000000 ) ) ;
#235367=CARTESIAN_POINT ( 'NONE',  ( -22.47071067811865319, 7.720074744509219933, -133.9009075452974002 ) ) ;
#235375=DIRECTION ( 'NONE',  ( 0.000000000000000000, -1.000000000000000000, 0.000000000000000000 ) ) ;
#235385=EDGE_CURVE ( 'NONE', #991, #170581, #203697, .T. ) ;
#235414=CARTESIAN_POINT ( 'NONE',  ( 18.55857864376267941, 10.36715728753653565, -158.7500000000000000 ) ) ;
#235416=CARTESIAN_POINT ( 'NONE',  ( 20.94999999999999574, -1.835341550213255957, -145.6551512925629766 ) ) ;
#235417=DIRECTION ( 'NONE',  ( 0.000000000000000000, 0.000000000000000000, -1.000000000000000000 ) ) ;
#235420=ADVANCED_FACE ( 'NONE', ( #25085 ), #186713, .T. ) ;
#235435=AXIS2_PLACEMENT_3D ( 'NONE', #202808, #43742, #4596 ) ;
#235436=DIRECTION ( 'NONE',  ( -3.265361837132813093E-16, 1.000000000000000000, 0.000000000000000000 ) ) ;
#235444=ORIENTED_EDGE ( 'NONE', *, *, #97080, .T. ) ;
#235469=DIRECTION ( 'NONE',  ( -1.000000000000000000, 0.000000000000000000, 0.000000000000000000 ) ) ;
#235512=EDGE_CURVE ( 'NONE', #169023, #160394, #31509, .T. ) ;
#235525=CARTESIAN_POINT ( 'NONE',  ( -20.94999999999999929, 1.835341550235569663, -145.5551512925629822 ) ) ;
#235576=FACE_OUTER_BOUND ( 'NONE', #237503, .T. ) ;
#235619=CARTESIAN_POINT ( 'NONE',  ( -21.05000000000000071, 6.257814610492680174, -133.9022097086908332 ) ) ;
#235663=EDGE_CURVE ( 'NONE', #238843, #170246, #113233, .T. ) ;
#235685=VECTOR ( 'NONE', #109796, 1000.000000000000000 ) ;
#235691=CARTESIAN_POINT ( 'NONE',  ( -20.54999999999999716, 2.000000000011154189, -154.2753780772379173 ) ) ;
#235701=DIRECTION ( 'NONE',  ( 0.000000000000000000, 0.000000000000000000, -1.000000000000000000 ) ) ;
#235715=CARTESIAN_POINT ( 'NONE',  ( -20.54999999999999716, -9.499999999988848032, -143.8939691226524644 ) ) ;
#235722=DIRECTION ( 'NONE',  ( 0.000000000000000000, 0.000000000000000000, -1.000000000000000000 ) ) ;
#235727=ORIENTED_EDGE ( 'NONE', *, *, #152435, .T. ) ;
#235743=CARTESIAN_POINT ( 'NONE',  ( -21.05000000000000071, 11.60000000001115517, -160.5717967697245285 ) ) ;
#235753=DIRECTION ( 'NONE',  ( -1.000000000000000000, -2.952720810173289112E-16, 0.000000000000000000 ) ) ;
#235779=DIRECTION ( 'NONE',  ( 0.000000000000000000, 0.000000000000000000, 1.000000000000000000 ) ) ;
#235782=VECTOR ( 'NONE', #30095, 1000.000000000000227 ) ;
#235797=FACE_OUTER_BOUND ( 'NONE', #35218, .T. ) ;
#235866=ORIENTED_EDGE ( 'NONE', *, *, #117581, .T. ) ;
#235884=EDGE_CURVE ( 'NONE', #158228, #117707, #92757, .T. ) ;
#235915=DIRECTION ( 'NONE',  ( 0.000000000000000000, 0.000000000000000000, -1.000000000000000000 ) ) ;
#235926=EDGE_CURVE ( 'NONE', #47961, #226140, #84331, .T. ) ;
#235953=CARTESIAN_POINT ( 'NONE',  ( 21.07928932188134397, 1.115600667400684642E-11, -134.0000000000000000 ) ) ;
#235968=DIRECTION ( 'NONE',  ( 0.000000000000000000, 0.000000000000000000, 1.000000000000000000 ) ) ;
#235974=TOROIDAL_SURFACE ( 'NONE', #148508, 0.2000000000000000111, 0.1000000000000000056 ) ;
#235996=AXIS2_PLACEMENT_3D ( 'NONE', #211853, #55295, #214400 ) ;
#236039=AXIS2_PLACEMENT_3D ( 'NONE', #181629, #138599, #22555 ) ;
#236052=DIRECTION ( 'NONE',  ( 0.000000000000000000, 0.000000000000000000, 1.000000000000000000 ) ) ;
#236072=FILL_AREA_STYLE ('',( #255585 ) ) ;
#236077=VECTOR ( 'NONE', #83823, 1000.000000000000000 ) ;
#236093=TOROIDAL_SURFACE ( 'NONE', #256892, 12.97499999999999787, 0.1000000000000000056 ) ;
#236094=AXIS2_PLACEMENT_3D ( 'NONE', #243627, #126240, #106661 ) ;
#236117=DIRECTION ( 'NONE',  ( 1.000000000000000000, 0.000000000000000000, 0.000000000000000000 ) ) ;
#236137=CARTESIAN_POINT ( 'NONE',  ( -20.64999999999999858, 2.400000000011155432, -154.2753780772379173 ) ) ;
#236160=EDGE_LOOP ( 'NONE', ( #135241, #25128, #64980, #180648 ) ) ;
#236186=LINE ( 'NONE', #77114, #217514 ) ;
#236221=VECTOR ( 'NONE', #165792, 1000.000000000000000 ) ;
#236255=DIRECTION ( 'NONE',  ( 0.000000000000000000, 0.1350103645451876666, -0.9908441862701600211 ) ) ;
#236277=EDGE_CURVE ( 'NONE', #72782, #49547, #47476, .T. ) ;
#236341=DIRECTION ( 'NONE',  ( -0.000000000000000000, -0.2605042016806452532, -0.9654727137038777718 ) ) ;
#236363=FACE_OUTER_BOUND ( 'NONE', #150440, .T. ) ;
#236383=CARTESIAN_POINT ( 'NONE',  ( -20.64999999999999858, 1.925233644870972816, -146.7302435331261563 ) ) ;
#236390=ORIENTED_EDGE ( 'NONE', *, *, #160012, .T. ) ;
#236397=DIRECTION ( 'NONE',  ( 0.000000000000000000, 0.000000000000000000, -1.000000000000000000 ) ) ;
#236413=CARTESIAN_POINT ( 'NONE',  ( 20.95512820512820440, 10.62384868372303259, -146.1500000000000341 ) ) ;
#236420=CARTESIAN_POINT ( 'NONE',  ( 18.39999999999999858, -9.599999999988845900, -174.1001893912220737 ) ) ;
#236433=CIRCLE ( 'NONE', #182286, 11.64999999999999325 ) ;
#236448=EDGE_LOOP ( 'NONE', ( #124617, #208421, #35888, #163186 ) ) ;
#236464=DIRECTION ( 'NONE',  ( 0.000000000000000000, 0.000000000000000000, 1.000000000000000000 ) ) ;
#236473=VERTEX_POINT ( 'NONE', #130607 ) ;
#236500=ORIENTED_EDGE ( 'NONE', *, *, #45224, .T. ) ;
#236503=CARTESIAN_POINT ( 'NONE',  ( 21.14999999999999858, 1.115600667400684642E-11, -127.4593430482987912 ) ) ;
#236521=VERTEX_POINT ( 'NONE', #148905 ) ;
#236525=DIRECTION ( 'NONE',  ( 0.000000000000000000, 0.9915357197604972583, -0.1298341882519109536 ) ) ;
#236544=EDGE_LOOP ( 'NONE', ( #58227, #225894, #62601, #18590 ) ) ;
#236584=CARTESIAN_POINT ( 'NONE',  ( -21.05000000000000071, 5.850000000011105428, -144.1324972242779836 ) ) ;
#236647=ADVANCED_FACE ( 'NONE', ( #56190 ), #172359, .F. ) ;
#236667=DIRECTION ( 'NONE',  ( 1.000000000000000000, 0.000000000000000000, 0.000000000000000000 ) ) ;
#236677=AXIS2_PLACEMENT_3D ( 'NONE', #253604, #131105, #211943 ) ;
#236684=CARTESIAN_POINT ( 'NONE',  ( 21.11101077988997332, 6.423684734737198809, -133.9847147310856883 ) ) ;
#236691=ADVANCED_FACE ( 'NONE', ( #121363 ), #226936, .T. ) ;
#236699=ORIENTED_EDGE ( 'NONE', *, *, #66674, .T. ) ;
#236717=AXIS2_PLACEMENT_3D ( 'NONE', #175918, #15561, #230746 ) ;
#236720=DIRECTION ( 'NONE',  ( 0.000000000000000000, -1.000000000000000000, 0.000000000000000000 ) ) ;
#236747=CARTESIAN_POINT ( 'NONE',  ( -20.54999999999999716, 1.925233644870972816, -146.7302435331261563 ) ) ;
#236748=EDGE_LOOP ( 'NONE', ( #144265, #89997, #45360, #211708 ) ) ;
#236796=AXIS2_PLACEMENT_3D ( 'NONE', #40433, #138186, #39136 ) ;
#236805=AXIS2_PLACEMENT_3D ( 'NONE', #127855, #167011, #246501 ) ;
#236824=PLANE ( 'NONE',  #166885 ) ;
#236859=DIRECTION ( 'NONE',  ( 0.000000000000000000, 0.8660254037844383745, -0.5000000000000003331 ) ) ;
#236879=CARTESIAN_POINT ( 'NONE',  ( -23.25000000000000000, 1.115600667400684642E-11, -134.0000000000000000 ) ) ;
#236887=EDGE_CURVE ( 'NONE', #102830, #208289, #235131, .T. ) ;
#236893=VERTEX_POINT ( 'NONE', #29950 ) ;
#236955=FACE_OUTER_BOUND ( 'NONE', #16125, .T. ) ;
#236985=CIRCLE ( 'NONE', #224506, 0.09999999999999939493 ) ;
#237015=ORIENTED_EDGE ( 'NONE', *, *, #6121, .T. ) ;
#237017=AXIS2_PLACEMENT_3D ( 'NONE', #257758, #115740, #253947 ) ;
#237024=ORIENTED_EDGE ( 'NONE', *, *, #66823, .F. ) ;
#237035=CYLINDRICAL_SURFACE ( 'NONE', #38703, 0.09999999999998898659 ) ;
#237082=LINE ( 'NONE', #179685, #77475 ) ;
#237128=VERTEX_POINT ( 'NONE', #62323 ) ;
#237168=AXIS2_PLACEMENT_3D ( 'NONE', #121443, #122717, #61437 ) ;
#237198=LINE ( 'NONE', #41585, #150920 ) ;
#237204=EDGE_CURVE ( 'NONE', #46322, #111978, #102697, .T. ) ;
#237217=VERTEX_POINT ( 'NONE', #220115 ) ;
#237254=CARTESIAN_POINT ( 'NONE',  ( -22.49544290803720870, 11.74987023786906981, -133.9346880407418894 ) ) ;
#237260=ORIENTED_EDGE ( 'NONE', *, *, #203050, .F. ) ;
#237261=EDGE_CURVE ( 'NONE', #47711, #207209, #48048, .T. ) ;
#237293=ORIENTED_EDGE ( 'NONE', *, *, #103764, .T. ) ;
#237303=CARTESIAN_POINT ( 'NONE',  ( -23.25000000000000000, 1.115600667400684642E-11, -134.0000000000000000 ) ) ;
#237356=CARTESIAN_POINT ( 'NONE',  ( 21.05000000000000071, -11.64999999998883595, -164.4000000000000057 ) ) ;
#237367=ORIENTED_EDGE ( 'NONE', *, *, #244823, .T. ) ;
#237370=EDGE_CURVE ( 'NONE', #54116, #29064, #167865, .T. ) ;
#237373=ORIENTED_EDGE ( 'NONE', *, *, #53896, .F. ) ;
#237380=CARTESIAN_POINT ( 'NONE',  ( 20.93302460841142931, 10.31565961587945246, -173.0364194119178478 ) ) ;
#237426=DIRECTION ( 'NONE',  ( 1.000000000000000000, 0.000000000000000000, 0.000000000000000000 ) ) ;
#237466=EDGE_CURVE ( 'NONE', #239914, #44452, #52307, .T. ) ;
#237498=ADVANCED_FACE ( 'NONE', ( #232967 ), #149580, .T. ) ;
#237502=DIRECTION ( 'NONE',  ( -1.000000000000000000, 0.000000000000000000, 0.000000000000000000 ) ) ;
#237503=EDGE_LOOP ( 'NONE', ( #12175, #170472, #31827, #122376 ) ) ;
#237513=CARTESIAN_POINT ( 'NONE',  ( 20.12500000000000000, 9.750000000011153745, -155.1500000000000057 ) ) ;
#237520=CARTESIAN_POINT ( 'NONE',  ( -23.15000000000000213, 11.75000000001115907, -160.6583993101029648 ) ) ;
#237531=DIRECTION ( 'NONE',  ( 0.000000000000000000, 0.000000000000000000, -1.000000000000000000 ) ) ;
#237611=CIRCLE ( 'NONE', #141734, 0.09999999999998898659 ) ;
#237651=CARTESIAN_POINT ( 'NONE',  ( -18.50000000000000000, -9.419084502802133940, -174.3299078070254495 ) ) ;
#237666=LINE ( 'NONE', #198530, #233117 ) ;
#237703=ORIENTED_EDGE ( 'NONE', *, *, #30549, .F. ) ;
#237707=DIRECTION ( 'NONE',  ( -0.000000000000000000, -0.000000000000000000, -1.000000000000000000 ) ) ;
#237716=AXIS2_PLACEMENT_3D ( 'NONE', #93469, #11384, #90908 ) ;
#237730=CIRCLE ( 'NONE', #37850, 11.75000000000001066 ) ;
#237731=CARTESIAN_POINT ( 'NONE',  ( 21.05000000000000071, 1.115600667400684642E-11, -167.5000000000000284 ) ) ;
#237755=ORIENTED_EDGE ( 'NONE', *, *, #1134, .T. ) ;
#237776=ORIENTED_EDGE ( 'NONE', *, *, #52279, .F. ) ;
#237828=AXIS2_PLACEMENT_3D ( 'NONE', #100717, #1639, #65476 ) ;
#237843=DIRECTION ( 'NONE',  ( 1.000000000000000000, 0.000000000000000000, 0.000000000000000000 ) ) ;
#237859=ORIENTED_EDGE ( 'NONE', *, *, #79109, .F. ) ;
#237876=CYLINDRICAL_SURFACE ( 'NONE', #149003, 0.09999999999999939493 ) ;
#237884=ORIENTED_EDGE ( 'NONE', *, *, #76995, .T. ) ;
#237885=PLANE ( 'NONE',  #77063 ) ;
#237893=DIRECTION ( 'NONE',  ( 0.000000000000000000, 3.552713678800413366E-15, -1.000000000000000000 ) ) ;
#237897=CARTESIAN_POINT ( 'NONE',  ( -21.05000000000000071, 0.09779029131994770863, -127.7421853895239252 ) ) ;
#237927=DIRECTION ( 'NONE',  ( -1.000000000000000000, 0.000000000000000000, 0.000000000000000000 ) ) ;
#237934=VERTEX_POINT ( 'NONE', #45857 ) ;
#237946=DIRECTION ( 'NONE',  ( 1.000000000000000000, 0.000000000000000000, 0.000000000000000000 ) ) ;
#237978=ADVANCED_FACE ( 'NONE', ( #73156 ), #90096, .T. ) ;
#237981=EDGE_LOOP ( 'NONE', ( #156812, #88418, #70880, #42725 ) ) ;
#237995=CARTESIAN_POINT ( 'NONE',  ( 23.14999999999999503, 6.550000000011156231, -155.1500000000000057 ) ) ;
#238002=EDGE_LOOP ( 'NONE', ( #143068, #131255, #196076, #146306 ) ) ;
#238011=ADVANCED_FACE ( 'NONE', ( #153995 ), #120953, .F. ) ;
#238014=DIRECTION ( 'NONE',  ( 1.000000000000000000, 0.000000000000000000, 0.000000000000000000 ) ) ;
#238016=DIRECTION ( 'NONE',  ( 0.000000000000000000, -0.3738317757009345654, 0.9274965247785492695 ) ) ;
#238027=VECTOR ( 'NONE', #88116, 1000.000000000000000 ) ;
#238034=ORIENTED_EDGE ( 'NONE', *, *, #6731, .T. ) ;
#238066=EDGE_LOOP ( 'NONE', ( #235727, #130305, #181540, #6295 ) ) ;
#238091=DIRECTION ( 'NONE',  ( 0.000000000000000000, 0.000000000000000000, -1.000000000000000000 ) ) ;
#238100=AXIS2_PLACEMENT_3D ( 'NONE', #19512, #193010, #39086 ) ;
#238119=ORIENTED_EDGE ( 'NONE', *, *, #18445, .T. ) ;
#238132=DIRECTION ( 'NONE',  ( -1.000000000000000000, -0.000000000000000000, 0.000000000000000000 ) ) ;
#238138=CIRCLE ( 'NONE', #13308, 0.09999999999998898659 ) ;
#238147=CARTESIAN_POINT ( 'NONE',  ( -23.15000000000000213, 1.115600667400684642E-11, -167.5000000000000284 ) ) ;
#238158=AXIS2_PLACEMENT_3D ( 'NONE', #206834, #144261, #107727 ) ;
#238179=CARTESIAN_POINT ( 'NONE',  ( -18.42609945526410442, -9.499999710479542614, -140.9993624902473925 ) ) ;
#238207=CIRCLE ( 'NONE', #125774, 0.09999999999998898659 ) ;
#238209=EDGE_CURVE ( 'NONE', #99799, #101967, #69286, .T. ) ;
#238236=CIRCLE ( 'NONE', #246614, 0.09999999999998898659 ) ;
#238264=FACE_OUTER_BOUND ( 'NONE', #155905, .T. ) ;
#238266=FACE_OUTER_BOUND ( 'NONE', #36439, .T. ) ;
#238275=DIRECTION ( 'NONE',  ( -1.000000000000000000, -0.000000000000000000, -0.000000000000000000 ) ) ;
#238343=CARTESIAN_POINT ( 'NONE',  ( 23.24999999999999289, 11.65000000001116298, -146.1500000000000341 ) ) ;
#238347=AXIS2_PLACEMENT_3D ( 'NONE', #172592, #9602, #214240 ) ;
#238349=DIRECTION ( 'NONE',  ( 1.000000000000000000, -0.000000000000000000, -0.000000000000000000 ) ) ;
#238355=FACE_OUTER_BOUND ( 'NONE', #38390, .T. ) ;
#238358=VECTOR ( 'NONE', #132971, 1000.000000000000000 ) ;
#238382=DIRECTION ( 'NONE',  ( 0.000000000000000000, 0.000000000000000000, -1.000000000000000000 ) ) ;
#238401=ADVANCED_FACE ( 'NONE', ( #233764 ), #58929, .T. ) ;
#238433=EDGE_LOOP ( 'NONE', ( #139588, #180080, #37573, #59674 ) ) ;
#238486=EDGE_CURVE ( 'NONE', #148690, #244782, #6900, .T. ) ;
#238504=DIRECTION ( 'NONE',  ( -0.000000000000000000, 1.000000000000000000, -0.000000000000000000 ) ) ;
#238523=CARTESIAN_POINT ( 'NONE',  ( -21.44999999999999929, 7.150000000011155876, -155.2500000000000284 ) ) ;
#238594=DIRECTION ( 'NONE',  ( 0.7071067811865388020, -0.7071067811865561215, 0.000000000000000000 ) ) ;
#238613=CIRCLE ( 'NONE', #47051, 1.900000000000012790 ) ;
#238614=EDGE_CURVE ( 'NONE', #27375, #196020, #223544, .T. ) ;
#238641=CARTESIAN_POINT ( 'NONE',  ( 19.75857864376268935, 11.65000000001115943, -158.7500000000000284 ) ) ;
#238659=CARTESIAN_POINT ( 'NONE',  ( 20.94999999999999929, 10.29270135741298731, -172.9573618871519329 ) ) ;
#238662=CARTESIAN_POINT ( 'NONE',  ( -23.15000000000000213, -11.64999999998884483, -122.2500000000000284 ) ) ;
#238663=ADVANCED_FACE ( 'NONE', ( #84910 ), #244006, .T. ) ;
#238672=CYLINDRICAL_SURFACE ( 'NONE', #60564, 0.09999999999999939493 ) ;
#238683=EDGE_LOOP ( 'NONE', ( #116346, #182103, #25230, #231362, #130947 ) ) ;
#238701=EDGE_CURVE ( 'NONE', #20940, #68680, #146193, .T. ) ;
#238706=AXIS2_PLACEMENT_3D ( 'NONE', #130801, #190819, #135924 ) ;
#238710=AXIS2_PLACEMENT_3D ( 'NONE', #219629, #82663, #140084 ) ;
#238712=LINE ( 'NONE', #177491, #14827 ) ;
#238740=ORIENTED_EDGE ( 'NONE', *, *, #102296, .F. ) ;
#238745=EDGE_CURVE ( 'NONE', #163431, #171037, #246579, .T. ) ;
#238756=CYLINDRICAL_SURFACE ( 'NONE', #135956, 0.09999999999999939493 ) ;
#238787=ADVANCED_FACE ( 'NONE', ( #190495 ), #206181, .T. ) ;
#238816=ORIENTED_EDGE ( 'NONE', *, *, #150629, .T. ) ;
#238843=VERTEX_POINT ( 'NONE', #34002 ) ;
#238851=EDGE_CURVE ( 'NONE', #205417, #81104, #123807, .T. ) ;
#238875=CARTESIAN_POINT ( 'NONE',  ( -22.57320508075687115, 11.75000000001115552, -134.0000000000000000 ) ) ;
#238882=ORIENTED_EDGE ( 'NONE', *, *, #188464, .T. ) ;
#238892=TOROIDAL_SURFACE ( 'NONE', #113976, 11.65000000000000036, 0.1000000000000000056 ) ;
#238897=CARTESIAN_POINT ( 'NONE',  ( 21.14999999999999858, 11.75000000001116263, -122.2500000000000284 ) ) ;
#238917=CARTESIAN_POINT ( 'NONE',  ( -23.15000000000000213, -11.48912529306489994, -164.4000000000000057 ) ) ;
#238921=VERTEX_POINT ( 'NONE', #117354 ) ;
#238925=ORIENTED_EDGE ( 'NONE', *, *, #7982, .F. ) ;
#238946=CIRCLE ( 'NONE', #201503, 0.09999999999999817368 ) ;
#238975=EDGE_CURVE ( 'NONE', #91128, #50799, #131985, .T. ) ;
#238981=CARTESIAN_POINT ( 'NONE',  ( 21.05000000000000426, 6.258817194692633201, -133.9663672646664168 ) ) ;
#239003=CYLINDRICAL_SURFACE ( 'NONE', #190378, 11.80000000000000426 ) ;
#239010=VERTEX_POINT ( 'NONE', #160361 ) ;
#239036=ORIENTED_EDGE ( 'NONE', *, *, #192947, .F. ) ;
#239050=DIRECTION ( 'NONE',  ( 0.000000000000000000, 0.008583690987127625890, 0.9999631594459055250 ) ) ;
#239071=CARTESIAN_POINT ( 'NONE',  ( -21.05000000000000071, 0.09779029131994770863, -127.7421853895239252 ) ) ;
#239091=CARTESIAN_POINT ( 'NONE',  ( 20.94999999999999929, -8.999999999988844479, -143.8939691226524644 ) ) ;
#239096=DIRECTION ( 'NONE',  ( -1.000000000000000000, 0.000000000000000000, 0.000000000000000000 ) ) ;
#239120=CARTESIAN_POINT ( 'NONE',  ( -20.95613430942402644, 11.75000000001115552, -140.8571626482203101 ) ) ;
#239125=AXIS2_PLACEMENT_3D ( 'NONE', #116679, #37170, #219625 ) ;
#239217=DIRECTION ( 'NONE',  ( 0.000000000000000000, 0.1298341882520022694, 0.9915357197604852679 ) ) ;
#239232=EDGE_CURVE ( 'NONE', #14142, #174088, #232147, .T. ) ;
#239247=DIRECTION ( 'NONE',  ( 1.000000000000000000, 3.265361837132813093E-16, -0.000000000000000000 ) ) ;
#239252=EDGE_LOOP ( 'NONE', ( #65761, #217098, #234424, #230795 ) ) ;
#239349=DIRECTION ( 'NONE',  ( 1.000000000000000000, 2.952720810173289112E-16, -0.000000000000000000 ) ) ;
#239355=DIRECTION ( 'NONE',  ( -1.000000000000000000, 0.000000000000000000, 0.000000000000000000 ) ) ;
#239370=DIRECTION ( 'NONE',  ( -1.000000000000000000, 0.000000000000000000, 0.000000000000000000 ) ) ;
#239387=VERTEX_POINT ( 'NONE', #62206 ) ;
#239456=ORIENTED_EDGE ( 'NONE', *, *, #174564, .T. ) ;
#239460=ORIENTED_EDGE ( 'NONE', *, *, #226467, .T. ) ;
#239483=CARTESIAN_POINT ( 'NONE',  ( -21.14999999999999858, -11.74999999998884448, -134.0000000000000000 ) ) ;
#239507=DIRECTION ( 'NONE',  ( 0.000000000000000000, 0.6728971962617388280, 0.7397360091702248619 ) ) ;
#239510=CARTESIAN_POINT ( 'NONE',  ( 22.48660254037843842, 11.75000000001115730, -133.9500000000000171 ) ) ;
#239516=AXIS2_PLACEMENT_3D ( 'NONE', #123318, #162454, #64608 ) ;
#239534=CARTESIAN_POINT ( 'NONE',  ( -18.39999999999999858, -9.599999999988844124, -141.0320693966996828 ) ) ;
#239544=PLANE ( 'NONE',  #97425 ) ;
#239565=DIRECTION ( 'NONE',  ( 1.000000000000000000, -0.000000000000000000, -0.000000000000000000 ) ) ;
#239594=CIRCLE ( 'NONE', #118801, 0.09999999999998898659 ) ;
#239619=CARTESIAN_POINT ( 'NONE',  ( 23.14999999999999858, 1.115625160336667635E-11, -165.5000000000000284 ) ) ;
#239634=EDGE_LOOP ( 'NONE', ( #57331, #179954, #2640 ) ) ;
#239643=ORIENTED_EDGE ( 'NONE', *, *, #232215, .T. ) ;
#239644=AXIS2_PLACEMENT_3D ( 'NONE', #211409, #31518, #151452 ) ;
#239653=DIRECTION ( 'NONE',  ( -0.000000000000000000, -0.1298341882520022694, -0.9915357197604853789 ) ) ;
#239667=ORIENTED_EDGE ( 'NONE', *, *, #24728, .F. ) ;
#239669=CARTESIAN_POINT ( 'NONE',  ( -20.00857864376270001, 9.350000000011156942, -155.2500000000000284 ) ) ;
#239710=ADVANCED_FACE ( 'NONE', ( #126687 ), #182635, .T. ) ;
#239825=DIRECTION ( 'NONE',  ( 0.000000000000000000, 1.000000000000000000, 0.000000000000000000 ) ) ;
#239836=CARTESIAN_POINT ( 'NONE',  ( 20.94999999999999574, -11.64999999998883595, -136.9000000000000341 ) ) ;
#239863=CARTESIAN_POINT ( 'NONE',  ( 18.39999999999999858, -9.499999999988842703, -174.1001893912220737 ) ) ;
#239864=CIRCLE ( 'NONE', #256339, 12.77500000000000036 ) ;
#239882=CARTESIAN_POINT ( 'NONE',  ( 23.24999999999999645, 4.775700934590584090, -145.8487681040459734 ) ) ;
#239914=VERTEX_POINT ( 'NONE', #233508 ) ;
#239965=EDGE_CURVE ( 'NONE', #196244, #251858, #174850, .T. ) ;
#240000=TOROIDAL_SURFACE ( 'NONE', #19223, 11.89999999999999858, 0.1000000000000000056 ) ;
#240025=DIRECTION ( 'NONE',  ( 1.000000000000000000, 0.000000000000000000, -0.000000000000000000 ) ) ;
#240034=ORIENTED_EDGE ( 'NONE', *, *, #95693, .T. ) ;
#240037=ORIENTED_EDGE ( 'NONE', *, *, #105977, .F. ) ;
#240043=ORIENTED_EDGE ( 'NONE', *, *, #20376, .T. ) ;
#240044=DIRECTION ( 'NONE',  ( 1.000000000000000000, 0.000000000000000000, -0.000000000000000000 ) ) ;
#240051=VERTEX_POINT ( 'NONE', #97792 ) ;
#240063=ORIENTED_EDGE ( 'NONE', *, *, #102294, .F. ) ;
#240091=EDGE_LOOP ( 'NONE', ( #216886, #80859, #208476, #168581 ) ) ;
#240109=DIRECTION ( 'NONE',  ( 0.000000000000000000, -0.8660254037844384856, 0.5000000000000002220 ) ) ;
#240126=CARTESIAN_POINT ( 'NONE',  ( -21.37071067811865532, 8.070710678129811910, -146.2500000000000284 ) ) ;
#240150=CARTESIAN_POINT ( 'NONE',  ( -21.44999999999999929, 7.250000000011155521, -155.1500000000000057 ) ) ;
#240151=DIRECTION ( 'NONE',  ( 0.000000000000000000, 1.953992523340277404E-14, 1.000000000000000000 ) ) ;
#240154=AXIS2_PLACEMENT_3D ( 'NONE', #63850, #208515, #207225 ) ;
#240185=PLANE ( 'NONE',  #61913 ) ;
#240196=ADVANCED_FACE ( 'NONE', ( #199517 ), #219042, .T. ) ;
#240211=ORIENTED_EDGE ( 'NONE', *, *, #248670, .F. ) ;
#240212=DIRECTION ( 'NONE',  ( 0.000000000000000000, 0.000000000000000000, -1.000000000000000000 ) ) ;
#240234=CARTESIAN_POINT ( 'NONE',  ( 21.05000000000000071, 11.75000000001115907, -160.6583993101029364 ) ) ;
#240235=VECTOR ( 'NONE', #252684, 1000.000000000000000 ) ;
#240244=ORIENTED_EDGE ( 'NONE', *, *, #109488, .T. ) ;
#240251=ADVANCED_FACE ( 'NONE', ( #225452 ), #51945, .T. ) ;
#240262=VECTOR ( 'NONE', #120658, 1000.000000000000000 ) ;
#240270=LINE ( 'NONE', #77315, #46990 ) ;
#240283=CARTESIAN_POINT ( 'NONE',  ( 21.11344571971254069, 10.61787902352924817, -146.2460208924022425 ) ) ;
#240308=DIRECTION ( 'NONE',  ( 0.000000000000000000, 0.000000000000000000, -1.000000000000000000 ) ) ;
#240316=EDGE_CURVE ( 'NONE', #94099, #5925, #49408, .T. ) ;
#240377=AXIS2_PLACEMENT_3D ( 'NONE', #54623, #224597, #233293 ) ;
#240380=CARTESIAN_POINT ( 'NONE',  ( -23.25000000000000000, 11.75000000001115552, -134.0000000000000000 ) ) ;
#240406=ORIENTED_EDGE ( 'NONE', *, *, #152515, .T. ) ;
#240471=CIRCLE ( 'NONE', #140496, 0.09999999999999939493 ) ;
#240502=DIRECTION ( 'NONE',  ( -0.000000000000000000, 0.8660254037844411501, 0.4999999999999956701 ) ) ;
#240508=ORIENTED_EDGE ( 'NONE', *, *, #230286, .T. ) ;
#240530=VERTEX_POINT ( 'NONE', #223858 ) ;
#240537=ORIENTED_EDGE ( 'NONE', *, *, #65002, .F. ) ;
#240570=DIRECTION ( 'NONE',  ( -0.000000000000000000, 0.1350103645451904977, 0.9908441862701597991 ) ) ;
#240583=CARTESIAN_POINT ( 'NONE',  ( -18.59999999999999787, 11.65000000001115232, -167.5000000000000284 ) ) ;
#240623=ADVANCED_FACE ( 'NONE', ( #131187 ), #74113, .F. ) ;
#240629=CARTESIAN_POINT ( 'NONE',  ( 18.52928932188133970, 10.27928932189250411, -158.7500000000000284 ) ) ;
#240650=DIRECTION ( 'NONE',  ( 0.7071067811865388020, -0.7071067811865561215, 0.000000000000000000 ) ) ;
#240686=AXIS2_PLACEMENT_3D ( 'NONE', #199251, #179688, #20621 ) ;
#240722=CARTESIAN_POINT ( 'NONE',  ( -18.50000000000000000, 11.65000000001115232, -122.2500000000000284 ) ) ;
#240731=AXIS2_PLACEMENT_3D ( 'NONE', #161956, #164516, #244025 ) ;
#240742=CARTESIAN_POINT ( 'NONE',  ( -21.13422380239033771, 1.115470038567900342E-11, -127.5066734851939003 ) ) ;
#240768=DIRECTION ( 'NONE',  ( 0.000000000000000000, 1.000000000000000000, 0.000000000000000000 ) ) ;
#240773=CARTESIAN_POINT ( 'NONE',  ( -18.59999996769639097, -9.363273769819199899, -141.1814939154657793 ) ) ;
#240775=DIRECTION ( 'NONE',  ( 0.000000000000000000, 1.000000000000000000, 0.000000000000000000 ) ) ;
#240778=VERTEX_POINT ( 'NONE', #235416 ) ;
#240791=ADVANCED_FACE ( 'NONE', ( #16407 ), #174076, .F. ) ;
#240796=AXIS2_PLACEMENT_3D ( 'NONE', #88292, #195157, #193853 ) ;
#240822=ORIENTED_EDGE ( 'NONE', *, *, #179235, .F. ) ;
#240828=ORIENTED_EDGE ( 'NONE', *, *, #178575, .F. ) ;
#240874=VECTOR ( 'NONE', #217748, 1000.000000000000000 ) ;
#240897=CARTESIAN_POINT ( 'NONE',  ( 21.14999999999999858, 10.71339244341104013, -146.2500000000000284 ) ) ;
#240914=CARTESIAN_POINT ( 'NONE',  ( 20.94999999999999929, 8.776282895303628706, -142.5586289951409640 ) ) ;
#240927=CARTESIAN_POINT ( 'NONE',  ( 22.40736611211992368, 1.115600667400684642E-11, -122.3504291924552234 ) ) ;
#240933=AXIS2_PLACEMENT_3D ( 'NONE', #239836, #56021, #256765 ) ;
#241021=EDGE_CURVE ( 'NONE', #126194, #111115, #61787, .T. ) ;
#241062=ORIENTED_EDGE ( 'NONE', *, *, #112348, .F. ) ;
#241160=CARTESIAN_POINT ( 'NONE',  ( 20.94999999999999929, 5.500000000011153745, -155.0947339810869323 ) ) ;
#241173=CARTESIAN_POINT ( 'NONE',  ( -20.54999999999999716, 7.150000000011155876, -146.3500000000000227 ) ) ;
#241217=ORIENTED_EDGE ( 'NONE', *, *, #220299, .T. ) ;
#241225=VERTEX_POINT ( 'NONE', #17379 ) ;
#241226=CARTESIAN_POINT ( 'NONE',  ( 21.13435531349810859, 1.115406763810579610E-11, -127.5062789364073694 ) ) ;
#241227=DIRECTION ( 'NONE',  ( 1.000000000000000000, 0.000000000000000000, 0.000000000000000000 ) ) ;
#241274=DIRECTION ( 'NONE',  ( -1.000000000000000000, 0.000000000000000000, 0.000000000000000000 ) ) ;
#241284=LINE ( 'NONE', #87310, #226382 ) ;
#241294=ORIENTED_EDGE ( 'NONE', *, *, #197839, .T. ) ;
#241300=ORIENTED_EDGE ( 'NONE', *, *, #187229, .T. ) ;
#241311=EDGE_CURVE ( 'NONE', #224095, #45297, #78525, .T. ) ;
#241362=EDGE_CURVE ( 'NONE', #44452, #28264, #178525, .T. ) ;
#241381=CIRCLE ( 'NONE', #83099, 4.049999999999998046 ) ;
#241426=CIRCLE ( 'NONE', #12297, 0.4000000000000114575 ) ;
#241442=ORIENTED_EDGE ( 'NONE', *, *, #168992, .T. ) ;
#241456=FACE_OUTER_BOUND ( 'NONE', #251978, .T. ) ;
#241459=CIRCLE ( 'NONE', #16622, 0.1999999999999987899 ) ;
#241475=CARTESIAN_POINT ( 'NONE',  ( -20.85000000000000142, 7.021664781911246322, -171.3335654018973173 ) ) ;
#241481=DIRECTION ( 'NONE',  ( 0.000000000000000000, 0.000000000000000000, -1.000000000000000000 ) ) ;
#241486=EDGE_CURVE ( 'NONE', #149669, #239387, #186896, .T. ) ;
#241502=CARTESIAN_POINT ( 'NONE',  ( 20.85000000000000142, 11.75000000001115907, -160.7161343370219129 ) ) ;
#241503=DIRECTION ( 'NONE',  ( 1.000000000000000000, 0.000000000000000000, -0.000000000000000000 ) ) ;
#241507=ORIENTED_EDGE ( 'NONE', *, *, #62102, .T. ) ;
#241524=CIRCLE ( 'NONE', #37525, 0.09999999999998898659 ) ;
#241586=ORIENTED_EDGE ( 'NONE', *, *, #149560, .F. ) ;
#241589=ORIENTED_EDGE ( 'NONE', *, *, #248653, .F. ) ;
#241617=DIRECTION ( 'NONE',  ( 1.000000000000000000, -0.000000000000000000, -0.000000000000000000 ) ) ;
#241618=EDGE_CURVE ( 'NONE', #123059, #13549, #224275, .T. ) ;
#241637=DIRECTION ( 'NONE',  ( 0.000000000000000000, 0.000000000000000000, -1.000000000000000000 ) ) ;
#241647=ORIENTED_EDGE ( 'NONE', *, *, #9159, .T. ) ;
#241651=CARTESIAN_POINT ( 'NONE',  ( -23.15000000000000213, 1.115600667400684642E-11, -169.6000000000000227 ) ) ;
#241667=EDGE_CURVE ( 'NONE', #254695, #100941, #210372, .T. ) ;
#241673=CARTESIAN_POINT ( 'NONE',  ( 20.59588692710267921, 10.36872342118052259, -141.6390810945103169 ) ) ;
#241771=AXIS2_PLACEMENT_3D ( 'NONE', #75953, #56361, #158101 ) ;
#241780=DIRECTION ( 'NONE',  ( 0.000000000000000000, 0.000000000000000000, -1.000000000000000000 ) ) ;
#241816=CIRCLE ( 'NONE', #83573, 0.09999999999998898659 ) ;
#241817=VERTEX_POINT ( 'NONE', #85236 ) ;
#241834=AXIS2_PLACEMENT_3D ( 'NONE', #227216, #66865, #48578 ) ;
#241842=VERTEX_POINT ( 'NONE', #73448 ) ;
#241843=ORIENTED_EDGE ( 'NONE', *, *, #14102, .F. ) ;
#241847=ORIENTED_EDGE ( 'NONE', *, *, #134256, .F. ) ;
#241891=ADVANCED_FACE ( 'NONE', ( #151706 ), #50000, .T. ) ;
#241894=ORIENTED_EDGE ( 'NONE', *, *, #88223, .T. ) ;
#241908=CARTESIAN_POINT ( 'NONE',  ( -21.05000000000000071, 1.115600667400684642E-11, -141.9000000000000341 ) ) ;
#241930=CYLINDRICAL_SURFACE ( 'NONE', #235435, 0.09999999999999939493 ) ;
#241944=EDGE_CURVE ( 'NONE', #89497, #205134, #55102, .T. ) ;
#241946=CIRCLE ( 'NONE', #104556, 2.100000000000002309 ) ;
#241987=CARTESIAN_POINT ( 'NONE',  ( 19.86930884467607328, 11.68691006698174739, -158.7392226389382870 ) ) ;
#241999=ORIENTED_EDGE ( 'NONE', *, *, #213710, .T. ) ;
#242008=VERTEX_POINT ( 'NONE', #198494 ) ;
#242054=CARTESIAN_POINT ( 'NONE',  ( -18.39999999999999503, -9.499999999988851584, -174.1001893912220737 ) ) ;
#242063=CARTESIAN_POINT ( 'NONE',  ( 23.15000000000000213, -11.64999999998883595, -164.4000000000000057 ) ) ;
#242081=CARTESIAN_POINT ( 'NONE',  ( 22.47071067811865319, 7.720074744509197728, -133.9009075452974002 ) ) ;
#242089=CARTESIAN_POINT ( 'NONE',  ( 21.46681500597193093, 1.115539681028482333E-11, -127.1424888405652212 ) ) ;
#242115=DIRECTION ( 'NONE',  ( 1.000000000000000000, 0.000000000000000000, 0.000000000000000000 ) ) ;
#242135=ORIENTED_EDGE ( 'NONE', *, *, #246273, .F. ) ;
#242156=EDGE_CURVE ( 'NONE', #139686, #161202, #74840, .T. ) ;
#242159=EDGE_CURVE ( 'NONE', #122938, #180099, #116505, .T. ) ;
#242172=FACE_OUTER_BOUND ( 'NONE', #214968, .T. ) ;
#242205=CARTESIAN_POINT ( 'NONE',  ( -18.50000000000000000, 9.250000000011157297, -155.1500000000000057 ) ) ;
#242221=DIRECTION ( 'NONE',  ( 0.000000000000000000, 0.000000000000000000, -1.000000000000000000 ) ) ;
#242265=EDGE_LOOP ( 'NONE', ( #107436, #94286, #129764, #11473, #21038, #76867, #194311, #242909, #46918, #50173, #122147, #16089, #244618, #165531, #34443, #224381, #163930, #240043, #205857, #159500, #185362, #240034, #241507, #204790, #49465, #102906, #221817 ) ) ;
#242274=CIRCLE ( 'NONE', #79764, 0.5000000000000004441 ) ;
#242284=AXIS2_PLACEMENT_3D ( 'NONE', #93908, #232158, #155206 ) ;
#242292=ORIENTED_EDGE ( 'NONE', *, *, #56481, .T. ) ;
#242303=ORIENTED_EDGE ( 'NONE', *, *, #215428, .F. ) ;
#242340=DIRECTION ( 'NONE',  ( 0.000000000000000000, -1.000000000000000000, 0.000000000000000000 ) ) ;
#242350=LINE ( 'NONE', #162842, #13422 ) ;
#242357=CIRCLE ( 'NONE', #159009, 0.09999999999999939493 ) ;
#242380=APPLICATION_CONTEXT ( 'automotive_design' ) ;
#242381=CARTESIAN_POINT ( 'NONE',  ( -20.64999999999999858, 1.115600667400684642E-11, -154.6250000000000284 ) ) ;
#242384=EDGE_CURVE ( 'NONE', #239387, #253858, #178906, .T. ) ;
#242399=CARTESIAN_POINT ( 'NONE',  ( 22.50927854361889402, -0.1008580735143376206, -122.2504328739731108 ) ) ;
#242570=DIRECTION ( 'NONE',  ( -1.000000000000000000, 0.000000000000000000, 0.000000000000000000 ) ) ;
#242576=CARTESIAN_POINT ( 'NONE',  ( 21.05000000000000071, 1.115623935689868526E-11, -165.6000000000000227 ) ) ;
#242592=VERTEX_POINT ( 'NONE', #5087 ) ;
#242595=ORIENTED_EDGE ( 'NONE', *, *, #13110, .F. ) ;
#242601=CARTESIAN_POINT ( 'NONE',  ( -21.44999999999999929, 7.150000000011155876, -146.2500000000000284 ) ) ;
#242602=SPHERICAL_SURFACE ( 'NONE', #106812, 0.1000000000000000056 ) ;
#242605=CIRCLE ( 'NONE', #126068, 0.09999999999999158173 ) ;
#242611=VECTOR ( 'NONE', #75562, 1000.000000000000000 ) ;
#242624=ORIENTED_EDGE ( 'NONE', *, *, #59276, .F. ) ;
#242625=ADVANCED_FACE ( 'NONE', ( #161658 ), #62526, .F. ) ;
#242658=ORIENTED_EDGE ( 'NONE', *, *, #122314, .F. ) ;
#242665=CARTESIAN_POINT ( 'NONE',  ( 23.14999999999999858, -11.74999999998883560, -122.2500000000000284 ) ) ;
#242666=DIRECTION ( 'NONE',  ( 0.000000000000000000, 0.000000000000000000, -1.000000000000000000 ) ) ;
#242686=AXIS2_PLACEMENT_3D ( 'NONE', #163499, #222158, #243025 ) ;
#242697=CARTESIAN_POINT ( 'NONE',  ( -21.05000000000000071, 6.257814610487270279, -133.9022097086912311 ) ) ;
#242718=DIRECTION ( 'NONE',  ( 0.000000000000000000, 0.000000000000000000, -1.000000000000000000 ) ) ;
#242720=ORIENTED_EDGE ( 'NONE', *, *, #136992, .T. ) ;
#242726=CARTESIAN_POINT ( 'NONE',  ( 21.05000000000000071, 10.62872031401550288, -141.6649135690876449 ) ) ;
#242739=FACE_OUTER_BOUND ( 'NONE', #51065, .T. ) ;
#242786=FACE_OUTER_BOUND ( 'NONE', #67804, .T. ) ;
#242806=EDGE_LOOP ( 'NONE', ( #2380, #195780, #42112, #233199 ) ) ;
#242824=ORIENTED_EDGE ( 'NONE', *, *, #33100, .F. ) ;
#242855=DIRECTION ( 'NONE',  ( 0.000000000000000000, 0.000000000000000000, -1.000000000000000000 ) ) ;
#242858=AXIS2_PLACEMENT_3D ( 'NONE', #63950, #204723, #182627 ) ;
#242874=CARTESIAN_POINT ( 'NONE',  ( -18.59999999999999787, 11.65000000001115232, -141.0148057706540214 ) ) ;
#242909=ORIENTED_EDGE ( 'NONE', *, *, #86709, .T. ) ;
#242929=DIRECTION ( 'NONE',  ( 0.000000000000000000, 1.000000000000000000, 0.000000000000000000 ) ) ;
#242936=AXIS2_PLACEMENT_3D ( 'NONE', #39468, #293, #240212 ) ;
#242959=AXIS2_PLACEMENT_3D ( 'NONE', #110194, #154505, #73681 ) ;
#242985=ORIENTED_EDGE ( 'NONE', *, *, #75002, .T. ) ;
#243025=DIRECTION ( 'NONE',  ( 0.000000000000000000, -8.881784197001263367E-15, -1.000000000000000000 ) ) ;
#243029=DIRECTION ( 'NONE',  ( 1.000000000000000000, -0.000000000000000000, -0.000000000000000000 ) ) ;
#243073=CARTESIAN_POINT ( 'NONE',  ( -18.39999999999999858, -9.499999999988849808, -140.9992856778388841 ) ) ;
#243100=VERTEX_POINT ( 'NONE', #110325 ) ;
#243148=DIRECTION ( 'NONE',  ( 0.000000000000000000, 0.000000000000000000, -1.000000000000000000 ) ) ;
#243154=DIRECTION ( 'NONE',  ( 0.000000000000000000, 0.1495327102803792052, -0.9887567792719320625 ) ) ;
#243175=CARTESIAN_POINT ( 'NONE',  ( -21.44999999999999929, 7.250000000011155521, -155.2500000000000284 ) ) ;
#243212=DIRECTION ( 'NONE',  ( -1.836970198721029934E-16, 1.000000000000000000, 0.000000000000000000 ) ) ;
#243215=EDGE_CURVE ( 'NONE', #104618, #154183, #150743, .T. ) ;
#243254=AXIS2_PLACEMENT_3D ( 'NONE', #179967, #241227, #144662 ) ;
#243267=CARTESIAN_POINT ( 'NONE',  ( 18.52643265882457868, 10.31973158071402885, -173.0505334713354841 ) ) ;
#243287=DIRECTION ( 'NONE',  ( -0.000000000000000000, -0.000000000000000000, 1.000000000000000000 ) ) ;
#243305=CIRCLE ( 'NONE', #14402, 0.1000000000000096922 ) ;
#243315=CARTESIAN_POINT ( 'NONE',  ( 23.24999999999999645, 5.000000000011153745, -146.4052660189131245 ) ) ;
#243322=LINE ( 'NONE', #84196, #91564 ) ;
#243328=AXIS2_PLACEMENT_3D ( 'NONE', #214006, #109300, #248842 ) ;
#243338=DIRECTION ( 'NONE',  ( -0.000000000000000000, -0.000000000000000000, -1.000000000000000000 ) ) ;
#243346=AXIS2_PLACEMENT_3D ( 'NONE', #235691, #117043, #136582 ) ;
#243380=CARTESIAN_POINT ( 'NONE',  ( -20.94999999999999929, -1.164121893230052995, -175.4148480855716059 ) ) ;
#243426=EDGE_CURVE ( 'NONE', #101165, #113973, #216983, .T. ) ;
#243427=AXIS2_PLACEMENT_3D ( 'NONE', #239091, #182979, #65578 ) ;
#243448=CARTESIAN_POINT ( 'NONE',  ( 23.25000000000000000, -9.599999999988845900, -143.8939691226524644 ) ) ;
#243458=DIRECTION ( 'NONE',  ( 0.000000000000000000, 1.897661533703519897E-16, -1.000000000000000000 ) ) ;
#243467=AXIS2_PLACEMENT_3D ( 'NONE', #230376, #127429, #68746 ) ;
#243480=DIRECTION ( 'NONE',  ( 0.000000000000000000, 1.000000000000000000, 0.000000000000000000 ) ) ;
#243516=DIRECTION ( 'NONE',  ( 1.000000000000000000, -0.000000000000000000, -0.000000000000000000 ) ) ;
#243521=CARTESIAN_POINT ( 'NONE',  ( 20.12500000000000355, 10.24195072709382970, -141.8602037270861445 ) ) ;
#243575=CARTESIAN_POINT ( 'NONE',  ( -18.47140463609785854, -9.671474685209730637, -174.1727604582741833 ) ) ;
#243597=DIRECTION ( 'NONE',  ( 0.000000000000000000, 0.9876197685951252359, -0.1568667991644863424 ) ) ;
#243610=EDGE_LOOP ( 'NONE', ( #186712, #103493, #120490, #48692 ) ) ;
#243619=VERTEX_POINT ( 'NONE', #79545 ) ;
#243627=CARTESIAN_POINT ( 'NONE',  ( 18.59999999999999076, -1.164121893230052995, -175.4148480855716059 ) ) ;
#243631=CARTESIAN_POINT ( 'NONE',  ( 18.39999999999999858, -9.519327731081283162, -140.9729763765593589 ) ) ;
#243643=EDGE_CURVE ( 'NONE', #111004, #43473, #67344, .T. ) ;
#243651=CARTESIAN_POINT ( 'NONE',  ( 21.05000000000000071, -0.09999999998884338825, -122.3504291924552234 ) ) ;
#243693=ORIENTED_EDGE ( 'NONE', *, *, #154890, .F. ) ;
#243697=CARTESIAN_POINT ( 'NONE',  ( -23.25000000000000000, -11.64999999998884483, -134.0000000000000000 ) ) ;
#243700=CIRCLE ( 'NONE', #127171, 0.1000000000000002554 ) ;
#243734=ADVANCED_FACE ( 'NONE', ( #3881 ), #164821, .T. ) ;
#243737=DIRECTION ( 'NONE',  ( 3.469446951953728416E-14, -0.8660254037844309360, 0.5000000000000134337 ) ) ;
#243739=CIRCLE ( 'NONE', #214505, 0.09999999999999939493 ) ;
#243756=CARTESIAN_POINT ( 'NONE',  ( 18.45036689428330590, -9.490184143317831555, -141.0126958274863682 ) ) ;
#243791=ORIENTED_EDGE ( 'NONE', *, *, #18524, .T. ) ;
#243805=CARTESIAN_POINT ( 'NONE',  ( -22.47007471830799830, 7.720710651937627844, -134.0000000000000000 ) ) ;
#243818=CARTESIAN_POINT ( 'NONE',  ( -20.64999999999999858, -9.499999999988846255, -157.6060308773475924 ) ) ;
#243838=AXIS2_PLACEMENT_3D ( 'NONE', #19292, #36309, #196637 ) ;
#243875=EDGE_LOOP ( 'NONE', ( #99246, #5164, #189218, #116893 ) ) ;
#243877=CARTESIAN_POINT ( 'NONE',  ( -20.94999999999999929, -1.835859311432479268, -179.0044391687985410 ) ) ;
#243916=CARTESIAN_POINT ( 'NONE',  ( 20.95512820512820440, 8.876151316299271343, -142.5586289951409640 ) ) ;
#243947=CARTESIAN_POINT ( 'NONE',  ( 21.51976009735019346, 6.910458441670357388, -134.0000000000000000 ) ) ;
#243960=DIRECTION ( 'NONE',  ( 0.000000000000000000, 0.000000000000000000, 1.000000000000000000 ) ) ;
#243971=DIRECTION ( 'NONE',  ( 0.000000000000000000, -0.9915357197604792727, 0.1298341882520475943 ) ) ;
#243976=CARTESIAN_POINT ( 'NONE',  ( 20.94999999999999929, -11.29603075032412995, -137.0478991596638991 ) ) ;
#243982=CARTESIAN_POINT ( 'NONE',  ( 18.49999999999996803, 7.070967871809997973, -171.2465642218683115 ) ) ;
#243983=FACE_OUTER_BOUND ( 'NONE', #12890, .T. ) ;
#243990=DIRECTION ( 'NONE',  ( 0.000000000000000000, 0.4930308989874729320, 0.8700118002898605818 ) ) ;
#244001=B_SPLINE_CURVE_WITH_KNOTS ( 'NONE', 3,
 ( #205721, #141899, #243575, #27132, #24551, #221417, #106605, #166643 ),
 .UNSPECIFIED., .F., .F.,
 ( 4, 2, 2, 4 ),
 ( 0.000000000000000000, 0.0001094981963948554304, 0.0002189963927897108607, 0.0004379927855794217215 ),
 .UNSPECIFIED. ) ;
#244006=CYLINDRICAL_SURFACE ( 'NONE', #161216, 12.87499999999999822 ) ;
#244009=CARTESIAN_POINT ( 'NONE',  ( 20.94999999999999929, 10.47338541492405106, -141.5786544642485580 ) ) ;
#244015=ADVANCED_FACE ( 'NONE', ( #246038 ), #67393, .T. ) ;
#244025=DIRECTION ( 'NONE',  ( 0.000000000000000000, 0.000000000000000000, 1.000000000000000000 ) ) ;
#244027=CYLINDRICAL_SURFACE ( 'NONE', #207667, 0.5000000000000004441 ) ;
#244028=EDGE_CURVE ( 'NONE', #153561, #171180, #223878, .T. ) ;
#244059=CARTESIAN_POINT ( 'NONE',  ( -23.25000000000000000, 1.115600667400684642E-11, -171.4000000000000341 ) ) ;
#244068=ORIENTED_EDGE ( 'NONE', *, *, #228875, .T. ) ;
#244084=EDGE_CURVE ( 'NONE', #89005, #48580, #66107, .T. ) ;
#244087=ORIENTED_EDGE ( 'NONE', *, *, #177607, .F. ) ;
#244100=LINE ( 'NONE', #185423, #90577 ) ;
#244127=CARTESIAN_POINT ( 'NONE',  ( -20.64999999999999858, -9.499999999988846255, -157.6060308773475924 ) ) ;
#244143=DIRECTION ( 'NONE',  ( -1.000000000000000000, -2.952720810173289112E-16, 0.000000000000000000 ) ) ;
#244171=PLANE ( 'NONE',  #153241 ) ;
#244214=DIRECTION ( 'NONE',  ( 1.000000000000000000, -0.000000000000000000, -0.000000000000000000 ) ) ;
#244228=LINE ( 'NONE', #3048, #112046 ) ;
#244246=ORIENTED_EDGE ( 'NONE', *, *, #86688, .T. ) ;
#244290=CARTESIAN_POINT ( 'NONE',  ( 18.39999999999999858, -9.599999999988845900, -174.2001893912220680 ) ) ;
#244388=ORIENTED_EDGE ( 'NONE', *, *, #185596, .F. ) ;
#244399=EDGE_CURVE ( 'NONE', #64013, #91812, #159320, .T. ) ;
#244401=ADVANCED_FACE ( 'NONE', ( #94649 ), #136319, .T. ) ;
#244415=ORIENTED_EDGE ( 'NONE', *, *, #159403, .F. ) ;
#244461=EDGE_LOOP ( 'NONE', ( #202503, #32529, #124130, #91981 ) ) ;
#244474=CARTESIAN_POINT ( 'NONE',  ( -22.39999999999999858, 11.75000000001115552, -133.9000000000000057 ) ) ;
#244478=TOROIDAL_SURFACE ( 'NONE', #161308, 0.9750000000000019762, 0.1000000000000000056 ) ;
#244503=FACE_OUTER_BOUND ( 'NONE', #46391, .T. ) ;
#244536=ADVANCED_FACE ( 'NONE', ( #201451 ), #188327, .F. ) ;
#244557=CARTESIAN_POINT ( 'NONE',  ( 18.53317502108576775, 10.32263460347359896, -173.0605957968672328 ) ) ;
#244566=CIRCLE ( 'NONE', #128060, 0.1000000000000000472 ) ;
#244574=ORIENTED_EDGE ( 'NONE', *, *, #191744, .T. ) ;
#244584=ADVANCED_FACE ( 'NONE', ( #142751 ), #63420, .F. ) ;
#244601=DIRECTION ( 'NONE',  ( 1.000000000000000000, 0.000000000000000000, 0.000000000000000000 ) ) ;
#244606=EDGE_CURVE ( 'NONE', #130320, #39562, #101022, .T. ) ;
#244618=ORIENTED_EDGE ( 'NONE', *, *, #28896, .T. ) ;
#244620=CARTESIAN_POINT ( 'NONE',  ( -18.58744394320951088, -9.566385154537224267, -174.3228480538763279 ) ) ;
#244642=LINE ( 'NONE', #88111, #157106 ) ;
#244652=CARTESIAN_POINT ( 'NONE',  ( 20.94999999999999929, 1.360870587203197646, -142.0729979270909951 ) ) ;
#244675=LINE ( 'NONE', #7359, #95478 ) ;
#244686=VERTEX_POINT ( 'NONE', #31844 ) ;
#244714=DIRECTION ( 'NONE',  ( 1.000000000000000000, -0.000000000000000000, -0.000000000000000000 ) ) ;
#244732=EDGE_CURVE ( 'NONE', #149809, #65489, #255767, .T. ) ;
#244782=VERTEX_POINT ( 'NONE', #27997 ) ;
#244798=EDGE_CURVE ( 'NONE', #125106, #224742, #30983, .T. ) ;
#244816=DIRECTION ( 'NONE',  ( 0.000000000000000000, 0.000000000000000000, -1.000000000000000000 ) ) ;
#244823=EDGE_CURVE ( 'NONE', #221150, #144444, #257226, .T. ) ;
#244870=DIRECTION ( 'NONE',  ( -1.000000000000000000, 0.000000000000000000, -0.000000000000000000 ) ) ;
#244876=AXIS2_PLACEMENT_3D ( 'NONE', #235525, #255030, #238091 ) ;
#244890=ADVANCED_FACE ( 'NONE', ( #77342 ), #255941, .F. ) ;
#244907=DIRECTION ( 'NONE',  ( 0.000000000000000000, 2.664535259100315349E-15, 1.000000000000000000 ) ) ;
#244918=CARTESIAN_POINT ( 'NONE',  ( -22.39999999999999858, 7.790779598384560245, -133.9000000000000057 ) ) ;
#244919=EDGE_CURVE ( 'NONE', #206030, #116136, #230699, .T. ) ;
#244934=CIRCLE ( 'NONE', #45023, 0.1000000000000013933 ) ;
#244959=DIRECTION ( 'NONE',  ( 0.000000000000000000, -1.000000000000000000, 0.000000000000000000 ) ) ;
#245020=ORIENTED_EDGE ( 'NONE', *, *, #191744, .F. ) ;
#245042=CARTESIAN_POINT ( 'NONE',  ( 18.40000000000000213, -9.499999999988844479, -141.0320693966996828 ) ) ;
#245044=CARTESIAN_POINT ( 'NONE',  ( -21.51976009735018991, 6.910458441670358276, -134.0000000000000000 ) ) ;
#245075=ADVANCED_FACE ( 'NONE', ( #26384 ), #146307, .F. ) ;
#245081=VERTEX_POINT ( 'NONE', #8102 ) ;
#245101=DIRECTION ( 'NONE',  ( 1.000000000000000000, -0.000000000000000000, -0.000000000000000000 ) ) ;
#245134=VECTOR ( 'NONE', #254219, 1000.000000000000000 ) ;
#245147=VERTEX_POINT ( 'NONE', #185448 ) ;
#245160=AXIS2_PLACEMENT_3D ( 'NONE', #167001, #45728, #49585 ) ;
#245162=EDGE_LOOP ( 'NONE', ( #171086, #85049, #241217, #96252, #159510, #90466, #126222, #2904, #41912 ) ) ;
#245206=ADVANCED_FACE ( 'NONE', ( #54904 ), #222648, .T. ) ;
#245220=CARTESIAN_POINT ( 'NONE',  ( 23.24999999999999645, 4.775700934590591196, -155.6512318959540551 ) ) ;
#245223=FACE_OUTER_BOUND ( 'NONE', #59929, .T. ) ;
#245230=EDGE_CURVE ( 'NONE', #206051, #199909, #68561, .T. ) ;
#245261=DIRECTION ( 'NONE',  ( 0.000000000000000000, 0.000000000000000000, -1.000000000000000000 ) ) ;
#245295=FACE_OUTER_BOUND ( 'NONE', #85222, .T. ) ;
#245331=DIRECTION ( 'NONE',  ( -3.265361837132813093E-16, 1.000000000000000000, 0.000000000000000000 ) ) ;
#245353=VECTOR ( 'NONE', #92212, 1000.000000000000000 ) ;
#245361=DIRECTION ( 'NONE',  ( 0.000000000000000000, 0.000000000000000000, -1.000000000000000000 ) ) ;
#245362=CARTESIAN_POINT ( 'NONE',  ( 21.05000000000000071, 11.60000000001116049, -160.5717967697245285 ) ) ;
#245378=DIRECTION ( 'NONE',  ( 1.000000000000000000, 0.000000000000000000, -0.000000000000000000 ) ) ;
#245401=CIRCLE ( 'NONE', #91284, 0.09999999999998898659 ) ;
#245418=VERTEX_POINT ( 'NONE', #136564 ) ;
#245426=CYLINDRICAL_SURFACE ( 'NONE', #94662, 7.899999999999990585 ) ;
#245433=DIRECTION ( 'NONE',  ( 0.000000000000000000, -1.000000000000000000, -2.891205793294679805E-16 ) ) ;
#245462=EDGE_CURVE ( 'NONE', #244782, #142484, #138851, .T. ) ;
#245465=DIRECTION ( 'NONE',  ( 0.000000000000000000, -1.000000000000000000, 0.000000000000000000 ) ) ;
#245466=AXIS2_PLACEMENT_3D ( 'NONE', #153487, #196402, #17751 ) ;
#245469=ORIENTED_EDGE ( 'NONE', *, *, #79109, .T. ) ;
#245546=CIRCLE ( 'NONE', #70605, 11.64999999999999325 ) ;
#245582=AXIS2_PLACEMENT_3D ( 'NONE', #32568, #195483, #15560 ) ;
#245612=CARTESIAN_POINT ( 'NONE',  ( 23.14999999999999858, 1.115600667400684642E-11, -167.5000000000000284 ) ) ;
#245634=PLANE ( 'NONE',  #221378 ) ;
#245677=DIRECTION ( 'NONE',  ( 0.000000000000000000, 0.000000000000000000, -1.000000000000000000 ) ) ;
#245704=CIRCLE ( 'NONE', #133283, 0.09999999999998898659 ) ;
#245710=CARTESIAN_POINT ( 'NONE',  ( -21.05000000000000071, -9.519327731081284938, -140.9729763765593589 ) ) ;
#245724=PLANE ( 'NONE',  #29213 ) ;
#245753=EDGE_CURVE ( 'NONE', #20940, #220754, #197712, .T. ) ;
#245762=DIRECTION ( 'NONE',  ( -1.000000000000000000, 0.000000000000000000, 0.000000000000000000 ) ) ;
#245780=CIRCLE ( 'NONE', #116778, 0.09999999999998898659 ) ;
#245821=CARTESIAN_POINT ( 'NONE',  ( 23.24999999999997513, 11.75000000001116263, -160.4851942293460638 ) ) ;
#245823=CARTESIAN_POINT ( 'NONE',  ( -18.50000000000000000, 1.340746217944851715, -123.7271374945788409 ) ) ;
#245833=ORIENTED_EDGE ( 'NONE', *, *, #246539, .F. ) ;
#245847=CARTESIAN_POINT ( 'NONE',  ( 20.01093837587850288, 11.75000000001116263, -158.7543974345976494 ) ) ;
#245869=ADVANCED_FACE ( 'NONE', ( #225663 ), #67903, .T. ) ;
#245945=CARTESIAN_POINT ( 'NONE',  ( 23.15000000000000213, -8.663551401858002876, -143.5241011180673070 ) ) ;
#245967=DIRECTION ( 'NONE',  ( 1.000000000000000000, 0.000000000000000000, 0.000000000000000000 ) ) ;
#245987=CIRCLE ( 'NONE', #200194, 0.09999999999998898659 ) ;
#246019=EDGE_CURVE ( 'NONE', #90426, #254695, #116292, .T. ) ;
#246020=DIRECTION ( 'NONE',  ( -1.000000000000000000, 0.000000000000000000, 0.000000000000000000 ) ) ;
#246031=ORIENTED_EDGE ( 'NONE', *, *, #182169, .F. ) ;
#246038=FACE_OUTER_BOUND ( 'NONE', #16552, .T. ) ;
#246040=CARTESIAN_POINT ( 'NONE',  ( -20.94999999999999929, 10.29288807859936661, -172.9580020160121876 ) ) ;
#246059=LINE ( 'NONE', #121002, #191430 ) ;
#246084=AXIS2_PLACEMENT_3D ( 'NONE', #68423, #247036, #147957 ) ;
#246093=AXIS2_PLACEMENT_3D ( 'NONE', #37697, #61075, #19397 ) ;
#246108=CARTESIAN_POINT ( 'NONE',  ( 22.59999999999999432, 0.1000000000111554016, -122.3504291924552234 ) ) ;
#246116=ADVANCED_FACE ( 'NONE', ( #81987 ), #74969, .T. ) ;
#246162=DIRECTION ( 'NONE',  ( -2.915501640297153790E-16, 1.000000000000000000, 0.000000000000000000 ) ) ;
#246165=ORIENTED_EDGE ( 'NONE', *, *, #121271, .T. ) ;
#246184=DIRECTION ( 'NONE',  ( -3.265361837132813093E-16, 1.000000000000000000, 0.000000000000000000 ) ) ;
#246192=ORIENTED_EDGE ( 'NONE', *, *, #192144, .F. ) ;
#246212=DIRECTION ( 'NONE',  ( 0.000000000000000000, 0.000000000000000000, 1.000000000000000000 ) ) ;
#246228=CARTESIAN_POINT ( 'NONE',  ( -21.53551880898957904, 0.09896973458281840830, -127.2152022385837142 ) ) ;
#246244=ORIENTED_EDGE ( 'NONE', *, *, #21274, .T. ) ;
#246263=DIRECTION ( 'NONE',  ( -1.000000000000000000, 0.000000000000000000, 0.000000000000000000 ) ) ;
#246267=CARTESIAN_POINT ( 'NONE',  ( -21.05000000000000426, 11.60000000001115872, -140.9282032302755852 ) ) ;
#246273=EDGE_CURVE ( 'NONE', #43801, #26579, #67595, .T. ) ;
#246280=VERTEX_POINT ( 'NONE', #88415 ) ;
#246289=CIRCLE ( 'NONE', #104777, 0.09999999999999892308 ) ;
#246294=PLANE ( 'NONE',  #66058 ) ;
#246321=VERTEX_POINT ( 'NONE', #113140 ) ;
#246329=DIRECTION ( 'NONE',  ( 0.000000000000000000, 0.000000000000000000, -1.000000000000000000 ) ) ;
#246335=ORIENTED_EDGE ( 'NONE', *, *, #66804, .F. ) ;
#246346=CARTESIAN_POINT ( 'NONE',  ( 21.05000000000000071, 0.09779029132038138949, -127.7421853895184825 ) ) ;
#246349=EDGE_CURVE ( 'NONE', #196020, #162055, #249729, .T. ) ;
#246352=CARTESIAN_POINT ( 'NONE',  ( 20.94999999999999929, 1.115649653272650466E-11, -163.5000000000000284 ) ) ;
#246357=ORIENTED_EDGE ( 'NONE', *, *, #14102, .T. ) ;
#246361=ORIENTED_EDGE ( 'NONE', *, *, #5020, .F. ) ;
#246396=DIRECTION ( 'NONE',  ( 0.000000000000000000, 0.000000000000000000, 1.000000000000000000 ) ) ;
#246400=CIRCLE ( 'NONE', #171413, 0.09999999999998898659 ) ;
#246448=ORIENTED_EDGE ( 'NONE', *, *, #47955, .T. ) ;
#246464=FACE_OUTER_BOUND ( 'NONE', #198989, .T. ) ;
#246501=DIRECTION ( 'NONE',  ( 0.000000000000000000, -1.000000000000000000, 0.000000000000000000 ) ) ;
#246514=CARTESIAN_POINT ( 'NONE',  ( -18.59999999999999787, 1.115600667400684642E-11, -167.5000000000000284 ) ) ;
#246522=LINE ( 'NONE', #129160, #31821 ) ;
#246539=EDGE_CURVE ( 'NONE', #82879, #126714, #50006, .T. ) ;
#246548=CARTESIAN_POINT ( 'NONE',  ( -18.50000000000000000, -1.162701749926853712, -142.1000000000000227 ) ) ;
#246555=EDGE_CURVE ( 'NONE', #97103, #178186, #224943, .T. ) ;
#246557=VERTEX_POINT ( 'NONE', #19170 ) ;
#246579=LINE ( 'NONE', #229599, #69647 ) ;
#246583=CARTESIAN_POINT ( 'NONE',  ( 21.11345278033253692, 8.882122073382257454, -146.2460221707567030 ) ) ;
#246589=DIRECTION ( 'NONE',  ( 0.000000000000000000, 1.000000000000000000, 0.000000000000000000 ) ) ;
#246593=FACE_OUTER_BOUND ( 'NONE', #239634, .T. ) ;
#246614=AXIS2_PLACEMENT_3D ( 'NONE', #140134, #103571, #25372 ) ;
#246636=PLANE ( 'NONE',  #219728 ) ;
#246643=DIRECTION ( 'NONE',  ( 2.694716079187272946E-16, -1.000000000000000000, 0.000000000000000000 ) ) ;
#246649=EDGE_LOOP ( 'NONE', ( #19044, #140041, #115533, #194700 ) ) ;
#246652=ADVANCED_FACE ( 'NONE', ( #204217 ), #105083, .T. ) ;
#246661=DIRECTION ( 'NONE',  ( 1.000000000000000000, 0.000000000000000000, 0.000000000000000000 ) ) ;
#246679=CARTESIAN_POINT ( 'NONE',  ( -23.15000000000000213, 2.000000000011154189, -146.7246219227621111 ) ) ;
#246692=CARTESIAN_POINT ( 'NONE',  ( 21.05000000000000071, 5.400000000011154988, -157.6060308773475640 ) ) ;
#246705=DIRECTION ( 'NONE',  ( 0.7071067811865474617, 0.7071067811865474617, 2.044391222244499837E-16 ) ) ;
#246765=VECTOR ( 'NONE', #28772, 1000.000000000000000 ) ;
#246780=ADVANCED_FACE ( 'NONE', ( #188511 ), #208098, .F. ) ;
#246794=EDGE_LOOP ( 'NONE', ( #223854, #90556, #21499, #16693, #216430, #189451 ) ) ;
#246828=DIRECTION ( 'NONE',  ( 0.000000000000000000, 0.000000000000000000, 1.000000000000000000 ) ) ;
#246856=CYLINDRICAL_SURFACE ( 'NONE', #42396, 0.09999999999998898659 ) ;
#246907=DIRECTION ( 'NONE',  ( 0.000000000000000000, 1.000000000000000000, -1.224646799147353207E-16 ) ) ;
#246928=TOROIDAL_SURFACE ( 'NONE', #105437, 0.2000000000000000111, 0.1000000000000000056 ) ;
#246950=CIRCLE ( 'NONE', #134507, 0.09999999999999158173 ) ;
#246990=ADVANCED_FACE ( 'NONE', ( #67938 ), #46075, .F. ) ;
#247008=CARTESIAN_POINT ( 'NONE',  ( 21.05000000000000071, 1.115600667400684642E-11, -134.0000000000000000 ) ) ;
#247022=AXIS2_PLACEMENT_3D ( 'NONE', #56406, #214225, #171293 ) ;
#247028=AXIS2_PLACEMENT_3D ( 'NONE', #153393, #212055, #55490 ) ;
#247036=DIRECTION ( 'NONE',  ( -1.000000000000000000, 0.000000000000000000, 0.000000000000000000 ) ) ;
#247052=ORIENTED_EDGE ( 'NONE', *, *, #133833, .T. ) ;
#247098=CARTESIAN_POINT ( 'NONE',  ( 23.15000000000000213, -9.599999999988842347, -157.6060308773475640 ) ) ;
#247119=DIRECTION ( 'NONE',  ( 0.9880948137434723000, 0.1538461538461484146, -0.000000000000000000 ) ) ;
#247122=CARTESIAN_POINT ( 'NONE',  ( 23.15000000000000213, -8.999999999988844479, -143.8939691226524644 ) ) ;
#247124=AXIS2_PLACEMENT_3D ( 'NONE', #62674, #87342, #242570 ) ;
#247152=EDGE_CURVE ( 'NONE', #104087, #43473, #4377, .T. ) ;
#247182=VECTOR ( 'NONE', #185397, 1000.000000000000000 ) ;
#247230=DIRECTION ( 'NONE',  ( 0.000000000000000000, -0.9908441862701596881, 0.1350103645451904977 ) ) ;
#247283=DIRECTION ( 'NONE',  ( 0.000000000000000000, 0.000000000000000000, -1.000000000000000000 ) ) ;
#247307=ADVANCED_FACE ( 'NONE', ( #199466 ), #59907, .T. ) ;
#247338=DIRECTION ( 'NONE',  ( 0.000000000000000000, 0.000000000000000000, -1.000000000000000000 ) ) ;
#247368=LINE ( 'NONE', #148284, #218678 ) ;
#247378=DIRECTION ( 'NONE',  ( 0.000000000000000000, 0.000000000000000000, -1.000000000000000000 ) ) ;
#247402=AXIS2_PLACEMENT_3D ( 'NONE', #130503, #224467, #76949 ) ;
#247409=FACE_OUTER_BOUND ( 'NONE', #98233, .T. ) ;
#247410=AXIS2_PLACEMENT_3D ( 'NONE', #65944, #25544, #125900 ) ;
#247417=ORIENTED_EDGE ( 'NONE', *, *, #38022, .F. ) ;
#247435=FACE_OUTER_BOUND ( 'NONE', #253443, .T. ) ;
#247444=LINE ( 'NONE', #31006, #245353 ) ;
#247478=CARTESIAN_POINT ( 'NONE',  ( -21.07928932188134041, 0.09889514566555068775, -127.6714833436067238 ) ) ;
#247507=DIRECTION ( 'NONE',  ( 0.000000000000000000, 0.000000000000000000, -1.000000000000000000 ) ) ;
#247531=DIRECTION ( 'NONE',  ( 0.000000000000000000, 1.000000000000000000, 0.000000000000000000 ) ) ;
#247540=EDGE_CURVE ( 'NONE', #42010, #82203, #46772, .T. ) ;
#247578=ADVANCED_FACE ( 'NONE', ( #186310 ), #96162, .T. ) ;
#247600=VERTEX_POINT ( 'NONE', #33693 ) ;
#247608=AXIS2_PLACEMENT_3D ( 'NONE', #115793, #256519, #160074 ) ;
#247617=CARTESIAN_POINT ( 'NONE',  ( -18.59999999999999787, 11.65000000001115232, -146.1500000000000341 ) ) ;
#247620=ORIENTED_EDGE ( 'NONE', *, *, #17173, .F. ) ;
#247623=DIRECTION ( 'NONE',  ( 1.000000000000000000, 0.000000000000000000, 0.000000000000000000 ) ) ;
#247665=ORIENTED_EDGE ( 'NONE', *, *, #130374, .T. ) ;
#247667=LINE ( 'NONE', #149875, #86105 ) ;
#247701=EDGE_LOOP ( 'NONE', ( #170154, #152150, #242303, #216560 ) ) ;
#247723=ORIENTED_EDGE ( 'NONE', *, *, #145265, .F. ) ;
#247738=ORIENTED_EDGE ( 'NONE', *, *, #191058, .F. ) ;
#247765=CARTESIAN_POINT ( 'NONE',  ( 21.05000000000000071, -9.399999999988844834, -157.6060308773475640 ) ) ;
#247769=LINE ( 'NONE', #75254, #206027 ) ;
#247828=CARTESIAN_POINT ( 'NONE',  ( -20.54999999999999716, 2.000000000011154189, -147.2246219227621111 ) ) ;
#247885=DIRECTION ( 'NONE',  ( -0.000000000000000000, -1.000000000000000000, -0.000000000000000000 ) ) ;
#247887=DIRECTION ( 'NONE',  ( 1.000000000000000000, 0.000000000000000000, 0.000000000000000000 ) ) ;
#247905=CARTESIAN_POINT ( 'NONE',  ( 22.39999999999999503, 0.1000000000111554016, -126.2092204016266379 ) ) ;
#247906=ORIENTED_EDGE ( 'NONE', *, *, #22940, .F. ) ;
#247919=AXIS2_PLACEMENT_3D ( 'NONE', #123283, #243212, #24195 ) ;
#247934=ORIENTED_EDGE ( 'NONE', *, *, #202472, .T. ) ;
#247940=CARTESIAN_POINT ( 'NONE',  ( 18.42555734704283665, -9.497158361925551517, -141.0398304977349824 ) ) ;
#247952=ORIENTED_EDGE ( 'NONE', *, *, #255759, .F. ) ;
#247963=VERTEX_POINT ( 'NONE', #145564 ) ;
#247984=CARTESIAN_POINT ( 'NONE',  ( -20.85000000000000142, -1.249999999988843369, -175.3004807544151049 ) ) ;
#247998=DIRECTION ( 'NONE',  ( -1.000000000000000000, 0.000000000000000000, 0.000000000000000000 ) ) ;
#248003=ADVANCED_FACE ( 'NONE', ( #226366 ), #146837, .F. ) ;
#248020=CARTESIAN_POINT ( 'NONE',  ( -20.94999999999999929, -11.39257802169451672, -137.0739495798319467 ) ) ;
#248023=DIRECTION ( 'NONE',  ( -1.000000000000000000, -2.952720810173289112E-16, 0.000000000000000000 ) ) ;
#248031=ADVANCED_FACE ( 'NONE', ( #88132 ), #248523, .T. ) ;
#248077=SPHERICAL_SURFACE ( 'NONE', #115450, 0.1000000000000000056 ) ;
#248087=DIRECTION ( 'NONE',  ( 1.000000000000000000, 0.000000000000000000, 0.000000000000000000 ) ) ;
#248090=ORIENTED_EDGE ( 'NONE', *, *, #153750, .T. ) ;
#248104=DIRECTION ( 'NONE',  ( -1.000000000000000000, -2.952720810173289112E-16, 0.000000000000000000 ) ) ;
#248151=DIRECTION ( 'NONE',  ( 4.239556034732056743E-17, -0.1298341882520022972, -0.9915357197604853789 ) ) ;
#248153=CIRCLE ( 'NONE', #164771, 0.6000000000000015321 ) ;
#248178=DIRECTION ( 'NONE',  ( 2.952720810173289112E-16, -1.000000000000000000, 0.000000000000000000 ) ) ;
#248180=ORIENTED_EDGE ( 'NONE', *, *, #133997, .T. ) ;
#248200=CYLINDRICAL_SURFACE ( 'NONE', #133733, 0.09999999999999939493 ) ;
#248214=CIRCLE ( 'NONE', #168953, 0.09999999999998898659 ) ;
#248239=ORIENTED_EDGE ( 'NONE', *, *, #206587, .F. ) ;
#248240=CARTESIAN_POINT ( 'NONE',  ( 20.94999999999999929, 1.115600667400684642E-11, -134.0000000000000000 ) ) ;
#248242=DIRECTION ( 'NONE',  ( -1.000000000000000000, 0.000000000000000000, 0.000000000000000000 ) ) ;
#248257=AXIS2_PLACEMENT_3D ( 'NONE', #168677, #69543, #53811 ) ;
#248285=CARTESIAN_POINT ( 'NONE',  ( 20.04142135623730070, 11.65000000001115943, -155.2500000000000284 ) ) ;
#248286=DIRECTION ( 'NONE',  ( 0.000000000000000000, 0.000000000000000000, -1.000000000000000000 ) ) ;
#248292=AXIS2_PLACEMENT_3D ( 'NONE', #70733, #150259, #254445 ) ;
#248314=CARTESIAN_POINT ( 'NONE',  ( 21.87500000000000355, 9.750000000011153745, -155.2500000000000284 ) ) ;
#248320=DIRECTION ( 'NONE',  ( -1.000000000000000000, 0.000000000000000000, 0.000000000000000000 ) ) ;
#248334=AXIS2_PLACEMENT_3D ( 'NONE', #103923, #962, #183497 ) ;
#248374=EDGE_CURVE ( 'NONE', #82203, #40580, #158716, .T. ) ;
#248406=DIRECTION ( 'NONE',  ( 0.000000000000000000, -0.4999999999999348299, 0.8660254037844762331 ) ) ;
#248434=AXIS2_PLACEMENT_3D ( 'NONE', #205288, #201445, #223564 ) ;
#248462=EDGE_CURVE ( 'NONE', #11797, #220002, #5375, .T. ) ;
#248483=CARTESIAN_POINT ( 'NONE',  ( -18.50000000000000000, 10.29288807859935950, -172.9580020160122160 ) ) ;
#248498=ORIENTED_EDGE ( 'NONE', *, *, #186682, .T. ) ;
#248523=CYLINDRICAL_SURFACE ( 'NONE', #154817, 0.1000000000000000472 ) ;
#248530=AXIS2_PLACEMENT_3D ( 'NONE', #119301, #239247, #103558 ) ;
#248554=DIRECTION ( 'NONE',  ( 0.000000000000000000, -1.000000000000000000, 0.000000000000000000 ) ) ;
#248557=CIRCLE ( 'NONE', #219342, 0.09999999999999911737 ) ;
#248575=CARTESIAN_POINT ( 'NONE',  ( -22.49231231312463208, 11.64998490368843953, -133.9389471123986368 ) ) ;
#248583=LINE ( 'NONE', #149510, #201192 ) ;
#248597=EDGE_CURVE ( 'NONE', #188779, #171037, #229984, .T. ) ;
#248606=DIRECTION ( 'NONE',  ( 0.000000000000000000, -0.9876197685951252359, -0.1568667991644863424 ) ) ;
#248652=VERTEX_POINT ( 'NONE', #12857 ) ;
#248653=EDGE_CURVE ( 'NONE', #51770, #44689, #38443, .T. ) ;
#248670=EDGE_CURVE ( 'NONE', #137714, #204820, #136611, .T. ) ;
#248674=AXIS2_PLACEMENT_3D ( 'NONE', #15137, #232916, #54238 ) ;
#248683=ADVANCED_FACE ( 'NONE', ( #177068 ), #112893, .F. ) ;
#248686=ORIENTED_EDGE ( 'NONE', *, *, #176494, .T. ) ;
#248731=EDGE_LOOP ( 'NONE', ( #212149, #166879, #41261, #228061 ) ) ;
#248736=CIRCLE ( 'NONE', #236805, 0.1000000000000002554 ) ;
#248745=DIRECTION ( 'NONE',  ( 0.000000000000000000, 0.9915357197604973694, -0.1298341882519105928 ) ) ;
#248793=CARTESIAN_POINT ( 'NONE',  ( 21.05000000000000071, -9.399999999988846611, -143.8939691226524644 ) ) ;
#248842=DIRECTION ( 'NONE',  ( 0.000000000000000000, -1.000000000000000000, 0.000000000000000000 ) ) ;
#248851=VERTEX_POINT ( 'NONE', #182186 ) ;
#248854=AXIS2_PLACEMENT_3D ( 'NONE', #234067, #153296, #95825 ) ;
#248881=EDGE_CURVE ( 'NONE', #228115, #164020, #221206, .T. ) ;
#248891=CIRCLE ( 'NONE', #215552, 0.09999999999998898659 ) ;
#248892=CARTESIAN_POINT ( 'NONE',  ( 21.08134388332232234, 6.334680580529113314, -133.9241810824929928 ) ) ;
#248899=( BOUNDED_SURFACE ( )  B_SPLINE_SURFACE ( 3, 2, ( 
 ( #252485, #137663, #232963 ),
 ( #173013, #54285, #16480 ),
 ( #254998, #95974, #38591 ),
 ( #133832, #197648, #37323 ),
 ( #76417, #215918, #196369 ),
 ( #213359, #19017, #17719 ) ),
 .UNSPECIFIED., .F., .F., .F. ) 
 B_SPLINE_SURFACE_WITH_KNOTS ( ( 4, 2, 4 ),
 ( 3, 3 ),
 ( 1.570796326794897668, 2.356194490192346169, 3.141592653589794448 ),
 ( 0.000000000000000000, 1.000000000000000000 ),
 .UNSPECIFIED. ) 
 GEOMETRIC_REPRESENTATION_ITEM ( )  RATIONAL_B_SPLINE_SURFACE ( (
 ( 1.000000000000000000, 0.7071067811865475727, 1.000000000000000000),
 ( 1.000000000000000000, 0.6611148371778342581, 1.000000000000000000),
 ( 1.000000000000000000, 0.6092287576696778784, 1.000000000000000000),
 ( 1.000000000000000000, 0.5278258667056651143, 1.000000000000000000),
 ( 1.000000000000000000, 0.4993418825335158018, 1.000000000000000000),
 ( 1.000000000000000000, 0.5000000000000260902, 1.000000000000000000) ) ) 
 REPRESENTATION_ITEM ( '' )  SURFACE ( )  );
#248904=DIRECTION ( 'NONE',  ( 0.000000000000000000, 0.008583690987128059571, -0.9999631594459056361 ) ) ;
#248914=ORIENTED_EDGE ( 'NONE', *, *, #172471, .T. ) ;
#248917=AXIS2_PLACEMENT_3D ( 'NONE', #182373, #172781, #149347 ) ;
#248919=CARTESIAN_POINT ( 'NONE',  ( -18.59999999999999787, 1.835341550235567887, -145.5551512925629822 ) ) ;
#248945=DIRECTION ( 'NONE',  ( 0.000000000000000000, 0.000000000000000000, -1.000000000000000000 ) ) ;
#248950=CIRCLE ( 'NONE', #36595, 4.149999999999999467 ) ;
#248964=FACE_OUTER_BOUND ( 'NONE', #190866, .T. ) ;
#248999=ADVANCED_FACE ( 'NONE', ( #26979 ), #91229, .T. ) ;
#249015=AXIS2_PLACEMENT_3D ( 'NONE', #7438, #102667, #25731 ) ;
#249016=EDGE_CURVE ( 'NONE', #45962, #238843, #137992, .T. ) ;
#249017=CARTESIAN_POINT ( 'NONE',  ( 18.59999999999999076, 10.20857864377385127, -155.2500000000000284 ) ) ;
#249029=ORIENTED_EDGE ( 'NONE', *, *, #89977, .T. ) ;
#249072=LINE ( 'NONE', #229498, #246765 ) ;
#249087=DIRECTION ( 'NONE',  ( -1.000000000000000000, 0.000000000000000000, 0.000000000000000000 ) ) ;
#249091=ORIENTED_EDGE ( 'NONE', *, *, #62978, .F. ) ;
#249097=DIRECTION ( 'NONE',  ( 0.000000000000000000, 0.000000000000000000, -1.000000000000000000 ) ) ;
#249128=EDGE_CURVE ( 'NONE', #256406, #202799, #125726, .T. ) ;
#249191=CARTESIAN_POINT ( 'NONE',  ( 22.49999999999999645, 11.64976291804307884, -133.9111900236131021 ) ) ;
#249218=DIRECTION ( 'NONE',  ( 0.000000000000000000, 1.000000000000000000, 0.000000000000000000 ) ) ;
#249235=CARTESIAN_POINT ( 'NONE',  ( 18.58143601961908331, 10.43572941510574026, -158.7500000000000284 ) ) ;
#249262=EDGE_LOOP ( 'NONE', ( #218578, #72324, #66166, #137468, #110876 ) ) ;
#249286=EDGE_CURVE ( 'NONE', #121616, #175543, #42346, .T. ) ;
#249300=CIRCLE ( 'NONE', #236796, 0.09999999999998898659 ) ;
#249316=DIRECTION ( 'NONE',  ( 0.000000000000000000, 0.000000000000000000, -1.000000000000000000 ) ) ;
#249320=CARTESIAN_POINT ( 'NONE',  ( -23.25000000000000000, -1.736705739456431807, -179.0174225876237415 ) ) ;
#249331=CARTESIAN_POINT ( 'NONE',  ( -23.25000000000000000, 1.115600667400684642E-11, -167.5000000000000284 ) ) ;
#249365=ADVANCED_FACE ( 'NONE', ( #185970 ), #25620, .F. ) ;
#249380=DIRECTION ( 'NONE',  ( 1.000000000000000000, -0.000000000000000000, -0.000000000000000000 ) ) ;
#249384=EDGE_CURVE ( 'NONE', #91733, #141490, #146556, .T. ) ;
#249417=LINE ( 'NONE', #186884, #219996 ) ;
#249423=DIRECTION ( 'NONE',  ( 0.000000000000000000, -1.000000000000000000, 0.000000000000000000 ) ) ;
#249440=AXIS2_PLACEMENT_3D ( 'NONE', #27318, #109355, #108103 ) ;
#249461=ORIENTED_EDGE ( 'NONE', *, *, #113534, .F. ) ;
#249464=CARTESIAN_POINT ( 'NONE',  ( 18.59999999999999076, 1.250000000011167511, -142.0000000000000284 ) ) ;
#249502=EDGE_CURVE ( 'NONE', #38036, #32896, #238138, .T. ) ;
#249520=ADVANCED_FACE ( 'NONE', ( #251065 ), #72462, .T. ) ;
#249542=CARTESIAN_POINT ( 'NONE',  ( -23.15000000000000213, 4.350000000011156054, -146.2500000000000284 ) ) ;
#249580=DIRECTION ( 'NONE',  ( -0.000000000000000000, 1.000000000000000000, 0.000000000000000000 ) ) ;
#249633=EDGE_CURVE ( 'NONE', #35508, #3992, #192551, .T. ) ;
#249655=EDGE_CURVE ( 'NONE', #120342, #248652, #63132, .T. ) ;
#249670=DIRECTION ( 'NONE',  ( 0.000000000000000000, 0.000000000000000000, 1.000000000000000000 ) ) ;
#249671=VECTOR ( 'NONE', #96153, 1000.000000000000000 ) ;
#249677=CARTESIAN_POINT ( 'NONE',  ( -21.65000000000000213, 7.708578643773852157, -155.2500000000000284 ) ) ;
#249679=EDGE_CURVE ( 'NONE', #82520, #187371, #196631, .T. ) ;
#249729=CIRCLE ( 'NONE', #183110, 7.800000000000001599 ) ;
#249730=EDGE_LOOP ( 'NONE', ( #177550, #121239, #242824, #221161 ) ) ;
#249750=ADVANCED_FACE ( 'NONE', ( #102236 ), #149129, .T. ) ;
#249766=CARTESIAN_POINT ( 'NONE',  ( -18.59117750673696889, 10.33248238083634796, -173.0948465439131496 ) ) ;
#249770=EDGE_CURVE ( 'NONE', #15173, #35759, #142465, .T. ) ;
#249786=CARTESIAN_POINT ( 'NONE',  ( -21.55000000000000426, 7.750000000011155521, -146.3500000000000227 ) ) ;
#249803=AXIS2_PLACEMENT_3D ( 'NONE', #86149, #44503, #181450 ) ;
#249814=CARTESIAN_POINT ( 'NONE',  ( -21.78635804494510708, 7.035661485164336426, -133.9009949344923314 ) ) ;
#249831=DIRECTION ( 'NONE',  ( -1.000000000000000000, 0.000000000000000000, 0.000000000000000000 ) ) ;
#249894=AXIS2_PLACEMENT_3D ( 'NONE', #19902, #156863, #57711 ) ;
#249908=DIRECTION ( 'NONE',  ( 1.000000000000000000, 0.000000000000000000, 0.000000000000000000 ) ) ;
#249917=CARTESIAN_POINT ( 'NONE',  ( 21.05000000000000071, 1.115600667400684642E-11, -164.6000000000000227 ) ) ;
#249921=LINE ( 'NONE', #71305, #89596 ) ;
#249928=VERTEX_POINT ( 'NONE', #159395 ) ;
#249941=ORIENTED_EDGE ( 'NONE', *, *, #202191, .T. ) ;
#249960=AXIS2_PLACEMENT_3D ( 'NONE', #185066, #106802, #246329 ) ;
#249983=EDGE_LOOP ( 'NONE', ( #83435, #10037, #151590, #14844 ) ) ;
#250006=DIRECTION ( 'NONE',  ( 0.000000000000000000, 0.8660254037844385966, -0.5000000000000003331 ) ) ;
#250017=AXIS2_PLACEMENT_3D ( 'NONE', #175575, #255026, #150857 ) ;
#250049=CARTESIAN_POINT ( 'NONE',  ( -21.08198257630413508, 0.07264332379574613141, -127.6634032659849680 ) ) ;
#250075=VERTEX_POINT ( 'NONE', #184072 ) ;
#250124=AXIS2_PLACEMENT_3D ( 'NONE', #252328, #155834, #151992 ) ;
#250145=CARTESIAN_POINT ( 'NONE',  ( -20.94999999999999929, -1.162701749926853712, -142.0000000000000284 ) ) ;
#250153=CARTESIAN_POINT ( 'NONE',  ( -21.14999999999999858, 1.115600667400684642E-11, -134.0000000000000000 ) ) ;
#250190=SPHERICAL_SURFACE ( 'NONE', #22821, 0.1000000000000000056 ) ;
#250197=DIRECTION ( 'NONE',  ( 3.469446951953498700E-14, -0.7899159663865300551, -0.6132151058540831201 ) ) ;
#250216=FACE_OUTER_BOUND ( 'NONE', #187159, .T. ) ;
#250225=CARTESIAN_POINT ( 'NONE',  ( -21.53699400381697160, 6.787711793192025667, -134.0000000000000000 ) ) ;
#250246=ORIENTED_EDGE ( 'NONE', *, *, #60838, .T. ) ;
#250247=DIRECTION ( 'NONE',  ( 1.000000000000000000, -0.000000000000000000, -0.000000000000000000 ) ) ;
#250254=CARTESIAN_POINT ( 'NONE',  ( 18.46921299892754931, -9.509378177812605415, -140.9865787093704625 ) ) ;
#250302=AXIS2_PLACEMENT_3D ( 'NONE', #162039, #139865, #79878 ) ;
#250304=ORIENTED_EDGE ( 'NONE', *, *, #183954, .F. ) ;
#250310=ORIENTED_EDGE ( 'NONE', *, *, #167198, .T. ) ;
#250314=ORIENTED_EDGE ( 'NONE', *, *, #8284, .T. ) ;
#250335=DIRECTION ( 'NONE',  ( 0.000000000000000000, 0.4999999999999543698, 0.8660254037844650199 ) ) ;
#250369=ORIENTED_EDGE ( 'NONE', *, *, #206223, .T. ) ;
#250370=CARTESIAN_POINT ( 'NONE',  ( -20.94999999999999929, 1.162701749949165642, -142.1000000000000227 ) ) ;
#250442=DIRECTION ( 'NONE',  ( 0.000000000000000000, 0.000000000000000000, -1.000000000000000000 ) ) ;
#250448=CARTESIAN_POINT ( 'NONE',  ( -18.50000000000000000, 1.866714910068465239, -145.7526752462820241 ) ) ;
#250452=CARTESIAN_POINT ( 'NONE',  ( -21.05000000000000071, 5.900000000011162093, -157.2809002353436654 ) ) ;
#250488=AXIS2_PLACEMENT_3D ( 'NONE', #172221, #114764, #134301 ) ;
#250491=DIRECTION ( 'NONE',  ( 6.938893903907991995E-14, 0.000000000000000000, 1.000000000000000000 ) ) ;
#250495=CARTESIAN_POINT ( 'NONE',  ( 18.49999999999999289, 10.20857864609425825, -158.7025068656296014 ) ) ;
#250496=ORIENTED_EDGE ( 'NONE', *, *, #73247, .T. ) ;
#250520=VECTOR ( 'NONE', #81377, 1000.000000000000000 ) ;
#250535=SPHERICAL_SURFACE ( 'NONE', #116781, 0.1000000000000000056 ) ;
#250563=ORIENTED_EDGE ( 'NONE', *, *, #39337, .T. ) ;
#250617=CIRCLE ( 'NONE', #167460, 0.09999999999998898659 ) ;
#250622=SPHERICAL_SURFACE ( 'NONE', #145973, 0.1000000000000000056 ) ;
#250629=CARTESIAN_POINT ( 'NONE',  ( 18.59999999999999076, 6.450000000011156587, -144.0170271704400307 ) ) ;
#250638=ORIENTED_EDGE ( 'NONE', *, *, #9631, .T. ) ;
#250666=DIRECTION ( 'NONE',  ( 2.952720810173289112E-16, -1.000000000000000000, 0.000000000000000000 ) ) ;
#250674=EDGE_LOOP ( 'NONE', ( #22653, #232051, #93570, #73872, #139056, #226902, #17549 ) ) ;
#250679=CARTESIAN_POINT ( 'NONE',  ( 23.15000000000000213, -11.48912529306489994, -164.4000000000000057 ) ) ;
#250731=ADVANCED_FACE ( 'NONE', ( #72838 ), #238892, .T. ) ;
#250763=CARTESIAN_POINT ( 'NONE',  ( 21.05000000000000071, 1.115600667400684642E-11, -171.6000000000000227 ) ) ;
#250810=CARTESIAN_POINT ( 'NONE',  ( 23.14999999999999147, 1.115600667400684642E-11, -134.0000000000000000 ) ) ;
#250856=ORIENTED_EDGE ( 'NONE', *, *, #75245, .T. ) ;
#250866=DIRECTION ( 'NONE',  ( 0.000000000000000000, -0.8660254037844247188, 0.5000000000000245359 ) ) ;
#250879=CARTESIAN_POINT ( 'NONE',  ( -20.64999999999999858, 1.925233644870967487, -154.7697564668738721 ) ) ;
#250889=DIRECTION ( 'NONE',  ( 0.000000000000000000, 1.000000000000000000, 0.000000000000000000 ) ) ;
#250895=DIRECTION ( 'NONE',  ( -1.000000000000000000, -0.000000000000000000, -0.000000000000000000 ) ) ;
#250899=EDGE_LOOP ( 'NONE', ( #144285, #10442, #228583 ) ) ;
#250908=ORIENTED_EDGE ( 'NONE', *, *, #67061, .T. ) ;
#250967=AXIS2_PLACEMENT_3D ( 'NONE', #231631, #188633, #51663 ) ;
#251000=FACE_OUTER_BOUND ( 'NONE', #55945, .T. ) ;
#251003=ORIENTED_EDGE ( 'NONE', *, *, #175125, .T. ) ;
#251018=AXIS2_PLACEMENT_3D ( 'NONE', #191660, #156382, #215035 ) ;
#251043=AXIS2_PLACEMENT_3D ( 'NONE', #150407, #149122, #130820 ) ;
#251065=FACE_OUTER_BOUND ( 'NONE', #180093, .T. ) ;
#251104=ORIENTED_EDGE ( 'NONE', *, *, #43085, .F. ) ;
#251106=CARTESIAN_POINT ( 'NONE',  ( 18.45139536634706801, -9.486081720270043149, -174.1405116178106596 ) ) ;
#251108=CARTESIAN_POINT ( 'NONE',  ( 20.85000000000000142, 1.115600667400684642E-11, -167.5000000000000284 ) ) ;
#251115=VECTOR ( 'NONE', #166389, 1000.000000000000227 ) ;
#251133=ORIENTED_EDGE ( 'NONE', *, *, #37365, .T. ) ;
#251141=B_SPLINE_CURVE_WITH_KNOTS ( 'NONE', 3,
 ( #72519, #137288, #152061, #188587, #171640, #227710, #230281, #209435 ),
 .UNSPECIFIED., .F., .F.,
 ( 4, 2, 2, 4 ),
 ( 0.000000000000000000, 0.0002181133598168667081, 0.0003271700397253312059, 0.0004362267196337957036 ),
 .UNSPECIFIED. ) ;
#251153=EDGE_LOOP ( 'NONE', ( #22328, #77696, #110756, #96342 ) ) ;
#251210=CARTESIAN_POINT ( 'NONE',  ( 21.05000000000000071, -9.499999999988848032, -143.8939691226524644 ) ) ;
#251211=ORIENTED_EDGE ( 'NONE', *, *, #113526, .F. ) ;
#251242=CARTESIAN_POINT ( 'NONE',  ( -21.59142135623730852, 7.850000000011158718, -155.2500000000000284 ) ) ;
#251296=CARTESIAN_POINT ( 'NONE',  ( -21.05000000000000071, 0.05132743235296114565, -127.6998166637300187 ) ) ;
#251306=ORIENTED_EDGE ( 'NONE', *, *, #163647, .T. ) ;
#251392=AXIS2_PLACEMENT_3D ( 'NONE', #139653, #40626, #122710 ) ;
#251421=DIRECTION ( 'NONE',  ( 0.000000000000000000, 0.8660254037844411501, 0.4999999999999956701 ) ) ;
#251432=CARTESIAN_POINT ( 'NONE',  ( 21.05000000000000071, -1.849084418615859926, -145.6560105214471434 ) ) ;
#251443=CARTESIAN_POINT ( 'NONE',  ( -20.54999999999999716, 1.115600667400684642E-11, -167.5000000000000284 ) ) ;
#251445=TOROIDAL_SURFACE ( 'NONE', #217537, 2.100000000000002309, 0.1000000000000000056 ) ;
#251479=AXIS2_PLACEMENT_3D ( 'NONE', #74127, #55770, #113212 ) ;
#251506=CIRCLE ( 'NONE', #139040, 0.09999999999998898659 ) ;
#251536=DIRECTION ( 'NONE',  ( 0.000000000000000000, -0.4999999999999348299, 0.8660254037844762331 ) ) ;
#251543=EDGE_CURVE ( 'NONE', #160394, #43801, #201654, .T. ) ;
#251548=VERTEX_POINT ( 'NONE', #100395 ) ;
#251578=VECTOR ( 'NONE', #56701, 1000.000000000000000 ) ;
#251605=ORIENTED_EDGE ( 'NONE', *, *, #199284, .F. ) ;
#251612=DIRECTION ( 'NONE',  ( 0.000000000000000000, -0.000000000000000000, 1.000000000000000000 ) ) ;
#251632=CARTESIAN_POINT ( 'NONE',  ( -22.47071067811865319, 1.115600667400684642E-11, -134.0000000000000000 ) ) ;
#251634=DIRECTION ( 'NONE',  ( 1.000000000000000000, -0.000000000000000000, -0.000000000000000000 ) ) ;
#251650=ORIENTED_EDGE ( 'NONE', *, *, #56339, .T. ) ;
#251659=ORIENTED_EDGE ( 'NONE', *, *, #149217, .T. ) ;
#251687=CARTESIAN_POINT ( 'NONE',  ( 20.94999999999999574, 8.926614585098251453, -142.4716830192231498 ) ) ;
#251741=FACE_OUTER_BOUND ( 'NONE', #48353, .T. ) ;
#251757=CARTESIAN_POINT ( 'NONE',  ( 20.94999999999999929, 8.926614585098249677, -142.4716830192231498 ) ) ;
#251758=AXIS2_PLACEMENT_3D ( 'NONE', #237731, #177781, #240308 ) ;
#251768=CIRCLE ( 'NONE', #60222, 0.09999999999999939493 ) ;
#251771=CIRCLE ( 'NONE', #130968, 0.09999999999998898659 ) ;
#251773=ORIENTED_EDGE ( 'NONE', *, *, #143262, .T. ) ;
#251776=EDGE_LOOP ( 'NONE', ( #106809, #177192, #110168, #150213 ) ) ;
#251787=LINE ( 'NONE', #232250, #123088 ) ;
#251789=CARTESIAN_POINT ( 'NONE',  ( -18.50000000000000711, 11.75000000001115197, -141.0148057706539930 ) ) ;
#251844=VECTOR ( 'NONE', #51712, 1000.000000000000000 ) ;
#251858=VERTEX_POINT ( 'NONE', #214918 ) ;
#251881=VECTOR ( 'NONE', #91473, 1000.000000000000000 ) ;
#251883=VERTEX_POINT ( 'NONE', #197914 ) ;
#251968=LINE ( 'NONE', #152908, #156857 ) ;
#251973=CYLINDRICAL_SURFACE ( 'NONE', #228960, 0.09999999999998898659 ) ;
#251978=EDGE_LOOP ( 'NONE', ( #45988, #170610, #180105, #109248 ) ) ;
#252002=DIRECTION ( 'NONE',  ( 0.000000000000000000, -1.000000000000000000, 0.000000000000000000 ) ) ;
#252028=CIRCLE ( 'NONE', #39857, 0.5000000000000004441 ) ;
#252031=DIRECTION ( 'NONE',  ( 1.000000000000000000, -0.000000000000000000, 0.000000000000000000 ) ) ;
#252047=DIRECTION ( 'NONE',  ( 0.000000000000000000, 0.000000000000000000, -1.000000000000000000 ) ) ;
#252066=CARTESIAN_POINT ( 'NONE',  ( 23.14999999999999858, 1.115600667400684642E-11, -167.5000000000000284 ) ) ;
#252073=DIRECTION ( 'NONE',  ( -1.000000000000000000, -0.000000000000000000, -0.000000000000000000 ) ) ;
#252090=DIRECTION ( 'NONE',  ( 0.000000000000000000, 0.8660254037844411501, 0.4999999999999956701 ) ) ;
#252115=AXIS2_PLACEMENT_3D ( 'NONE', #155170, #14370, #32666 ) ;
#252119=FACE_OUTER_BOUND ( 'NONE', #84121, .T. ) ;
#252142=ADVANCED_FACE ( 'NONE', ( #166530 ), #47879, .T. ) ;
#252151=CARTESIAN_POINT ( 'NONE',  ( -20.54999999999999716, 1.115624548013267999E-11, -165.6000000000000227 ) ) ;
#252156=CARTESIAN_POINT ( 'NONE',  ( -18.59999999999999787, 5.950000000011100632, -144.3057023050348846 ) ) ;
#252175=DIRECTION ( 'NONE',  ( 0.000000000000000000, 0.000000000000000000, -1.000000000000000000 ) ) ;
#252189=LINE ( 'NONE', #69733, #122214 ) ;
#252201=AXIS2_PLACEMENT_3D ( 'NONE', #41851, #203475, #106920 ) ;
#252267=ORIENTED_EDGE ( 'NONE', *, *, #184730, .T. ) ;
#252300=CARTESIAN_POINT ( 'NONE',  ( 21.07964655665547227, 8.774889614989714204, -146.2219165829640701 ) ) ;
#252302=ORIENTED_EDGE ( 'NONE', *, *, #244028, .F. ) ;
#252316=EDGE_CURVE ( 'NONE', #85287, #212843, #181385, .T. ) ;
#252320=CARTESIAN_POINT ( 'NONE',  ( 21.40925344232282868, 0.09895018863080314031, -127.3414811406095595 ) ) ;
#252325=TOROIDAL_SURFACE ( 'NONE', #248257, 0.2000000000000000111, 0.1000000000000000056 ) ;
#252328=CARTESIAN_POINT ( 'NONE',  ( -18.50000000000000000, 1.115600667400684642E-11, -134.0000000000000000 ) ) ;
#252356=CARTESIAN_POINT ( 'NONE',  ( -21.17356465864818205, 6.422803126252873973, -133.9010887589861625 ) ) ;
#252385=DIRECTION ( 'NONE',  ( 0.000000000000000000, 0.000000000000000000, -1.000000000000000000 ) ) ;
#252464=DIRECTION ( 'NONE',  ( 0.000000000000000000, 0.000000000000000000, 1.000000000000000000 ) ) ;
#252470=EDGE_CURVE ( 'NONE', #25818, #51735, #52170, .T. ) ;
#252485=CARTESIAN_POINT ( 'NONE',  ( -20.94999999999999929, 11.65000000001115055, -160.7161343370219129 ) ) ;
#252494=DIRECTION ( 'NONE',  ( 0.000000000000000000, -1.000000000000000000, -2.891205793294679805E-16 ) ) ;
#252517=DIRECTION ( 'NONE',  ( 0.000000000000000000, 0.000000000000000000, 1.000000000000000000 ) ) ;
#252520=DIRECTION ( 'NONE',  ( 1.000000000000000000, -7.304098846218134667E-16, 0.000000000000000000 ) ) ;
#252567=PLANE ( 'NONE',  #133282 ) ;
#252568=AXIS2_PLACEMENT_3D ( 'NONE', #30141, #232190, #250442 ) ;
#252572=B_SPLINE_CURVE_WITH_KNOTS ( 'NONE', 3,
 ( #68467, #89292, #167583, #148000 ),
 .UNSPECIFIED., .F., .F.,
 ( 4, 4 ),
 ( 0.000000000000000000, 0.0001048066582182432421 ),
 .UNSPECIFIED. ) ;
#252582=DIRECTION ( 'NONE',  ( 0.000000000000000000, 1.000000000000000000, 0.000000000000000000 ) ) ;
#252583=DIRECTION ( 'NONE',  ( -1.000000000000000000, -0.000000000000000000, -0.000000000000000000 ) ) ;
#252616=CARTESIAN_POINT ( 'NONE',  ( -21.13435531349819030, 6.493721063603186572, -134.0000000000000284 ) ) ;
#252666=LINE ( 'NONE', #17908, #249671 ) ;
#252684=DIRECTION ( 'NONE',  ( -1.000000000000000000, 0.000000000000000000, 0.000000000000000000 ) ) ;
#252737=ORIENTED_EDGE ( 'NONE', *, *, #191605, .F. ) ;
#252813=EDGE_CURVE ( 'NONE', #224878, #178186, #10545, .T. ) ;
#252814=LINE ( 'NONE', #33827, #122160 ) ;
#252833=EDGE_LOOP ( 'NONE', ( #187201, #83805, #106568, #21220 ) ) ;
#252835=TOROIDAL_SURFACE ( 'NONE', #236094, 0.2000000000000000111, 0.1000000000000000056 ) ;
#252840=CARTESIAN_POINT ( 'NONE',  ( 21.05000000000000071, 8.776282895303632259, -142.5586289951409640 ) ) ;
#252875=CARTESIAN_POINT ( 'NONE',  ( 18.59999999999998721, 19.85039924724470950, -136.2803030578013761 ) ) ;
#252913=ORIENTED_EDGE ( 'NONE', *, *, #169257, .T. ) ;
#252917=CARTESIAN_POINT ( 'NONE',  ( -20.94999999999999929, -1.362429037182149694, -175.3888812479212334 ) ) ;
#252942=DIRECTION ( 'NONE',  ( 0.000000000000000000, 0.000000000000000000, -1.000000000000000000 ) ) ;
#252971=AXIS2_PLACEMENT_3D ( 'NONE', #252875, #89951, #151232 ) ;
#253010=FACE_OUTER_BOUND ( 'NONE', #163823, .T. ) ;
#253017=CARTESIAN_POINT ( 'NONE',  ( -21.14999999999999503, 11.75000000001115197, -140.9191472459588113 ) ) ;
#253028=AXIS2_PLACEMENT_3D ( 'NONE', #212039, #198872, #200169 ) ;
#253050=FACE_OUTER_BOUND ( 'NONE', #209929, .T. ) ;
#253070=CARTESIAN_POINT ( 'NONE',  ( 18.45068634130097607, -9.486506073331600675, -141.0687784311681128 ) ) ;
#253122=CYLINDRICAL_SURFACE ( 'NONE', #222889, 0.09999999999999939493 ) ;
#253123=B_SPLINE_CURVE_WITH_KNOTS ( 'NONE', 3,
 ( #34574, #131082, #114077, #171530, #112812, #193632, #95788, #253586, #252300, #13702, #73710, #232774, #54108, #94513, #154540, #234029 ),
 .UNSPECIFIED., .F., .F.,
 ( 4, 3, 3, 3, 3, 4 ),
 ( 0.000000000000000000, 2.372700795694929318E-05, 5.739057815867159087E-05, 9.073899019181866019E-05, 0.0001243544287365815515, 0.0001585386695601353146 ),
 .UNSPECIFIED. ) ;
#253131=EDGE_CURVE ( 'NONE', #231902, #147657, #190114, .T. ) ;
#253143=VERTEX_POINT ( 'NONE', #196383 ) ;
#253156=CARTESIAN_POINT ( 'NONE',  ( -18.59999999999999787, 7.021664781911246322, -171.2335654018973230 ) ) ;
#253162=ORIENTED_EDGE ( 'NONE', *, *, #79356, .F. ) ;
#253166=ADVANCED_FACE ( 'NONE', ( #221077 ), #240000, .T. ) ;
#253189=TOROIDAL_SURFACE ( 'NONE', #136657, 0.2000000000000000111, 0.1000000000000000056 ) ;
#253224=ORIENTED_EDGE ( 'NONE', *, *, #132477, .F. ) ;
#253225=VECTOR ( 'NONE', #161677, 1000.000000000000000 ) ;
#253236=FACE_OUTER_BOUND ( 'NONE', #217924, .T. ) ;
#253265=VERTEX_POINT ( 'NONE', #77707 ) ;
#253268=AXIS2_PLACEMENT_3D ( 'NONE', #131337, #68818, #51782 ) ;
#253282=DIRECTION ( 'NONE',  ( 1.000000000000000000, 7.304098846218134667E-16, 0.000000000000000000 ) ) ;
#253296=CARTESIAN_POINT ( 'NONE',  ( -21.65000000000000213, 7.708578643773852157, -146.2500000000000284 ) ) ;
#253328=CARTESIAN_POINT ( 'NONE',  ( -20.94999999999999929, -11.64999999998884483, -136.9000000000000341 ) ) ;
#253341=B_SPLINE_CURVE_WITH_KNOTS ( 'NONE', 3,
 ( #239071, #104648, #184215, #78685, #27755, #185511 ),
 .UNSPECIFIED., .F., .F.,
 ( 4, 2, 4 ),
 ( 0.000000000000000000, 0.0001891491689349617238, 0.0003782983378699234477 ),
 .UNSPECIFIED. ) ;
#253367=ORIENTED_EDGE ( 'NONE', *, *, #139581, .T. ) ;
#253407=ORIENTED_EDGE ( 'NONE', *, *, #34887, .F. ) ;
#253443=EDGE_LOOP ( 'NONE', ( #158694, #17153, #215915, #209278 ) ) ;
#253448=DIRECTION ( 'NONE',  ( -1.000000000000000000, -2.952720810173289112E-16, 0.000000000000000000 ) ) ;
#253453=ADVANCED_FACE ( 'NONE', ( #14908 ), #151859, .F. ) ;
#253485=CARTESIAN_POINT ( 'NONE',  ( -21.05000000000000071, 14.00000000001115374, -162.0729074696175473 ) ) ;
#253509=DIRECTION ( 'NONE',  ( 0.000000000000000000, 0.000000000000000000, -1.000000000000000000 ) ) ;
#253528=DIRECTION ( 'NONE',  ( 1.000000000000000000, 0.000000000000000000, 0.000000000000000000 ) ) ;
#253531=CARTESIAN_POINT ( 'NONE',  ( 21.05000000000000071, 1.115600667400684642E-11, -134.0000000000000000 ) ) ;
#253564=ADVANCED_FACE ( 'NONE', ( #219492 ), #159545, .T. ) ;
#253565=CIRCLE ( 'NONE', #57754, 0.09999999999999363565 ) ;
#253566=ORIENTED_EDGE ( 'NONE', *, *, #43085, .T. ) ;
#253569=FILL_AREA_STYLE_COLOUR ( '', #139786 ) ;
#253586=CARTESIAN_POINT ( 'NONE',  ( 21.07199075132372101, 8.774944999127242795, -146.2135321616128749 ) ) ;
#253604=CARTESIAN_POINT ( 'NONE',  ( -21.05000000000000071, 1.115600667400684642E-11, -134.0000000000000000 ) ) ;
#253619=ORIENTED_EDGE ( 'NONE', *, *, #110661, .F. ) ;
#253648=EDGE_CURVE ( 'NONE', #61931, #220134, #243700, .T. ) ;
#253667=CARTESIAN_POINT ( 'NONE',  ( 20.95512820512820440, 10.62384868372303615, -146.1500000000000341 ) ) ;
#253669=EDGE_CURVE ( 'NONE', #135320, #102830, #185517, .T. ) ;
#253676=EDGE_CURVE ( 'NONE', #123059, #55661, #123092, .T. ) ;
#253684=DIRECTION ( 'NONE',  ( -1.000000000000000000, -0.000000000000000000, -0.000000000000000000 ) ) ;
#253727=ADVANCED_FACE ( 'NONE', ( #165981 ), #177283, .F. ) ;
#253750=ORIENTED_EDGE ( 'NONE', *, *, #129135, .F. ) ;
#253776=CARTESIAN_POINT ( 'NONE',  ( 18.59999999999999076, 10.20857864377385127, -155.3500000000000227 ) ) ;
#253811=CARTESIAN_POINT ( 'NONE',  ( 22.50000000000000000, 7.790779598384538929, -133.9000000000000057 ) ) ;
#253835=DIRECTION ( 'NONE',  ( -1.000000000000000000, -0.000000000000000000, 0.000000000000000000 ) ) ;
#253853=CARTESIAN_POINT ( 'NONE',  ( 22.32929514600007792, 7.578647565387638174, -133.9009243218860945 ) ) ;
#253857=TOROIDAL_SURFACE ( 'NONE', #158073, 0.6000000000000017542, 0.1000000000000000056 ) ;
#253858=VERTEX_POINT ( 'NONE', #150258 ) ;
#253862=VERTEX_POINT ( 'NONE', #113675 ) ;
#253899=CARTESIAN_POINT ( 'NONE',  ( -21.05000000000000071, 6.478078221105875834, -134.0999999353045098 ) ) ;
#253938=CARTESIAN_POINT ( 'NONE',  ( 21.05000000000000071, -1.736257131586239844, -145.5686523290175387 ) ) ;
#253939=CARTESIAN_POINT ( 'NONE',  ( -18.50000000000000355, -1.263275465206102233, -175.4018646667464338 ) ) ;
#253947=DIRECTION ( 'NONE',  ( -1.000000000000000000, 0.000000000000000000, 0.000000000000000000 ) ) ;
#253956=AXIS2_PLACEMENT_3D ( 'NONE', #70959, #170071, #154361 ) ;
#253962=ORIENTED_EDGE ( 'NONE', *, *, #218595, .T. ) ;
#253987=CIRCLE ( 'NONE', #191680, 0.4000000000000114575 ) ;
#253995=AXIS2_PLACEMENT_3D ( 'NONE', #199094, #97389, #137817 ) ;
#254015=CARTESIAN_POINT ( 'NONE',  ( -20.94999999999999929, 1.115600667400684642E-11, -141.9000000000000341 ) ) ;
#254020=DIRECTION ( 'NONE',  ( 1.000000000000000000, -7.304098846218135653E-16, 0.000000000000000000 ) ) ;
#254022=ORIENTED_EDGE ( 'NONE', *, *, #82634, .T. ) ;
#254026=ORIENTED_EDGE ( 'NONE', *, *, #80919, .T. ) ;
#254036=ADVANCED_FACE ( 'NONE', ( #221737 ), #44428, .T. ) ;
#254076=AXIS2_PLACEMENT_3D ( 'NONE', #250679, #167328, #8239 ) ;
#254079=ORIENTED_EDGE ( 'NONE', *, *, #190794, .F. ) ;
#254104=ORIENTED_EDGE ( 'NONE', *, *, #246555, .F. ) ;
#254156=DIRECTION ( 'NONE',  ( -1.000000000000000000, -1.836970198721029934E-16, 0.000000000000000000 ) ) ;
#254163=EDGE_CURVE ( 'NONE', #25295, #255163, #40089, .T. ) ;
#254204=CIRCLE ( 'NONE', #116843, 0.09999999999999939493 ) ;
#254206=DIRECTION ( 'NONE',  ( -0.000000000000000000, -0.000000000000000000, 1.000000000000000000 ) ) ;
#254219=DIRECTION ( 'NONE',  ( -1.000000000000000000, 0.000000000000000000, 0.000000000000000000 ) ) ;
#254240=CYLINDRICAL_SURFACE ( 'NONE', #93185, 0.09999999999998898659 ) ;
#254249=CYLINDRICAL_SURFACE ( 'NONE', #242284, 7.899999999999990585 ) ;
#254263=CARTESIAN_POINT ( 'NONE',  ( -23.15000000000000213, 11.65000000001115588, -146.1500000000000341 ) ) ;
#254291=AXIS2_PLACEMENT_3D ( 'NONE', #233390, #54719, #174725 ) ;
#254341=ORIENTED_EDGE ( 'NONE', *, *, #90626, .F. ) ;
#254388=EDGE_CURVE ( 'NONE', #140279, #154872, #135724, .T. ) ;
#254401=ORIENTED_EDGE ( 'NONE', *, *, #145031, .T. ) ;
#254410=ORIENTED_EDGE ( 'NONE', *, *, #192046, .F. ) ;
#254437=ORIENTED_EDGE ( 'NONE', *, *, #38474, .T. ) ;
#254445=DIRECTION ( 'NONE',  ( 0.000000000000000000, 0.8660254037844411501, 0.4999999999999956701 ) ) ;
#254477=AXIS2_PLACEMENT_3D ( 'NONE', #210245, #52421, #35479 ) ;
#254513=AXIS2_PLACEMENT_3D ( 'NONE', #85831, #225359, #46726 ) ;
#254519=CARTESIAN_POINT ( 'NONE',  ( -20.85000000000000142, -1.835859311432481045, -179.0044391687985410 ) ) ;
#254551=ORIENTED_EDGE ( 'NONE', *, *, #48956, .F. ) ;
#254585=FACE_OUTER_BOUND ( 'NONE', #204736, .T. ) ;
#254586=CARTESIAN_POINT ( 'NONE',  ( -20.94999999999999929, 1.835341550235569663, -145.5551512925629822 ) ) ;
#254606=CIRCLE ( 'NONE', #67186, 11.75000000000001066 ) ;
#254629=DIRECTION ( 'NONE',  ( 0.000000000000000000, -1.000000000000000000, 0.000000000000000000 ) ) ;
#254656=CARTESIAN_POINT ( 'NONE',  ( 20.97468175916176847, 10.62526516438217605, -146.2547614354128314 ) ) ;
#254664=ORIENTED_EDGE ( 'NONE', *, *, #12537, .T. ) ;
#254684=CARTESIAN_POINT ( 'NONE',  ( 21.05000000000000071, 6.413978881499349249, -134.0857991162740177 ) ) ;
#254695=VERTEX_POINT ( 'NONE', #219525 ) ;
#254702=DIRECTION ( 'NONE',  ( -1.000000000000000000, 0.000000000000000000, 0.000000000000000000 ) ) ;
#254704=CARTESIAN_POINT ( 'NONE',  ( -23.15000000000000213, 11.65000000001115588, -134.0000000000000000 ) ) ;
#254708=DIRECTION ( 'NONE',  ( 0.000000000000000000, -1.000000000000000000, 0.000000000000000000 ) ) ;
#254722=CIRCLE ( 'NONE', #250488, 0.09999999999999971412 ) ;
#254726=VECTOR ( 'NONE', #157459, 1000.000000000000000 ) ;
#254744=DIRECTION ( 'NONE',  ( 0.5000000000001141309, 0.000000000000000000, -0.8660254037843729824 ) ) ;
#254773=ADVANCED_FACE ( 'NONE', ( #164710 ), #11757, .T. ) ;
#254804=ORIENTED_EDGE ( 'NONE', *, *, #25214, .F. ) ;
#254809=ORIENTED_EDGE ( 'NONE', *, *, #244798, .T. ) ;
#254832=ORIENTED_EDGE ( 'NONE', *, *, #173386, .T. ) ;
#254847=EDGE_CURVE ( 'NONE', #223143, #176594, #36353, .T. ) ;
#254855=DIRECTION ( 'NONE',  ( 0.000000000000000000, 0.000000000000000000, 1.000000000000000000 ) ) ;
#254865=DIRECTION ( 'NONE',  ( 0.000000000000000000, -0.9915357197604972583, 0.1298341882519109536 ) ) ;
#254872=CARTESIAN_POINT ( 'NONE',  ( -23.25000000000000000, -0.09999999998884338825, -122.3504291924552234 ) ) ;
#254907=AXIS2_PLACEMENT_3D ( 'NONE', #175962, #1119, #78102 ) ;
#254910=CIRCLE ( 'NONE', #92661, 0.09999999999998898659 ) ;
#254914=CARTESIAN_POINT ( 'NONE',  ( 21.13498764882293557, 6.495618143485025975, -133.9983436052687011 ) ) ;
#254932=CARTESIAN_POINT ( 'NONE',  ( 21.14999999999999503, -0.09999999998884338825, -122.3504291924552234 ) ) ;
#254982=ORIENTED_EDGE ( 'NONE', *, *, #199825, .T. ) ;
#254986=EDGE_LOOP ( 'NONE', ( #27634, #171396 ) ) ;
#254998=CARTESIAN_POINT ( 'NONE',  ( -20.96077737575314970, 11.62390063401601381, -160.6407919571068135 ) ) ;
#255007=AXIS2_PLACEMENT_3D ( 'NONE', #205946, #87264, #108137 ) ;
#255026=DIRECTION ( 'NONE',  ( -1.000000000000000000, -0.000000000000000000, -0.000000000000000000 ) ) ;
#255030=DIRECTION ( 'NONE',  ( 1.000000000000000000, 0.000000000000000000, 0.000000000000000000 ) ) ;
#255063=EDGE_CURVE ( 'NONE', #48580, #224075, #132666, .T. ) ;
#255075=CARTESIAN_POINT ( 'NONE',  ( -21.55000000000000071, 7.350000000011155166, -155.1500000000000057 ) ) ;
#255106=CARTESIAN_POINT ( 'NONE',  ( -21.07928932188134041, 0.09889514566555070163, -127.6714833436066954 ) ) ;
#255108=ORIENTED_EDGE ( 'NONE', *, *, #52420, .T. ) ;
#255131=CARTESIAN_POINT ( 'NONE',  ( -18.50000000000000000, 9.150000000011157653, -122.2500000000000284 ) ) ;
#255137=CARTESIAN_POINT ( 'NONE',  ( -21.05000000000000071, 6.258842723548820430, -133.9679863068126338 ) ) ;
#255163=VERTEX_POINT ( 'NONE', #105682 ) ;
#255175=CIRCLE ( 'NONE', #171892, 0.4000000000000114575 ) ;
#255217=AXIS2_PLACEMENT_3D ( 'NONE', #126200, #205738, #246162 ) ;
#255223=ADVANCED_FACE ( 'NONE', ( #48305 ), #136937, .T. ) ;
#255249=AXIS2_PLACEMENT_3D ( 'NONE', #113476, #32709, #193032 ) ;
#255264=ORIENTED_EDGE ( 'NONE', *, *, #24392, .T. ) ;
#255292=CARTESIAN_POINT ( 'NONE',  ( 18.59999999999997655, -1.164121893230052995, -175.4148480855716059 ) ) ;
#255308=AXIS2_PLACEMENT_3D ( 'NONE', #58106, #235469, #252464 ) ;
#255314=EDGE_CURVE ( 'NONE', #39881, #159476, #49455, .T. ) ;
#255380=CARTESIAN_POINT ( 'NONE',  ( 23.15000000000000213, -11.64999999998883595, -164.4000000000000057 ) ) ;
#255421=CARTESIAN_POINT ( 'NONE',  ( 22.39999999999999503, 11.75000000001116263, -133.9000000000000057 ) ) ;
#255432=CARTESIAN_POINT ( 'NONE',  ( 21.05000000000000071, 11.60000000001116227, -160.5717967697245285 ) ) ;
#255433=ORIENTED_EDGE ( 'NONE', *, *, #62671, .T. ) ;
#255436=AXIS2_PLACEMENT_3D ( 'NONE', #71025, #139939, #179123 ) ;
#255447=CARTESIAN_POINT ( 'NONE',  ( 20.85000000000000142, -1.362429037182151470, -175.3888812479212334 ) ) ;
#255455=CARTESIAN_POINT ( 'NONE',  ( -18.59999999999999787, 6.933893972137497030, -171.2856458343736108 ) ) ;
#255498=ORIENTED_EDGE ( 'NONE', *, *, #255694, .F. ) ;
#255510=EDGE_LOOP ( 'NONE', ( #251306, #81911, #176604, #66096, #163603, #232985, #101524, #148268, #21497, #23602 ) ) ;
#255517=DIRECTION ( 'NONE',  ( 0.000000000000000000, 0.000000000000000000, -1.000000000000000000 ) ) ;
#255545=EDGE_CURVE ( 'NONE', #226085, #136324, #113416, .T. ) ;
#255565=FACE_OUTER_BOUND ( 'NONE', #145876, .T. ) ;
#255582=DIRECTION ( 'NONE',  ( 0.000000000000000000, 1.224646799142185182E-16, 1.000000000000000000 ) ) ;
#255585=FILL_AREA_STYLE_COLOUR ( '', #180739 ) ;
#255590=DIRECTION ( 'NONE',  ( 1.000000000000000000, -7.304098846218134667E-16, -4.217023435051626718E-16 ) ) ;
#255616=ORIENTED_EDGE ( 'NONE', *, *, #195398, .F. ) ;
#255633=CARTESIAN_POINT ( 'NONE',  ( 20.04142135623730070, 11.65000000001115943, -155.3500000000000227 ) ) ;
#255635=ORIENTED_EDGE ( 'NONE', *, *, #146400, .T. ) ;
#255641=VECTOR ( 'NONE', #122297, 1000.000000000000000 ) ;
#255672=EDGE_LOOP ( 'NONE', ( #19433, #182602, #116370, #152324, #43288 ) ) ;
#255673=ADVANCED_FACE ( 'NONE', ( #109242 ), #231785, .F. ) ;
#255694=EDGE_CURVE ( 'NONE', #171180, #70632, #63502, .T. ) ;
#255707=ORIENTED_EDGE ( 'NONE', *, *, #72415, .F. ) ;
#255714=EDGE_LOOP ( 'NONE', ( #39303, #1371, #112657, #29830 ) ) ;
#255719=VECTOR ( 'NONE', #119650, 1000.000000000000000 ) ;
#255738=DIRECTION ( 'NONE',  ( -1.000000000000000000, 0.000000000000000000, 0.000000000000000000 ) ) ;
#255743=CYLINDRICAL_SURFACE ( 'NONE', #197241, 0.09999999999999939493 ) ;
#255752=AXIS2_PLACEMENT_3D ( 'NONE', #175136, #128576, #90716 ) ;
#255759=EDGE_CURVE ( 'NONE', #21635, #139646, #55657, .T. ) ;
#255767=CIRCLE ( 'NONE', #18299, 12.87499999999999822 ) ;
#255795=ORIENTED_EDGE ( 'NONE', *, *, #122054, .T. ) ;
#255796=DIRECTION ( 'NONE',  ( -0.000000000000000000, -1.000000000000000000, -0.000000000000000000 ) ) ;
#255849=SPHERICAL_SURFACE ( 'NONE', #221026, 0.1000000000000000056 ) ;
#255904=EDGE_CURVE ( 'NONE', #203005, #207677, #76161, .T. ) ;
#255922=DIRECTION ( 'NONE',  ( 0.000000000000000000, 0.000000000000000000, 1.000000000000000000 ) ) ;
#255932=EDGE_CURVE ( 'NONE', #208712, #217297, #21716, .T. ) ;
#255941=CYLINDRICAL_SURFACE ( 'NONE', #68378, 0.09999999999998898659 ) ;
#255962=CARTESIAN_POINT ( 'NONE',  ( 21.14999999999999858, 6.540656951712402467, -134.0000000000000284 ) ) ;
#255970=ORIENTED_EDGE ( 'NONE', *, *, #214153, .T. ) ;
#255982=DIRECTION ( 'NONE',  ( 0.000000000000000000, 0.000000000000000000, -1.000000000000000000 ) ) ;
#255985=DIRECTION ( 'NONE',  ( 0.000000000000000000, 0.000000000000000000, -1.000000000000000000 ) ) ;
#256042=CYLINDRICAL_SURFACE ( 'NONE', #144587, 0.09999999999999881206 ) ;
#256048=CONICAL_SURFACE ( 'NONE', #181126, 4.049999999999998046, 0.7853981633974604915 ) ;
#256074=EDGE_CURVE ( 'NONE', #73136, #83407, #86793, .T. ) ;
#256087=VECTOR ( 'NONE', #145590, 1000.000000000000000 ) ;
#256143=AXIS2_PLACEMENT_3D ( 'NONE', #236420, #216850, #38236 ) ;
#256154=DIRECTION ( 'NONE',  ( 0.000000000000000000, 0.000000000000000000, -1.000000000000000000 ) ) ;
#256158=DIRECTION ( 'NONE',  ( 1.000000000000000000, 0.000000000000000000, 0.000000000000000000 ) ) ;
#256172=ORIENTED_EDGE ( 'NONE', *, *, #83722, .T. ) ;
#256175=CARTESIAN_POINT ( 'NONE',  ( -23.25000000000000000, 11.75000000001115552, -122.2500000000000284 ) ) ;
#256177=EDGE_CURVE ( 'NONE', #60099, #84586, #213727, .T. ) ;
#256199=DIRECTION ( 'NONE',  ( -1.000000000000000000, 0.000000000000000000, 0.000000000000000000 ) ) ;
#256200=CARTESIAN_POINT ( 'NONE',  ( 18.49999999999999289, 11.65000000001115588, -167.5000000000000284 ) ) ;
#256261=CIRCLE ( 'NONE', #148179, 0.2000000000000057288 ) ;
#256291=ORIENTED_EDGE ( 'NONE', *, *, #7114, .T. ) ;
#256294=EDGE_CURVE ( 'NONE', #42831, #185781, #155508, .T. ) ;
#256300=EDGE_CURVE ( 'NONE', #116221, #42831, #252814, .T. ) ;
#256313=DIRECTION ( 'NONE',  ( -1.000000000000000000, 0.000000000000000000, 0.000000000000000000 ) ) ;
#256337=EDGE_CURVE ( 'NONE', #130320, #43656, #59761, .T. ) ;
#256339=AXIS2_PLACEMENT_3D ( 'NONE', #125658, #190810, #155536 ) ;
#256351=AXIS2_PLACEMENT_3D ( 'NONE', #136735, #232021, #91213 ) ;
#256371=AXIS2_PLACEMENT_3D ( 'NONE', #153897, #211249, #33947 ) ;
#256374=AXIS2_PLACEMENT_3D ( 'NONE', #62426, #118563, #58545 ) ;
#256388=CARTESIAN_POINT ( 'NONE',  ( -21.14999999999999858, -11.64999999998884483, -134.0000000000000000 ) ) ;
#256394=AXIS2_PLACEMENT_3D ( 'NONE', #20538, #217412, #63477 ) ;
#256396=CARTESIAN_POINT ( 'NONE',  ( -20.64999999999999858, -9.399999999988846611, -157.6060308773475924 ) ) ;
#256405=CYLINDRICAL_SURFACE ( 'NONE', #177963, 0.09999999999999939493 ) ;
#256406=VERTEX_POINT ( 'NONE', #122303 ) ;
#256418=LINE ( 'NONE', #140379, #136220 ) ;
#256453=ORIENTED_EDGE ( 'NONE', *, *, #79738, .T. ) ;
#256466=AXIS2_PLACEMENT_3D ( 'NONE', #231936, #235753, #16736 ) ;
#256476=ORIENTED_EDGE ( 'NONE', *, *, #256933, .T. ) ;
#256519=DIRECTION ( 'NONE',  ( 0.000000000000000000, 0.01562499999998609446, -0.9998779222360101304 ) ) ;
#256640=AXIS2_PLACEMENT_3D ( 'NONE', #198470, #135914, #177662 ) ;
#256648=AXIS2_PLACEMENT_3D ( 'NONE', #49107, #27018, #189914 ) ;
#256662=ADVANCED_FACE ( 'NONE', ( #186450 ), #22401, .T. ) ;
#256705=EDGE_CURVE ( 'NONE', #40935, #153112, #51562, .T. ) ;
#256723=DIRECTION ( 'NONE',  ( -0.7071067811865388020, 0.7071067811865561215, 0.000000000000000000 ) ) ;
#256739=FACE_OUTER_BOUND ( 'NONE', #142891, .T. ) ;
#256747=CARTESIAN_POINT ( 'NONE',  ( 21.05000000000000071, -8.999999999988844479, -143.8939691226524644 ) ) ;
#256750=SPHERICAL_SURFACE ( 'NONE', #129193, 0.1000000000000000056 ) ;
#256765=DIRECTION ( 'NONE',  ( -1.000000000000000000, 0.000000000000000000, 0.000000000000000000 ) ) ;
#256820=CARTESIAN_POINT ( 'NONE',  ( 20.94999999999999929, 6.450000000011156587, -144.0170271704400307 ) ) ;
#256821=CIRCLE ( 'NONE', #169632, 0.09999999999999839573 ) ;
#256828=AXIS2_PLACEMENT_3D ( 'NONE', #202323, #143628, #104477 ) ;
#256850=EDGE_LOOP ( 'NONE', ( #135520, #57214, #155409, #172350 ) ) ;
#256851=CARTESIAN_POINT ( 'NONE',  ( -23.15000000000000213, -11.64999999998884483, -164.5000000000000000 ) ) ;
#256861=EDGE_CURVE ( 'NONE', #240778, #135871, #251506, .T. ) ;
#256892=AXIS2_PLACEMENT_3D ( 'NONE', #163154, #47021, #242666 ) ;
#256904=VERTEX_POINT ( 'NONE', #103991 ) ;
#256907=DIRECTION ( 'NONE',  ( 1.000000000000000000, 0.000000000000000000, 0.000000000000000000 ) ) ;
#256915=CARTESIAN_POINT ( 'NONE',  ( -20.64999999999999858, 7.250000000011155521, -146.2500000000000284 ) ) ;
#256933=EDGE_CURVE ( 'NONE', #6309, #213361, #164226, .T. ) ;
#256938=CIRCLE ( 'NONE', #148678, 0.09999999999999062417 ) ;
#256943=ADVANCED_FACE ( 'NONE', ( #170468 ), #226509, .F. ) ;
#256959=ADVANCED_FACE ( 'NONE', ( #124875 ), #225226, .F. ) ;
#256960=AXIS2_PLACEMENT_3D ( 'NONE', #114210, #95912, #175489 ) ;
#256975=CARTESIAN_POINT ( 'NONE',  ( -23.25000000000000000, -0.1008583690875562017, -122.2504328765106294 ) ) ;
#256985=ORIENTED_EDGE ( 'NONE', *, *, #98015, .F. ) ;
#257034=DIRECTION ( 'NONE',  ( -1.000000000000000000, -0.000000000000000000, -0.000000000000000000 ) ) ;
#257109=ADVANCED_FACE ( 'NONE', ( #132580 ), #91699, .F. ) ;
#257121=CARTESIAN_POINT ( 'NONE',  ( -20.54999999999999716, 4.350000000011156054, -155.2500000000000284 ) ) ;
#257122=AXIS2_PLACEMENT_3D ( 'NONE', #247828, #70515, #24954 ) ;
#257144=ORIENTED_EDGE ( 'NONE', *, *, #93600, .F. ) ;
#257166=ORIENTED_EDGE ( 'NONE', *, *, #32987, .T. ) ;
#257210=DIRECTION ( 'NONE',  ( 0.000000000000000000, -1.000000000000000000, 0.000000000000000000 ) ) ;
#257226=LINE ( 'NONE', #17390, #72478 ) ;
#257244=EDGE_LOOP ( 'NONE', ( #64280, #148609, #221046 ) ) ;
#257269=FACE_OUTER_BOUND ( 'NONE', #114676, .T. ) ;
#257273=DIRECTION ( 'NONE',  ( 0.000000000000000000, 0.000000000000000000, -1.000000000000000000 ) ) ;
#257284=VERTEX_POINT ( 'NONE', #19040 ) ;
#257362=VERTEX_POINT ( 'NONE', #45028 ) ;
#257370=DIRECTION ( 'NONE',  ( 0.000000000000000000, 0.000000000000000000, 1.000000000000000000 ) ) ;
#257382=CARTESIAN_POINT ( 'NONE',  ( -21.05000000000000071, 1.115600667400684642E-11, -134.0000000000000000 ) ) ;
#257417=CARTESIAN_POINT ( 'NONE',  ( -20.54999999999999716, -11.74999999998884448, -155.1500000000000057 ) ) ;
#257432=CARTESIAN_POINT ( 'NONE',  ( 20.94999999999999929, -11.39257802169451317, -164.4260504201680817 ) ) ;
#257447=ORIENTED_EDGE ( 'NONE', *, *, #82679, .T. ) ;
#257470=DIRECTION ( 'NONE',  ( 0.000000000000000000, 0.000000000000000000, -1.000000000000000000 ) ) ;
#257485=CARTESIAN_POINT ( 'NONE',  ( 21.08376601933332495, 6.341947271286813681, -133.9362239890700153 ) ) ;
#257496=CARTESIAN_POINT ( 'NONE',  ( -20.64999999999999858, 7.150000000011155876, -146.2500000000000284 ) ) ;
#257498=DIRECTION ( 'NONE',  ( 1.000000000000000000, 0.000000000000000000, 0.000000000000000000 ) ) ;
#257499=EDGE_LOOP ( 'NONE', ( #166086, #194493, #87180, #129276 ) ) ;
#257520=CARTESIAN_POINT ( 'NONE',  ( 23.14999999999999503, 11.65000000001116298, -160.4851942293460638 ) ) ;
#257524=CARTESIAN_POINT ( 'NONE',  ( 20.94999999999999929, 7.021664781911246322, -171.3335654018973173 ) ) ;
#257544=CIRCLE ( 'NONE', #145167, 0.09999999999998898659 ) ;
#257549=CARTESIAN_POINT ( 'NONE',  ( 21.05000000000000071, 1.115600667400684642E-11, -167.5000000000000284 ) ) ;
#257585=AXIS2_PLACEMENT_3D ( 'NONE', #34558, #14995, #12433 ) ;
#257615=ORIENTED_EDGE ( 'NONE', *, *, #84884, .T. ) ;
#257643=ADVANCED_FACE ( 'NONE', ( #181369 ), #18648, .T. ) ;
#257654=CIRCLE ( 'NONE', #149994, 0.09999999999998898659 ) ;
#257665=DIRECTION ( 'NONE',  ( 0.000000000000000000, 0.000000000000000000, -1.000000000000000000 ) ) ;
#257695=CARTESIAN_POINT ( 'NONE',  ( -18.49346865148318386, -9.443073798513808015, -141.1851962553153328 ) ) ;
#257758=CARTESIAN_POINT ( 'NONE',  ( 21.14999999999999503, -11.64999999998883595, -122.2500000000000284 ) ) ;
#257760=ORIENTED_EDGE ( 'NONE', *, *, #198917, .T. ) ;
#257789=LINE ( 'NONE', #41391, #112188 ) ;
#257798=EDGE_LOOP ( 'NONE', ( #79399, #92292, #66733 ) ) ;
#257802=AXIS2_PLACEMENT_3D ( 'NONE', #99202, #161795, #181353 ) ;
#257831=VERTEX_POINT ( 'NONE', #14287 ) ;
#257842=B_SPLINE_CURVE_WITH_KNOTS ( 'NONE', 3,
 ( #194550, #116283, #191980, #150273, #130686, #94127, #13322, #210247 ),
 .UNSPECIFIED., .F., .F.,
 ( 4, 2, 2, 4 ),
 ( 0.000000000000000000, 0.0001306511400391254711, 0.0001959767100586882202, 0.0002613022800782509422 ),
 .UNSPECIFIED. ) ;
#257862=ORIENTED_EDGE ( 'NONE', *, *, #50616, .T. ) ;
#257865=CARTESIAN_POINT ( 'NONE',  ( 22.45301702632625762, 0.01521087972134078925, -122.3502077757396336 ) ) ;
#257880=ORIENTED_EDGE ( 'NONE', *, *, #229332, .T. ) ;
#257882=CARTESIAN_POINT ( 'NONE',  ( -21.14999999999999858, 11.75000000001115552, -140.7261306360592243 ) ) ;
#257890=CARTESIAN_POINT ( 'NONE',  ( 18.59999999999999076, 5.950000000011100632, -144.3057023050348846 ) ) ;
#257906=DIRECTION ( 'NONE',  ( 0.000000000000000000, 0.000000000000000000, -1.000000000000000000 ) ) ;
#257913=EDGE_LOOP ( 'NONE', ( #13356, #1090, #218673, #178467 ) ) ;
#257926=CARTESIAN_POINT ( 'NONE',  ( 18.49999999999999645, -1.162701749926855266, -142.1000000000000227 ) ) ;
#257928=DIRECTION ( 'NONE',  ( -1.000000000000000000, -0.000000000000000000, -0.000000000000000000 ) ) ;
#257940=CARTESIAN_POINT ( 'NONE',  ( -18.59999999999999787, -9.499999999988849808, -142.1000000000000227 ) ) ;
#257944=ORIENTED_EDGE ( 'NONE', *, *, #163467, .T. ) ;
#257948=FACE_OUTER_BOUND ( 'NONE', #208087, .T. ) ;
#257964=VERTEX_POINT ( 'NONE', #160218 ) ;
#257998=EDGE_CURVE ( 'NONE', #140176, #208557, #114506, .T. ) ;
#258028=ORIENTED_EDGE ( 'NONE', *, *, #48100, .T. ) ;
#258030=( BOUNDED_CURVE ( )  B_SPLINE_CURVE ( 3, ( #10916, #206534, #29226, #46166 ),
 .UNSPECIFIED., .F., .F. ) 
 B_SPLINE_CURVE_WITH_KNOTS ( ( 4, 4 ),
 ( 4.712388980384689674, 6.283185307179586232 ),
 .UNSPECIFIED. ) 
 CURVE ( )  GEOMETRIC_REPRESENTATION_ITEM ( )  RATIONAL_B_SPLINE_CURVE ( ( 1.000000000000000000, 0.8047378541243649375, 0.8047378541243649375, 1.000000000000000000 ) ) 
 REPRESENTATION_ITEM ( '' )  );
#258044=DIRECTION ( 'NONE',  ( -1.000000000000000000, 0.000000000000000000, 0.000000000000000000 ) ) ;
ENDSEC;
END-ISO-10303-21;
